ISO-10303-21;
HEADER;
/* Generated by software containing ST-Developer
 * from STEP Tools, Inc. (www.steptools.com) 
 */

FILE_DESCRIPTION(
/* description */ ('PAT-054'),
/* implementation_level */ '2;1');

FILE_NAME(
/* name */ 'Supported TR12x3 screw.step',
/* time_stamp */ '2026-10-29T16:38:13-07:00',
/* author */ (''),
/* organization */ (''),
/* preprocessor_version */ 'ST-DEVELOPER v20.2',
/* originating_system */ 'Autodesk Translation Framework v15.17.0.0',
/* authorisation */ '');

FILE_SCHEMA (('AUTOMOTIVE_DESIGN { 1 0 10303 214 3 1 1 }'));
ENDSEC;

DATA;
#10=MECHANICAL_DESIGN_GEOMETRIC_PRESENTATION_REPRESENTATION('',(#948),#33981);
#13=B_SPLINE_SURFACE_WITH_KNOTS('',3,3,((#29192,#29193,#29194,#29195,#29196,
#29197,#29198,#29199,#29200,#29201,#29202,#29203,#29204,#29205,#29206,#29207,
#29208,#29209,#29210,#29211,#29212,#29213,#29214,#29215,#29216,#29217,#29218,
#29219,#29220,#29221,#29222,#29223,#29224,#29225,#29226,#29227,#29228,#29229,
#29230,#29231,#29232,#29233,#29234,#29235,#29236,#29237,#29238,#29239,#29240,
#29241,#29242,#29243,#29244,#29245,#29246,#29247,#29248,#29249,#29250,#29251,
#29252,#29253,#29254,#29255,#29256,#29257,#29258,#29259,#29260,#29261,#29262,
#29263,#29264,#29265,#29266,#29267,#29268,#29269,#29270,#29271,#29272,#29273,
#29274,#29275,#29276,#29277,#29278,#29279,#29280,#29281,#29282,#29283,#29284,
#29285,#29286,#29287,#29288,#29289,#29290,#29291,#29292,#29293,#29294,#29295,
#29296,#29297,#29298,#29299,#29300,#29301,#29302,#29303,#29304,#29305,#29306,
#29307,#29308,#29309,#29310,#29311,#29312,#29313,#29314,#29315,#29316,#29317,
#29318,#29319,#29320,#29321,#29322,#29323,#29324,#29325,#29326,#29327,#29328,
#29329,#29330,#29331,#29332,#29333,#29334,#29335,#29336,#29337,#29338,#29339,
#29340,#29341,#29342,#29343,#29344,#29345,#29346,#29347,#29348,#29349,#29350,
#29351,#29352,#29353,#29354,#29355,#29356,#29357,#29358,#29359,#29360,#29361,
#29362,#29363,#29364,#29365,#29366,#29367,#29368,#29369,#29370,#29371,#29372,
#29373,#29374,#29375,#29376,#29377,#29378,#29379,#29380,#29381,#29382,#29383,
#29384,#29385,#29386,#29387,#29388,#29389,#29390,#29391,#29392,#29393,#29394,
#29395,#29396,#29397,#29398,#29399,#29400,#29401,#29402,#29403,#29404,#29405,
#29406,#29407,#29408,#29409,#29410,#29411,#29412,#29413,#29414,#29415,#29416,
#29417,#29418,#29419,#29420,#29421,#29422,#29423,#29424,#29425,#29426,#29427,
#29428,#29429,#29430,#29431,#29432,#29433,#29434,#29435,#29436,#29437,#29438,
#29439,#29440,#29441,#29442,#29443,#29444,#29445,#29446,#29447,#29448,#29449,
#29450,#29451,#29452,#29453,#29454,#29455,#29456,#29457,#29458,#29459,#29460,
#29461,#29462,#29463,#29464,#29465,#29466,#29467,#29468,#29469,#29470,#29471,
#29472,#29473,#29474,#29475,#29476,#29477,#29478,#29479,#29480,#29481,#29482,
#29483,#29484,#29485,#29486,#29487,#29488,#29489,#29490,#29491,#29492,#29493,
#29494,#29495,#29496,#29497,#29498,#29499,#29500,#29501,#29502,#29503,#29504,
#29505,#29506,#29507,#29508,#29509,#29510,#29511,#29512,#29513,#29514,#29515,
#29516,#29517,#29518,#29519,#29520,#29521,#29522,#29523,#29524,#29525,#29526,
#29527,#29528,#29529,#29530,#29531,#29532,#29533,#29534,#29535,#29536,#29537,
#29538,#29539,#29540,#29541,#29542,#29543,#29544,#29545,#29546,#29547,#29548,
#29549,#29550,#29551,#29552,#29553,#29554,#29555,#29556,#29557,#29558,#29559,
#29560,#29561,#29562,#29563,#29564,#29565,#29566,#29567,#29568,#29569,#29570,
#29571,#29572,#29573,#29574,#29575,#29576,#29577,#29578,#29579,#29580,#29581,
#29582,#29583,#29584,#29585,#29586,#29587,#29588,#29589,#29590,#29591,#29592,
#29593,#29594,#29595,#29596,#29597,#29598,#29599,#29600,#29601,#29602,#29603,
#29604,#29605,#29606,#29607,#29608,#29609,#29610,#29611,#29612,#29613,#29614,
#29615,#29616,#29617,#29618,#29619,#29620,#29621,#29622,#29623,#29624,#29625,
#29626,#29627,#29628,#29629,#29630,#29631,#29632,#29633,#29634,#29635,#29636,
#29637,#29638,#29639,#29640,#29641,#29642,#29643,#29644,#29645,#29646,#29647,
#29648,#29649,#29650,#29651,#29652,#29653,#29654,#29655,#29656,#29657,#29658,
#29659,#29660,#29661,#29662,#29663,#29664,#29665,#29666,#29667,#29668,#29669,
#29670,#29671,#29672,#29673,#29674,#29675,#29676,#29677,#29678,#29679,#29680,
#29681,#29682,#29683,#29684,#29685,#29686,#29687,#29688,#29689),(#29690,
#29691,#29692,#29693,#29694,#29695,#29696,#29697,#29698,#29699,#29700,#29701,
#29702,#29703,#29704,#29705,#29706,#29707,#29708,#29709,#29710,#29711,#29712,
#29713,#29714,#29715,#29716,#29717,#29718,#29719,#29720,#29721,#29722,#29723,
#29724,#29725,#29726,#29727,#29728,#29729,#29730,#29731,#29732,#29733,#29734,
#29735,#29736,#29737,#29738,#29739,#29740,#29741,#29742,#29743,#29744,#29745,
#29746,#29747,#29748,#29749,#29750,#29751,#29752,#29753,#29754,#29755,#29756,
#29757,#29758,#29759,#29760,#29761,#29762,#29763,#29764,#29765,#29766,#29767,
#29768,#29769,#29770,#29771,#29772,#29773,#29774,#29775,#29776,#29777,#29778,
#29779,#29780,#29781,#29782,#29783,#29784,#29785,#29786,#29787,#29788,#29789,
#29790,#29791,#29792,#29793,#29794,#29795,#29796,#29797,#29798,#29799,#29800,
#29801,#29802,#29803,#29804,#29805,#29806,#29807,#29808,#29809,#29810,#29811,
#29812,#29813,#29814,#29815,#29816,#29817,#29818,#29819,#29820,#29821,#29822,
#29823,#29824,#29825,#29826,#29827,#29828,#29829,#29830,#29831,#29832,#29833,
#29834,#29835,#29836,#29837,#29838,#29839,#29840,#29841,#29842,#29843,#29844,
#29845,#29846,#29847,#29848,#29849,#29850,#29851,#29852,#29853,#29854,#29855,
#29856,#29857,#29858,#29859,#29860,#29861,#29862,#29863,#29864,#29865,#29866,
#29867,#29868,#29869,#29870,#29871,#29872,#29873,#29874,#29875,#29876,#29877,
#29878,#29879,#29880,#29881,#29882,#29883,#29884,#29885,#29886,#29887,#29888,
#29889,#29890,#29891,#29892,#29893,#29894,#29895,#29896,#29897,#29898,#29899,
#29900,#29901,#29902,#29903,#29904,#29905,#29906,#29907,#29908,#29909,#29910,
#29911,#29912,#29913,#29914,#29915,#29916,#29917,#29918,#29919,#29920,#29921,
#29922,#29923,#29924,#29925,#29926,#29927,#29928,#29929,#29930,#29931,#29932,
#29933,#29934,#29935,#29936,#29937,#29938,#29939,#29940,#29941,#29942,#29943,
#29944,#29945,#29946,#29947,#29948,#29949,#29950,#29951,#29952,#29953,#29954,
#29955,#29956,#29957,#29958,#29959,#29960,#29961,#29962,#29963,#29964,#29965,
#29966,#29967,#29968,#29969,#29970,#29971,#29972,#29973,#29974,#29975,#29976,
#29977,#29978,#29979,#29980,#29981,#29982,#29983,#29984,#29985,#29986,#29987,
#29988,#29989,#29990,#29991,#29992,#29993,#29994,#29995,#29996,#29997,#29998,
#29999,#30000,#30001,#30002,#30003,#30004,#30005,#30006,#30007,#30008,#30009,
#30010,#30011,#30012,#30013,#30014,#30015,#30016,#30017,#30018,#30019,#30020,
#30021,#30022,#30023,#30024,#30025,#30026,#30027,#30028,#30029,#30030,#30031,
#30032,#30033,#30034,#30035,#30036,#30037,#30038,#30039,#30040,#30041,#30042,
#30043,#30044,#30045,#30046,#30047,#30048,#30049,#30050,#30051,#30052,#30053,
#30054,#30055,#30056,#30057,#30058,#30059,#30060,#30061,#30062,#30063,#30064,
#30065,#30066,#30067,#30068,#30069,#30070,#30071,#30072,#30073,#30074,#30075,
#30076,#30077,#30078,#30079,#30080,#30081,#30082,#30083,#30084,#30085,#30086,
#30087,#30088,#30089,#30090,#30091,#30092,#30093,#30094,#30095,#30096,#30097,
#30098,#30099,#30100,#30101,#30102,#30103,#30104,#30105,#30106,#30107,#30108,
#30109,#30110,#30111,#30112,#30113,#30114,#30115,#30116,#30117,#30118,#30119,
#30120,#30121,#30122,#30123,#30124,#30125,#30126,#30127,#30128,#30129,#30130,
#30131,#30132,#30133,#30134,#30135,#30136,#30137,#30138,#30139,#30140,#30141,
#30142,#30143,#30144,#30145,#30146,#30147,#30148,#30149,#30150,#30151,#30152,
#30153,#30154,#30155,#30156,#30157,#30158,#30159,#30160,#30161,#30162,#30163,
#30164,#30165,#30166,#30167,#30168,#30169,#30170,#30171,#30172,#30173,#30174,
#30175,#30176,#30177,#30178,#30179,#30180,#30181,#30182,#30183,#30184,#30185,
#30186,#30187),(#30188,#30189,#30190,#30191,#30192,#30193,#30194,#30195,
#30196,#30197,#30198,#30199,#30200,#30201,#30202,#30203,#30204,#30205,#30206,
#30207,#30208,#30209,#30210,#30211,#30212,#30213,#30214,#30215,#30216,#30217,
#30218,#30219,#30220,#30221,#30222,#30223,#30224,#30225,#30226,#30227,#30228,
#30229,#30230,#30231,#30232,#30233,#30234,#30235,#30236,#30237,#30238,#30239,
#30240,#30241,#30242,#30243,#30244,#30245,#30246,#30247,#30248,#30249,#30250,
#30251,#30252,#30253,#30254,#30255,#30256,#30257,#30258,#30259,#30260,#30261,
#30262,#30263,#30264,#30265,#30266,#30267,#30268,#30269,#30270,#30271,#30272,
#30273,#30274,#30275,#30276,#30277,#30278,#30279,#30280,#30281,#30282,#30283,
#30284,#30285,#30286,#30287,#30288,#30289,#30290,#30291,#30292,#30293,#30294,
#30295,#30296,#30297,#30298,#30299,#30300,#30301,#30302,#30303,#30304,#30305,
#30306,#30307,#30308,#30309,#30310,#30311,#30312,#30313,#30314,#30315,#30316,
#30317,#30318,#30319,#30320,#30321,#30322,#30323,#30324,#30325,#30326,#30327,
#30328,#30329,#30330,#30331,#30332,#30333,#30334,#30335,#30336,#30337,#30338,
#30339,#30340,#30341,#30342,#30343,#30344,#30345,#30346,#30347,#30348,#30349,
#30350,#30351,#30352,#30353,#30354,#30355,#30356,#30357,#30358,#30359,#30360,
#30361,#30362,#30363,#30364,#30365,#30366,#30367,#30368,#30369,#30370,#30371,
#30372,#30373,#30374,#30375,#30376,#30377,#30378,#30379,#30380,#30381,#30382,
#30383,#30384,#30385,#30386,#30387,#30388,#30389,#30390,#30391,#30392,#30393,
#30394,#30395,#30396,#30397,#30398,#30399,#30400,#30401,#30402,#30403,#30404,
#30405,#30406,#30407,#30408,#30409,#30410,#30411,#30412,#30413,#30414,#30415,
#30416,#30417,#30418,#30419,#30420,#30421,#30422,#30423,#30424,#30425,#30426,
#30427,#30428,#30429,#30430,#30431,#30432,#30433,#30434,#30435,#30436,#30437,
#30438,#30439,#30440,#30441,#30442,#30443,#30444,#30445,#30446,#30447,#30448,
#30449,#30450,#30451,#30452,#30453,#30454,#30455,#30456,#30457,#30458,#30459,
#30460,#30461,#30462,#30463,#30464,#30465,#30466,#30467,#30468,#30469,#30470,
#30471,#30472,#30473,#30474,#30475,#30476,#30477,#30478,#30479,#30480,#30481,
#30482,#30483,#30484,#30485,#30486,#30487,#30488,#30489,#30490,#30491,#30492,
#30493,#30494,#30495,#30496,#30497,#30498,#30499,#30500,#30501,#30502,#30503,
#30504,#30505,#30506,#30507,#30508,#30509,#30510,#30511,#30512,#30513,#30514,
#30515,#30516,#30517,#30518,#30519,#30520,#30521,#30522,#30523,#30524,#30525,
#30526,#30527,#30528,#30529,#30530,#30531,#30532,#30533,#30534,#30535,#30536,
#30537,#30538,#30539,#30540,#30541,#30542,#30543,#30544,#30545,#30546,#30547,
#30548,#30549,#30550,#30551,#30552,#30553,#30554,#30555,#30556,#30557,#30558,
#30559,#30560,#30561,#30562,#30563,#30564,#30565,#30566,#30567,#30568,#30569,
#30570,#30571,#30572,#30573,#30574,#30575,#30576,#30577,#30578,#30579,#30580,
#30581,#30582,#30583,#30584,#30585,#30586,#30587,#30588,#30589,#30590,#30591,
#30592,#30593,#30594,#30595,#30596,#30597,#30598,#30599,#30600,#30601,#30602,
#30603,#30604,#30605,#30606,#30607,#30608,#30609,#30610,#30611,#30612,#30613,
#30614,#30615,#30616,#30617,#30618,#30619,#30620,#30621,#30622,#30623,#30624,
#30625,#30626,#30627,#30628,#30629,#30630,#30631,#30632,#30633,#30634,#30635,
#30636,#30637,#30638,#30639,#30640,#30641,#30642,#30643,#30644,#30645,#30646,
#30647,#30648,#30649,#30650,#30651,#30652,#30653,#30654,#30655,#30656,#30657,
#30658,#30659,#30660,#30661,#30662,#30663,#30664,#30665,#30666,#30667,#30668,
#30669,#30670,#30671,#30672,#30673,#30674,#30675,#30676,#30677,#30678,#30679,
#30680,#30681,#30682,#30683,#30684,#30685),(#30686,#30687,#30688,#30689,
#30690,#30691,#30692,#30693,#30694,#30695,#30696,#30697,#30698,#30699,#30700,
#30701,#30702,#30703,#30704,#30705,#30706,#30707,#30708,#30709,#30710,#30711,
#30712,#30713,#30714,#30715,#30716,#30717,#30718,#30719,#30720,#30721,#30722,
#30723,#30724,#30725,#30726,#30727,#30728,#30729,#30730,#30731,#30732,#30733,
#30734,#30735,#30736,#30737,#30738,#30739,#30740,#30741,#30742,#30743,#30744,
#30745,#30746,#30747,#30748,#30749,#30750,#30751,#30752,#30753,#30754,#30755,
#30756,#30757,#30758,#30759,#30760,#30761,#30762,#30763,#30764,#30765,#30766,
#30767,#30768,#30769,#30770,#30771,#30772,#30773,#30774,#30775,#30776,#30777,
#30778,#30779,#30780,#30781,#30782,#30783,#30784,#30785,#30786,#30787,#30788,
#30789,#30790,#30791,#30792,#30793,#30794,#30795,#30796,#30797,#30798,#30799,
#30800,#30801,#30802,#30803,#30804,#30805,#30806,#30807,#30808,#30809,#30810,
#30811,#30812,#30813,#30814,#30815,#30816,#30817,#30818,#30819,#30820,#30821,
#30822,#30823,#30824,#30825,#30826,#30827,#30828,#30829,#30830,#30831,#30832,
#30833,#30834,#30835,#30836,#30837,#30838,#30839,#30840,#30841,#30842,#30843,
#30844,#30845,#30846,#30847,#30848,#30849,#30850,#30851,#30852,#30853,#30854,
#30855,#30856,#30857,#30858,#30859,#30860,#30861,#30862,#30863,#30864,#30865,
#30866,#30867,#30868,#30869,#30870,#30871,#30872,#30873,#30874,#30875,#30876,
#30877,#30878,#30879,#30880,#30881,#30882,#30883,#30884,#30885,#30886,#30887,
#30888,#30889,#30890,#30891,#30892,#30893,#30894,#30895,#30896,#30897,#30898,
#30899,#30900,#30901,#30902,#30903,#30904,#30905,#30906,#30907,#30908,#30909,
#30910,#30911,#30912,#30913,#30914,#30915,#30916,#30917,#30918,#30919,#30920,
#30921,#30922,#30923,#30924,#30925,#30926,#30927,#30928,#30929,#30930,#30931,
#30932,#30933,#30934,#30935,#30936,#30937,#30938,#30939,#30940,#30941,#30942,
#30943,#30944,#30945,#30946,#30947,#30948,#30949,#30950,#30951,#30952,#30953,
#30954,#30955,#30956,#30957,#30958,#30959,#30960,#30961,#30962,#30963,#30964,
#30965,#30966,#30967,#30968,#30969,#30970,#30971,#30972,#30973,#30974,#30975,
#30976,#30977,#30978,#30979,#30980,#30981,#30982,#30983,#30984,#30985,#30986,
#30987,#30988,#30989,#30990,#30991,#30992,#30993,#30994,#30995,#30996,#30997,
#30998,#30999,#31000,#31001,#31002,#31003,#31004,#31005,#31006,#31007,#31008,
#31009,#31010,#31011,#31012,#31013,#31014,#31015,#31016,#31017,#31018,#31019,
#31020,#31021,#31022,#31023,#31024,#31025,#31026,#31027,#31028,#31029,#31030,
#31031,#31032,#31033,#31034,#31035,#31036,#31037,#31038,#31039,#31040,#31041,
#31042,#31043,#31044,#31045,#31046,#31047,#31048,#31049,#31050,#31051,#31052,
#31053,#31054,#31055,#31056,#31057,#31058,#31059,#31060,#31061,#31062,#31063,
#31064,#31065,#31066,#31067,#31068,#31069,#31070,#31071,#31072,#31073,#31074,
#31075,#31076,#31077,#31078,#31079,#31080,#31081,#31082,#31083,#31084,#31085,
#31086,#31087,#31088,#31089,#31090,#31091,#31092,#31093,#31094,#31095,#31096,
#31097,#31098,#31099,#31100,#31101,#31102,#31103,#31104,#31105,#31106,#31107,
#31108,#31109,#31110,#31111,#31112,#31113,#31114,#31115,#31116,#31117,#31118,
#31119,#31120,#31121,#31122,#31123,#31124,#31125,#31126,#31127,#31128,#31129,
#31130,#31131,#31132,#31133,#31134,#31135,#31136,#31137,#31138,#31139,#31140,
#31141,#31142,#31143,#31144,#31145,#31146,#31147,#31148,#31149,#31150,#31151,
#31152,#31153,#31154,#31155,#31156,#31157,#31158,#31159,#31160,#31161,#31162,
#31163,#31164,#31165,#31166,#31167,#31168,#31169,#31170,#31171,#31172,#31173,
#31174,#31175,#31176,#31177,#31178,#31179,#31180,#31181,#31182,#31183)),
 .UNSPECIFIED.,.F.,.F.,.F.,(4,4),(4,1,1,1,1,1,1,1,1,1,1,1,1,1,1,1,1,1,1,
1,1,1,1,1,1,1,1,1,1,1,1,1,1,1,1,1,1,1,1,1,1,1,1,1,1,1,1,1,1,1,1,1,1,1,1,
1,1,1,1,1,1,1,1,1,1,1,1,1,1,1,1,1,1,1,1,1,1,1,1,1,1,1,1,1,1,1,1,1,1,1,1,
1,1,1,1,1,1,1,1,1,1,1,1,1,1,1,1,1,1,1,1,1,1,1,1,1,1,1,1,1,1,1,1,1,1,1,1,
1,1,1,1,1,1,1,1,1,1,1,1,1,1,1,1,1,1,1,1,1,1,1,1,1,1,1,1,1,1,1,1,1,1,1,1,
1,1,1,1,1,1,1,1,1,1,1,1,1,1,1,1,1,1,1,1,1,1,1,1,1,1,1,1,1,1,1,1,1,1,1,1,
1,1,1,1,1,1,1,1,1,1,1,1,1,1,1,1,1,1,1,1,1,1,1,1,1,1,1,1,1,1,1,1,1,1,1,1,
1,1,1,1,1,1,1,1,1,1,1,1,1,1,1,1,1,1,1,1,1,1,1,1,1,1,1,1,1,1,1,1,1,1,1,1,
1,1,1,1,1,1,1,1,1,1,1,1,1,1,1,1,1,1,1,1,1,1,1,1,1,1,1,1,1,1,1,1,1,1,1,1,
1,1,1,1,1,1,1,1,1,1,1,1,1,1,1,1,1,1,1,1,1,1,1,1,1,1,1,1,1,1,1,1,1,1,1,1,
1,1,1,1,1,1,1,1,1,1,1,1,1,1,1,1,1,1,1,1,1,1,1,1,1,1,1,1,1,1,1,1,1,1,1,1,
1,1,1,1,1,1,1,1,1,1,1,1,1,1,1,1,1,1,1,1,1,1,1,1,1,1,1,1,1,1,1,1,1,1,1,1,
1,1,1,1,1,1,1,1,1,1,1,1,1,1,1,1,1,1,1,1,1,1,1,1,1,1,1,1,1,1,1,1,1,1,1,1,
1,1,1,1,1,1,1,1,1,1,1,1,1,1,1,1,1,1,1,1,1,1,1,1,1,1,1,1,1,1,1,1,1,1,1,1,
1,1,1,1,1,1,1,1,4),(0.,0.184512097253587),(8.98171729021681,9.48139635699984,
9.98107542378286,10.4807544905659,10.9804335573489,11.4801126241319,11.979791690915,
12.479470757698,12.979149824481,13.478828891264,13.9785079580471,14.4781870248301,
14.9778660916131,15.4775451583961,15.9772242251791,16.4769032919622,16.9765823587452,
17.4762614255282,17.9759404923112,18.4756195590943,18.9752986258773,19.4749776926603,
19.9746567594433,20.4743358262264,20.9740148930094,21.4736939597924,21.9733730265754,
22.4730520933585,22.9727311601415,23.4724102269245,23.9720892937075,24.4717683604905,
24.9714474272736,25.4711264940566,25.9708055608396,26.4704846276226,26.9701636944057,
27.4698427611887,27.9695218279717,28.4692008947547,28.9688799615378,29.4685590283208,
29.9682380951038,30.4679171618868,30.9675962286699,31.4672752954529,31.9669543622359,
32.4666334290189,32.966312495802,33.465991562585,33.965670629368,34.465349696151,
34.965028762934,35.4647078297171,35.9643868965001,36.4640659632831,36.9637450300661,
37.4634240968492,37.9631031636322,38.4627822304152,38.9624612971982,39.4621403639813,
39.9618194307643,40.4614984975473,40.9611775643303,41.4608566311134,41.9605356978964,
42.4602147646794,42.9598938314624,43.4595728982454,43.9592519650285,44.4589310318115,
44.9586100985945,45.4582891653775,45.9579682321606,46.4576472989436,46.9573263657266,
47.4570054325096,47.9566844992927,48.4563635660757,48.9560426328587,49.4557216996417,
49.9554007664248,50.4550798332078,50.9547588999908,51.4544379667738,51.9541170335568,
52.4537961003399,52.9534751671229,53.4531542339059,53.9528333006889,54.452512367472,
54.952191434255,55.451870501038,55.951549567821,56.4512286346041,56.9509077013871,
57.4505867681701,57.9502658349531,58.4499449017362,58.9496239685192,59.9489821020852,
60.9483402356513,61.9476983692173,62.9470565027834,63.9464146363494,64.9457727699155,
65.9451309034815,66.9444890370476,67.9438471706136,68.9432053041797,69.9425634377457,
70.9419215713118,71.9412797048778,72.9406378384438,73.9399959720099,74.9393541055759,
75.938712239142,76.938070372708,77.9374285062741,78.9367866398401,79.9361447734062,
80.9355029069722,81.9348610405383,82.9342191741043,83.9335773076704,84.9329354412364,
85.9322935748025,86.9316517083685,87.9310098419346,88.9303679755006,89.9297261090666,
90.9290842426327,91.9284423761987,92.9278005097648,93.9271586433308,94.9265167768969,
95.9258749104629,96.925233044029,97.924591177595,98.9239493111611,99.9233074447271,
100.922665578293,101.922023711859,102.921381845425,103.920739978991,104.920098112557,
105.919456246123,106.918814379689,107.918172513255,108.917530646822,109.916888780388,
110.916246913954,111.91560504752,112.914963181086,113.914321314652,114.913679448218,
115.913037581784,116.91239571535,117.911753848916,118.911111982482,119.910470116048,
120.909828249614,121.90918638318,122.908544516746,123.907902650312,124.907260783878,
125.906618917444,126.90597705101,127.905335184576,128.904693318142,129.904051451709,
130.903409585275,131.902767718841,132.902125852407,133.901483985973,134.900842119539,
135.900200253105,136.899558386671,137.898916520237,138.898274653803,139.897632787369,
140.896990920935,141.896349054501,142.895707188067,143.895065321633,144.894423455199,
145.893781588765,146.893139722331,147.892497855897,148.891855989463,149.891214123029,
150.890572256596,151.889930390162,152.889288523728,153.888646657294,154.88800479086,
155.887362924426,156.886721057992,157.886079191558,158.885437325124,159.88479545869,
160.884153592256,161.883511725822,162.882869859388,163.882227992954,164.88158612652,
165.880944260086,166.880302393652,167.879660527218,168.879018660784,169.87837679435,
170.877734927916,171.877093061483,172.876451195049,173.875809328615,174.875167462181,
175.874525595747,176.873883729313,177.873241862879,178.872599996445,179.871958130011,
180.871316263577,181.870674397143,182.870032530709,183.869390664275,184.868748797841,
185.868106931407,186.867465064973,187.866823198539,188.866181332105,189.865539465671,
190.864897599237,191.864255732803,192.86361386637,193.862971999936,194.862330133502,
195.861688267068,196.861046400634,197.8604045342,198.859762667766,199.859120801332,
200.858478934898,201.857837068464,202.85719520203,203.856553335596,204.855911469162,
205.855269602728,206.854627736294,207.85398586986,208.853344003426,209.852702136992,
210.852060270558,211.851418404124,212.85077653769,213.850134671257,214.849492804823,
215.848850938389,216.848209071955,217.847567205521,218.846925339087,219.846283472653,
220.845641606219,221.844999739785,222.844357873351,223.843716006917,224.843074140483,
225.842432274049,226.841790407615,227.841148541181,228.840506674747,229.839864808313,
230.839222941879,231.838581075445,232.837939209011,233.837297342577,234.836655476144,
235.83601360971,236.835371743276,237.834729876842,238.834088010408,239.833446143974,
240.83280427754,241.832162411106,242.831520544672,243.830878678238,244.830236811804,
245.82959494537,246.828953078936,247.828311212502,248.827669346068,249.827027479634,
250.8263856132,251.825743746766,252.825101880332,253.824460013898,254.823818147464,
255.82317628103,256.822534414597,257.821892548163,258.821250681729,259.820608815295,
260.819966948861,261.819325082427,262.818683215993,263.818041349559,264.817399483125,
265.816757616691,266.816115750257,267.815473883823,268.814832017389,269.814190150955,
270.813548284521,271.812906418087,272.812264551653,273.811622685219,274.810980818785,
275.810338952351,276.809697085917,277.809055219484,278.80841335305,279.807771486616,
280.807129620182,281.806487753748,282.805845887314,283.80520402088,284.804562154446,
285.803920288012,286.803278421578,287.802636555144,288.80199468871,289.801352822276,
290.800710955842,291.800069089408,292.799427222974,293.79878535654,294.798143490106,
295.797501623672,296.796859757238,297.796217890804,298.795576024371,299.794934157937,
300.794292291503,301.793650425069,302.793008558635,303.792366692201,304.791724825767,
305.791082959333,306.790441092899,307.789799226465,308.789157360031,309.788515493597,
310.787873627163,311.787231760729,312.786589894295,313.785948027861,314.785306161427,
315.784664294993,316.784022428559,317.783380562125,318.782738695691,319.782096829258,
320.781454962824,321.78081309639,322.780171229956,323.779529363522,324.778887497088,
325.778245630654,326.77760376422,327.776961897786,328.776320031352,329.775678164918,
330.775036298484,331.77439443205,332.773752565616,333.773110699182,334.772468832748,
335.771826966314,336.77118509988,337.770543233446,338.769901367012,339.769259500578,
340.768617634145,341.767975767711,342.767333901277,343.766692034843,344.766050168409,
345.765408301975,346.764766435541,347.764124569107,348.763482702673,349.762840836239,
350.762198969805,351.761557103371,352.760915236937,353.760273370503,354.259952437286,
354.759631504069,355.259310570852,355.758989637635,356.258668704418,356.758347771201,
357.258026837984,357.757705904767,358.25738497155,358.757064038333,359.256743105116,
359.756422171899,360.256101238682,360.755780305465,361.255459372248,361.755138439031,
362.254817505815,362.754496572598,363.254175639381,363.753854706164,364.253533772947,
364.75321283973,365.252891906513,365.752570973296,366.252250040079,366.751929106862,
367.251608173645,367.751287240428,368.250966307211,368.750645373994,369.250324440777,
369.75000350756,370.249682574343,370.749361641126,371.249040707909,371.748719774692,
372.248398841475,372.748077908258,373.247756975041,373.747436041824,374.247115108607,
374.74679417539,375.246473242173,375.746152308956,376.245831375739,376.745510442522,
377.245189509305,377.744868576088,378.244547642871,378.744226709654,379.243905776437,
379.74358484322,380.243263910003,380.742942976786,381.242622043569,381.742301110352,
382.241980177135,382.741659243918,383.241338310702,383.741017377485,384.240696444268,
384.740375511051,385.240054577834,385.739733644617,386.2394127114,386.739091778183,
387.238770844966,387.738449911749,388.238128978532,388.737808045315,389.237487112098,
389.737166178881,390.236845245664,390.736524312447,391.23620337923,391.735882446013,
392.235561512796,392.735240579579,393.234919646362,393.734598713145,394.234277779928,
394.733956846711,395.233635913494,395.733314980277,396.23299404706,396.732673113843,
397.232352180626,397.732031247409,398.231710314192,398.731389380975,399.231068447758,
399.730747514541,400.230426581324,400.730105648107,401.22978471489,401.729463781673,
402.229142848456,402.728821915239,403.228500982022,403.728180048805),
 .UNSPECIFIED.);
#14=B_SPLINE_SURFACE_WITH_KNOTS('',3,3,((#31277,#31278,#31279,#31280,#31281,
#31282,#31283,#31284,#31285,#31286,#31287,#31288,#31289,#31290,#31291,#31292,
#31293,#31294,#31295,#31296,#31297,#31298,#31299,#31300,#31301,#31302,#31303,
#31304,#31305,#31306,#31307,#31308,#31309,#31310,#31311,#31312,#31313,#31314,
#31315,#31316,#31317,#31318,#31319,#31320,#31321,#31322,#31323,#31324,#31325,
#31326,#31327,#31328,#31329,#31330,#31331,#31332,#31333,#31334,#31335,#31336,
#31337,#31338,#31339,#31340,#31341,#31342,#31343,#31344,#31345,#31346,#31347,
#31348,#31349,#31350,#31351,#31352,#31353,#31354,#31355,#31356,#31357,#31358,
#31359,#31360,#31361,#31362,#31363,#31364,#31365,#31366,#31367,#31368,#31369,
#31370,#31371,#31372,#31373,#31374,#31375,#31376,#31377,#31378,#31379,#31380,
#31381,#31382,#31383,#31384,#31385,#31386,#31387,#31388,#31389,#31390,#31391,
#31392,#31393,#31394,#31395,#31396,#31397,#31398,#31399,#31400,#31401,#31402,
#31403,#31404,#31405,#31406,#31407,#31408,#31409,#31410,#31411,#31412,#31413,
#31414,#31415,#31416,#31417,#31418,#31419,#31420,#31421,#31422,#31423,#31424,
#31425,#31426,#31427,#31428,#31429,#31430,#31431,#31432,#31433,#31434,#31435,
#31436,#31437,#31438,#31439,#31440,#31441,#31442,#31443,#31444,#31445,#31446,
#31447,#31448,#31449,#31450,#31451,#31452,#31453,#31454,#31455,#31456,#31457,
#31458,#31459,#31460,#31461,#31462,#31463,#31464,#31465,#31466,#31467,#31468,
#31469,#31470,#31471,#31472,#31473,#31474,#31475,#31476,#31477,#31478,#31479,
#31480,#31481,#31482,#31483,#31484,#31485,#31486,#31487,#31488,#31489,#31490,
#31491,#31492,#31493,#31494,#31495,#31496,#31497,#31498,#31499,#31500,#31501,
#31502,#31503,#31504,#31505,#31506,#31507,#31508,#31509,#31510,#31511,#31512,
#31513,#31514,#31515,#31516,#31517,#31518,#31519,#31520,#31521,#31522,#31523,
#31524,#31525,#31526,#31527,#31528,#31529,#31530,#31531,#31532,#31533,#31534,
#31535,#31536,#31537,#31538,#31539,#31540,#31541,#31542,#31543,#31544,#31545,
#31546,#31547,#31548,#31549,#31550,#31551,#31552,#31553,#31554,#31555,#31556,
#31557,#31558,#31559,#31560,#31561,#31562,#31563,#31564,#31565,#31566,#31567,
#31568,#31569,#31570,#31571,#31572,#31573,#31574,#31575,#31576,#31577,#31578,
#31579,#31580,#31581,#31582,#31583,#31584,#31585,#31586,#31587,#31588,#31589,
#31590,#31591,#31592,#31593,#31594,#31595,#31596,#31597,#31598,#31599,#31600,
#31601,#31602,#31603,#31604,#31605,#31606,#31607,#31608,#31609,#31610,#31611,
#31612,#31613,#31614,#31615,#31616,#31617,#31618,#31619,#31620,#31621,#31622,
#31623,#31624,#31625,#31626,#31627,#31628,#31629,#31630,#31631,#31632,#31633,
#31634,#31635,#31636,#31637,#31638,#31639,#31640,#31641,#31642,#31643,#31644,
#31645,#31646,#31647,#31648,#31649,#31650,#31651,#31652,#31653,#31654,#31655,
#31656,#31657,#31658,#31659,#31660,#31661,#31662,#31663,#31664,#31665,#31666,
#31667,#31668,#31669,#31670,#31671,#31672,#31673,#31674,#31675,#31676,#31677,
#31678,#31679,#31680,#31681,#31682,#31683,#31684,#31685,#31686,#31687,#31688,
#31689,#31690,#31691,#31692,#31693,#31694,#31695,#31696,#31697,#31698,#31699,
#31700,#31701,#31702,#31703,#31704,#31705,#31706,#31707,#31708,#31709,#31710,
#31711,#31712,#31713,#31714,#31715,#31716,#31717,#31718,#31719,#31720,#31721,
#31722,#31723,#31724,#31725,#31726,#31727,#31728,#31729,#31730,#31731,#31732,
#31733,#31734,#31735,#31736,#31737,#31738,#31739,#31740,#31741,#31742,#31743,
#31744,#31745,#31746,#31747,#31748,#31749,#31750,#31751,#31752,#31753,#31754,
#31755,#31756,#31757,#31758,#31759,#31760,#31761,#31762,#31763,#31764,#31765,
#31766,#31767,#31768,#31769,#31770,#31771,#31772,#31773,#31774),(#31775,
#31776,#31777,#31778,#31779,#31780,#31781,#31782,#31783,#31784,#31785,#31786,
#31787,#31788,#31789,#31790,#31791,#31792,#31793,#31794,#31795,#31796,#31797,
#31798,#31799,#31800,#31801,#31802,#31803,#31804,#31805,#31806,#31807,#31808,
#31809,#31810,#31811,#31812,#31813,#31814,#31815,#31816,#31817,#31818,#31819,
#31820,#31821,#31822,#31823,#31824,#31825,#31826,#31827,#31828,#31829,#31830,
#31831,#31832,#31833,#31834,#31835,#31836,#31837,#31838,#31839,#31840,#31841,
#31842,#31843,#31844,#31845,#31846,#31847,#31848,#31849,#31850,#31851,#31852,
#31853,#31854,#31855,#31856,#31857,#31858,#31859,#31860,#31861,#31862,#31863,
#31864,#31865,#31866,#31867,#31868,#31869,#31870,#31871,#31872,#31873,#31874,
#31875,#31876,#31877,#31878,#31879,#31880,#31881,#31882,#31883,#31884,#31885,
#31886,#31887,#31888,#31889,#31890,#31891,#31892,#31893,#31894,#31895,#31896,
#31897,#31898,#31899,#31900,#31901,#31902,#31903,#31904,#31905,#31906,#31907,
#31908,#31909,#31910,#31911,#31912,#31913,#31914,#31915,#31916,#31917,#31918,
#31919,#31920,#31921,#31922,#31923,#31924,#31925,#31926,#31927,#31928,#31929,
#31930,#31931,#31932,#31933,#31934,#31935,#31936,#31937,#31938,#31939,#31940,
#31941,#31942,#31943,#31944,#31945,#31946,#31947,#31948,#31949,#31950,#31951,
#31952,#31953,#31954,#31955,#31956,#31957,#31958,#31959,#31960,#31961,#31962,
#31963,#31964,#31965,#31966,#31967,#31968,#31969,#31970,#31971,#31972,#31973,
#31974,#31975,#31976,#31977,#31978,#31979,#31980,#31981,#31982,#31983,#31984,
#31985,#31986,#31987,#31988,#31989,#31990,#31991,#31992,#31993,#31994,#31995,
#31996,#31997,#31998,#31999,#32000,#32001,#32002,#32003,#32004,#32005,#32006,
#32007,#32008,#32009,#32010,#32011,#32012,#32013,#32014,#32015,#32016,#32017,
#32018,#32019,#32020,#32021,#32022,#32023,#32024,#32025,#32026,#32027,#32028,
#32029,#32030,#32031,#32032,#32033,#32034,#32035,#32036,#32037,#32038,#32039,
#32040,#32041,#32042,#32043,#32044,#32045,#32046,#32047,#32048,#32049,#32050,
#32051,#32052,#32053,#32054,#32055,#32056,#32057,#32058,#32059,#32060,#32061,
#32062,#32063,#32064,#32065,#32066,#32067,#32068,#32069,#32070,#32071,#32072,
#32073,#32074,#32075,#32076,#32077,#32078,#32079,#32080,#32081,#32082,#32083,
#32084,#32085,#32086,#32087,#32088,#32089,#32090,#32091,#32092,#32093,#32094,
#32095,#32096,#32097,#32098,#32099,#32100,#32101,#32102,#32103,#32104,#32105,
#32106,#32107,#32108,#32109,#32110,#32111,#32112,#32113,#32114,#32115,#32116,
#32117,#32118,#32119,#32120,#32121,#32122,#32123,#32124,#32125,#32126,#32127,
#32128,#32129,#32130,#32131,#32132,#32133,#32134,#32135,#32136,#32137,#32138,
#32139,#32140,#32141,#32142,#32143,#32144,#32145,#32146,#32147,#32148,#32149,
#32150,#32151,#32152,#32153,#32154,#32155,#32156,#32157,#32158,#32159,#32160,
#32161,#32162,#32163,#32164,#32165,#32166,#32167,#32168,#32169,#32170,#32171,
#32172,#32173,#32174,#32175,#32176,#32177,#32178,#32179,#32180,#32181,#32182,
#32183,#32184,#32185,#32186,#32187,#32188,#32189,#32190,#32191,#32192,#32193,
#32194,#32195,#32196,#32197,#32198,#32199,#32200,#32201,#32202,#32203,#32204,
#32205,#32206,#32207,#32208,#32209,#32210,#32211,#32212,#32213,#32214,#32215,
#32216,#32217,#32218,#32219,#32220,#32221,#32222,#32223,#32224,#32225,#32226,
#32227,#32228,#32229,#32230,#32231,#32232,#32233,#32234,#32235,#32236,#32237,
#32238,#32239,#32240,#32241,#32242,#32243,#32244,#32245,#32246,#32247,#32248,
#32249,#32250,#32251,#32252,#32253,#32254,#32255,#32256,#32257,#32258,#32259,
#32260,#32261,#32262,#32263,#32264,#32265,#32266,#32267,#32268,#32269,#32270,
#32271,#32272),(#32273,#32274,#32275,#32276,#32277,#32278,#32279,#32280,
#32281,#32282,#32283,#32284,#32285,#32286,#32287,#32288,#32289,#32290,#32291,
#32292,#32293,#32294,#32295,#32296,#32297,#32298,#32299,#32300,#32301,#32302,
#32303,#32304,#32305,#32306,#32307,#32308,#32309,#32310,#32311,#32312,#32313,
#32314,#32315,#32316,#32317,#32318,#32319,#32320,#32321,#32322,#32323,#32324,
#32325,#32326,#32327,#32328,#32329,#32330,#32331,#32332,#32333,#32334,#32335,
#32336,#32337,#32338,#32339,#32340,#32341,#32342,#32343,#32344,#32345,#32346,
#32347,#32348,#32349,#32350,#32351,#32352,#32353,#32354,#32355,#32356,#32357,
#32358,#32359,#32360,#32361,#32362,#32363,#32364,#32365,#32366,#32367,#32368,
#32369,#32370,#32371,#32372,#32373,#32374,#32375,#32376,#32377,#32378,#32379,
#32380,#32381,#32382,#32383,#32384,#32385,#32386,#32387,#32388,#32389,#32390,
#32391,#32392,#32393,#32394,#32395,#32396,#32397,#32398,#32399,#32400,#32401,
#32402,#32403,#32404,#32405,#32406,#32407,#32408,#32409,#32410,#32411,#32412,
#32413,#32414,#32415,#32416,#32417,#32418,#32419,#32420,#32421,#32422,#32423,
#32424,#32425,#32426,#32427,#32428,#32429,#32430,#32431,#32432,#32433,#32434,
#32435,#32436,#32437,#32438,#32439,#32440,#32441,#32442,#32443,#32444,#32445,
#32446,#32447,#32448,#32449,#32450,#32451,#32452,#32453,#32454,#32455,#32456,
#32457,#32458,#32459,#32460,#32461,#32462,#32463,#32464,#32465,#32466,#32467,
#32468,#32469,#32470,#32471,#32472,#32473,#32474,#32475,#32476,#32477,#32478,
#32479,#32480,#32481,#32482,#32483,#32484,#32485,#32486,#32487,#32488,#32489,
#32490,#32491,#32492,#32493,#32494,#32495,#32496,#32497,#32498,#32499,#32500,
#32501,#32502,#32503,#32504,#32505,#32506,#32507,#32508,#32509,#32510,#32511,
#32512,#32513,#32514,#32515,#32516,#32517,#32518,#32519,#32520,#32521,#32522,
#32523,#32524,#32525,#32526,#32527,#32528,#32529,#32530,#32531,#32532,#32533,
#32534,#32535,#32536,#32537,#32538,#32539,#32540,#32541,#32542,#32543,#32544,
#32545,#32546,#32547,#32548,#32549,#32550,#32551,#32552,#32553,#32554,#32555,
#32556,#32557,#32558,#32559,#32560,#32561,#32562,#32563,#32564,#32565,#32566,
#32567,#32568,#32569,#32570,#32571,#32572,#32573,#32574,#32575,#32576,#32577,
#32578,#32579,#32580,#32581,#32582,#32583,#32584,#32585,#32586,#32587,#32588,
#32589,#32590,#32591,#32592,#32593,#32594,#32595,#32596,#32597,#32598,#32599,
#32600,#32601,#32602,#32603,#32604,#32605,#32606,#32607,#32608,#32609,#32610,
#32611,#32612,#32613,#32614,#32615,#32616,#32617,#32618,#32619,#32620,#32621,
#32622,#32623,#32624,#32625,#32626,#32627,#32628,#32629,#32630,#32631,#32632,
#32633,#32634,#32635,#32636,#32637,#32638,#32639,#32640,#32641,#32642,#32643,
#32644,#32645,#32646,#32647,#32648,#32649,#32650,#32651,#32652,#32653,#32654,
#32655,#32656,#32657,#32658,#32659,#32660,#32661,#32662,#32663,#32664,#32665,
#32666,#32667,#32668,#32669,#32670,#32671,#32672,#32673,#32674,#32675,#32676,
#32677,#32678,#32679,#32680,#32681,#32682,#32683,#32684,#32685,#32686,#32687,
#32688,#32689,#32690,#32691,#32692,#32693,#32694,#32695,#32696,#32697,#32698,
#32699,#32700,#32701,#32702,#32703,#32704,#32705,#32706,#32707,#32708,#32709,
#32710,#32711,#32712,#32713,#32714,#32715,#32716,#32717,#32718,#32719,#32720,
#32721,#32722,#32723,#32724,#32725,#32726,#32727,#32728,#32729,#32730,#32731,
#32732,#32733,#32734,#32735,#32736,#32737,#32738,#32739,#32740,#32741,#32742,
#32743,#32744,#32745,#32746,#32747,#32748,#32749,#32750,#32751,#32752,#32753,
#32754,#32755,#32756,#32757,#32758,#32759,#32760,#32761,#32762,#32763,#32764,
#32765,#32766,#32767,#32768,#32769,#32770),(#32771,#32772,#32773,#32774,
#32775,#32776,#32777,#32778,#32779,#32780,#32781,#32782,#32783,#32784,#32785,
#32786,#32787,#32788,#32789,#32790,#32791,#32792,#32793,#32794,#32795,#32796,
#32797,#32798,#32799,#32800,#32801,#32802,#32803,#32804,#32805,#32806,#32807,
#32808,#32809,#32810,#32811,#32812,#32813,#32814,#32815,#32816,#32817,#32818,
#32819,#32820,#32821,#32822,#32823,#32824,#32825,#32826,#32827,#32828,#32829,
#32830,#32831,#32832,#32833,#32834,#32835,#32836,#32837,#32838,#32839,#32840,
#32841,#32842,#32843,#32844,#32845,#32846,#32847,#32848,#32849,#32850,#32851,
#32852,#32853,#32854,#32855,#32856,#32857,#32858,#32859,#32860,#32861,#32862,
#32863,#32864,#32865,#32866,#32867,#32868,#32869,#32870,#32871,#32872,#32873,
#32874,#32875,#32876,#32877,#32878,#32879,#32880,#32881,#32882,#32883,#32884,
#32885,#32886,#32887,#32888,#32889,#32890,#32891,#32892,#32893,#32894,#32895,
#32896,#32897,#32898,#32899,#32900,#32901,#32902,#32903,#32904,#32905,#32906,
#32907,#32908,#32909,#32910,#32911,#32912,#32913,#32914,#32915,#32916,#32917,
#32918,#32919,#32920,#32921,#32922,#32923,#32924,#32925,#32926,#32927,#32928,
#32929,#32930,#32931,#32932,#32933,#32934,#32935,#32936,#32937,#32938,#32939,
#32940,#32941,#32942,#32943,#32944,#32945,#32946,#32947,#32948,#32949,#32950,
#32951,#32952,#32953,#32954,#32955,#32956,#32957,#32958,#32959,#32960,#32961,
#32962,#32963,#32964,#32965,#32966,#32967,#32968,#32969,#32970,#32971,#32972,
#32973,#32974,#32975,#32976,#32977,#32978,#32979,#32980,#32981,#32982,#32983,
#32984,#32985,#32986,#32987,#32988,#32989,#32990,#32991,#32992,#32993,#32994,
#32995,#32996,#32997,#32998,#32999,#33000,#33001,#33002,#33003,#33004,#33005,
#33006,#33007,#33008,#33009,#33010,#33011,#33012,#33013,#33014,#33015,#33016,
#33017,#33018,#33019,#33020,#33021,#33022,#33023,#33024,#33025,#33026,#33027,
#33028,#33029,#33030,#33031,#33032,#33033,#33034,#33035,#33036,#33037,#33038,
#33039,#33040,#33041,#33042,#33043,#33044,#33045,#33046,#33047,#33048,#33049,
#33050,#33051,#33052,#33053,#33054,#33055,#33056,#33057,#33058,#33059,#33060,
#33061,#33062,#33063,#33064,#33065,#33066,#33067,#33068,#33069,#33070,#33071,
#33072,#33073,#33074,#33075,#33076,#33077,#33078,#33079,#33080,#33081,#33082,
#33083,#33084,#33085,#33086,#33087,#33088,#33089,#33090,#33091,#33092,#33093,
#33094,#33095,#33096,#33097,#33098,#33099,#33100,#33101,#33102,#33103,#33104,
#33105,#33106,#33107,#33108,#33109,#33110,#33111,#33112,#33113,#33114,#33115,
#33116,#33117,#33118,#33119,#33120,#33121,#33122,#33123,#33124,#33125,#33126,
#33127,#33128,#33129,#33130,#33131,#33132,#33133,#33134,#33135,#33136,#33137,
#33138,#33139,#33140,#33141,#33142,#33143,#33144,#33145,#33146,#33147,#33148,
#33149,#33150,#33151,#33152,#33153,#33154,#33155,#33156,#33157,#33158,#33159,
#33160,#33161,#33162,#33163,#33164,#33165,#33166,#33167,#33168,#33169,#33170,
#33171,#33172,#33173,#33174,#33175,#33176,#33177,#33178,#33179,#33180,#33181,
#33182,#33183,#33184,#33185,#33186,#33187,#33188,#33189,#33190,#33191,#33192,
#33193,#33194,#33195,#33196,#33197,#33198,#33199,#33200,#33201,#33202,#33203,
#33204,#33205,#33206,#33207,#33208,#33209,#33210,#33211,#33212,#33213,#33214,
#33215,#33216,#33217,#33218,#33219,#33220,#33221,#33222,#33223,#33224,#33225,
#33226,#33227,#33228,#33229,#33230,#33231,#33232,#33233,#33234,#33235,#33236,
#33237,#33238,#33239,#33240,#33241,#33242,#33243,#33244,#33245,#33246,#33247,
#33248,#33249,#33250,#33251,#33252,#33253,#33254,#33255,#33256,#33257,#33258,
#33259,#33260,#33261,#33262,#33263,#33264,#33265,#33266,#33267,#33268)),
 .UNSPECIFIED.,.F.,.F.,.F.,(4,4),(4,1,1,1,1,1,1,1,1,1,1,1,1,1,1,1,1,1,1,
1,1,1,1,1,1,1,1,1,1,1,1,1,1,1,1,1,1,1,1,1,1,1,1,1,1,1,1,1,1,1,1,1,1,1,1,
1,1,1,1,1,1,1,1,1,1,1,1,1,1,1,1,1,1,1,1,1,1,1,1,1,1,1,1,1,1,1,1,1,1,1,1,
1,1,1,1,1,1,1,1,1,1,1,1,1,1,1,1,1,1,1,1,1,1,1,1,1,1,1,1,1,1,1,1,1,1,1,1,
1,1,1,1,1,1,1,1,1,1,1,1,1,1,1,1,1,1,1,1,1,1,1,1,1,1,1,1,1,1,1,1,1,1,1,1,
1,1,1,1,1,1,1,1,1,1,1,1,1,1,1,1,1,1,1,1,1,1,1,1,1,1,1,1,1,1,1,1,1,1,1,1,
1,1,1,1,1,1,1,1,1,1,1,1,1,1,1,1,1,1,1,1,1,1,1,1,1,1,1,1,1,1,1,1,1,1,1,1,
1,1,1,1,1,1,1,1,1,1,1,1,1,1,1,1,1,1,1,1,1,1,1,1,1,1,1,1,1,1,1,1,1,1,1,1,
1,1,1,1,1,1,1,1,1,1,1,1,1,1,1,1,1,1,1,1,1,1,1,1,1,1,1,1,1,1,1,1,1,1,1,1,
1,1,1,1,1,1,1,1,1,1,1,1,1,1,1,1,1,1,1,1,1,1,1,1,1,1,1,1,1,1,1,1,1,1,1,1,
1,1,1,1,1,1,1,1,1,1,1,1,1,1,1,1,1,1,1,1,1,1,1,1,1,1,1,1,1,1,1,1,1,1,1,1,
1,1,1,1,1,1,1,1,1,1,1,1,1,1,1,1,1,1,1,1,1,1,1,1,1,1,1,1,1,1,1,1,1,1,1,1,
1,1,1,1,1,1,1,1,1,1,1,1,1,1,1,1,1,1,1,1,1,1,1,1,1,1,1,1,1,1,1,1,1,1,1,1,
1,1,1,1,1,1,1,1,1,1,1,1,1,1,1,1,1,1,1,1,1,1,1,1,1,1,1,1,1,1,1,1,1,1,1,1,
1,1,1,1,1,1,1,1,4),(0.,0.184512097253587),(12.0092477762453,12.5089268430284,
13.0086059098114,13.5082849765944,14.0079640433774,14.5076431101605,15.0073221769435,
15.5070012437265,16.0066803105095,16.5063593772925,17.0060384440756,17.5057175108586,
18.0053965776416,18.5050756444246,19.0047547112077,19.5044337779907,20.0041128447737,
20.5037919115567,21.0034709783398,21.5031500451228,22.0028291119058,22.5025081786888,
23.0021872454719,23.5018663122549,24.0015453790379,24.5012244458209,25.0009035126039,
25.500582579387,26.00026164617,26.499940712953,26.999619779736,27.4992988465191,
27.9989779133021,28.4986569800851,28.9983360468681,29.4980151136512,29.9976941804342,
30.4973732472172,30.9970523140002,31.4967313807832,31.9964104475663,32.4960895143493,
32.9957685811323,33.4954476479153,33.9951267146984,34.4948057814814,34.9944848482644,
35.4941639150474,35.9938429818305,36.4935220486135,36.9932011153965,37.4928801821795,
37.9925592489626,38.4922383157456,38.9919173825286,39.4915964493116,39.9912755160946,
40.4909545828777,40.9906336496607,41.4903127164437,41.9899917832267,42.4896708500098,
42.9893499167928,43.4890289835758,43.9887080503588,44.4883871171419,44.9880661839249,
45.4877452507079,45.9874243174909,46.4871033842739,46.986782451057,47.48646151784,
47.986140584623,48.485819651406,48.9854987181891,49.4851777849721,49.9848568517551,
50.4845359185381,50.9842149853212,51.4838940521042,51.9835731188872,52.4832521856702,
52.9829312524532,53.4826103192363,53.9822893860193,54.4819684528023,54.9816475195853,
55.4813265863684,55.9810056531514,56.4806847199344,56.9803637867174,57.4800428535005,
57.9797219202835,58.4794009870665,58.9790800538495,59.4787591206325,59.9784381874156,
60.4781172541986,60.9777963209816,61.4774753877646,61.9771544545477,62.9765125881137,
63.9758707216798,64.9752288552458,65.9745869888119,66.9739451223779,67.9733032559439,
68.97266138951,69.972019523076,70.9713776566421,71.9707357902081,72.9700939237742,
73.9694520573402,74.9688101909063,75.9681683244723,76.9675264580384,77.9668845916044,
78.9662427251705,79.9656008587365,80.9649589923026,81.9643171258686,82.9636752594347,
83.9630333930007,84.9623915265667,85.9617496601328,86.9611077936988,87.9604659272649,
88.9598240608309,89.959182194397,90.958540327963,91.9578984615291,92.9572565950951,
93.9566147286612,94.9559728622272,95.9553309957932,96.9546891293593,97.9540472629253,
98.9534053964914,99.9527635300574,100.952121663623,101.95147979719,102.950837930756,
103.950196064322,104.949554197888,105.948912331454,106.94827046502,107.947628598586,
108.946986732152,109.946344865718,110.945702999284,111.94506113285,112.944419266416,
113.943777399982,114.943135533548,115.942493667114,116.94185180068,117.941209934246,
118.940568067812,119.939926201378,120.939284334944,121.93864246851,122.938000602077,
123.937358735643,124.936716869209,125.936075002775,126.935433136341,127.934791269907,
128.934149403473,129.933507537039,130.932865670605,131.932223804171,132.931581937737,
133.930940071303,134.930298204869,135.929656338435,136.929014472001,137.928372605567,
138.927730739133,139.927088872699,140.926447006265,141.925805139831,142.925163273397,
143.924521406963,144.92387954053,145.923237674096,146.922595807662,147.921953941228,
148.921312074794,149.92067020836,150.920028341926,151.919386475492,152.918744609058,
153.918102742624,154.91746087619,155.916819009756,156.916177143322,157.915535276888,
158.914893410454,159.91425154402,160.913609677586,161.912967811152,162.912325944718,
163.911684078284,164.91104221185,165.910400345416,166.909758478983,167.909116612549,
168.908474746115,169.907832879681,170.907191013247,171.906549146813,172.905907280379,
173.905265413945,174.904623547511,175.903981681077,176.903339814643,177.902697948209,
178.902056081775,179.901414215341,180.900772348907,181.900130482473,182.899488616039,
183.898846749605,184.898204883171,185.897563016737,186.896921150303,187.89627928387,
188.895637417436,189.894995551002,190.894353684568,191.893711818134,192.8930699517,
193.892428085266,194.891786218832,195.891144352398,196.890502485964,197.88986061953,
198.889218753096,199.888576886662,200.887935020228,201.887293153794,202.88665128736,
203.886009420926,204.885367554492,205.884725688058,206.884083821624,207.88344195519,
208.882800088756,209.882158222323,210.881516355889,211.880874489455,212.880232623021,
213.879590756587,214.878948890153,215.878307023719,216.877665157285,217.877023290851,
218.876381424417,219.875739557983,220.875097691549,221.874455825115,222.873813958681,
223.873172092247,224.872530225813,225.871888359379,226.871246492945,227.870604626511,
228.869962760077,229.869320893643,230.86867902721,231.868037160776,232.867395294342,
233.866753427908,234.866111561474,235.86546969504,236.864827828606,237.864185962172,
238.863544095738,239.862902229304,240.86226036287,241.861618496436,242.860976630002,
243.860334763568,244.859692897134,245.8590510307,246.858409164266,247.857767297832,
248.857125431398,249.856483564964,250.85584169853,251.855199832097,252.854557965663,
253.853916099229,254.853274232795,255.852632366361,256.851990499927,257.851348633493,
258.850706767059,259.850064900625,260.849423034191,261.848781167757,262.848139301323,
263.847497434889,264.846855568455,265.846213702021,266.845571835587,267.844929969153,
268.844288102719,269.843646236285,270.843004369851,271.842362503417,272.841720636983,
273.84107877055,274.840436904116,275.839795037682,276.839153171248,277.838511304814,
278.83786943838,279.837227571946,280.836585705512,281.835943839078,282.835301972644,
283.83466010621,284.834018239776,285.833376373342,286.832734506908,287.832092640474,
288.83145077404,289.830808907606,290.830167041172,291.829525174738,292.828883308304,
293.82824144187,294.827599575437,295.826957709003,296.826315842569,297.825673976135,
298.825032109701,299.824390243267,300.823748376833,301.823106510399,302.822464643965,
303.821822777531,304.821180911097,305.820539044663,306.819897178229,307.819255311795,
308.818613445361,309.817971578927,310.817329712493,311.816687846059,312.816045979625,
313.815404113191,314.814762246757,315.814120380323,316.81347851389,317.812836647456,
318.812194781022,319.811552914588,320.810911048154,321.81026918172,322.809627315286,
323.808985448852,324.808343582418,325.807701715984,326.80705984955,327.806417983116,
328.805776116682,329.805134250248,330.804492383814,331.80385051738,332.803208650946,
333.802566784512,334.801924918078,335.801283051644,336.80064118521,337.799999318776,
338.799357452343,339.798715585909,340.798073719475,341.797431853041,342.796789986607,
343.796148120173,344.795506253739,345.794864387305,346.794222520871,347.793580654437,
348.792938788003,349.792296921569,350.791655055135,351.791013188701,352.790371322267,
353.789729455833,354.789087589399,355.788445722965,356.787803856531,357.287482923314,
357.787161990097,358.28684105688,358.786520123663,359.286199190446,359.78587825723,
360.285557324013,360.785236390796,361.284915457579,361.784594524362,362.284273591145,
362.783952657928,363.283631724711,363.783310791494,364.282989858277,364.78266892506,
365.282347991843,365.782027058626,366.281706125409,366.781385192192,367.281064258975,
367.780743325758,368.280422392541,368.780101459324,369.279780526107,369.77945959289,
370.279138659673,370.778817726456,371.278496793239,371.778175860022,372.277854926805,
372.777533993588,373.277213060371,373.776892127154,374.276571193937,374.77625026072,
375.275929327503,375.775608394286,376.275287461069,376.774966527852,377.274645594635,
377.774324661418,378.274003728201,378.773682794984,379.273361861767,379.77304092855,
380.272719995333,380.772399062117,381.2720781289,381.771757195683,382.271436262466,
382.771115329249,383.270794396032,383.770473462815,384.270152529598,384.769831596381,
385.269510663164,385.769189729947,386.26886879673,386.768547863513,387.268226930296,
387.767905997079,388.267585063862,388.767264130645,389.266943197428,389.766622264211,
390.266301330994,390.765980397777,391.26565946456,391.765338531343,392.265017598126,
392.764696664909,393.264375731692,393.764054798475,394.263733865258,394.763412932041,
395.263091998824,395.762771065607,396.26245013239,396.762129199173,397.261808265956,
397.761487332739,398.261166399522,398.760845466305,399.260524533088,399.760203599871,
400.259882666654,400.759561733437,401.25924080022,401.758919867003,402.258598933787,
402.75827800057,403.257957067353,403.757636134136,404.257315200919,404.756994267702,
405.256673334485,405.756352401268,406.256031468051,406.755710534834),
 .UNSPECIFIED.);
#478=B_SPLINE_CURVE_WITH_KNOTS('',3,(#23709,#23710,#23711,#23712,#23713,
#23714,#23715,#23716,#23717,#23718,#23719,#23720,#23721,#23722,#23723,#23724,
#23725,#23726,#23727),.UNSPECIFIED.,.F.,.F.,(4,3,3,3,3,3,4),(-3.69871549170445,
-3.49775346748116,-2.99807440069814,-2.49839533391511,-1.99871626713209,
-1.49903720034907,-1.00018350866767),.UNSPECIFIED.);
#479=B_SPLINE_CURVE_WITH_KNOTS('',3,(#23730,#23731,#23732,#23733),
 .UNSPECIFIED.,.F.,.F.,(4,4),(0.,0.443060670554495),.UNSPECIFIED.);
#480=B_SPLINE_CURVE_WITH_KNOTS('',3,(#23738,#23739,#23740,#23741,#23742,
#23743,#23744,#23745,#23746,#23747,#23748,#23749,#23750,#23751,#23752,#23753,
#23754,#23755,#23756,#23757,#23758,#23759,#23760,#23761,#23762,#23763,#23764,
#23765,#23766,#23767,#23768,#23769,#23770,#23771,#23772,#23773,#23774,#23775,
#23776,#23777),.UNSPECIFIED.,.F.,.F.,(4,3,3,3,3,3,3,3,3,3,3,3,3,4),(-9.98190079888403,
-9.49390226887744,-8.99422320209442,-8.4945441353114,-7.99486506852837,
-7.49518600174535,-6.99550693496233,-6.4958278681793,-5.99614880139628,
-5.49646973461325,-4.99679066783023,-4.49711160104721,-3.99743253426419,
-3.69871549170445),.UNSPECIFIED.);
#481=B_SPLINE_CURVE_WITH_KNOTS('',3,(#23778,#23779,#23780,#23781,#23782,
#23783,#23784,#23785,#23786,#23787,#23788,#23789,#23790,#23791,#23792,#23793,
#23794,#23795,#23796,#23797,#23798,#23799,#23800,#23801,#23802,#23803,#23804,
#23805,#23806,#23807,#23808,#23809,#23810,#23811,#23812,#23813,#23814,#23815,
#23816,#23817,#23818,#23819,#23820),.UNSPECIFIED.,.F.,.F.,(4,3,3,3,3,3,
3,3,3,3,3,3,3,3,4),(0.443060670554495,0.49967906678306,0.999358133566079,
1.4990372003491,1.99871626713212,2.49839533391514,2.99807440069816,3.49775346748117,
3.99743253426419,4.49711160104721,4.99679066783023,5.49646973461325,5.99614880139627,
6.49582786817929,6.72624597773408),.UNSPECIFIED.);
#482=B_SPLINE_CURVE_WITH_KNOTS('',3,(#23825,#23826,#23827,#23828,#23829,
#23830,#23831,#23832,#23833,#23834,#23835,#23836,#23837,#23838,#23839,#23840,
#23841,#23842,#23843,#23844,#23845,#23846,#23847,#23848,#23849,#23850,#23851,
#23852,#23853,#23854,#23855,#23856,#23857,#23858,#23859,#23860,#23861,#23862,
#23863,#23864,#23865,#23866,#23867),.UNSPECIFIED.,.F.,.F.,(4,3,3,3,3,3,
3,3,3,3,3,3,3,3,4),(-16.2650861060636,-15.9897301370567,-15.4900510702737,
-14.9903720034907,-14.4906929367077,-13.9910138699247,-13.4913348031416,
-12.9916557363586,-12.4919766695756,-11.9922976027926,-11.4926185360095,
-10.9929394692265,-10.4932604024435,-9.99358133566046,-9.98190079888403),
 .UNSPECIFIED.);
#483=B_SPLINE_CURVE_WITH_KNOTS('',3,(#23868,#23869,#23870,#23871,#23872,
#23873,#23874,#23875,#23876,#23877,#23878,#23879,#23880,#23881,#23882,#23883,
#23884,#23885,#23886,#23887,#23888,#23889,#23890,#23891,#23892,#23893,#23894,
#23895,#23896,#23897,#23898,#23899,#23900,#23901,#23902,#23903,#23904,#23905,
#23906,#23907,#23908,#23909,#23910),.UNSPECIFIED.,.F.,.F.,(4,3,3,3,3,3,
3,3,3,3,3,3,3,3,4),(6.72624597773408,6.99550693496231,7.49518600174534,
7.99486506852837,8.49454413531139,8.99422320209442,9.49390226887745,9.99358133566048,
10.4932604024435,10.9929394692265,11.4926185360096,11.9922976027926,12.4919766695756,
12.9916557363586,13.0094312849137),.UNSPECIFIED.);
#484=B_SPLINE_CURVE_WITH_KNOTS('',3,(#23915,#23916,#23917,#23918,#23919,
#23920,#23921,#23922,#23923,#23924,#23925,#23926,#23927,#23928,#23929,#23930,
#23931,#23932,#23933,#23934,#23935,#23936,#23937,#23938,#23939,#23940,#23941,
#23942,#23943,#23944,#23945,#23946,#23947,#23948,#23949,#23950,#23951,#23952,
#23953,#23954,#23955,#23956,#23957),.UNSPECIFIED.,.F.,.F.,(4,3,3,3,3,3,
3,3,3,3,3,3,3,3,4),(-22.5482714132432,-22.485558005236,-21.985878938453,
-21.48619987167,-20.986520804887,-20.486841738104,-19.9871626713209,-19.4874836045379,
-18.9878045377549,-18.4881254709719,-17.9884464041888,-17.4887673374058,
-16.9890882706228,-16.4894092038398,-16.2650861060636),.UNSPECIFIED.);
#485=B_SPLINE_CURVE_WITH_KNOTS('',3,(#23958,#23959,#23960,#23961,#23962,
#23963,#23964,#23965,#23966,#23967,#23968,#23969,#23970,#23971,#23972,#23973,
#23974,#23975,#23976,#23977,#23978,#23979,#23980,#23981,#23982,#23983,#23984,
#23985,#23986,#23987,#23988,#23989,#23990,#23991,#23992,#23993,#23994,#23995,
#23996,#23997),.UNSPECIFIED.,.F.,.F.,(4,3,3,3,3,3,3,3,3,3,3,3,3,4),(13.0094312849137,
13.4913348031417,13.9910138699247,14.4906929367077,14.9903720034907,15.4900510702737,
15.9897301370568,16.4894092038398,16.9890882706228,17.4887673374058,17.9884464041888,
18.4881254709718,18.9878045377549,19.2926165920933),.UNSPECIFIED.);
#486=B_SPLINE_CURVE_WITH_KNOTS('',3,(#24002,#24003,#24004,#24005,#24006,
#24007,#24008,#24009,#24010,#24011,#24012,#24013,#24014,#24015,#24016,#24017,
#24018,#24019,#24020,#24021,#24022,#24023,#24024,#24025,#24026,#24027,#24028,
#24029,#24030,#24031,#24032,#24033,#24034,#24035,#24036,#24037,#24038,#24039,
#24040,#24041),.UNSPECIFIED.,.F.,.F.,(4,3,3,3,3,3,3,3,3,3,3,3,3,4),(-28.8314567204228,
-28.4817068066323,-27.9820277398493,-27.4823486730663,-26.9826696062833,
-26.4829905395002,-25.9833114727172,-25.4836324059342,-24.9839533391512,
-24.4842742723681,-23.9845952055851,-23.4849161388021,-22.9852370720191,
-22.5482714132432),.UNSPECIFIED.);
#487=B_SPLINE_CURVE_WITH_KNOTS('',3,(#24042,#24043,#24044,#24045,#24046,
#24047,#24048,#24049,#24050,#24051,#24052,#24053,#24054,#24055,#24056,#24057,
#24058,#24059,#24060,#24061,#24062,#24063,#24064,#24065,#24066,#24067,#24068,
#24069,#24070,#24071,#24072,#24073,#24074,#24075,#24076,#24077,#24078,#24079,
#24080,#24081,#24082,#24083,#24084),.UNSPECIFIED.,.F.,.F.,(4,3,3,3,3,3,
3,3,3,3,3,3,3,3,4),(19.2926165920933,19.4874836045379,19.9871626713209,
20.4868417381039,20.986520804887,21.48619987167,21.985878938453,22.4855580052361,
22.9852370720191,23.4849161388021,23.9845952055851,24.4842742723682,24.9839533391512,
25.4836324059342,25.5758018992728),.UNSPECIFIED.);
#488=B_SPLINE_CURVE_WITH_KNOTS('',3,(#24089,#24090,#24091,#24092,#24093,
#24094,#24095,#24096,#24097,#24098,#24099,#24100,#24101,#24102,#24103,#24104,
#24105,#24106,#24107,#24108,#24109,#24110,#24111,#24112,#24113,#24114,#24115,
#24116,#24117,#24118,#24119,#24120,#24121,#24122,#24123,#24124,#24125,#24126,
#24127,#24128,#24129,#24130,#24131),.UNSPECIFIED.,.F.,.F.,(4,3,3,3,3,3,
3,3,3,3,3,3,3,3,4),(-35.1146420276024,-34.9775346748116,-34.4778556080286,
-33.9781765412456,-33.4784974744626,-32.9788184076795,-32.4791393408965,
-31.9794602741135,-31.4797812073305,-30.9801021405474,-30.4804230737644,
-29.9807440069814,-29.4810649401984,-28.9813858734153,-28.8314567204228),
 .UNSPECIFIED.);
#489=B_SPLINE_CURVE_WITH_KNOTS('',3,(#24132,#24133,#24134,#24135,#24136,
#24137,#24138,#24139,#24140,#24141,#24142,#24143,#24144,#24145,#24146,#24147,
#24148,#24149,#24150,#24151,#24152,#24153,#24154,#24155,#24156,#24157,#24158,
#24159,#24160,#24161,#24162,#24163,#24164,#24165,#24166,#24167,#24168,#24169,
#24170,#24171),.UNSPECIFIED.,.F.,.F.,(4,3,3,3,3,3,3,3,3,3,3,3,3,4),(25.5758018992728,
25.9833114727172,26.4829905395003,26.9826696062833,27.4823486730663,27.9820277398493,
28.4817068066324,28.9813858734154,29.4810649401984,29.9807440069814,30.4804230737645,
30.9801021405475,31.4797812073305,31.8589872064524),.UNSPECIFIED.);
#490=B_SPLINE_CURVE_WITH_KNOTS('',3,(#24176,#24177,#24178,#24179,#24180,
#24181,#24182,#24183,#24184,#24185,#24186,#24187,#24188,#24189,#24190,#24191,
#24192,#24193,#24194,#24195,#24196,#24197,#24198,#24199,#24200,#24201,#24202,
#24203,#24204,#24205,#24206,#24207,#24208,#24209,#24210,#24211,#24212,#24213,
#24214,#24215),.UNSPECIFIED.,.F.,.F.,(4,3,3,3,3,3,3,3,3,3,3,3,3,4),(-41.397827334782,
-40.9736834762079,-40.4740044094249,-39.9743253426419,-39.4746462758588,
-38.9749672090758,-38.4752881422928,-37.9756090755098,-37.4759300087267,
-36.9762509419437,-36.4765718751607,-35.9768928083777,-35.4772137415947,
-35.1146420276024),.UNSPECIFIED.);
#491=B_SPLINE_CURVE_WITH_KNOTS('',3,(#24216,#24217,#24218,#24219,#24220,
#24221,#24222,#24223,#24224,#24225,#24226,#24227,#24228,#24229,#24230,#24231,
#24232,#24233,#24234,#24235,#24236,#24237,#24238,#24239,#24240,#24241,#24242,
#24243,#24244,#24245,#24246,#24247,#24248,#24249,#24250,#24251,#24252,#24253,
#24254,#24255,#24256,#24257,#24258),.UNSPECIFIED.,.F.,.F.,(4,3,3,3,3,3,
3,3,3,3,3,3,3,3,4),(31.8589872064524,31.9794602741135,32.4791393408966,
32.9788184076796,33.4784974744626,33.9781765412456,34.4778556080286,34.9775346748117,
35.4772137415947,35.9768928083777,36.4765718751607,36.9762509419437,37.4759300087267,
37.9756090755098,38.142172513632),.UNSPECIFIED.);
#492=B_SPLINE_CURVE_WITH_KNOTS('',3,(#24263,#24264,#24265,#24266,#24267,
#24268,#24269,#24270,#24271,#24272,#24273,#24274,#24275,#24276,#24277,#24278,
#24279,#24280,#24281,#24282,#24283,#24284,#24285,#24286,#24287,#24288,#24289,
#24290,#24291,#24292,#24293,#24294,#24295,#24296,#24297,#24298,#24299,#24300,
#24301,#24302,#24303,#24304,#24305),.UNSPECIFIED.,.F.,.F.,(4,3,3,3,3,3,
3,3,3,3,3,3,3,3,4),(-47.6810126419616,-47.4695113443872,-46.9698322776042,
-46.4701532108212,-45.9704741440381,-45.4707950772551,-44.9711160104721,
-44.4714369436891,-43.971757876906,-43.472078810123,-42.97239974334,-42.472720676557,
-41.973041609774,-41.4733625429909,-41.397827334782),.UNSPECIFIED.);
#493=B_SPLINE_CURVE_WITH_KNOTS('',3,(#24306,#24307,#24308,#24309,#24310,
#24311,#24312,#24313,#24314,#24315,#24316,#24317,#24318,#24319,#24320,#24321,
#24322,#24323,#24324,#24325,#24326,#24327,#24328,#24329,#24330,#24331,#24332,
#24333,#24334,#24335,#24336,#24337,#24338,#24339,#24340,#24341,#24342,#24343,
#24344,#24345),.UNSPECIFIED.,.F.,.F.,(4,3,3,3,3,3,3,3,3,3,3,3,3,4),(38.142172513632,
38.4752881422928,38.9749672090758,39.4746462758589,39.9743253426419,40.4740044094249,
40.973683476208,41.473362542991,41.973041609774,42.472720676557,42.9723997433401,
43.4720788101231,43.9717578769061,44.4253578208116),.UNSPECIFIED.);
#494=B_SPLINE_CURVE_WITH_KNOTS('',3,(#24350,#24351,#24352,#24353,#24354,
#24355,#24356,#24357,#24358,#24359,#24360,#24361,#24362,#24363,#24364,#24365,
#24366,#24367,#24368,#24369,#24370,#24371,#24372,#24373,#24374,#24375,#24376,
#24377),.UNSPECIFIED.,.F.,.F.,(4,3,3,3,3,3,3,3,3,4),(-53.9641979491412,
-52.9659810790005,-51.9666229454344,-50.9672648118684,-49.9679066783023,
-49.4682276115193,-48.9685485447363,-48.4688694779533,-47.9691904111702,
-47.6810126419616),.UNSPECIFIED.);
#495=B_SPLINE_CURVE_WITH_KNOTS('',3,(#24378,#24379,#24380,#24381,#24382,
#24383,#24384,#24385,#24386,#24387,#24388,#24389,#24390,#24391,#24392,#24393,
#24394,#24395,#24396,#24397,#24398,#24399,#24400,#24401,#24402,#24403,#24404,
#24405,#24406,#24407,#24408,#24409,#24410,#24411,#24412,#24413,#24414,#24415,
#24416,#24417),.UNSPECIFIED.,.F.,.F.,(4,3,3,3,3,3,3,3,3,3,3,3,3,4),(44.4253578208116,
44.4714369436892,44.9711160104722,45.4707950772552,45.9704741440382,46.4701532108212,
46.9698322776042,47.4695113443873,47.9691904111703,48.4688694779533,48.9685485447363,
49.4682276115193,49.9679066783024,50.7085431279912),.UNSPECIFIED.);
#496=B_SPLINE_CURVE_WITH_KNOTS('',3,(#24422,#24423,#24424,#24425,#24426,
#24427,#24428,#24429,#24430,#24431,#24432,#24433,#24434,#24435,#24436,#24437,
#24438,#24439,#24440,#24441,#24442,#24443),.UNSPECIFIED.,.F.,.F.,(4,3,3,
3,3,3,3,4),(-60.2473832563207,-59.9614880139628,-58.9621298803968,-57.9627717468307,
-56.9634136132647,-55.9640554796986,-54.9646973461326,-53.9641979491412),
 .UNSPECIFIED.);
#497=B_SPLINE_CURVE_WITH_KNOTS('',3,(#24444,#24445,#24446,#24447,#24448,
#24449,#24450,#24451,#24452,#24453,#24454,#24455,#24456,#24457,#24458,#24459,
#24460,#24461,#24462,#24463,#24464,#24465,#24466,#24467,#24468),
 .UNSPECIFIED.,.F.,.F.,(4,3,3,3,3,3,3,3,4),(50.7085431279912,50.9672648118684,
51.9666229454345,52.9659810790005,53.9653392125666,54.9646973461326,55.9640554796987,
56.9634136132647,56.9917284351708),.UNSPECIFIED.);
#498=B_SPLINE_CURVE_WITH_KNOTS('',3,(#24473,#24474,#24475,#24476,#24477,
#24478,#24479,#24480,#24481,#24482,#24483,#24484,#24485,#24486,#24487,#24488,
#24489,#24490,#24491,#24492,#24493,#24494),.UNSPECIFIED.,.F.,.F.,(4,3,3,
3,3,3,3,4),(-66.5305685635003,-65.9576368153591,-64.958278681793,-63.958920548227,
-62.9595624146609,-61.9602042810949,-60.9608461475288,-60.2473832563207),
 .UNSPECIFIED.);
#499=B_SPLINE_CURVE_WITH_KNOTS('',3,(#24495,#24496,#24497,#24498,#24499,
#24500,#24501,#24502,#24503,#24504,#24505,#24506,#24507,#24508,#24509,#24510,
#24511,#24512,#24513,#24514,#24515,#24516),.UNSPECIFIED.,.F.,.F.,(4,3,3,
3,3,3,3,4),(56.9917284351708,57.9627717468308,58.9621298803968,59.9614880139629,
60.9608461475289,61.960204281095,62.959562414661,63.2749137423504),
 .UNSPECIFIED.);
#500=B_SPLINE_CURVE_WITH_KNOTS('',3,(#24521,#24522,#24523,#24524,#24525,
#24526,#24527,#24528,#24529,#24530,#24531,#24532,#24533,#24534,#24535,#24536,
#24537,#24538,#24539,#24540,#24541,#24542),.UNSPECIFIED.,.F.,.F.,(4,3,3,
3,3,3,3,4),(-72.8137538706799,-71.9537856167554,-70.9544274831893,-69.9550693496233,
-68.9557112160572,-67.9563530824912,-66.9569949489251,-66.5305685635003),
 .UNSPECIFIED.);
#501=B_SPLINE_CURVE_WITH_KNOTS('',3,(#24543,#24544,#24545,#24546,#24547,
#24548,#24549,#24550,#24551,#24552,#24553,#24554,#24555,#24556,#24557,#24558,
#24559,#24560,#24561,#24562,#24563,#24564),.UNSPECIFIED.,.F.,.F.,(4,3,3,
3,3,3,3,4),(63.2749137423504,63.958920548227,64.9582786817931,65.9576368153591,
66.9569949489252,67.9563530824912,68.9557112160573,69.55809904953),
 .UNSPECIFIED.);
#502=B_SPLINE_CURVE_WITH_KNOTS('',3,(#24569,#24570,#24571,#24572,#24573,
#24574,#24575,#24576,#24577,#24578,#24579,#24580,#24581,#24582,#24583,#24584,
#24585,#24586,#24587,#24588,#24589,#24590,#24591,#24592,#24593),
 .UNSPECIFIED.,.F.,.F.,(4,3,3,3,3,3,3,3,4),(-79.0969391778595,-78.9492925517177,
-77.9499344181516,-76.9505762845856,-75.9512181510195,-74.9518600174535,
-73.9525018838875,-72.9531437503214,-72.8137538706799),.UNSPECIFIED.);
#503=B_SPLINE_CURVE_WITH_KNOTS('',3,(#24594,#24595,#24596,#24597,#24598,
#24599,#24600,#24601,#24602,#24603,#24604,#24605,#24606,#24607,#24608,#24609,
#24610,#24611,#24612,#24613,#24614,#24615),.UNSPECIFIED.,.F.,.F.,(4,3,3,
3,3,3,3,4),(69.55809904953,69.9550693496233,70.9544274831893,71.9537856167554,
72.9531437503215,73.9525018838875,74.9518600174536,75.8412843567096),
 .UNSPECIFIED.);
#504=B_SPLINE_CURVE_WITH_KNOTS('',3,(#24620,#24621,#24622,#24623,#24624,
#24625,#24626,#24627,#24628,#24629,#24630,#24631,#24632,#24633,#24634,#24635,
#24636,#24637,#24638,#24639,#24640,#24641),.UNSPECIFIED.,.F.,.F.,(4,3,3,
3,3,3,3,4),(-85.3801244850391,-84.945441353114,-83.9460832195479,-82.9467250859819,
-81.9473669524158,-80.9480088188498,-79.9486506852837,-79.0969391778595),
 .UNSPECIFIED.);
#505=B_SPLINE_CURVE_WITH_KNOTS('',3,(#24642,#24643,#24644,#24645,#24646,
#24647,#24648,#24649,#24650,#24651,#24652,#24653,#24654,#24655,#24656,#24657,
#24658,#24659,#24660,#24661,#24662,#24663,#24664,#24665,#24666),
 .UNSPECIFIED.,.F.,.F.,(4,3,3,3,3,3,3,3,4),(75.8412843567096,75.9512181510196,
76.9505762845857,77.9499344181517,78.9492925517178,79.9486506852838,80.9480088188499,
81.9473669524159,82.1244696638892),.UNSPECIFIED.);
#506=B_SPLINE_CURVE_WITH_KNOTS('',3,(#24671,#24672,#24673,#24674,#24675,
#24676,#24677,#24678,#24679,#24680,#24681,#24682,#24683,#24684,#24685,#24686,
#24687,#24688,#24689,#24690,#24691,#24692),.UNSPECIFIED.,.F.,.F.,(4,3,3,
3,3,3,3,4),(-91.6633097922187,-90.9415901545102,-89.9422320209442,-88.9428738873782,
-87.9435157538121,-86.944157620246,-85.94479948668,-85.3801244850391),
 .UNSPECIFIED.);
#507=B_SPLINE_CURVE_WITH_KNOTS('',3,(#24693,#24694,#24695,#24696,#24697,
#24698,#24699,#24700,#24701,#24702,#24703,#24704,#24705,#24706,#24707,#24708,
#24709,#24710,#24711,#24712,#24713,#24714),.UNSPECIFIED.,.F.,.F.,(4,3,3,
3,3,3,3,4),(82.1244696638892,82.946725085982,83.946083219548,84.9454413531141,
85.9447994866801,86.9441576202461,87.9435157538122,88.4076549710687),
 .UNSPECIFIED.);
#508=B_SPLINE_CURVE_WITH_KNOTS('',3,(#24719,#24720,#24721,#24722,#24723,
#24724,#24725,#24726,#24727,#24728,#24729,#24730,#24731,#24732,#24733,#24734,
#24735,#24736,#24737,#24738,#24739,#24740,#24741,#24742,#24743),
 .UNSPECIFIED.,.F.,.F.,(4,3,3,3,3,3,3,3,4),(-97.9464950993983,-97.9370970894726,
-96.9377389559065,-95.9383808223405,-94.9390226887744,-93.9396645552084,
-92.9403064216423,-91.9409482880763,-91.6633097922187),.UNSPECIFIED.);
#509=B_SPLINE_CURVE_WITH_KNOTS('',3,(#24744,#24745,#24746,#24747,#24748,
#24749,#24750,#24751,#24752,#24753,#24754,#24755,#24756,#24757,#24758,#24759,
#24760,#24761,#24762,#24763,#24764,#24765),.UNSPECIFIED.,.F.,.F.,(4,3,3,
3,3,3,3,4),(88.4076549710687,88.9428738873782,89.9422320209442,90.9415901545103,
91.9409482880763,92.9403064216424,93.9396645552084,94.6908402782483),
 .UNSPECIFIED.);
#510=B_SPLINE_CURVE_WITH_KNOTS('',3,(#24770,#24771,#24772,#24773,#24774,
#24775,#24776,#24777,#24778,#24779,#24780,#24781,#24782,#24783,#24784,#24785,
#24786,#24787,#24788,#24789,#24790,#24791),.UNSPECIFIED.,.F.,.F.,(4,3,3,
3,3,3,3,4),(-104.229680406578,-103.933245890869,-102.933887757303,-101.934529623737,
-100.935171490171,-99.9358133566047,-98.9364552230386,-97.9464950993983),
 .UNSPECIFIED.);
#511=B_SPLINE_CURVE_WITH_KNOTS('',3,(#24792,#24793,#24794,#24795,#24796,
#24797,#24798,#24799,#24800,#24801,#24802,#24803,#24804,#24805,#24806,#24807,
#24808,#24809,#24810,#24811,#24812,#24813,#24814,#24815,#24816),
 .UNSPECIFIED.,.F.,.F.,(4,3,3,3,3,3,3,3,4),(94.6908402782483,94.9390226887745,
95.9383808223405,96.9377389559065,97.9370970894726,98.9364552230386,99.9358133566047,
100.935171490171,100.974025585428),.UNSPECIFIED.);
#512=B_SPLINE_CURVE_WITH_KNOTS('',3,(#24821,#24822,#24823,#24824,#24825,
#24826,#24827,#24828,#24829,#24830,#24831,#24832,#24833,#24834,#24835,#24836,
#24837,#24838,#24839,#24840,#24841,#24842),.UNSPECIFIED.,.F.,.F.,(4,3,3,
3,3,3,3,4),(-110.512865713757,-109.929394692265,-108.930036558699,-107.930678425133,
-106.931320291567,-105.931962158001,-104.932604024435,-104.229680406578),
 .UNSPECIFIED.);
#513=B_SPLINE_CURVE_WITH_KNOTS('',3,(#24843,#24844,#24845,#24846,#24847,
#24848,#24849,#24850,#24851,#24852,#24853,#24854,#24855,#24856,#24857,#24858,
#24859,#24860,#24861,#24862,#24863,#24864),.UNSPECIFIED.,.F.,.F.,(4,3,3,
3,3,3,3,4),(100.974025585428,101.934529623737,102.933887757303,103.933245890869,
104.932604024435,105.931962158001,106.931320291567,107.257210892608),
 .UNSPECIFIED.);
#514=B_SPLINE_CURVE_WITH_KNOTS('',3,(#24869,#24870,#24871,#24872,#24873,
#24874,#24875,#24876,#24877,#24878,#24879,#24880,#24881,#24882,#24883,#24884,
#24885,#24886,#24887,#24888,#24889,#24890),.UNSPECIFIED.,.F.,.F.,(4,3,3,
3,3,3,3,4),(-116.796051020937,-115.925543493661,-114.926185360095,-113.926827226529,
-112.927469092963,-111.928110959397,-110.928752825831,-110.512865713757),
 .UNSPECIFIED.);
#515=B_SPLINE_CURVE_WITH_KNOTS('',3,(#24891,#24892,#24893,#24894,#24895,
#24896,#24897,#24898,#24899,#24900,#24901,#24902,#24903,#24904,#24905,#24906,
#24907,#24908,#24909,#24910,#24911,#24912),.UNSPECIFIED.,.F.,.F.,(4,3,3,
3,3,3,3,4),(107.257210892608,107.930678425133,108.930036558699,109.929394692265,
110.928752825831,111.928110959397,112.927469092963,113.540396199787),
 .UNSPECIFIED.);
#516=B_SPLINE_CURVE_WITH_KNOTS('',3,(#24917,#24918,#24919,#24920,#24921,
#24922,#24923,#24924,#24925,#24926,#24927,#24928,#24929,#24930,#24931,#24932,
#24933,#24934,#24935,#24936,#24937,#24938,#24939,#24940,#24941),
 .UNSPECIFIED.,.F.,.F.,(4,3,3,3,3,3,3,3,4),(-123.079236328117,-122.921050428624,
-121.921692295058,-120.922334161492,-119.922976027926,-118.92361789436,
-117.924259760793,-116.924901627227,-116.796051020937),.UNSPECIFIED.);
#517=B_SPLINE_CURVE_WITH_KNOTS('',3,(#24942,#24943,#24944,#24945,#24946,
#24947,#24948,#24949,#24950,#24951,#24952,#24953,#24954,#24955,#24956,#24957,
#24958,#24959,#24960,#24961,#24962,#24963),.UNSPECIFIED.,.F.,.F.,(4,3,3,
3,3,3,3,4),(113.540396199787,113.926827226529,114.926185360095,115.925543493661,
116.924901627228,117.924259760794,118.92361789436,119.823581506967),
 .UNSPECIFIED.);
#518=B_SPLINE_CURVE_WITH_KNOTS('',3,(#24968,#24969,#24970,#24971,#24972,
#24973,#24974,#24975,#24976,#24977,#24978,#24979,#24980,#24981,#24982,#24983,
#24984,#24985,#24986,#24987,#24988,#24989),.UNSPECIFIED.,.F.,.F.,(4,3,3,
3,3,3,3,4),(-129.362421635296,-128.91719923002,-127.917841096454,-126.918482962888,
-125.919124829322,-124.919766695756,-123.92040856219,-123.079236328117),
 .UNSPECIFIED.);
#519=B_SPLINE_CURVE_WITH_KNOTS('',3,(#24990,#24991,#24992,#24993,#24994,
#24995,#24996,#24997,#24998,#24999,#25000,#25001,#25002,#25003,#25004,#25005,
#25006,#25007,#25008,#25009,#25010,#25011,#25012,#25013,#25014),
 .UNSPECIFIED.,.F.,.F.,(4,3,3,3,3,3,3,3,4),(119.823581506967,119.922976027926,
120.922334161492,121.921692295058,122.921050428624,123.92040856219,124.919766695756,
125.919124829322,126.106766814146),.UNSPECIFIED.);
#520=B_SPLINE_CURVE_WITH_KNOTS('',3,(#25019,#25020,#25021,#25022,#25023,
#25024,#25025,#25026,#25027,#25028,#25029,#25030,#25031,#25032,#25033,#25034,
#25035,#25036,#25037,#25038,#25039,#25040),.UNSPECIFIED.,.F.,.F.,(4,3,3,
3,3,3,3,4),(-135.645606942476,-134.913348031416,-133.91398989785,-132.914631764284,
-131.915273630718,-130.915915497152,-129.916557363586,-129.362421635296),
 .UNSPECIFIED.);
#521=B_SPLINE_CURVE_WITH_KNOTS('',3,(#25041,#25042,#25043,#25044,#25045,
#25046,#25047,#25048,#25049,#25050,#25051,#25052,#25053,#25054,#25055,#25056,
#25057,#25058,#25059,#25060,#25061,#25062),.UNSPECIFIED.,.F.,.F.,(4,3,3,
3,3,3,3,4),(126.106766814146,126.918482962888,127.917841096454,128.91719923002,
129.916557363586,130.915915497152,131.915273630718,132.389952121326),
 .UNSPECIFIED.);
#522=B_SPLINE_CURVE_WITH_KNOTS('',3,(#25067,#25068,#25069,#25070,#25071,
#25072,#25073,#25074,#25075,#25076,#25077,#25078,#25079,#25080,#25081,#25082,
#25083,#25084,#25085,#25086,#25087,#25088,#25089,#25090,#25091),
 .UNSPECIFIED.,.F.,.F.,(4,3,3,3,3,3,3,3,4),(-141.928792249655,-141.908854966379,
-140.909496832813,-139.910138699247,-138.91078056568,-137.911422432114,
-136.912064298548,-135.912706164982,-135.645606942476),.UNSPECIFIED.);
#523=B_SPLINE_CURVE_WITH_KNOTS('',3,(#25092,#25093,#25094,#25095,#25096,
#25097,#25098,#25099,#25100,#25101,#25102,#25103,#25104,#25105,#25106,#25107,
#25108,#25109,#25110,#25111,#25112,#25113),.UNSPECIFIED.,.F.,.F.,(4,3,3,
3,3,3,3,4),(132.389952121326,132.914631764284,133.91398989785,134.913348031416,
135.912706164982,136.912064298549,137.911422432115,138.673137428505),
 .UNSPECIFIED.);
#524=B_SPLINE_CURVE_WITH_KNOTS('',3,(#25118,#25119,#25120,#25121,#25122,
#25123,#25124,#25125,#25126,#25127,#25128,#25129,#25130,#25131,#25132,#25133,
#25134,#25135,#25136,#25137,#25138,#25139),.UNSPECIFIED.,.F.,.F.,(4,3,3,
3,3,3,3,4),(-148.211977556835,-147.905003767775,-146.905645634209,-145.906287500643,
-144.906929367077,-143.907571233511,-142.908213099945,-141.928792249655),
 .UNSPECIFIED.);
#525=B_SPLINE_CURVE_WITH_KNOTS('',3,(#25140,#25141,#25142,#25143,#25144,
#25145,#25146,#25147,#25148,#25149,#25150,#25151,#25152,#25153,#25154,#25155,
#25156,#25157,#25158,#25159,#25160,#25161,#25162,#25163,#25164),
 .UNSPECIFIED.,.F.,.F.,(4,3,3,3,3,3,3,3,4),(138.673137428505,138.910780565681,
139.910138699247,140.909496832813,141.908854966379,142.908213099945,143.907571233511,
144.906929367077,144.956322735685),.UNSPECIFIED.);
#526=B_SPLINE_CURVE_WITH_KNOTS('',3,(#25169,#25170,#25171,#25172,#25173,
#25174,#25175,#25176,#25177,#25178,#25179,#25180,#25181,#25182,#25183,#25184,
#25185,#25186,#25187,#25188,#25189,#25190),.UNSPECIFIED.,.F.,.F.,(4,3,3,
3,3,3,3,4),(-154.495162864015,-153.901152569171,-152.901794435605,-151.902436302039,
-150.903078168473,-149.903720034907,-148.904361901341,-148.211977556835),
 .UNSPECIFIED.);
#527=B_SPLINE_CURVE_WITH_KNOTS('',3,(#25191,#25192,#25193,#25194,#25195,
#25196,#25197,#25198,#25199,#25200,#25201,#25202,#25203,#25204,#25205,#25206,
#25207,#25208,#25209,#25210,#25211,#25212),.UNSPECIFIED.,.F.,.F.,(4,3,3,
3,3,3,3,4),(144.956322735685,145.906287500643,146.905645634209,147.905003767775,
148.904361901341,149.903720034907,150.903078168473,151.239508042865),
 .UNSPECIFIED.);
#528=B_SPLINE_CURVE_WITH_KNOTS('',3,(#25217,#25218,#25219,#25220,#25221,
#25222,#25223,#25224,#25225,#25226,#25227,#25228,#25229,#25230,#25231,#25232,
#25233,#25234,#25235,#25236,#25237,#25238),.UNSPECIFIED.,.F.,.F.,(4,3,3,
3,3,3,3,4),(-160.778348171194,-159.897301370567,-158.897943237001,-157.898585103435,
-156.899226969869,-155.899868836303,-154.900510702737,-154.495162864015),
 .UNSPECIFIED.);
#529=B_SPLINE_CURVE_WITH_KNOTS('',3,(#25239,#25240,#25241,#25242,#25243,
#25244,#25245,#25246,#25247,#25248,#25249,#25250,#25251,#25252,#25253,#25254,
#25255,#25256,#25257,#25258,#25259,#25260),.UNSPECIFIED.,.F.,.F.,(4,3,3,
3,3,3,3,4),(151.239508042865,151.902436302039,152.901794435605,153.901152569171,
154.900510702737,155.899868836303,156.899226969869,157.522693350044),
 .UNSPECIFIED.);
#530=B_SPLINE_CURVE_WITH_KNOTS('',3,(#25265,#25266,#25267,#25268,#25269,
#25270,#25271,#25272,#25273,#25274,#25275,#25276,#25277,#25278,#25279,#25280,
#25281,#25282,#25283,#25284,#25285,#25286,#25287,#25288,#25289),
 .UNSPECIFIED.,.F.,.F.,(4,3,3,3,3,3,3,3,4),(-167.061533478374,-166.89280830553,
-165.893450171964,-164.894092038398,-163.894733904832,-162.895375771266,
-161.8960176377,-160.896659504134,-160.778348171194),.UNSPECIFIED.);
#531=B_SPLINE_CURVE_WITH_KNOTS('',3,(#25290,#25291,#25292,#25293,#25294,
#25295,#25296,#25297,#25298,#25299,#25300,#25301,#25302,#25303,#25304,#25305,
#25306,#25307,#25308,#25309,#25310,#25311),.UNSPECIFIED.,.F.,.F.,(4,3,3,
3,3,3,3,4),(157.522693350044,157.898585103435,158.897943237002,159.897301370568,
160.896659504134,161.8960176377,162.895375771266,163.805878657224),
 .UNSPECIFIED.);
#532=B_SPLINE_CURVE_WITH_KNOTS('',3,(#25316,#25317,#25318,#25319,#25320,
#25321,#25322,#25323,#25324,#25325,#25326,#25327,#25328,#25329,#25330,#25331,
#25332,#25333,#25334,#25335,#25336,#25337),.UNSPECIFIED.,.F.,.F.,(4,3,3,
3,3,3,3,4),(-173.344718785553,-172.888957106926,-171.88959897336,-170.890240839794,
-169.890882706228,-168.891524572662,-167.892166439096,-167.061533478374),
 .UNSPECIFIED.);
#533=B_SPLINE_CURVE_WITH_KNOTS('',3,(#25338,#25339,#25340,#25341,#25342,
#25343,#25344,#25345,#25346,#25347,#25348,#25349,#25350,#25351,#25352,#25353,
#25354,#25355,#25356,#25357,#25358,#25359,#25360,#25361,#25362),
 .UNSPECIFIED.,.F.,.F.,(4,3,3,3,3,3,3,3,4),(163.805878657224,163.894733904832,
164.894092038398,165.893450171964,166.89280830553,167.892166439096,168.891524572662,
169.890882706228,170.089063964403),.UNSPECIFIED.);
#534=B_SPLINE_CURVE_WITH_KNOTS('',3,(#25367,#25368,#25369,#25370,#25371,
#25372,#25373,#25374,#25375,#25376,#25377,#25378,#25379,#25380,#25381,#25382,
#25383,#25384,#25385,#25386,#25387,#25388),.UNSPECIFIED.,.F.,.F.,(4,3,3,
3,3,3,3,4),(-179.627904092733,-178.885105908322,-177.885747774756,-176.88638964119,
-175.887031507624,-174.887673374058,-173.888315240492,-173.344718785553),
 .UNSPECIFIED.);
#535=B_SPLINE_CURVE_WITH_KNOTS('',3,(#25389,#25390,#25391,#25392,#25393,
#25394,#25395,#25396,#25397,#25398,#25399,#25400,#25401,#25402,#25403,#25404,
#25405,#25406,#25407,#25408,#25409,#25410),.UNSPECIFIED.,.F.,.F.,(4,3,3,
3,3,3,3,4),(170.089063964403,170.890240839794,171.88959897336,172.888957106926,
173.888315240492,174.887673374058,175.887031507624,176.372249271583),
 .UNSPECIFIED.);
#536=B_SPLINE_CURVE_WITH_KNOTS('',3,(#25415,#25416,#25417,#25418,#25419,
#25420,#25421,#25422,#25423,#25424,#25425,#25426,#25427,#25428,#25429,#25430,
#25431,#25432,#25433,#25434,#25435,#25436,#25437,#25438,#25439),
 .UNSPECIFIED.,.F.,.F.,(4,3,3,3,3,3,3,3,4),(-185.911089399912,-185.880612843285,
-184.881254709719,-183.881896576153,-182.882538442587,-181.88318030902,
-180.883822175454,-179.884464041888,-179.627904092733),.UNSPECIFIED.);
#537=B_SPLINE_CURVE_WITH_KNOTS('',3,(#25440,#25441,#25442,#25443,#25444,
#25445,#25446,#25447,#25448,#25449,#25450,#25451,#25452,#25453,#25454,#25455,
#25456,#25457,#25458,#25459,#25460,#25461),.UNSPECIFIED.,.F.,.F.,(4,3,3,
3,3,3,3,4),(176.372249271583,176.88638964119,177.885747774756,178.885105908322,
179.884464041889,180.883822175455,181.883180309021,182.655434578762),
 .UNSPECIFIED.);
#538=B_SPLINE_CURVE_WITH_KNOTS('',3,(#25466,#25467,#25468,#25469,#25470,
#25471,#25472,#25473,#25474,#25475,#25476,#25477,#25478,#25479,#25480,#25481,
#25482,#25483,#25484,#25485,#25486,#25487),.UNSPECIFIED.,.F.,.F.,(4,3,3,
3,3,3,3,4),(-192.194274707092,-191.876761644681,-190.877403511115,-189.878045377549,
-188.878687243983,-187.879329110417,-186.879970976851,-185.911089399912),
 .UNSPECIFIED.);
#539=B_SPLINE_CURVE_WITH_KNOTS('',3,(#25488,#25489,#25490,#25491,#25492,
#25493,#25494,#25495,#25496,#25497,#25498,#25499,#25500,#25501,#25502,#25503,
#25504,#25505,#25506,#25507,#25508,#25509,#25510,#25511,#25512),
 .UNSPECIFIED.,.F.,.F.,(4,3,3,3,3,3,3,3,4),(182.655434578762,182.882538442587,
183.881896576153,184.881254709719,185.880612843285,186.879970976851,187.879329110417,
188.878687243983,188.938619885942),.UNSPECIFIED.);
#540=B_SPLINE_CURVE_WITH_KNOTS('',3,(#25517,#25518,#25519,#25520,#25521,
#25522,#25523,#25524,#25525,#25526,#25527,#25528,#25529,#25530,#25531,#25532,
#25533,#25534,#25535,#25536,#25537,#25538),.UNSPECIFIED.,.F.,.F.,(4,3,3,
3,3,3,3,4),(-198.477460014271,-197.872910446077,-196.873552312511,-195.874194178945,
-194.874836045379,-193.875477911813,-192.876119778247,-192.194274707092),
 .UNSPECIFIED.);
#541=B_SPLINE_CURVE_WITH_KNOTS('',3,(#25539,#25540,#25541,#25542,#25543,
#25544,#25545,#25546,#25547,#25548,#25549,#25550,#25551,#25552,#25553,#25554,
#25555,#25556,#25557,#25558,#25559,#25560),.UNSPECIFIED.,.F.,.F.,(4,3,3,
3,3,3,3,4),(188.938619885942,189.878045377549,190.877403511115,191.876761644681,
192.876119778247,193.875477911813,194.874836045379,195.221805193122),
 .UNSPECIFIED.);
#542=B_SPLINE_CURVE_WITH_KNOTS('',3,(#25565,#25566,#25567,#25568,#25569,
#25570,#25571,#25572,#25573,#25574,#25575,#25576,#25577,#25578,#25579,#25580,
#25581,#25582,#25583,#25584,#25585,#25586),.UNSPECIFIED.,.F.,.F.,(4,3,3,
3,3,3,3,4),(-204.760645321451,-203.869059247473,-202.869701113907,-201.870342980341,
-200.870984846775,-199.871626713209,-198.872268579643,-198.477460014271),
 .UNSPECIFIED.);
#543=B_SPLINE_CURVE_WITH_KNOTS('',3,(#25587,#25588,#25589,#25590,#25591,
#25592,#25593,#25594,#25595,#25596,#25597,#25598,#25599,#25600,#25601,#25602,
#25603,#25604,#25605,#25606,#25607,#25608),.UNSPECIFIED.,.F.,.F.,(4,3,3,
3,3,3,3,4),(195.221805193122,195.874194178945,196.873552312511,197.872910446077,
198.872268579643,199.871626713209,200.870984846776,201.504990500301),
 .UNSPECIFIED.);
#544=B_SPLINE_CURVE_WITH_KNOTS('',3,(#25613,#25614,#25615,#25616,#25617,
#25618,#25619,#25620,#25621,#25622,#25623,#25624,#25625,#25626,#25627,#25628,
#25629,#25630,#25631,#25632,#25633,#25634,#25635,#25636,#25637),
 .UNSPECIFIED.,.F.,.F.,(4,3,3,3,3,3,3,3,4),(-211.043830628631,-210.864566182436,
-209.86520804887,-208.865849915304,-207.866491781738,-206.867133648172,
-205.867775514606,-204.86841738104,-204.760645321451),.UNSPECIFIED.);
#545=B_SPLINE_CURVE_WITH_KNOTS('',3,(#25638,#25639,#25640,#25641,#25642,
#25643,#25644,#25645,#25646,#25647,#25648,#25649,#25650,#25651,#25652,#25653,
#25654,#25655,#25656,#25657,#25658,#25659),.UNSPECIFIED.,.F.,.F.,(4,3,3,
3,3,3,3,4),(201.504990500301,201.870342980342,202.869701113908,203.869059247474,
204.86841738104,205.867775514606,206.867133648172,207.788175807481),
 .UNSPECIFIED.);
#546=B_SPLINE_CURVE_WITH_KNOTS('',3,(#25664,#25665,#25666,#25667,#25668,
#25669,#25670,#25671,#25672,#25673,#25674,#25675,#25676,#25677,#25678,#25679,
#25680,#25681,#25682,#25683,#25684,#25685),.UNSPECIFIED.,.F.,.F.,(4,3,3,
3,3,3,3,4),(-217.32701593581,-216.860714983832,-215.861356850266,-214.8619987167,
-213.862640583134,-212.863282449568,-211.863924316002,-211.043830628631),
 .UNSPECIFIED.);
#547=B_SPLINE_CURVE_WITH_KNOTS('',3,(#25686,#25687,#25688,#25689,#25690,
#25691,#25692,#25693,#25694,#25695,#25696,#25697,#25698,#25699,#25700,#25701,
#25702,#25703,#25704,#25705,#25706,#25707,#25708,#25709,#25710),
 .UNSPECIFIED.,.F.,.F.,(4,3,3,3,3,3,3,3,4),(207.788175807481,207.866491781738,
208.865849915304,209.86520804887,210.864566182436,211.863924316002,212.863282449568,
213.862640583134,214.07136111466),.UNSPECIFIED.);
#548=B_SPLINE_CURVE_WITH_KNOTS('',3,(#25715,#25716,#25717,#25718,#25719,
#25720,#25721,#25722,#25723,#25724,#25725,#25726,#25727,#25728,#25729,#25730,
#25731,#25732,#25733,#25734,#25735,#25736),.UNSPECIFIED.,.F.,.F.,(4,3,3,
3,3,3,3,4),(-223.61020124299,-222.856863785228,-221.857505651662,-220.858147518096,
-219.85878938453,-218.859431250964,-217.860073117398,-217.32701593581),
 .UNSPECIFIED.);
#549=B_SPLINE_CURVE_WITH_KNOTS('',3,(#25737,#25738,#25739,#25740,#25741,
#25742,#25743,#25744,#25745,#25746,#25747,#25748,#25749,#25750,#25751,#25752,
#25753,#25754,#25755,#25756,#25757,#25758),.UNSPECIFIED.,.F.,.F.,(4,3,3,
3,3,3,3,4),(214.07136111466,214.8619987167,215.861356850266,216.860714983832,
217.860073117398,218.859431250964,219.85878938453,220.35454642184),
 .UNSPECIFIED.);
#550=B_SPLINE_CURVE_WITH_KNOTS('',3,(#25763,#25764,#25765,#25766,#25767,
#25768,#25769,#25770,#25771,#25772,#25773,#25774,#25775,#25776,#25777,#25778,
#25779,#25780,#25781,#25782,#25783,#25784,#25785,#25786,#25787),
 .UNSPECIFIED.,.F.,.F.,(4,3,3,3,3,3,3,3,4),(-229.893386550169,-229.852370720191,
-228.853012586625,-227.853654453059,-226.854296319493,-225.854938185927,
-224.85558005236,-223.856221918794,-223.61020124299),.UNSPECIFIED.);
#551=B_SPLINE_CURVE_WITH_KNOTS('',3,(#25788,#25789,#25790,#25791,#25792,
#25793,#25794,#25795,#25796,#25797,#25798,#25799,#25800,#25801,#25802,#25803,
#25804,#25805,#25806,#25807,#25808,#25809),.UNSPECIFIED.,.F.,.F.,(4,3,3,
3,3,3,3,4),(220.35454642184,220.858147518096,221.857505651663,222.856863785229,
223.856221918795,224.855580052361,225.854938185927,226.637731729019),
 .UNSPECIFIED.);
#552=B_SPLINE_CURVE_WITH_KNOTS('',3,(#25814,#25815,#25816,#25817,#25818,
#25819,#25820,#25821,#25822,#25823,#25824,#25825,#25826,#25827,#25828,#25829,
#25830,#25831,#25832,#25833,#25834,#25835),.UNSPECIFIED.,.F.,.F.,(4,3,3,
3,3,3,3,4),(-236.176571857349,-235.848519521587,-234.849161388021,-233.849803254455,
-232.850445120889,-231.851086987323,-230.851728853757,-229.893386550169),
 .UNSPECIFIED.);
#553=B_SPLINE_CURVE_WITH_KNOTS('',3,(#25836,#25837,#25838,#25839,#25840,
#25841,#25842,#25843,#25844,#25845,#25846,#25847,#25848,#25849,#25850,#25851,
#25852,#25853,#25854,#25855,#25856,#25857,#25858,#25859,#25860),
 .UNSPECIFIED.,.F.,.F.,(4,3,3,3,3,3,3,3,4),(226.637731729019,226.854296319493,
227.853654453059,228.853012586625,229.852370720191,230.851728853757,231.851086987323,
232.850445120889,232.920917036199),.UNSPECIFIED.);
#554=B_SPLINE_CURVE_WITH_KNOTS('',3,(#25865,#25866,#25867,#25868,#25869,
#25870,#25871,#25872,#25873,#25874,#25875,#25876,#25877,#25878,#25879,#25880,
#25881,#25882,#25883,#25884,#25885,#25886),.UNSPECIFIED.,.F.,.F.,(4,3,3,
3,3,3,3,4),(-242.459757164528,-241.844668322983,-240.845310189417,-239.845952055851,
-238.846593922285,-237.847235788719,-236.847877655153,-236.176571857349),
 .UNSPECIFIED.);
#555=B_SPLINE_CURVE_WITH_KNOTS('',3,(#25887,#25888,#25889,#25890,#25891,
#25892,#25893,#25894,#25895,#25896,#25897,#25898,#25899,#25900,#25901,#25902,
#25903,#25904,#25905,#25906,#25907,#25908),.UNSPECIFIED.,.F.,.F.,(4,3,3,
3,3,3,3,4),(232.920917036199,233.849803254455,234.849161388021,235.848519521587,
236.847877655153,237.847235788719,238.846593922285,239.204102343378),
 .UNSPECIFIED.);
#556=B_SPLINE_CURVE_WITH_KNOTS('',3,(#25913,#25914,#25915,#25916,#25917,
#25918,#25919,#25920,#25921,#25922,#25923,#25924,#25925,#25926,#25927,#25928,
#25929,#25930,#25931,#25932,#25933,#25934),.UNSPECIFIED.,.F.,.F.,(4,3,3,
3,3,3,3,4),(-248.742942471708,-247.84081712438,-246.841458990814,-245.842100857247,
-244.842742723681,-243.843384590115,-242.844026456549,-242.459757164528),
 .UNSPECIFIED.);
#557=B_SPLINE_CURVE_WITH_KNOTS('',3,(#25935,#25936,#25937,#25938,#25939,
#25940,#25941,#25942,#25943,#25944,#25945,#25946,#25947,#25948,#25949,#25950,
#25951,#25952,#25953,#25954,#25955,#25956),.UNSPECIFIED.,.F.,.F.,(4,3,3,
3,3,3,3,4),(239.204102343378,239.845952055851,240.845310189417,241.844668322983,
242.84402645655,243.843384590116,244.842742723682,245.487287650558),
 .UNSPECIFIED.);
#558=B_SPLINE_CURVE_WITH_KNOTS('',3,(#25961,#25962,#25963,#25964,#25965,
#25966,#25967,#25968,#25969,#25970,#25971,#25972,#25973,#25974,#25975,#25976,
#25977,#25978,#25979,#25980,#25981,#25982,#25983,#25984,#25985),
 .UNSPECIFIED.,.F.,.F.,(4,3,3,3,3,3,3,3,4),(-255.026127778888,-254.836324059342,
-253.836965925776,-252.83760779221,-251.838249658644,-250.838891525078,
-249.839533391512,-248.840175257946,-248.742942471708),.UNSPECIFIED.);
#559=B_SPLINE_CURVE_WITH_KNOTS('',3,(#25986,#25987,#25988,#25989,#25990,
#25991,#25992,#25993,#25994,#25995,#25996,#25997,#25998,#25999,#26000,#26001,
#26002,#26003,#26004,#26005,#26006,#26007),.UNSPECIFIED.,.F.,.F.,(4,3,3,
3,3,3,3,4),(245.487287650558,245.842100857248,246.841458990814,247.84081712438,
248.840175257946,249.839533391512,250.838891525078,251.770472957738),
 .UNSPECIFIED.);
#560=B_SPLINE_CURVE_WITH_KNOTS('',3,(#26012,#26013,#26014,#26015,#26016,
#26017,#26018,#26019,#26020,#26021,#26022,#26023,#26024,#26025,#26026,#26027,
#26028,#26029,#26030,#26031,#26032,#26033),.UNSPECIFIED.,.F.,.F.,(4,3,3,
3,3,3,3,4),(-261.309313086067,-260.832472860738,-259.833114727172,-258.833756593606,
-257.83439846004,-256.835040326474,-255.835682192908,-255.026127778888),
 .UNSPECIFIED.);
#561=B_SPLINE_CURVE_WITH_KNOTS('',3,(#26034,#26035,#26036,#26037,#26038,
#26039,#26040,#26041,#26042,#26043,#26044,#26045,#26046,#26047,#26048,#26049,
#26050,#26051,#26052,#26053,#26054,#26055,#26056,#26057,#26058),
 .UNSPECIFIED.,.F.,.F.,(4,3,3,3,3,3,3,3,4),(251.770472957738,251.838249658644,
252.83760779221,253.836965925776,254.836324059342,255.835682192908,256.835040326474,
257.83439846004,258.053658264917),.UNSPECIFIED.);
#562=B_SPLINE_CURVE_WITH_KNOTS('',3,(#26063,#26064,#26065,#26066,#26067,
#26068,#26069,#26070,#26071,#26072,#26073,#26074,#26075,#26076,#26077,#26078,
#26079,#26080,#26081,#26082,#26083,#26084),.UNSPECIFIED.,.F.,.F.,(4,3,3,
3,3,3,3,4),(-267.592498393247,-266.828621662134,-265.829263528568,-264.829905395002,
-263.830547261436,-262.83118912787,-261.831830994304,-261.309313086067),
 .UNSPECIFIED.);
#563=B_SPLINE_CURVE_WITH_KNOTS('',3,(#26085,#26086,#26087,#26088,#26089,
#26090,#26091,#26092,#26093,#26094,#26095,#26096,#26097,#26098,#26099,#26100,
#26101,#26102,#26103,#26104,#26105,#26106),.UNSPECIFIED.,.F.,.F.,(4,3,3,
3,3,3,3,4),(258.053658264917,258.833756593606,259.833114727172,260.832472860738,
261.831830994304,262.83118912787,263.830547261436,264.336843572097),
 .UNSPECIFIED.);
#564=B_SPLINE_CURVE_WITH_KNOTS('',3,(#26111,#26112,#26113,#26114,#26115,
#26116,#26117,#26118,#26119,#26120,#26121,#26122,#26123,#26124,#26125,#26126,
#26127,#26128,#26129,#26130,#26131,#26132,#26133,#26134,#26135),
 .UNSPECIFIED.,.F.,.F.,(4,3,3,3,3,3,3,3,4),(-273.875683700426,-273.824128597097,
-272.824770463531,-271.825412329965,-270.826054196399,-269.826696062833,
-268.827337929266,-267.8279797957,-267.592498393247),.UNSPECIFIED.);
#565=B_SPLINE_CURVE_WITH_KNOTS('',3,(#26136,#26137,#26138,#26139,#26140,
#26141,#26142,#26143,#26144,#26145,#26146,#26147,#26148,#26149,#26150,#26151,
#26152,#26153,#26154,#26155,#26156,#26157),.UNSPECIFIED.,.F.,.F.,(4,3,3,
3,3,3,3,4),(264.336843572097,264.829905395003,265.829263528569,266.828621662135,
267.827979795701,268.827337929267,269.826696062833,270.620028879276),
 .UNSPECIFIED.);
#566=B_SPLINE_CURVE_WITH_KNOTS('',3,(#26162,#26163,#26164,#26165,#26166,
#26167,#26168,#26169,#26170,#26171,#26172,#26173,#26174,#26175,#26176,#26177,
#26178,#26179,#26180,#26181,#26182,#26183),.UNSPECIFIED.,.F.,.F.,(4,3,3,
3,3,3,3,4),(-280.158869007606,-279.820277398493,-278.820919264927,-277.821561131361,
-276.822202997795,-275.822844864229,-274.823486730663,-273.875683700426),
 .UNSPECIFIED.);
#567=B_SPLINE_CURVE_WITH_KNOTS('',3,(#26184,#26185,#26186,#26187,#26188,
#26189,#26190,#26191,#26192,#26193,#26194,#26195,#26196,#26197,#26198,#26199,
#26200,#26201,#26202,#26203,#26204,#26205,#26206,#26207,#26208),
 .UNSPECIFIED.,.F.,.F.,(4,3,3,3,3,3,3,3,4),(270.620028879276,270.826054196399,
271.825412329965,272.824770463531,273.824128597097,274.823486730663,275.822844864229,
276.822202997795,276.903214186456),.UNSPECIFIED.);
#568=B_SPLINE_CURVE_WITH_KNOTS('',3,(#26213,#26214,#26215,#26216,#26217,
#26218,#26219,#26220,#26221,#26222,#26223,#26224,#26225,#26226,#26227,#26228,
#26229,#26230,#26231,#26232,#26233,#26234),.UNSPECIFIED.,.F.,.F.,(4,3,3,
3,3,3,3,4),(-286.442054314785,-285.816426199889,-284.817068066323,-283.817709932757,
-282.818351799191,-281.818993665625,-280.819635532059,-280.158869007606),
 .UNSPECIFIED.);
#569=B_SPLINE_CURVE_WITH_KNOTS('',3,(#26235,#26236,#26237,#26238,#26239,
#26240,#26241,#26242,#26243,#26244,#26245,#26246,#26247,#26248,#26249,#26250,
#26251,#26252,#26253,#26254,#26255,#26256),.UNSPECIFIED.,.F.,.F.,(4,3,3,
3,3,3,3,4),(276.903214186456,277.821561131361,278.820919264927,279.820277398493,
280.819635532059,281.818993665625,282.818351799191,283.186399493635),
 .UNSPECIFIED.);
#570=B_SPLINE_CURVE_WITH_KNOTS('',3,(#26261,#26262,#26263,#26264,#26265,
#26266,#26267,#26268,#26269,#26270,#26271,#26272,#26273,#26274,#26275,#26276,
#26277,#26278,#26279,#26280,#26281,#26282),.UNSPECIFIED.,.F.,.F.,(4,3,3,
3,3,3,3,4),(-292.725239621965,-291.812575001286,-290.81321686772,-289.813858734153,
-288.814500600587,-287.815142467021,-286.815784333455,-286.442054314785),
 .UNSPECIFIED.);
#571=B_SPLINE_CURVE_WITH_KNOTS('',3,(#26283,#26284,#26285,#26286,#26287,
#26288,#26289,#26290,#26291,#26292,#26293,#26294,#26295,#26296,#26297,#26298,
#26299,#26300,#26301,#26302,#26303,#26304),.UNSPECIFIED.,.F.,.F.,(4,3,3,
3,3,3,3,4),(283.186399493635,283.817709932757,284.817068066323,285.81642619989,
286.815784333456,287.815142467022,288.814500600588,289.469584800815),
 .UNSPECIFIED.);
#572=B_SPLINE_CURVE_WITH_KNOTS('',3,(#26309,#26310,#26311,#26312,#26313,
#26314,#26315,#26316,#26317,#26318,#26319,#26320,#26321,#26322,#26323,#26324,
#26325,#26326,#26327,#26328,#26329,#26330,#26331,#26332,#26333),
 .UNSPECIFIED.,.F.,.F.,(4,3,3,3,3,3,3,3,4),(-299.008424929145,-298.808081936248,
-297.808723802682,-296.809365669116,-295.81000753555,-294.810649401984,
-293.811291268418,-292.811933134852,-292.725239621965),.UNSPECIFIED.);
#573=B_SPLINE_CURVE_WITH_KNOTS('',3,(#26334,#26335,#26336,#26337,#26338,
#26339,#26340,#26341,#26342,#26343,#26344,#26345,#26346,#26347,#26348,#26349,
#26350,#26351,#26352,#26353,#26354,#26355),.UNSPECIFIED.,.F.,.F.,(4,3,3,
3,3,3,3,4),(289.469584800815,289.813858734154,290.81321686772,291.812575001286,
292.811933134852,293.811291268418,294.810649401984,295.752770107995),
 .UNSPECIFIED.);
#574=B_SPLINE_CURVE_WITH_KNOTS('',3,(#26360,#26361,#26362,#26363,#26364,
#26365,#26366,#26367,#26368,#26369,#26370,#26371,#26372,#26373,#26374,#26375,
#26376,#26377,#26378,#26379,#26380,#26381),.UNSPECIFIED.,.F.,.F.,(4,3,3,
3,3,3,3,4),(-305.291610236324,-304.804230737644,-303.804872604078,-302.805514470512,
-301.806156336946,-300.80679820338,-299.807440069814,-299.008424929145),
 .UNSPECIFIED.);
#575=B_SPLINE_CURVE_WITH_KNOTS('',3,(#26382,#26383,#26384,#26385,#26386,
#26387,#26388,#26389,#26390,#26391,#26392,#26393,#26394,#26395,#26396,#26397,
#26398,#26399,#26400,#26401,#26402,#26403,#26404,#26405,#26406),
 .UNSPECIFIED.,.F.,.F.,(4,3,3,3,3,3,3,3,4),(295.752770107995,295.81000753555,
296.809365669116,297.808723802682,298.808081936248,299.807440069814,300.80679820338,
301.806156336946,302.035955415174),.UNSPECIFIED.);
#576=B_SPLINE_CURVE_WITH_KNOTS('',3,(#26411,#26412,#26413,#26414,#26415,
#26416,#26417,#26418,#26419,#26420,#26421,#26422,#26423,#26424,#26425,#26426,
#26427,#26428,#26429,#26430,#26431,#26432),.UNSPECIFIED.,.F.,.F.,(4,3,3,
3,3,3,3,4),(-311.574795543504,-310.80037953904,-309.801021405475,-308.801663271908,
-307.802305138342,-306.802947004776,-305.80358887121,-305.291610236324),
 .UNSPECIFIED.);
#577=B_SPLINE_CURVE_WITH_KNOTS('',3,(#26433,#26434,#26435,#26436,#26437,
#26438,#26439,#26440,#26441,#26442,#26443,#26444,#26445,#26446,#26447,#26448,
#26449,#26450,#26451,#26452,#26453,#26454),.UNSPECIFIED.,.F.,.F.,(4,3,3,
3,3,3,3,4),(302.035955415174,302.805514470512,303.804872604078,304.804230737644,
305.80358887121,306.802947004777,307.802305138343,308.319140722354),
 .UNSPECIFIED.);
#578=B_SPLINE_CURVE_WITH_KNOTS('',3,(#26459,#26460,#26461,#26462,#26463,
#26464,#26465,#26466,#26467,#26468,#26469,#26470,#26471,#26472,#26473,#26474,
#26475,#26476,#26477,#26478,#26479,#26480,#26481,#26482,#26483),
 .UNSPECIFIED.,.F.,.F.,(4,3,3,3,3,3,3,3,4),(-317.857980850683,-317.795886474003,
-316.796528340437,-315.797170206871,-314.797812073305,-313.798453939739,
-312.799095806173,-311.799737672607,-311.574795543504),.UNSPECIFIED.);
#579=B_SPLINE_CURVE_WITH_KNOTS('',3,(#26484,#26485,#26486,#26487,#26488,
#26489,#26490,#26491,#26492,#26493,#26494,#26495,#26496,#26497,#26498,#26499,
#26500,#26501,#26502,#26503,#26504,#26505),.UNSPECIFIED.,.F.,.F.,(4,3,3,
3,3,3,3,4),(308.319140722354,308.801663271909,309.801021405475,310.800379539041,
311.799737672607,312.799095806173,313.798453939739,314.602326029533),
 .UNSPECIFIED.);
#580=B_SPLINE_CURVE_WITH_KNOTS('',3,(#26510,#26511,#26512,#26513,#26514,
#26515,#26516,#26517,#26518,#26519,#26520,#26521,#26522,#26523,#26524,#26525,
#26526,#26527,#26528,#26529,#26530,#26531),.UNSPECIFIED.,.F.,.F.,(4,3,3,
3,3,3,3,4),(-324.141166157863,-323.792035275399,-322.792677141833,-321.793319008267,
-320.793960874701,-319.794602741135,-318.795244607569,-317.857980850683),
 .UNSPECIFIED.);
#581=B_SPLINE_CURVE_WITH_KNOTS('',3,(#26532,#26533,#26534,#26535,#26536,
#26537,#26538,#26539,#26540,#26541,#26542,#26543,#26544,#26545,#26546,#26547,
#26548,#26549,#26550,#26551,#26552,#26553,#26554,#26555,#26556),
 .UNSPECIFIED.,.F.,.F.,(4,3,3,3,3,3,3,3,4),(314.602326029533,314.797812073305,
315.797170206871,316.796528340437,317.795886474003,318.795244607569,319.794602741135,
320.793960874701,320.885511336713),.UNSPECIFIED.);
#582=B_SPLINE_CURVE_WITH_KNOTS('',3,(#26561,#26562,#26563,#26564,#26565,
#26566,#26567,#26568,#26569,#26570,#26571,#26572,#26573,#26574,#26575,#26576,
#26577,#26578,#26579,#26580,#26581,#26582),.UNSPECIFIED.,.F.,.F.,(4,3,3,
3,3,3,3,4),(-330.424351465042,-329.788184076795,-328.788825943229,-327.789467809663,
-326.790109676097,-325.790751542531,-324.791393408965,-324.141166157863),
 .UNSPECIFIED.);
#583=B_SPLINE_CURVE_WITH_KNOTS('',3,(#26583,#26584,#26585,#26586,#26587,
#26588,#26589,#26590,#26591,#26592,#26593,#26594,#26595,#26596,#26597,#26598,
#26599,#26600,#26601,#26602,#26603,#26604),.UNSPECIFIED.,.F.,.F.,(4,3,3,
3,3,3,3,4),(320.885511336713,321.793319008267,322.792677141833,323.792035275399,
324.791393408965,325.790751542531,326.790109676097,327.168696643892),
 .UNSPECIFIED.);
#584=B_SPLINE_CURVE_WITH_KNOTS('',3,(#26609,#26610,#26611,#26612,#26613,
#26614,#26615,#26616,#26617,#26618,#26619,#26620,#26621,#26622,#26623,#26624,
#26625,#26626,#26627,#26628,#26629,#26630),.UNSPECIFIED.,.F.,.F.,(4,3,3,
3,3,3,3,4),(-336.707536772222,-335.784332878192,-334.784974744626,-333.78561661106,
-332.786258477494,-331.786900343927,-330.787542210361,-330.424351465042),
 .UNSPECIFIED.);
#585=B_SPLINE_CURVE_WITH_KNOTS('',3,(#26631,#26632,#26633,#26634,#26635,
#26636,#26637,#26638,#26639,#26640,#26641,#26642,#26643,#26644,#26645,#26646,
#26647,#26648,#26649,#26650,#26651,#26652),.UNSPECIFIED.,.F.,.F.,(4,3,3,
3,3,3,3,4),(327.168696643892,327.789467809663,328.78882594323,329.788184076796,
330.787542210362,331.786900343928,332.786258477494,333.451881951072),
 .UNSPECIFIED.);
#586=B_SPLINE_CURVE_WITH_KNOTS('',3,(#26657,#26658,#26659,#26660,#26661,
#26662,#26663,#26664,#26665,#26666,#26667,#26668,#26669,#26670,#26671,#26672,
#26673,#26674,#26675,#26676,#26677,#26678,#26679,#26680,#26681),
 .UNSPECIFIED.,.F.,.F.,(4,3,3,3,3,3,3,3,4),(-342.990722079402,-342.779839813154,
-341.780481679588,-340.781123546022,-339.781765412456,-338.78240727889,
-337.783049145324,-336.783691011758,-336.707536772222),.UNSPECIFIED.);
#587=B_SPLINE_CURVE_WITH_KNOTS('',3,(#26682,#26683,#26684,#26685,#26686,
#26687,#26688,#26689,#26690,#26691,#26692,#26693,#26694,#26695,#26696,#26697,
#26698,#26699,#26700,#26701,#26702,#26703),.UNSPECIFIED.,.F.,.F.,(4,3,3,
3,3,3,3,4),(333.451881951072,333.78561661106,334.784974744626,335.784332878192,
336.783691011758,337.783049145324,338.78240727889,339.735067258252),
 .UNSPECIFIED.);
#588=B_SPLINE_CURVE_WITH_KNOTS('',3,(#26708,#26709,#26710,#26711,#26712,
#26713,#26714,#26715,#26716,#26717,#26718,#26719,#26720,#26721,#26722,#26723,
#26724,#26725,#26726,#26727,#26728,#26729,#26730,#26731,#26732,#26733,#26734,
#26735,#26736,#26737,#26738,#26739,#26740,#26741),.UNSPECIFIED.,.F.,.F.,
(4,3,3,3,3,3,3,3,3,3,3,4),(-349.273907386581,-348.77598861455,-348.276309547767,
-347.776630480984,-347.276951414201,-346.777272347418,-346.277593280635,
-345.777914213852,-345.278235147069,-344.778556080286,-343.77919794672,
-342.990722079402),.UNSPECIFIED.);
#589=B_SPLINE_CURVE_WITH_KNOTS('',3,(#26742,#26743,#26744,#26745,#26746,
#26747,#26748,#26749,#26750,#26751,#26752,#26753,#26754,#26755,#26756,#26757,
#26758,#26759,#26760,#26761,#26762,#26763,#26764,#26765,#26766,#26767,#26768,
#26769),.UNSPECIFIED.,.F.,.F.,(4,3,3,3,3,3,3,3,3,4),(339.735067258252,339.781765412456,
340.781123546022,341.780481679588,342.779839813154,343.77919794672,344.778556080286,
345.278235147069,345.777914213852,346.018252565431),.UNSPECIFIED.);
#590=B_SPLINE_CURVE_WITH_KNOTS('',3,(#26774,#26775,#26776,#26777,#26778,
#26779,#26780,#26781,#26782,#26783,#26784,#26785,#26786,#26787,#26788,#26789,
#26790,#26791,#26792,#26793,#26794,#26795,#26796,#26797,#26798,#26799,#26800,
#26801,#26802,#26803,#26804,#26805,#26806,#26807,#26808,#26809,#26810,#26811,
#26812,#26813,#26814,#26815,#26816),.UNSPECIFIED.,.F.,.F.,(4,3,3,3,3,3,
3,3,3,3,3,3,3,3,4),(-355.557092693761,-355.27181648273,-354.772137415947,
-354.272458349164,-353.77277928238,-353.273100215597,-352.773421148814,
-352.273742082031,-351.774063015248,-351.274383948465,-350.774704881682,
-350.275025814899,-349.775346748116,-349.275667681333,-349.273907386581),
 .UNSPECIFIED.);
#591=B_SPLINE_CURVE_WITH_KNOTS('',3,(#26817,#26818,#26819,#26820,#26821,
#26822,#26823,#26824,#26825,#26826,#26827,#26828,#26829,#26830,#26831,#26832,
#26833,#26834,#26835,#26836,#26837,#26838,#26839,#26840,#26841,#26842,#26843,
#26844,#26845,#26846,#26847,#26848,#26849,#26850,#26851,#26852,#26853,#26854,
#26855,#26856,#26857,#26858,#26859),.UNSPECIFIED.,.F.,.F.,(4,3,3,3,3,3,
3,3,3,3,3,3,3,3,4),(346.018252565431,346.277593280635,346.777272347418,
347.276951414201,347.776630480984,348.276309547767,348.77598861455,349.275667681334,
349.775346748116,350.2750258149,350.774704881683,351.274383948466,351.774063015249,
352.273742082032,352.301437872611),.UNSPECIFIED.);
#592=B_SPLINE_CURVE_WITH_KNOTS('',3,(#26864,#26865,#26866,#26867,#26868,
#26869,#26870,#26871,#26872,#26873,#26874,#26875,#26876,#26877,#26878,#26879,
#26880,#26881,#26882,#26883,#26884,#26885,#26886,#26887,#26888,#26889,#26890,
#26891,#26892,#26893,#26894,#26895,#26896,#26897,#26898,#26899,#26900,#26901,
#26902,#26903,#26904,#26905,#26906),.UNSPECIFIED.,.F.,.F.,(4,3,3,3,3,3,
3,3,3,3,3,3,3,3,4),(-361.84027800094,-361.767644350909,-361.267965284126,
-360.768286217343,-360.26860715056,-359.768928083777,-359.269249016994,
-358.769569950211,-358.269890883428,-357.770211816645,-357.270532749862,
-356.770853683079,-356.271174616296,-355.771495549513,-355.557092693761),
 .UNSPECIFIED.);
#593=B_SPLINE_CURVE_WITH_KNOTS('',3,(#26907,#26908,#26909,#26910,#26911,
#26912,#26913,#26914,#26915,#26916,#26917,#26918,#26919,#26920,#26921,#26922,
#26923,#26924,#26925,#26926,#26927,#26928,#26929,#26930,#26931,#26932,#26933,
#26934,#26935,#26936,#26937,#26938,#26939,#26940,#26941,#26942,#26943,#26944,
#26945,#26946),.UNSPECIFIED.,.F.,.F.,(4,3,3,3,3,3,3,3,3,3,3,3,3,4),(352.301437872611,
352.773421148815,353.273100215598,353.772779282381,354.272458349164,354.772137415947,
355.27181648273,355.771495549513,356.271174616296,356.770853683079,357.270532749862,
357.770211816645,358.269890883428,358.58462317979),.UNSPECIFIED.);
#594=B_SPLINE_CURVE_WITH_KNOTS('',3,(#26951,#26952,#26953,#26954,#26955,
#26956,#26957,#26958,#26959,#26960,#26961,#26962,#26963,#26964,#26965,#26966,
#26967,#26968,#26969,#26970,#26971,#26972,#26973,#26974,#26975,#26976,#26977,
#26978,#26979,#26980,#26981,#26982,#26983,#26984,#26985,#26986,#26987,#26988,
#26989,#26990),.UNSPECIFIED.,.F.,.F.,(4,3,3,3,3,3,3,3,3,3,3,3,3,4),(-368.12346330812,
-367.763793152305,-367.264114085522,-366.764435018739,-366.264755951956,
-365.765076885173,-365.26539781839,-364.765718751607,-364.266039684824,
-363.766360618041,-363.266681551258,-362.767002484475,-362.267323417692,
-361.84027800094),.UNSPECIFIED.);
#595=B_SPLINE_CURVE_WITH_KNOTS('',3,(#26991,#26992,#26993,#26994,#26995,
#26996,#26997,#26998,#26999,#27000,#27001,#27002,#27003,#27004,#27005,#27006,
#27007,#27008,#27009,#27010,#27011,#27012,#27013,#27014,#27015,#27016,#27017,
#27018,#27019,#27020,#27021,#27022,#27023,#27024,#27025,#27026,#27027,#27028,
#27029,#27030,#27031,#27032,#27033),.UNSPECIFIED.,.F.,.F.,(4,3,3,3,3,3,
3,3,3,3,3,3,3,3,4),(358.58462317979,358.769569950211,359.269249016994,359.768928083777,
360.26860715056,360.768286217343,361.267965284126,361.767644350909,362.267323417692,
362.767002484475,363.266681551258,363.766360618041,364.266039684824,364.765718751607,
364.86780848697),.UNSPECIFIED.);
#596=B_SPLINE_CURVE_WITH_KNOTS('',3,(#27038,#27039,#27040,#27041,#27042,
#27043,#27044,#27045,#27046,#27047,#27048,#27049,#27050,#27051,#27052,#27053,
#27054,#27055,#27056,#27057,#27058,#27059,#27060,#27061,#27062,#27063,#27064,
#27065,#27066,#27067,#27068,#27069,#27070,#27071,#27072,#27073,#27074,#27075,
#27076,#27077,#27078,#27079,#27080),.UNSPECIFIED.,.F.,.F.,(4,3,3,3,3,3,
3,3,3,3,3,3,3,3,4),(-374.406648615299,-374.259621020484,-373.759941953701,
-373.260262886918,-372.760583820135,-372.260904753352,-371.761225686569,
-371.261546619786,-370.761867553003,-370.26218848622,-369.762509419437,
-369.262830352654,-368.763151285871,-368.263472219088,-368.12346330812),
 .UNSPECIFIED.);
#597=B_SPLINE_CURVE_WITH_KNOTS('',3,(#27081,#27082,#27083,#27084,#27085,
#27086,#27087,#27088,#27089,#27090,#27091,#27092,#27093,#27094,#27095,#27096,
#27097,#27098,#27099,#27100,#27101,#27102,#27103,#27104,#27105,#27106,#27107,
#27108,#27109,#27110,#27111,#27112,#27113,#27114,#27115,#27116,#27117,#27118,
#27119,#27120),.UNSPECIFIED.,.F.,.F.,(4,3,3,3,3,3,3,3,3,3,3,3,3,4),(364.86780848697,
365.26539781839,365.765076885173,366.264755951956,366.764435018739,367.264114085522,
367.763793152305,368.263472219088,368.763151285871,369.262830352654,369.762509419437,
370.26218848622,370.761867553004,371.150993794149),.UNSPECIFIED.);
#598=B_SPLINE_CURVE_WITH_KNOTS('',3,(#27125,#27126,#27127,#27128,#27129,
#27130,#27131,#27132,#27133,#27134,#27135,#27136,#27137,#27138,#27139,#27140,
#27141,#27142,#27143,#27144,#27145,#27146,#27147,#27148,#27149,#27150,#27151,
#27152,#27153,#27154,#27155,#27156,#27157,#27158,#27159,#27160,#27161,#27162,
#27163,#27164),.UNSPECIFIED.,.F.,.F.,(4,3,3,3,3,3,3,3,3,3,3,3,3,4),(-380.689833922479,
-380.255769821881,-379.756090755098,-379.256411688315,-378.756732621532,
-378.257053554749,-377.757374487966,-377.257695421183,-376.7580163544,-376.258337287616,
-375.758658220834,-375.25897915405,-374.759300087267,-374.406648615299),
 .UNSPECIFIED.);
#599=B_SPLINE_CURVE_WITH_KNOTS('',3,(#27165,#27166,#27167,#27168,#27169,
#27170,#27171,#27172,#27173,#27174,#27175,#27176,#27177,#27178,#27179,#27180,
#27181,#27182,#27183,#27184,#27185,#27186,#27187,#27188,#27189,#27190,#27191,
#27192,#27193,#27194,#27195,#27196,#27197,#27198,#27199,#27200,#27201,#27202,
#27203,#27204,#27205,#27206,#27207),.UNSPECIFIED.,.F.,.F.,(4,3,3,3,3,3,
3,3,3,3,3,3,3,3,4),(371.150993794149,371.261546619787,371.76122568657,372.260904753353,
372.760583820136,373.260262886919,373.759941953702,374.259621020485,374.759300087268,
375.258979154051,375.758658220834,376.258337287617,376.7580163544,377.257695421183,
377.434179101329),.UNSPECIFIED.);
#600=B_SPLINE_CURVE_WITH_KNOTS('',3,(#27212,#27213,#27214,#27215,#27216,
#27217,#27218,#27219,#27220,#27221,#27222,#27223,#27224,#27225,#27226,#27227,
#27228,#27229,#27230,#27231,#27232,#27233,#27234,#27235,#27236,#27237,#27238,
#27239,#27240,#27241,#27242,#27243,#27244,#27245,#27246,#27247,#27248,#27249,
#27250,#27251,#27252,#27253,#27254),.UNSPECIFIED.,.F.,.F.,(4,3,3,3,3,3,
3,3,3,3,3,3,3,3,4),(-386.973019229658,-386.75159769006,-386.251918623277,
-385.752239556494,-385.252560489711,-384.752881422928,-384.253202356145,
-383.753523289362,-383.253844222579,-382.754165155796,-382.254486089013,
-381.75480702223,-381.255127955447,-380.755448888664,-380.689833922479),
 .UNSPECIFIED.);
#601=B_SPLINE_CURVE_WITH_KNOTS('',3,(#27255,#27256,#27257,#27258,#27259,
#27260,#27261,#27262,#27263,#27264,#27265,#27266,#27267,#27268,#27269,#27270,
#27271,#27272,#27273,#27274,#27275,#27276,#27277,#27278,#27279,#27280,#27281,
#27282,#27283,#27284,#27285,#27286,#27287,#27288,#27289,#27290,#27291,#27292,
#27293,#27294),.UNSPECIFIED.,.F.,.F.,(4,3,3,3,3,3,3,3,3,3,3,3,3,4),(377.434179101329,
377.757374487966,378.257053554749,378.756732621532,379.256411688315,379.756090755098,
380.255769821881,380.755448888664,381.255127955447,381.75480702223,382.254486089013,
382.754165155796,383.253844222579,383.717364408508),.UNSPECIFIED.);
#602=B_SPLINE_CURVE_WITH_KNOTS('',3,(#27299,#27300,#27301,#27302,#27303,
#27304,#27305,#27306,#27307,#27308,#27309,#27310,#27311,#27312,#27313,#27314,
#27315,#27316,#27317,#27318,#27319,#27320,#27321,#27322,#27323,#27324,#27325,
#27326,#27327,#27328,#27329,#27330,#27331,#27332,#27333,#27334,#27335,#27336,
#27337,#27338,#27339,#27340,#27341),.UNSPECIFIED.,.F.,.F.,(4,3,3,3,3,3,
3,3,3,3,3,3,3,3,4),(-393.256204536838,-393.247425558239,-392.747746491456,
-392.248067424673,-391.74838835789,-391.248709291107,-390.749030224324,
-390.249351157541,-389.749672090758,-389.249993023975,-388.750313957192,
-388.250634890409,-387.750955823626,-387.251276756843,-386.973019229658),
 .UNSPECIFIED.);
#603=B_SPLINE_CURVE_WITH_KNOTS('',3,(#27342,#27343,#27344,#27345,#27346,
#27347,#27348,#27349,#27350,#27351,#27352,#27353,#27354,#27355,#27356,#27357,
#27358,#27359,#27360,#27361,#27362,#27363,#27364,#27365,#27366,#27367,#27368,
#27369,#27370,#27371,#27372,#27373,#27374,#27375,#27376,#27377,#27378,#27379,
#27380,#27381,#27382,#27383,#27384),.UNSPECIFIED.,.F.,.F.,(4,3,3,3,3,3,
3,3,3,3,3,3,3,3,4),(383.717364408508,383.753523289362,384.253202356145,
384.752881422928,385.252560489711,385.752239556494,386.251918623277,386.75159769006,
387.251276756843,387.750955823626,388.250634890409,388.750313957192,389.249993023975,
389.749672090758,390.000549715688),.UNSPECIFIED.);
#604=B_SPLINE_CURVE_WITH_KNOTS('',3,(#27390,#27391,#27392,#27393),
 .UNSPECIFIED.,.F.,.F.,(4,4),(405.265452313083,405.755527026166),
 .UNSPECIFIED.);
#605=B_SPLINE_CURVE_WITH_KNOTS('',3,(#27399,#27400,#27401,#27402,#27403,
#27404,#27405,#27406,#27407,#27408,#27409,#27410,#27411,#27412,#27413,#27414,
#27415),.UNSPECIFIED.,.F.,.F.,(4,1,1,1,1,1,1,1,1,1,1,1,1,1,4),(398.982267005903,
399.260524533088,399.760203599871,400.259882666654,400.759561733437,401.25924080022,
401.758919867003,402.258598933787,402.75827800057,403.257957067353,403.757636134136,
404.257315200919,404.756994267702,405.256673334485,405.265452313083),
 .UNSPECIFIED.);
#606=B_SPLINE_CURVE_WITH_KNOTS('',3,(#27418,#27419,#27420,#27421,#27422,
#27423,#27424,#27425,#27426,#27427,#27428,#27429,#27430),.UNSPECIFIED.,
 .F.,.F.,(4,1,1,1,1,1,1,1,1,1,4),(398.982267005904,399.231068447758,399.730747514541,
400.230426581324,400.730105648107,401.22978471489,401.729463781673,402.229142848456,
402.728821915239,403.228500982022,403.728180048805),.UNSPECIFIED.);
#607=B_SPLINE_CURVE_WITH_KNOTS('',3,(#27435,#27436,#27437,#27438,#27439,
#27440,#27441,#27442,#27443,#27444,#27445,#27446,#27447,#27448,#27449,#27450,
#27451),.UNSPECIFIED.,.F.,.F.,(4,1,1,1,1,1,1,1,1,1,1,1,1,1,4),(392.699081698724,
392.764696664909,393.264375731692,393.764054798475,394.263733865258,394.763412932041,
395.263091998824,395.762771065607,396.26245013239,396.762129199173,397.261808265956,
397.761487332739,398.261166399522,398.760845466305,398.982267005903),
 .UNSPECIFIED.);
#608=B_SPLINE_CURVE_WITH_KNOTS('',3,(#27452,#27453,#27454,#27455,#27456,
#27457,#27458,#27459,#27460,#27461,#27462,#27463,#27464,#27465,#27466,#27467,
#27468),.UNSPECIFIED.,.F.,.F.,(4,1,1,1,1,1,1,1,1,1,1,1,1,1,4),(392.699081698724,
392.735240579579,393.234919646362,393.734598713145,394.234277779928,394.733956846711,
395.233635913494,395.733314980277,396.23299404706,396.732673113843,397.232352180626,
397.732031247409,398.231710314192,398.731389380975,398.982267005904),
 .UNSPECIFIED.);
#609=B_SPLINE_CURVE_WITH_KNOTS('',3,(#27473,#27474,#27475,#27476,#27477,
#27478,#27479,#27480,#27481,#27482,#27483,#27484,#27485,#27486,#27487,#27488),
 .UNSPECIFIED.,.F.,.F.,(4,1,1,1,1,1,1,1,1,1,1,1,1,4),(386.415896391544,
386.768547863513,387.268226930296,387.767905997079,388.267585063862,388.767264130645,
389.266943197428,389.766622264211,390.266301330994,390.765980397777,391.26565946456,
391.765338531343,392.265017598126,392.699081698724),.UNSPECIFIED.);
#610=B_SPLINE_CURVE_WITH_KNOTS('',3,(#27489,#27490,#27491,#27492,#27493,
#27494,#27495,#27496,#27497,#27498,#27499,#27500,#27501,#27502,#27503,#27504),
 .UNSPECIFIED.,.F.,.F.,(4,1,1,1,1,1,1,1,1,1,1,1,1,4),(386.415896391545,
386.739091778183,387.238770844966,387.738449911749,388.238128978532,388.737808045315,
389.237487112098,389.737166178881,390.236845245664,390.736524312447,391.23620337923,
391.735882446013,392.235561512796,392.699081698724),.UNSPECIFIED.);
#611=B_SPLINE_CURVE_WITH_KNOTS('',3,(#27509,#27510,#27511,#27512,#27513,
#27514,#27515,#27516,#27517,#27518,#27519,#27520,#27521,#27522,#27523,#27524,
#27525),.UNSPECIFIED.,.F.,.F.,(4,1,1,1,1,1,1,1,1,1,1,1,1,1,4),(380.132711084365,
380.272719995333,380.772399062117,381.2720781289,381.771757195683,382.271436262466,
382.771115329249,383.270794396032,383.770473462815,384.270152529598,384.769831596381,
385.269510663164,385.769189729947,386.26886879673,386.415896391544),
 .UNSPECIFIED.);
#612=B_SPLINE_CURVE_WITH_KNOTS('',3,(#27526,#27527,#27528,#27529,#27530,
#27531,#27532,#27533,#27534,#27535,#27536,#27537,#27538,#27539,#27540,#27541,
#27542),.UNSPECIFIED.,.F.,.F.,(4,1,1,1,1,1,1,1,1,1,1,1,1,1,4),(380.132711084365,
380.243263910003,380.742942976786,381.242622043569,381.742301110352,382.241980177135,
382.741659243918,383.241338310702,383.741017377485,384.240696444268,384.740375511051,
385.240054577834,385.739733644617,386.2394127114,386.415896391545),
 .UNSPECIFIED.);
#613=B_SPLINE_CURVE_WITH_KNOTS('',3,(#27547,#27548,#27549,#27550,#27551,
#27552,#27553,#27554,#27555,#27556,#27557,#27558,#27559,#27560,#27561,#27562),
 .UNSPECIFIED.,.F.,.F.,(4,1,1,1,1,1,1,1,1,1,1,1,1,4),(373.849525777185,
374.276571193937,374.77625026072,375.275929327503,375.775608394286,376.275287461069,
376.774966527852,377.274645594635,377.774324661418,378.274003728201,378.773682794984,
379.273361861767,379.77304092855,380.132711084365),.UNSPECIFIED.);
#614=B_SPLINE_CURVE_WITH_KNOTS('',3,(#27563,#27564,#27565,#27566,#27567,
#27568,#27569,#27570,#27571,#27572,#27573,#27574,#27575,#27576,#27577,#27578),
 .UNSPECIFIED.,.F.,.F.,(4,1,1,1,1,1,1,1,1,1,1,1,1,4),(373.849525777185,
374.247115108607,374.74679417539,375.246473242173,375.746152308956,376.245831375739,
376.745510442522,377.245189509305,377.744868576088,378.244547642871,378.744226709654,
379.243905776437,379.74358484322,380.132711084365),.UNSPECIFIED.);
#615=B_SPLINE_CURVE_WITH_KNOTS('',3,(#27583,#27584,#27585,#27586,#27587,
#27588,#27589,#27590,#27591,#27592,#27593,#27594,#27595,#27596,#27597,#27598,
#27599),.UNSPECIFIED.,.F.,.F.,(4,1,1,1,1,1,1,1,1,1,1,1,1,1,4),(367.566340470006,
367.780743325758,368.280422392541,368.780101459324,369.279780526107,369.77945959289,
370.279138659673,370.778817726456,371.278496793239,371.778175860022,372.277854926805,
372.777533993588,373.277213060371,373.776892127154,373.849525777185),
 .UNSPECIFIED.);
#616=B_SPLINE_CURVE_WITH_KNOTS('',3,(#27600,#27601,#27602,#27603,#27604,
#27605,#27606,#27607,#27608,#27609,#27610,#27611,#27612,#27613,#27614,#27615,
#27616),.UNSPECIFIED.,.F.,.F.,(4,1,1,1,1,1,1,1,1,1,1,1,1,1,4),(367.566340470006,
367.751287240428,368.250966307211,368.750645373994,369.250324440777,369.75000350756,
370.249682574343,370.749361641126,371.249040707909,371.748719774692,372.248398841475,
372.748077908258,373.247756975041,373.747436041824,373.849525777185),
 .UNSPECIFIED.);
#617=B_SPLINE_CURVE_WITH_KNOTS('',3,(#27621,#27622,#27623,#27624,#27625,
#27626,#27627,#27628,#27629,#27630,#27631,#27632,#27633,#27634,#27635,#27636,
#27637),.UNSPECIFIED.,.F.,.F.,(4,1,1,1,1,1,1,1,1,1,1,1,1,1,4),(361.283155162826,
361.284915457579,361.784594524362,362.284273591145,362.783952657928,363.283631724711,
363.783310791494,364.282989858277,364.78266892506,365.282347991843,365.782027058626,
366.281706125409,366.781385192192,367.281064258975,367.566340470006),
 .UNSPECIFIED.);
#618=B_SPLINE_CURVE_WITH_KNOTS('',3,(#27638,#27639,#27640,#27641,#27642,
#27643,#27644,#27645,#27646,#27647,#27648,#27649,#27650,#27651,#27652,#27653),
 .UNSPECIFIED.,.F.,.F.,(4,1,1,1,1,1,1,1,1,1,1,1,1,4),(361.283155162826,
361.755138439031,362.254817505815,362.754496572598,363.254175639381,363.753854706164,
364.253533772947,364.75321283973,365.252891906513,365.752570973296,366.252250040079,
366.751929106862,367.251608173645,367.566340470006),.UNSPECIFIED.);
#619=B_SPLINE_CURVE_WITH_KNOTS('',3,(#27658,#27659,#27660,#27661,#27662,
#27663,#27664,#27665,#27666,#27667,#27668,#27669,#27670,#27671),
 .UNSPECIFIED.,.F.,.F.,(4,1,1,1,1,1,1,1,1,1,1,4),(354.999969855646,355.788445722965,
356.787803856531,357.287482923314,357.787161990097,358.28684105688,358.786520123663,
359.286199190446,359.78587825723,360.285557324013,360.785236390796,361.283155162826),
 .UNSPECIFIED.);
#620=B_SPLINE_CURVE_WITH_KNOTS('',3,(#27672,#27673,#27674,#27675,#27676,
#27677,#27678,#27679,#27680,#27681,#27682,#27683,#27684,#27685,#27686,#27687,
#27688),.UNSPECIFIED.,.F.,.F.,(4,1,1,1,1,1,1,1,1,1,1,1,1,1,4),(354.999969855647,
355.259310570852,355.758989637635,356.258668704418,356.758347771201,357.258026837984,
357.757705904767,358.25738497155,358.757064038333,359.256743105116,359.756422171899,
360.256101238682,360.755780305465,361.255459372248,361.283155162826),
 .UNSPECIFIED.);
#621=B_SPLINE_CURVE_WITH_KNOTS('',3,(#27693,#27694,#27695,#27696,#27697,
#27698,#27699,#27700,#27701,#27702,#27703),.UNSPECIFIED.,.F.,.F.,(4,1,1,
1,1,1,1,1,4),(348.716784548467,348.792938788003,349.792296921569,350.791655055135,
351.791013188701,352.790371322267,353.789729455833,354.789087589399,354.999969855646),
 .UNSPECIFIED.);
#622=B_SPLINE_CURVE_WITH_KNOTS('',3,(#27704,#27705,#27706,#27707,#27708,
#27709,#27710,#27711,#27712,#27713,#27714,#27715),.UNSPECIFIED.,.F.,.F.,
(4,1,1,1,1,1,1,1,1,4),(348.716784548467,348.763482702673,349.762840836239,
350.762198969805,351.761557103371,352.760915236937,353.760273370503,354.259952437286,
354.759631504069,354.999969855647),.UNSPECIFIED.);
#623=B_SPLINE_CURVE_WITH_KNOTS('',3,(#27720,#27721,#27722,#27723,#27724,
#27725,#27726,#27727,#27728,#27729),.UNSPECIFIED.,.F.,.F.,(4,1,1,1,1,1,
1,4),(342.433599241287,342.796789986607,343.796148120173,344.795506253739,
345.794864387305,346.794222520871,347.793580654437,348.716784548467),
 .UNSPECIFIED.);
#624=B_SPLINE_CURVE_WITH_KNOTS('',3,(#27730,#27731,#27732,#27733,#27734,
#27735,#27736,#27737,#27738,#27739),.UNSPECIFIED.,.F.,.F.,(4,1,1,1,1,1,
1,4),(342.433599241288,342.767333901277,343.766692034843,344.766050168409,
345.765408301975,346.764766435541,347.764124569107,348.716784548467),
 .UNSPECIFIED.);
#625=B_SPLINE_CURVE_WITH_KNOTS('',3,(#27744,#27745,#27746,#27747,#27748,
#27749,#27750,#27751,#27752,#27753),.UNSPECIFIED.,.F.,.F.,(4,1,1,1,1,1,
1,4),(336.150413934108,336.80064118521,337.799999318776,338.799357452343,
339.798715585909,340.798073719475,341.797431853041,342.433599241287),
 .UNSPECIFIED.);
#626=B_SPLINE_CURVE_WITH_KNOTS('',3,(#27754,#27755,#27756,#27757,#27758,
#27759,#27760,#27761,#27762,#27763),.UNSPECIFIED.,.F.,.F.,(4,1,1,1,1,1,
1,4),(336.150413934108,336.77118509988,337.770543233446,338.769901367012,
339.769259500578,340.768617634145,341.767975767711,342.433599241288),
 .UNSPECIFIED.);
#627=B_SPLINE_CURVE_WITH_KNOTS('',3,(#27768,#27769,#27770,#27771,#27772,
#27773,#27774,#27775,#27776,#27777),.UNSPECIFIED.,.F.,.F.,(4,1,1,1,1,1,
1,4),(329.867228626928,330.804492383814,331.80385051738,332.803208650946,
333.802566784512,334.801924918078,335.801283051644,336.150413934108),
 .UNSPECIFIED.);
#628=B_SPLINE_CURVE_WITH_KNOTS('',3,(#27778,#27779,#27780,#27781,#27782,
#27783,#27784,#27785,#27786,#27787),.UNSPECIFIED.,.F.,.F.,(4,1,1,1,1,1,
1,4),(329.867228626928,330.775036298484,331.77439443205,332.773752565616,
333.773110699182,334.772468832748,335.771826966314,336.150413934108),
 .UNSPECIFIED.);
#629=B_SPLINE_CURVE_WITH_KNOTS('',3,(#27792,#27793,#27794,#27795,#27796,
#27797,#27798,#27799,#27800,#27801,#27802),.UNSPECIFIED.,.F.,.F.,(4,1,1,
1,1,1,1,1,4),(323.584043319749,323.808985448852,324.808343582418,325.807701715984,
326.80705984955,327.806417983116,328.805776116682,329.805134250248,329.867228626928),
 .UNSPECIFIED.);
#630=B_SPLINE_CURVE_WITH_KNOTS('',3,(#27803,#27804,#27805,#27806,#27807,
#27808,#27809,#27810,#27811,#27812,#27813),.UNSPECIFIED.,.F.,.F.,(4,1,1,
1,1,1,1,1,4),(323.584043319749,323.779529363522,324.778887497088,325.778245630654,
326.77760376422,327.776961897786,328.776320031352,329.775678164918,329.867228626928),
 .UNSPECIFIED.);
#631=B_SPLINE_CURVE_WITH_KNOTS('',3,(#27818,#27819,#27820,#27821,#27822,
#27823,#27824,#27825,#27826,#27827),.UNSPECIFIED.,.F.,.F.,(4,1,1,1,1,1,
1,4),(317.300858012569,317.812836647456,318.812194781022,319.811552914588,
320.810911048154,321.81026918172,322.809627315286,323.584043319749),
 .UNSPECIFIED.);
#632=B_SPLINE_CURVE_WITH_KNOTS('',3,(#27828,#27829,#27830,#27831,#27832,
#27833,#27834,#27835,#27836,#27837),.UNSPECIFIED.,.F.,.F.,(4,1,1,1,1,1,
1,4),(317.300858012569,317.783380562125,318.782738695691,319.782096829258,
320.781454962824,321.78081309639,322.780171229956,323.584043319749),
 .UNSPECIFIED.);
#633=B_SPLINE_CURVE_WITH_KNOTS('',3,(#27842,#27843,#27844,#27845,#27846,
#27847,#27848,#27849,#27850,#27851),.UNSPECIFIED.,.F.,.F.,(4,1,1,1,1,1,
1,4),(311.017672705389,311.816687846059,312.816045979625,313.815404113191,
314.814762246757,315.814120380323,316.81347851389,317.300858012569),
 .UNSPECIFIED.);
#634=B_SPLINE_CURVE_WITH_KNOTS('',3,(#27852,#27853,#27854,#27855,#27856,
#27857,#27858,#27859,#27860,#27861),.UNSPECIFIED.,.F.,.F.,(4,1,1,1,1,1,
1,4),(311.01767270539,311.787231760729,312.786589894295,313.785948027861,
314.785306161427,315.784664294993,316.784022428559,317.300858012569),
 .UNSPECIFIED.);
#635=B_SPLINE_CURVE_WITH_KNOTS('',3,(#27866,#27867,#27868,#27869,#27870,
#27871,#27872,#27873,#27874,#27875,#27876),.UNSPECIFIED.,.F.,.F.,(4,1,1,
1,1,1,1,1,4),(304.73448739821,304.821180911097,305.820539044663,306.819897178229,
307.819255311795,308.818613445361,309.817971578927,310.817329712493,311.017672705389),
 .UNSPECIFIED.);
#636=B_SPLINE_CURVE_WITH_KNOTS('',3,(#27877,#27878,#27879,#27880,#27881,
#27882,#27883,#27884,#27885,#27886,#27887),.UNSPECIFIED.,.F.,.F.,(4,1,1,
1,1,1,1,1,4),(304.73448739821,304.791724825767,305.791082959333,306.790441092899,
307.789799226465,308.789157360031,309.788515493597,310.787873627163,311.01767270539),
 .UNSPECIFIED.);
#637=B_SPLINE_CURVE_WITH_KNOTS('',3,(#27892,#27893,#27894,#27895,#27896,
#27897,#27898,#27899,#27900,#27901),.UNSPECIFIED.,.F.,.F.,(4,1,1,1,1,1,
1,4),(298.45130209103,298.825032109701,299.824390243267,300.823748376833,
301.823106510399,302.822464643965,303.821822777531,304.73448739821),
 .UNSPECIFIED.);
#638=B_SPLINE_CURVE_WITH_KNOTS('',3,(#27902,#27903,#27904,#27905,#27906,
#27907,#27908,#27909,#27910,#27911),.UNSPECIFIED.,.F.,.F.,(4,1,1,1,1,1,
1,4),(298.451302091031,298.795576024371,299.794934157937,300.794292291503,
301.793650425069,302.793008558635,303.792366692201,304.73448739821),
 .UNSPECIFIED.);
#639=B_SPLINE_CURVE_WITH_KNOTS('',3,(#27916,#27917,#27918,#27919,#27920,
#27921,#27922,#27923,#27924,#27925),.UNSPECIFIED.,.F.,.F.,(4,1,1,1,1,1,
1,4),(292.168116783851,292.828883308304,293.82824144187,294.827599575437,
295.826957709003,296.826315842569,297.825673976135,298.45130209103),
 .UNSPECIFIED.);
#640=B_SPLINE_CURVE_WITH_KNOTS('',3,(#27926,#27927,#27928,#27929,#27930,
#27931,#27932,#27933,#27934,#27935),.UNSPECIFIED.,.F.,.F.,(4,1,1,1,1,1,
1,4),(292.168116783851,292.799427222974,293.79878535654,294.798143490106,
295.797501623672,296.796859757238,297.796217890804,298.451302091031),
 .UNSPECIFIED.);
#641=B_SPLINE_CURVE_WITH_KNOTS('',3,(#27940,#27941,#27942,#27943,#27944,
#27945,#27946,#27947,#27948,#27949),.UNSPECIFIED.,.F.,.F.,(4,1,1,1,1,1,
1,4),(285.884931476671,286.832734506908,287.832092640474,288.83145077404,
289.830808907606,290.830167041172,291.829525174738,292.168116783851),
 .UNSPECIFIED.);
#642=B_SPLINE_CURVE_WITH_KNOTS('',3,(#27950,#27951,#27952,#27953,#27954,
#27955,#27956,#27957,#27958,#27959),.UNSPECIFIED.,.F.,.F.,(4,1,1,1,1,1,
1,4),(285.884931476672,286.803278421578,287.802636555144,288.80199468871,
289.801352822276,290.800710955842,291.800069089408,292.168116783851),
 .UNSPECIFIED.);
#643=B_SPLINE_CURVE_WITH_KNOTS('',3,(#27964,#27965,#27966,#27967,#27968,
#27969,#27970,#27971,#27972,#27973,#27974),.UNSPECIFIED.,.F.,.F.,(4,1,1,
1,1,1,1,1,4),(279.601746169492,279.837227571946,280.836585705512,281.835943839078,
282.835301972644,283.83466010621,284.834018239776,285.833376373342,285.884931476671),
 .UNSPECIFIED.);
#644=B_SPLINE_CURVE_WITH_KNOTS('',3,(#27975,#27976,#27977,#27978,#27979,
#27980,#27981,#27982,#27983,#27984,#27985),.UNSPECIFIED.,.F.,.F.,(4,1,1,
1,1,1,1,1,4),(279.601746169492,279.807771486616,280.807129620182,281.806487753748,
282.805845887314,283.80520402088,284.804562154446,285.803920288012,285.884931476672),
 .UNSPECIFIED.);
#645=B_SPLINE_CURVE_WITH_KNOTS('',3,(#27990,#27991,#27992,#27993,#27994,
#27995,#27996,#27997,#27998,#27999),.UNSPECIFIED.,.F.,.F.,(4,1,1,1,1,1,
1,4),(273.318560862312,273.84107877055,274.840436904116,275.839795037682,
276.839153171248,277.838511304814,278.83786943838,279.601746169492),
 .UNSPECIFIED.);
#646=B_SPLINE_CURVE_WITH_KNOTS('',3,(#28000,#28001,#28002,#28003,#28004,
#28005,#28006,#28007,#28008,#28009),.UNSPECIFIED.,.F.,.F.,(4,1,1,1,1,1,
1,4),(273.318560862312,273.811622685219,274.810980818785,275.810338952351,
276.809697085917,277.809055219484,278.80841335305,279.601746169492),
 .UNSPECIFIED.);
#647=B_SPLINE_CURVE_WITH_KNOTS('',3,(#28014,#28015,#28016,#28017,#28018,
#28019,#28020,#28021,#28022,#28023),.UNSPECIFIED.,.F.,.F.,(4,1,1,1,1,1,
1,4),(267.035375555133,267.844929969153,268.844288102719,269.843646236285,
270.843004369851,271.842362503417,272.841720636983,273.318560862312),
 .UNSPECIFIED.);
#648=B_SPLINE_CURVE_WITH_KNOTS('',3,(#28024,#28025,#28026,#28027,#28028,
#28029,#28030,#28031,#28032,#28033),.UNSPECIFIED.,.F.,.F.,(4,1,1,1,1,1,
1,4),(267.035375555133,267.815473883823,268.814832017389,269.814190150955,
270.813548284521,271.812906418087,272.812264551653,273.318560862312),
 .UNSPECIFIED.);
#649=B_SPLINE_CURVE_WITH_KNOTS('',3,(#28038,#28039,#28040,#28041,#28042,
#28043,#28044,#28045,#28046,#28047,#28048),.UNSPECIFIED.,.F.,.F.,(4,1,1,
1,1,1,1,1,4),(260.752190247953,260.849423034191,261.848781167757,262.848139301323,
263.847497434889,264.846855568455,265.846213702021,266.845571835587,267.035375555133),
 .UNSPECIFIED.);
#650=B_SPLINE_CURVE_WITH_KNOTS('',3,(#28049,#28050,#28051,#28052,#28053,
#28054,#28055,#28056,#28057,#28058,#28059),.UNSPECIFIED.,.F.,.F.,(4,1,1,
1,1,1,1,1,4),(260.752190247953,260.819966948861,261.819325082427,262.818683215993,
263.818041349559,264.817399483125,265.816757616691,266.816115750257,267.035375555133),
 .UNSPECIFIED.);
#651=B_SPLINE_CURVE_WITH_KNOTS('',3,(#28064,#28065,#28066,#28067,#28068,
#28069,#28070,#28071,#28072,#28073),.UNSPECIFIED.,.F.,.F.,(4,1,1,1,1,1,
1,4),(254.469004940773,254.853274232795,255.852632366361,256.851990499927,
257.851348633493,258.850706767059,259.850064900625,260.752190247953),
 .UNSPECIFIED.);
#652=B_SPLINE_CURVE_WITH_KNOTS('',3,(#28074,#28075,#28076,#28077,#28078,
#28079,#28080,#28081,#28082,#28083),.UNSPECIFIED.,.F.,.F.,(4,1,1,1,1,1,
1,4),(254.469004940774,254.823818147464,255.82317628103,256.822534414597,
257.821892548163,258.821250681729,259.820608815295,260.752190247953),
 .UNSPECIFIED.);
#653=B_SPLINE_CURVE_WITH_KNOTS('',3,(#28088,#28089,#28090,#28091,#28092,
#28093,#28094,#28095,#28096,#28097),.UNSPECIFIED.,.F.,.F.,(4,1,1,1,1,1,
1,4),(248.185819633594,248.857125431398,249.856483564964,250.85584169853,
251.855199832097,252.854557965663,253.853916099229,254.469004940773),
 .UNSPECIFIED.);
#654=B_SPLINE_CURVE_WITH_KNOTS('',3,(#28098,#28099,#28100,#28101,#28102,
#28103,#28104,#28105,#28106,#28107),.UNSPECIFIED.,.F.,.F.,(4,1,1,1,1,1,
1,4),(248.185819633594,248.827669346068,249.827027479634,250.8263856132,
251.825743746766,252.825101880332,253.824460013898,254.469004940774),
 .UNSPECIFIED.);
#655=B_SPLINE_CURVE_WITH_KNOTS('',3,(#28112,#28113,#28114,#28115,#28116,
#28117,#28118,#28119,#28120,#28121),.UNSPECIFIED.,.F.,.F.,(4,1,1,1,1,1,
1,4),(241.902634326414,242.860976630002,243.860334763568,244.859692897134,
245.8590510307,246.858409164266,247.857767297832,248.185819633594),
 .UNSPECIFIED.);
#656=B_SPLINE_CURVE_WITH_KNOTS('',3,(#28122,#28123,#28124,#28125,#28126,
#28127,#28128,#28129,#28130,#28131),.UNSPECIFIED.,.F.,.F.,(4,1,1,1,1,1,
1,4),(241.902634326415,242.831520544672,243.830878678238,244.830236811804,
245.82959494537,246.828953078936,247.828311212502,248.185819633594),
 .UNSPECIFIED.);
#657=B_SPLINE_CURVE_WITH_KNOTS('',3,(#28136,#28137,#28138,#28139,#28140,
#28141,#28142,#28143,#28144,#28145,#28146),.UNSPECIFIED.,.F.,.F.,(4,1,1,
1,1,1,1,1,4),(235.619449019235,235.86546969504,236.864827828606,237.864185962172,
238.863544095738,239.862902229304,240.86226036287,241.861618496436,241.902634326414),
 .UNSPECIFIED.);
#658=B_SPLINE_CURVE_WITH_KNOTS('',3,(#28147,#28148,#28149,#28150,#28151,
#28152,#28153,#28154,#28155,#28156,#28157),.UNSPECIFIED.,.F.,.F.,(4,1,1,
1,1,1,1,1,4),(235.619449019235,235.83601360971,236.835371743276,237.834729876842,
238.834088010408,239.833446143974,240.83280427754,241.832162411106,241.902634326415),
 .UNSPECIFIED.);
#659=B_SPLINE_CURVE_WITH_KNOTS('',3,(#28162,#28163,#28164,#28165,#28166,
#28167,#28168,#28169,#28170,#28171),.UNSPECIFIED.,.F.,.F.,(4,1,1,1,1,1,
1,4),(229.336263712055,229.869320893643,230.86867902721,231.868037160776,
232.867395294342,233.866753427908,234.866111561474,235.619449019235),
 .UNSPECIFIED.);
#660=B_SPLINE_CURVE_WITH_KNOTS('',3,(#28172,#28173,#28174,#28175,#28176,
#28177,#28178,#28179,#28180,#28181),.UNSPECIFIED.,.F.,.F.,(4,1,1,1,1,1,
1,4),(229.336263712055,229.839864808313,230.839222941879,231.838581075445,
232.837939209011,233.837297342577,234.836655476144,235.619449019235),
 .UNSPECIFIED.);
#661=B_SPLINE_CURVE_WITH_KNOTS('',3,(#28186,#28187,#28188,#28189,#28190,
#28191,#28192,#28193,#28194,#28195),.UNSPECIFIED.,.F.,.F.,(4,1,1,1,1,1,
1,4),(223.053078404876,223.873172092247,224.872530225813,225.871888359379,
226.871246492945,227.870604626511,228.869962760077,229.336263712055),
 .UNSPECIFIED.);
#662=B_SPLINE_CURVE_WITH_KNOTS('',3,(#28196,#28197,#28198,#28199,#28200,
#28201,#28202,#28203,#28204,#28205),.UNSPECIFIED.,.F.,.F.,(4,1,1,1,1,1,
1,4),(223.053078404876,223.843716006917,224.843074140483,225.842432274049,
226.841790407615,227.841148541181,228.840506674747,229.336263712055),
 .UNSPECIFIED.);
#663=B_SPLINE_CURVE_WITH_KNOTS('',3,(#28210,#28211,#28212,#28213,#28214,
#28215,#28216,#28217,#28218,#28219,#28220),.UNSPECIFIED.,.F.,.F.,(4,1,1,
1,1,1,1,1,4),(216.769893097696,216.877665157285,217.877023290851,218.876381424417,
219.875739557983,220.875097691549,221.874455825115,222.873813958681,223.053078404876),
 .UNSPECIFIED.);
#664=B_SPLINE_CURVE_WITH_KNOTS('',3,(#28221,#28222,#28223,#28224,#28225,
#28226,#28227,#28228,#28229,#28230,#28231),.UNSPECIFIED.,.F.,.F.,(4,1,1,
1,1,1,1,1,4),(216.769893097696,216.848209071955,217.847567205521,218.846925339087,
219.846283472653,220.845641606219,221.844999739785,222.844357873351,223.053078404876),
 .UNSPECIFIED.);
#665=B_SPLINE_CURVE_WITH_KNOTS('',3,(#28236,#28237,#28238,#28239,#28240,
#28241,#28242,#28243,#28244,#28245),.UNSPECIFIED.,.F.,.F.,(4,1,1,1,1,1,
1,4),(210.486707790516,210.881516355889,211.880874489455,212.880232623021,
213.879590756587,214.878948890153,215.878307023719,216.769893097696),
 .UNSPECIFIED.);
#666=B_SPLINE_CURVE_WITH_KNOTS('',3,(#28246,#28247,#28248,#28249,#28250,
#28251,#28252,#28253,#28254,#28255),.UNSPECIFIED.,.F.,.F.,(4,1,1,1,1,1,
1,4),(210.486707790517,210.852060270558,211.851418404124,212.85077653769,
213.850134671257,214.849492804823,215.848850938389,216.769893097696),
 .UNSPECIFIED.);
#667=B_SPLINE_CURVE_WITH_KNOTS('',3,(#28260,#28261,#28262,#28263,#28264,
#28265,#28266,#28267,#28268,#28269),.UNSPECIFIED.,.F.,.F.,(4,1,1,1,1,1,
1,4),(204.203522483337,204.885367554492,205.884725688058,206.884083821624,
207.88344195519,208.882800088756,209.882158222323,210.486707790516),
 .UNSPECIFIED.);
#668=B_SPLINE_CURVE_WITH_KNOTS('',3,(#28270,#28271,#28272,#28273,#28274,
#28275,#28276,#28277,#28278,#28279),.UNSPECIFIED.,.F.,.F.,(4,1,1,1,1,1,
1,4),(204.203522483337,204.855911469162,205.855269602728,206.854627736294,
207.85398586986,208.853344003426,209.852702136992,210.486707790517),
 .UNSPECIFIED.);
#669=B_SPLINE_CURVE_WITH_KNOTS('',3,(#28284,#28285,#28286,#28287,#28288,
#28289,#28290,#28291,#28292,#28293),.UNSPECIFIED.,.F.,.F.,(4,1,1,1,1,1,
1,4),(197.920337176157,198.889218753096,199.888576886662,200.887935020228,
201.887293153794,202.88665128736,203.886009420926,204.203522483337),
 .UNSPECIFIED.);
#670=B_SPLINE_CURVE_WITH_KNOTS('',3,(#28294,#28295,#28296,#28297,#28298,
#28299,#28300,#28301,#28302,#28303),.UNSPECIFIED.,.F.,.F.,(4,1,1,1,1,1,
1,4),(197.920337176158,198.859762667766,199.859120801332,200.858478934898,
201.857837068464,202.85719520203,203.856553335596,204.203522483337),
 .UNSPECIFIED.);
#671=B_SPLINE_CURVE_WITH_KNOTS('',3,(#28308,#28309,#28310,#28311,#28312,
#28313,#28314,#28315,#28316,#28317,#28318),.UNSPECIFIED.,.F.,.F.,(4,1,1,
1,1,1,1,1,4),(191.637151868978,191.893711818134,192.8930699517,193.892428085266,
194.891786218832,195.891144352398,196.890502485964,197.88986061953,197.920337176157),
 .UNSPECIFIED.);
#672=B_SPLINE_CURVE_WITH_KNOTS('',3,(#28319,#28320,#28321,#28322,#28323,
#28324,#28325,#28326,#28327,#28328,#28329),.UNSPECIFIED.,.F.,.F.,(4,1,1,
1,1,1,1,1,4),(191.637151868978,191.864255732803,192.86361386637,193.862971999936,
194.862330133502,195.861688267068,196.861046400634,197.8604045342,197.920337176158),
 .UNSPECIFIED.);
#673=B_SPLINE_CURVE_WITH_KNOTS('',3,(#28334,#28335,#28336,#28337,#28338,
#28339,#28340,#28341,#28342,#28343),.UNSPECIFIED.,.F.,.F.,(4,1,1,1,1,1,
1,4),(185.353966561798,185.897563016737,186.896921150303,187.89627928387,
188.895637417436,189.894995551002,190.894353684568,191.637151868978),
 .UNSPECIFIED.);
#674=B_SPLINE_CURVE_WITH_KNOTS('',3,(#28344,#28345,#28346,#28347,#28348,
#28349,#28350,#28351,#28352,#28353),.UNSPECIFIED.,.F.,.F.,(4,1,1,1,1,1,
1,4),(185.353966561799,185.868106931407,186.867465064973,187.866823198539,
188.866181332105,189.865539465671,190.864897599237,191.637151868978),
 .UNSPECIFIED.);
#675=B_SPLINE_CURVE_WITH_KNOTS('',3,(#28358,#28359,#28360,#28361,#28362,
#28363,#28364,#28365,#28366,#28367),.UNSPECIFIED.,.F.,.F.,(4,1,1,1,1,1,
1,4),(179.070781254619,179.901414215341,180.900772348907,181.900130482473,
182.899488616039,183.898846749605,184.898204883171,185.353966561798),
 .UNSPECIFIED.);
#676=B_SPLINE_CURVE_WITH_KNOTS('',3,(#28368,#28369,#28370,#28371,#28372,
#28373,#28374,#28375,#28376,#28377),.UNSPECIFIED.,.F.,.F.,(4,1,1,1,1,1,
1,4),(179.070781254619,179.871958130011,180.871316263577,181.870674397143,
182.870032530709,183.869390664275,184.868748797841,185.353966561799),
 .UNSPECIFIED.);
#677=B_SPLINE_CURVE_WITH_KNOTS('',3,(#28382,#28383,#28384,#28385,#28386,
#28387,#28388,#28389,#28390,#28391,#28392),.UNSPECIFIED.,.F.,.F.,(4,1,1,
1,1,1,1,1,4),(172.787595947439,172.905907280379,173.905265413945,174.904623547511,
175.903981681077,176.903339814643,177.902697948209,178.902056081775,179.070781254619),
 .UNSPECIFIED.);
#678=B_SPLINE_CURVE_WITH_KNOTS('',3,(#28393,#28394,#28395,#28396,#28397,
#28398,#28399,#28400,#28401,#28402,#28403),.UNSPECIFIED.,.F.,.F.,(4,1,1,
1,1,1,1,1,4),(172.787595947439,172.876451195049,173.875809328615,174.875167462181,
175.874525595747,176.873883729313,177.873241862879,178.872599996445,179.070781254619),
 .UNSPECIFIED.);
#679=B_SPLINE_CURVE_WITH_KNOTS('',3,(#28408,#28409,#28410,#28411,#28412,
#28413,#28414,#28415,#28416,#28417),.UNSPECIFIED.,.F.,.F.,(4,1,1,1,1,1,
1,4),(166.504410640259,166.909758478983,167.909116612549,168.908474746115,
169.907832879681,170.907191013247,171.906549146813,172.787595947439),
 .UNSPECIFIED.);
#680=B_SPLINE_CURVE_WITH_KNOTS('',3,(#28418,#28419,#28420,#28421,#28422,
#28423,#28424,#28425,#28426,#28427),.UNSPECIFIED.,.F.,.F.,(4,1,1,1,1,1,
1,4),(166.50441064026,166.880302393652,167.879660527218,168.879018660784,
169.87837679435,170.877734927916,171.877093061483,172.787595947439),
 .UNSPECIFIED.);
#681=B_SPLINE_CURVE_WITH_KNOTS('',3,(#28432,#28433,#28434,#28435,#28436,
#28437,#28438,#28439,#28440,#28441),.UNSPECIFIED.,.F.,.F.,(4,1,1,1,1,1,
1,4),(160.22122533308,160.913609677586,161.912967811152,162.912325944718,
163.911684078284,164.91104221185,165.910400345416,166.504410640259),
 .UNSPECIFIED.);
#682=B_SPLINE_CURVE_WITH_KNOTS('',3,(#28442,#28443,#28444,#28445,#28446,
#28447,#28448,#28449,#28450,#28451),.UNSPECIFIED.,.F.,.F.,(4,1,1,1,1,1,
1,4),(160.22122533308,160.884153592256,161.883511725822,162.882869859388,
163.882227992954,164.88158612652,165.880944260086,166.50441064026),
 .UNSPECIFIED.);
#683=B_SPLINE_CURVE_WITH_KNOTS('',3,(#28456,#28457,#28458,#28459,#28460,
#28461,#28462,#28463,#28464,#28465),.UNSPECIFIED.,.F.,.F.,(4,1,1,1,1,1,
1,4),(153.9380400259,154.91746087619,155.916819009756,156.916177143322,
157.915535276888,158.914893410454,159.91425154402,160.22122533308),
 .UNSPECIFIED.);
#684=B_SPLINE_CURVE_WITH_KNOTS('',3,(#28466,#28467,#28468,#28469,#28470,
#28471,#28472,#28473,#28474,#28475),.UNSPECIFIED.,.F.,.F.,(4,1,1,1,1,1,
1,4),(153.938040025901,154.88800479086,155.887362924426,156.886721057992,
157.886079191558,158.885437325124,159.88479545869,160.22122533308),
 .UNSPECIFIED.);
#685=B_SPLINE_CURVE_WITH_KNOTS('',3,(#28480,#28481,#28482,#28483,#28484,
#28485,#28486,#28487,#28488,#28489,#28490),.UNSPECIFIED.,.F.,.F.,(4,1,1,
1,1,1,1,1,4),(147.654854718721,147.921953941228,148.921312074794,149.92067020836,
150.920028341926,151.919386475492,152.918744609058,153.918102742624,153.9380400259),
 .UNSPECIFIED.);
#686=B_SPLINE_CURVE_WITH_KNOTS('',3,(#28491,#28492,#28493,#28494,#28495,
#28496,#28497,#28498,#28499,#28500,#28501),.UNSPECIFIED.,.F.,.F.,(4,1,1,
1,1,1,1,1,4),(147.654854718721,147.892497855897,148.891855989463,149.891214123029,
150.890572256596,151.889930390162,152.889288523728,153.888646657294,153.938040025901),
 .UNSPECIFIED.);
#687=B_SPLINE_CURVE_WITH_KNOTS('',3,(#28506,#28507,#28508,#28509,#28510,
#28511,#28512,#28513,#28514,#28515),.UNSPECIFIED.,.F.,.F.,(4,1,1,1,1,1,
1,4),(141.371669411541,141.925805139831,142.925163273397,143.924521406963,
144.92387954053,145.923237674096,146.922595807662,147.654854718721),
 .UNSPECIFIED.);
#688=B_SPLINE_CURVE_WITH_KNOTS('',3,(#28516,#28517,#28518,#28519,#28520,
#28521,#28522,#28523,#28524,#28525),.UNSPECIFIED.,.F.,.F.,(4,1,1,1,1,1,
1,4),(141.371669411542,141.896349054501,142.895707188067,143.895065321633,
144.894423455199,145.893781588765,146.893139722331,147.654854718721),
 .UNSPECIFIED.);
#689=B_SPLINE_CURVE_WITH_KNOTS('',3,(#28530,#28531,#28532,#28533,#28534,
#28535,#28536,#28537,#28538,#28539),.UNSPECIFIED.,.F.,.F.,(4,1,1,1,1,1,
1,4),(135.088484104362,135.929656338435,136.929014472001,137.928372605567,
138.927730739133,139.927088872699,140.926447006265,141.371669411541),
 .UNSPECIFIED.);
#690=B_SPLINE_CURVE_WITH_KNOTS('',3,(#28540,#28541,#28542,#28543,#28544,
#28545,#28546,#28547,#28548,#28549),.UNSPECIFIED.,.F.,.F.,(4,1,1,1,1,1,
1,4),(135.088484104362,135.900200253105,136.899558386671,137.898916520237,
138.898274653803,139.897632787369,140.896990920935,141.371669411542),
 .UNSPECIFIED.);
#691=B_SPLINE_CURVE_WITH_KNOTS('',3,(#28554,#28555,#28556,#28557,#28558,
#28559,#28560,#28561,#28562,#28563,#28564),.UNSPECIFIED.,.F.,.F.,(4,1,1,
1,1,1,1,1,4),(128.805298797182,128.934149403473,129.933507537039,130.932865670605,
131.932223804171,132.931581937737,133.930940071303,134.930298204869,135.088484104362),
 .UNSPECIFIED.);
#692=B_SPLINE_CURVE_WITH_KNOTS('',3,(#28565,#28566,#28567,#28568,#28569,
#28570,#28571,#28572,#28573,#28574,#28575),.UNSPECIFIED.,.F.,.F.,(4,1,1,
1,1,1,1,1,4),(128.805298797182,128.904693318142,129.904051451709,130.903409585275,
131.902767718841,132.902125852407,133.901483985973,134.900842119539,135.088484104362),
 .UNSPECIFIED.);
#693=B_SPLINE_CURVE_WITH_KNOTS('',3,(#28580,#28581,#28582,#28583,#28584,
#28585,#28586,#28587,#28588,#28589),.UNSPECIFIED.,.F.,.F.,(4,1,1,1,1,1,
1,4),(122.522113490002,122.938000602077,123.937358735643,124.936716869209,
125.936075002775,126.935433136341,127.934791269907,128.805298797182),
 .UNSPECIFIED.);
#694=B_SPLINE_CURVE_WITH_KNOTS('',3,(#28590,#28591,#28592,#28593,#28594,
#28595,#28596,#28597,#28598,#28599),.UNSPECIFIED.,.F.,.F.,(4,1,1,1,1,1,
1,4),(122.522113490003,122.908544516746,123.907902650312,124.907260783878,
125.906618917444,126.90597705101,127.905335184576,128.805298797182),
 .UNSPECIFIED.);
#695=B_SPLINE_CURVE_WITH_KNOTS('',3,(#28604,#28605,#28606,#28607,#28608,
#28609,#28610,#28611,#28612,#28613),.UNSPECIFIED.,.F.,.F.,(4,1,1,1,1,1,
1,4),(116.238928182823,116.94185180068,117.941209934246,118.940568067812,
119.939926201378,120.939284334944,121.93864246851,122.522113490002),
 .UNSPECIFIED.);
#696=B_SPLINE_CURVE_WITH_KNOTS('',3,(#28614,#28615,#28616,#28617,#28618,
#28619,#28620,#28621,#28622,#28623),.UNSPECIFIED.,.F.,.F.,(4,1,1,1,1,1,
1,4),(116.238928182823,116.91239571535,117.911753848916,118.911111982482,
119.910470116048,120.909828249614,121.90918638318,122.522113490003),
 .UNSPECIFIED.);
#697=B_SPLINE_CURVE_WITH_KNOTS('',3,(#28628,#28629,#28630,#28631,#28632,
#28633,#28634,#28635,#28636,#28637),.UNSPECIFIED.,.F.,.F.,(4,1,1,1,1,1,
1,4),(109.955742875643,110.945702999284,111.94506113285,112.944419266416,
113.943777399982,114.943135533548,115.942493667114,116.238928182823),
 .UNSPECIFIED.);
#698=B_SPLINE_CURVE_WITH_KNOTS('',3,(#28638,#28639,#28640,#28641,#28642,
#28643,#28644,#28645,#28646,#28647),.UNSPECIFIED.,.F.,.F.,(4,1,1,1,1,1,
1,4),(109.955742875644,110.916246913954,111.91560504752,112.914963181086,
113.914321314652,114.913679448218,115.913037581784,116.238928182823),
 .UNSPECIFIED.);
#699=B_SPLINE_CURVE_WITH_KNOTS('',3,(#28652,#28653,#28654,#28655,#28656,
#28657,#28658,#28659,#28660,#28661,#28662),.UNSPECIFIED.,.F.,.F.,(4,1,1,
1,1,1,1,1,4),(103.672557568464,103.950196064322,104.949554197888,105.948912331454,
106.94827046502,107.947628598586,108.946986732152,109.946344865718,109.955742875643),
 .UNSPECIFIED.);
#700=B_SPLINE_CURVE_WITH_KNOTS('',3,(#28663,#28664,#28665,#28666,#28667,
#28668,#28669,#28670,#28671,#28672,#28673),.UNSPECIFIED.,.F.,.F.,(4,1,1,
1,1,1,1,1,4),(103.672557568464,103.920739978991,104.920098112557,105.919456246123,
106.918814379689,107.918172513255,108.917530646822,109.916888780388,109.955742875644),
 .UNSPECIFIED.);
#701=B_SPLINE_CURVE_WITH_KNOTS('',3,(#28678,#28679,#28680,#28681,#28682,
#28683,#28684,#28685,#28686,#28687),.UNSPECIFIED.,.F.,.F.,(4,1,1,1,1,1,
1,4),(97.3893722612841,97.9540472629253,98.9534053964914,99.9527635300574,
100.952121663623,101.95147979719,102.950837930756,103.672557568464),
 .UNSPECIFIED.);
#702=B_SPLINE_CURVE_WITH_KNOTS('',3,(#28688,#28689,#28690,#28691,#28692,
#28693,#28694,#28695,#28696,#28697),.UNSPECIFIED.,.F.,.F.,(4,1,1,1,1,1,
1,4),(97.3893722612845,97.924591177595,98.9239493111611,99.9233074447271,
100.922665578293,101.922023711859,102.921381845425,103.672557568464),
 .UNSPECIFIED.);
#703=B_SPLINE_CURVE_WITH_KNOTS('',3,(#28702,#28703,#28704,#28705,#28706,
#28707,#28708,#28709,#28710,#28711),.UNSPECIFIED.,.F.,.F.,(4,1,1,1,1,1,
1,4),(91.1061869541045,91.9578984615291,92.9572565950951,93.9566147286612,
94.9559728622272,95.9553309957932,96.9546891293593,97.3893722612841),
 .UNSPECIFIED.);
#704=B_SPLINE_CURVE_WITH_KNOTS('',3,(#28712,#28713,#28714,#28715,#28716,
#28717,#28718,#28719,#28720,#28721),.UNSPECIFIED.,.F.,.F.,(4,1,1,1,1,1,
1,4),(91.1061869541048,91.9284423761987,92.9278005097648,93.9271586433308,
94.9265167768969,95.9258749104629,96.925233044029,97.3893722612845),
 .UNSPECIFIED.);
#705=B_SPLINE_CURVE_WITH_KNOTS('',3,(#28726,#28727,#28728,#28729,#28730,
#28731,#28732,#28733,#28734,#28735,#28736),.UNSPECIFIED.,.F.,.F.,(4,1,1,
1,1,1,1,1,4),(84.8230016469249,84.9623915265667,85.9617496601328,86.9611077936988,
87.9604659272649,88.9598240608309,89.959182194397,90.958540327963,91.1061869541045),
 .UNSPECIFIED.);
#706=B_SPLINE_CURVE_WITH_KNOTS('',3,(#28737,#28738,#28739,#28740,#28741,
#28742,#28743,#28744,#28745,#28746,#28747),.UNSPECIFIED.,.F.,.F.,(4,1,1,
1,1,1,1,1,4),(84.8230016469253,84.9329354412364,85.9322935748025,86.9316517083685,
87.9310098419346,88.9303679755006,89.9297261090666,90.9290842426327,91.1061869541048),
 .UNSPECIFIED.);
#707=B_SPLINE_CURVE_WITH_KNOTS('',3,(#28752,#28753,#28754,#28755,#28756,
#28757,#28758,#28759,#28760,#28761),.UNSPECIFIED.,.F.,.F.,(4,1,1,1,1,1,
1,4),(78.5398163397454,78.9662427251705,79.9656008587365,80.9649589923026,
81.9643171258686,82.9636752594347,83.9630333930007,84.8230016469249),
 .UNSPECIFIED.);
#708=B_SPLINE_CURVE_WITH_KNOTS('',3,(#28762,#28763,#28764,#28765,#28766,
#28767,#28768,#28769,#28770,#28771),.UNSPECIFIED.,.F.,.F.,(4,1,1,1,1,1,
1,4),(78.5398163397457,78.9367866398401,79.9361447734062,80.9355029069722,
81.9348610405383,82.9342191741043,83.9335773076704,84.8230016469253),
 .UNSPECIFIED.);
#709=B_SPLINE_CURVE_WITH_KNOTS('',3,(#28776,#28777,#28778,#28779,#28780,
#28781,#28782,#28783,#28784,#28785),.UNSPECIFIED.,.F.,.F.,(4,1,1,1,1,1,
1,4),(72.2566310325658,72.9700939237742,73.9694520573402,74.9688101909063,
75.9681683244723,76.9675264580384,77.9668845916044,78.5398163397454),
 .UNSPECIFIED.);
#710=B_SPLINE_CURVE_WITH_KNOTS('',3,(#28786,#28787,#28788,#28789,#28790,
#28791,#28792,#28793,#28794,#28795),.UNSPECIFIED.,.F.,.F.,(4,1,1,1,1,1,
1,4),(72.2566310325661,72.9406378384438,73.9399959720099,74.9393541055759,
75.938712239142,76.938070372708,77.9374285062741,78.5398163397457),
 .UNSPECIFIED.);
#711=B_SPLINE_CURVE_WITH_KNOTS('',3,(#28800,#28801,#28802,#28803,#28804,
#28805,#28806,#28807,#28808,#28809,#28810),.UNSPECIFIED.,.F.,.F.,(4,1,1,
1,1,1,1,1,4),(65.9734457253862,65.9745869888119,66.9739451223779,67.9733032559439,
68.97266138951,69.972019523076,70.9713776566421,71.9707357902081,72.2566310325658),
 .UNSPECIFIED.);
#712=B_SPLINE_CURVE_WITH_KNOTS('',3,(#28811,#28812,#28813,#28814,#28815,
#28816,#28817,#28818,#28819,#28820),.UNSPECIFIED.,.F.,.F.,(4,1,1,1,1,1,
1,4),(65.9734457253865,66.9444890370476,67.9438471706136,68.9432053041797,
69.9425634377457,70.9419215713118,71.9412797048778,72.2566310325661),
 .UNSPECIFIED.);
#713=B_SPLINE_CURVE_WITH_KNOTS('',3,(#28825,#28826,#28827,#28828,#28829,
#28830,#28831,#28832,#28833,#28834,#28835,#28836),.UNSPECIFIED.,.F.,.F.,
(4,1,1,1,1,1,1,1,1,4),(59.6902604182066,59.9784381874156,60.4781172541986,
60.9777963209816,61.4774753877646,61.9771544545477,62.9765125881137,63.9758707216798,
64.9752288552458,65.9734457253862),.UNSPECIFIED.);
#714=B_SPLINE_CURVE_WITH_KNOTS('',3,(#28837,#28838,#28839,#28840,#28841,
#28842,#28843,#28844,#28845,#28846,#28847),.UNSPECIFIED.,.F.,.F.,(4,1,1,
1,1,1,1,1,4),(59.6902604182069,59.9489821020852,60.9483402356513,61.9476983692173,
62.9470565027834,63.9464146363494,64.9457727699155,65.9451309034815,65.9734457253865),
 .UNSPECIFIED.);
#715=B_SPLINE_CURVE_WITH_KNOTS('',3,(#28852,#28853,#28854,#28855,#28856,
#28857,#28858,#28859,#28860,#28861,#28862,#28863,#28864,#28865,#28866,#28867,
#28868),.UNSPECIFIED.,.F.,.F.,(4,1,1,1,1,1,1,1,1,1,1,1,1,1,4),(53.407075111027,
53.4826103192363,53.9822893860193,54.4819684528023,54.9816475195853,55.4813265863684,
55.9810056531514,56.4806847199344,56.9803637867174,57.4800428535005,57.9797219202835,
58.4794009870665,58.9790800538495,59.4787591206325,59.6902604182066),
 .UNSPECIFIED.);
#716=B_SPLINE_CURVE_WITH_KNOTS('',3,(#28869,#28870,#28871,#28872,#28873,
#28874,#28875,#28876,#28877,#28878,#28879,#28880,#28881,#28882,#28883,#28884),
 .UNSPECIFIED.,.F.,.F.,(4,1,1,1,1,1,1,1,1,1,1,1,1,4),(53.4070751110273,
53.4531542339059,53.9528333006889,54.452512367472,54.952191434255,55.451870501038,
55.951549567821,56.4512286346041,56.9509077013871,57.4505867681701,57.9502658349531,
58.4499449017362,58.9496239685192,59.6902604182069),.UNSPECIFIED.);
#717=B_SPLINE_CURVE_WITH_KNOTS('',3,(#28889,#28890,#28891,#28892,#28893,
#28894,#28895,#28896,#28897,#28898,#28899,#28900,#28901,#28902,#28903,#28904),
 .UNSPECIFIED.,.F.,.F.,(4,1,1,1,1,1,1,1,1,1,1,1,1,4),(47.1238898038474,
47.48646151784,47.986140584623,48.485819651406,48.9854987181891,49.4851777849721,
49.9848568517551,50.4845359185381,50.9842149853212,51.4838940521042,51.9835731188872,
52.4832521856702,52.9829312524532,53.407075111027),.UNSPECIFIED.);
#718=B_SPLINE_CURVE_WITH_KNOTS('',3,(#28905,#28906,#28907,#28908,#28909,
#28910,#28911,#28912,#28913,#28914,#28915,#28916,#28917,#28918,#28919,#28920),
 .UNSPECIFIED.,.F.,.F.,(4,1,1,1,1,1,1,1,1,1,1,1,1,4),(47.1238898038477,
47.4570054325096,47.9566844992927,48.4563635660757,48.9560426328587,49.4557216996417,
49.9554007664248,50.4550798332078,50.9547588999908,51.4544379667738,51.9541170335568,
52.4537961003399,52.9534751671229,53.4070751110273),.UNSPECIFIED.);
#719=B_SPLINE_CURVE_WITH_KNOTS('',3,(#28925,#28926,#28927,#28928,#28929,
#28930,#28931,#28932,#28933,#28934,#28935,#28936,#28937,#28938,#28939,#28940,
#28941),.UNSPECIFIED.,.F.,.F.,(4,1,1,1,1,1,1,1,1,1,1,1,1,1,4),(40.8407044966678,
40.9906336496607,41.4903127164437,41.9899917832267,42.4896708500098,42.9893499167928,
43.4890289835758,43.9887080503588,44.4883871171419,44.9880661839249,45.4877452507079,
45.9874243174909,46.4871033842739,46.986782451057,47.1238898038474),
 .UNSPECIFIED.);
#720=B_SPLINE_CURVE_WITH_KNOTS('',3,(#28942,#28943,#28944,#28945,#28946,
#28947,#28948,#28949,#28950,#28951,#28952,#28953,#28954,#28955,#28956,#28957,
#28958),.UNSPECIFIED.,.F.,.F.,(4,1,1,1,1,1,1,1,1,1,1,1,1,1,4),(40.8407044966681,
40.9611775643303,41.4608566311134,41.9605356978964,42.4602147646794,42.9598938314624,
43.4595728982454,43.9592519650285,44.4589310318115,44.9586100985945,45.4582891653775,
45.9579682321606,46.4576472989436,46.9573263657266,47.1238898038477),
 .UNSPECIFIED.);
#721=B_SPLINE_CURVE_WITH_KNOTS('',3,(#28963,#28964,#28965,#28966,#28967,
#28968,#28969,#28970,#28971,#28972,#28973,#28974,#28975,#28976,#28977,#28978),
 .UNSPECIFIED.,.F.,.F.,(4,1,1,1,1,1,1,1,1,1,1,1,1,4),(34.5575191894882,
34.9944848482644,35.4941639150474,35.9938429818305,36.4935220486135,36.9932011153965,
37.4928801821795,37.9925592489626,38.4922383157456,38.9919173825286,39.4915964493116,
39.9912755160946,40.4909545828777,40.8407044966678),.UNSPECIFIED.);
#722=B_SPLINE_CURVE_WITH_KNOTS('',3,(#28979,#28980,#28981,#28982,#28983,
#28984,#28985,#28986,#28987,#28988,#28989,#28990,#28991,#28992,#28993,#28994),
 .UNSPECIFIED.,.F.,.F.,(4,1,1,1,1,1,1,1,1,1,1,1,1,4),(34.5575191894886,
34.965028762934,35.4647078297171,35.9643868965001,36.4640659632831,36.9637450300661,
37.4634240968492,37.9631031636322,38.4627822304152,38.9624612971982,39.4621403639813,
39.9618194307643,40.4614984975473,40.8407044966681),.UNSPECIFIED.);
#723=B_SPLINE_CURVE_WITH_KNOTS('',3,(#28999,#29000,#29001,#29002,#29003,
#29004,#29005,#29006,#29007,#29008,#29009,#29010,#29011,#29012,#29013,#29014,
#29015),.UNSPECIFIED.,.F.,.F.,(4,1,1,1,1,1,1,1,1,1,1,1,1,1,4),(28.2743338823086,
28.4986569800851,28.9983360468681,29.4980151136512,29.9976941804342,30.4973732472172,
30.9970523140002,31.4967313807832,31.9964104475663,32.4960895143493,32.9957685811323,
33.4954476479153,33.9951267146984,34.4948057814814,34.5575191894882),
 .UNSPECIFIED.);
#724=B_SPLINE_CURVE_WITH_KNOTS('',3,(#29016,#29017,#29018,#29019,#29020,
#29021,#29022,#29023,#29024,#29025,#29026,#29027,#29028,#29029,#29030,#29031,
#29032),.UNSPECIFIED.,.F.,.F.,(4,1,1,1,1,1,1,1,1,1,1,1,1,1,4),(28.2743338823089,
28.4692008947547,28.9688799615378,29.4685590283208,29.9682380951038,30.4679171618868,
30.9675962286699,31.4672752954529,31.9669543622359,32.4666334290189,32.966312495802,
33.465991562585,33.965670629368,34.465349696151,34.5575191894886),
 .UNSPECIFIED.);
#725=B_SPLINE_CURVE_WITH_KNOTS('',3,(#29037,#29038,#29039,#29040,#29041,
#29042,#29043,#29044,#29045,#29046,#29047,#29048,#29049,#29050,#29051,#29052,
#29053),.UNSPECIFIED.,.F.,.F.,(4,1,1,1,1,1,1,1,1,1,1,1,1,1,4),(21.991148575129,
22.0028291119058,22.5025081786888,23.0021872454719,23.5018663122549,24.0015453790379,
24.5012244458209,25.0009035126039,25.500582579387,26.00026164617,26.499940712953,
26.999619779736,27.4992988465191,27.9989779133021,28.2743338823086),
 .UNSPECIFIED.);
#726=B_SPLINE_CURVE_WITH_KNOTS('',3,(#29054,#29055,#29056,#29057,#29058,
#29059,#29060,#29061,#29062,#29063,#29064,#29065,#29066,#29067,#29068,#29069),
 .UNSPECIFIED.,.F.,.F.,(4,1,1,1,1,1,1,1,1,1,1,1,1,4),(21.9911485751294,
22.4730520933585,22.9727311601415,23.4724102269245,23.9720892937075,24.4717683604905,
24.9714474272736,25.4711264940566,25.9708055608396,26.4704846276226,26.9701636944057,
27.4698427611887,27.9695218279717,28.2743338823089),.UNSPECIFIED.);
#727=B_SPLINE_CURVE_WITH_KNOTS('',3,(#29074,#29075,#29076,#29077,#29078,
#29079,#29080,#29081,#29082,#29083,#29084,#29085,#29086,#29087,#29088,#29089),
 .UNSPECIFIED.,.F.,.F.,(4,1,1,1,1,1,1,1,1,1,1,1,1,4),(15.7079632679495,
16.0066803105095,16.5063593772925,17.0060384440756,17.5057175108586,18.0053965776416,
18.5050756444246,19.0047547112077,19.5044337779907,20.0041128447737,20.5037919115567,
21.0034709783398,21.5031500451228,21.991148575129),.UNSPECIFIED.);
#728=B_SPLINE_CURVE_WITH_KNOTS('',3,(#29090,#29091,#29092,#29093,#29094,
#29095,#29096,#29097,#29098,#29099,#29100,#29101,#29102,#29103,#29104,#29105,
#29106),.UNSPECIFIED.,.F.,.F.,(4,1,1,1,1,1,1,1,1,1,1,1,1,1,4),(15.7079632679498,
15.9772242251791,16.4769032919622,16.9765823587452,17.4762614255282,17.9759404923112,
18.4756195590943,18.9752986258773,19.4749776926603,19.9746567594433,20.4743358262264,
20.9740148930094,21.4736939597924,21.9733730265754,21.9911485751294),
 .UNSPECIFIED.);
#729=B_SPLINE_CURVE_WITH_KNOTS('',3,(#29111,#29112,#29113,#29114,#29115,
#29116,#29117,#29118,#29119,#29120,#29121,#29122,#29123,#29124,#29125,#29126,
#29127,#29128,#29129,#29130,#29131,#29132,#29133,#29134,#29135,#29136,#29137,
#29138,#29139,#29140,#29141,#29142,#29143,#29144,#29145,#29146,#29147),
 .UNSPECIFIED.,.F.,.F.,(4,3,3,3,3,3,3,3,3,3,3,3,4),(0.,0.000373494560508806,
0.0620760815771024,0.112839239637108,0.153038169722591,0.175804963675793,
0.247183842626883,0.319084136954533,0.344742425233931,0.363606980156396,
0.439518700737557,0.51795432283266,0.534785019937482),.UNSPECIFIED.);
#730=B_SPLINE_CURVE_WITH_KNOTS('',3,(#29149,#29150,#29151,#29152,#29153,
#29154,#29155,#29156,#29157,#29158,#29159,#29160,#29161,#29162,#29163,#29164,
#29165,#29166,#29167,#29168,#29169,#29170,#29171,#29172,#29173,#29174,#29175,
#29176,#29177,#29178,#29179,#29180,#29181,#29182,#29183,#29184,#29185),
 .UNSPECIFIED.,.F.,.F.,(4,3,3,3,3,3,3,3,3,3,3,3,4),(0.,0.000511892384038064,
0.078754853834616,0.155070466132989,0.20164291816609,0.227017770490094,
0.290460834304131,0.352619921814331,0.383703668213755,0.403796492255862,
0.466621120797767,0.52704524650008,0.539097184344933),.UNSPECIFIED.);
#731=B_SPLINE_CURVE_WITH_KNOTS('',3,(#31185,#31186,#31187,#31188,#31189,
#31190,#31191,#31192,#31193,#31194,#31195,#31196,#31197,#31198,#31199,#31200,
#31201,#31202,#31203,#31204,#31205,#31206,#31207,#31208,#31209,#31210,#31211,
#31212,#31213,#31214,#31215,#31216,#31217,#31218,#31219,#31220,#31221,#31222,
#31223,#31224),.UNSPECIFIED.,.F.,.F.,(4,3,3,3,3,3,3,3,3,3,3,3,3,4),(-0.53478501993692,
-0.534277081309421,-0.456439695901019,-0.38064245929011,-0.348102919117109,
-0.328886681298388,-0.258595553176405,-0.246742105655551,-0.185056579241663,
-0.163339235199672,-0.143463957830519,-0.0808484674142256,-0.0206857924044652,
0.),.UNSPECIFIED.);
#732=B_SPLINE_CURVE_WITH_KNOTS('',3,(#31225,#31226,#31227,#31228,#31229,
#31230,#31231,#31232,#31233,#31234,#31235,#31236,#31237,#31238,#31239,#31240,
#31241,#31242,#31243,#31244,#31245,#31246,#31247,#31248,#31249),
 .UNSPECIFIED.,.F.,.F.,(4,3,3,3,3,3,3,3,4),(390.000549715688,390.249351157541,
390.749030224325,391.248709291108,391.748388357891,392.248067424674,392.747746491457,
393.24742555824,393.746279249921),.UNSPECIFIED.);
#733=B_SPLINE_CURVE_WITH_KNOTS('',3,(#31250,#31251,#31252,#31253,#31254,
#31255,#31256,#31257,#31258,#31259,#31260,#31261,#31262,#31263,#31264),
 .UNSPECIFIED.,.F.,.F.,(4,1,1,1,1,1,1,1,1,1,1,1,4),(9.98190079888485,10.4807544905659,
10.9804335573489,11.4801126241319,11.979791690915,12.479470757698,12.979149824481,
13.478828891264,13.9785079580471,14.4781870248301,14.9778660916131,15.4775451583961,
15.7079632679498),.UNSPECIFIED.);
#734=B_SPLINE_CURVE_WITH_KNOTS('',3,(#31266,#31267,#31268,#31269,#31270,
#31271,#31272,#31273,#31274,#31275,#31276),.UNSPECIFIED.,.F.,.F.,(4,1,1,
1,1,1,1,1,4),(12.0092477762453,12.5089268430284,13.0086059098114,13.5082849765944,
14.0079640433774,14.5076431101605,15.0073221769435,15.5070012437265,15.7079632679495),
 .UNSPECIFIED.);
#735=B_SPLINE_CURVE_WITH_KNOTS('',3,(#33270,#33271,#33272,#33273,#33274,
#33275,#33276,#33277,#33278,#33279,#33280,#33281,#33282,#33283,#33284,#33285,
#33286,#33287,#33288,#33289,#33290,#33291,#33292,#33293,#33294,#33295,#33296,
#33297,#33298,#33299,#33300,#33301,#33302,#33303,#33304,#33305,#33306,#33307,
#33308,#33309),.UNSPECIFIED.,.F.,.F.,(4,3,3,3,3,3,3,3,3,3,3,3,3,4),(-0.539097184344981,
-0.538720824057998,-0.476544551511477,-0.429912347101587,-0.401091234701428,
-0.381803774975435,-0.313681369269712,-0.290015733871917,-0.24230273417063,
-0.214804629165427,-0.192593514291413,-0.116696500404398,-0.0381316372362206,
0.),.UNSPECIFIED.);
#736=B_SPLINE_CURVE_WITH_KNOTS('',3,(#33310,#33311,#33312,#33313,#33314,
#33315,#33316,#33317,#33318,#33319),.UNSPECIFIED.,.F.,.F.,(4,3,3,4),(-394.746462758588,
-394.246783691805,-393.747104625022,-393.256204536838),.UNSPECIFIED.);
#845=SHAPE_REPRESENTATION_RELATIONSHIP('SRR','None',#34223,#889);
#889=ADVANCED_BREP_SHAPE_REPRESENTATION('',(#1003),#33971);
#948=STYLED_ITEM('',(#34524),#1003);
#1003=MANIFOLD_SOLID_BREP('Body1',#13063);
#1204=FACE_BOUND('',#3122,.T.);
#1205=FACE_BOUND('',#3134,.T.);
#1206=FACE_BOUND('',#3137,.T.);
#1207=FACE_BOUND('',#3140,.T.);
#1515=PLANE('',#14676);
#1516=PLANE('',#14681);
#1517=PLANE('',#14683);
#1518=PLANE('',#14684);
#1519=PLANE('',#14686);
#1520=PLANE('',#14687);
#1521=PLANE('',#14688);
#1522=PLANE('',#14693);
#1523=PLANE('',#14694);
#1524=PLANE('',#14699);
#2080=FACE_OUTER_BOUND('',#2995,.T.);
#2081=FACE_OUTER_BOUND('',#2996,.T.);
#2082=FACE_OUTER_BOUND('',#2997,.T.);
#2083=FACE_OUTER_BOUND('',#2998,.T.);
#2084=FACE_OUTER_BOUND('',#2999,.T.);
#2085=FACE_OUTER_BOUND('',#3000,.T.);
#2086=FACE_OUTER_BOUND('',#3001,.T.);
#2087=FACE_OUTER_BOUND('',#3002,.T.);
#2088=FACE_OUTER_BOUND('',#3003,.T.);
#2089=FACE_OUTER_BOUND('',#3004,.T.);
#2090=FACE_OUTER_BOUND('',#3005,.T.);
#2091=FACE_OUTER_BOUND('',#3006,.T.);
#2092=FACE_OUTER_BOUND('',#3007,.T.);
#2093=FACE_OUTER_BOUND('',#3008,.T.);
#2094=FACE_OUTER_BOUND('',#3009,.T.);
#2095=FACE_OUTER_BOUND('',#3010,.T.);
#2096=FACE_OUTER_BOUND('',#3011,.T.);
#2097=FACE_OUTER_BOUND('',#3012,.T.);
#2098=FACE_OUTER_BOUND('',#3013,.T.);
#2099=FACE_OUTER_BOUND('',#3014,.T.);
#2100=FACE_OUTER_BOUND('',#3015,.T.);
#2101=FACE_OUTER_BOUND('',#3016,.T.);
#2102=FACE_OUTER_BOUND('',#3017,.T.);
#2103=FACE_OUTER_BOUND('',#3018,.T.);
#2104=FACE_OUTER_BOUND('',#3019,.T.);
#2105=FACE_OUTER_BOUND('',#3020,.T.);
#2106=FACE_OUTER_BOUND('',#3021,.T.);
#2107=FACE_OUTER_BOUND('',#3022,.T.);
#2108=FACE_OUTER_BOUND('',#3023,.T.);
#2109=FACE_OUTER_BOUND('',#3024,.T.);
#2110=FACE_OUTER_BOUND('',#3025,.T.);
#2111=FACE_OUTER_BOUND('',#3026,.T.);
#2112=FACE_OUTER_BOUND('',#3027,.T.);
#2113=FACE_OUTER_BOUND('',#3028,.T.);
#2114=FACE_OUTER_BOUND('',#3029,.T.);
#2115=FACE_OUTER_BOUND('',#3030,.T.);
#2116=FACE_OUTER_BOUND('',#3031,.T.);
#2117=FACE_OUTER_BOUND('',#3032,.T.);
#2118=FACE_OUTER_BOUND('',#3033,.T.);
#2119=FACE_OUTER_BOUND('',#3034,.T.);
#2120=FACE_OUTER_BOUND('',#3035,.T.);
#2121=FACE_OUTER_BOUND('',#3036,.T.);
#2122=FACE_OUTER_BOUND('',#3037,.T.);
#2123=FACE_OUTER_BOUND('',#3038,.T.);
#2124=FACE_OUTER_BOUND('',#3039,.T.);
#2125=FACE_OUTER_BOUND('',#3040,.T.);
#2126=FACE_OUTER_BOUND('',#3041,.T.);
#2127=FACE_OUTER_BOUND('',#3042,.T.);
#2128=FACE_OUTER_BOUND('',#3043,.T.);
#2129=FACE_OUTER_BOUND('',#3044,.T.);
#2130=FACE_OUTER_BOUND('',#3045,.T.);
#2131=FACE_OUTER_BOUND('',#3046,.T.);
#2132=FACE_OUTER_BOUND('',#3047,.T.);
#2133=FACE_OUTER_BOUND('',#3048,.T.);
#2134=FACE_OUTER_BOUND('',#3049,.T.);
#2135=FACE_OUTER_BOUND('',#3050,.T.);
#2136=FACE_OUTER_BOUND('',#3051,.T.);
#2137=FACE_OUTER_BOUND('',#3052,.T.);
#2138=FACE_OUTER_BOUND('',#3053,.T.);
#2139=FACE_OUTER_BOUND('',#3054,.T.);
#2140=FACE_OUTER_BOUND('',#3055,.T.);
#2141=FACE_OUTER_BOUND('',#3056,.T.);
#2142=FACE_OUTER_BOUND('',#3057,.T.);
#2143=FACE_OUTER_BOUND('',#3058,.T.);
#2144=FACE_OUTER_BOUND('',#3059,.T.);
#2145=FACE_OUTER_BOUND('',#3060,.T.);
#2146=FACE_OUTER_BOUND('',#3061,.T.);
#2147=FACE_OUTER_BOUND('',#3062,.T.);
#2148=FACE_OUTER_BOUND('',#3063,.T.);
#2149=FACE_OUTER_BOUND('',#3064,.T.);
#2150=FACE_OUTER_BOUND('',#3065,.T.);
#2151=FACE_OUTER_BOUND('',#3066,.T.);
#2152=FACE_OUTER_BOUND('',#3067,.T.);
#2153=FACE_OUTER_BOUND('',#3068,.T.);
#2154=FACE_OUTER_BOUND('',#3069,.T.);
#2155=FACE_OUTER_BOUND('',#3070,.T.);
#2156=FACE_OUTER_BOUND('',#3071,.T.);
#2157=FACE_OUTER_BOUND('',#3072,.T.);
#2158=FACE_OUTER_BOUND('',#3073,.T.);
#2159=FACE_OUTER_BOUND('',#3074,.T.);
#2160=FACE_OUTER_BOUND('',#3075,.T.);
#2161=FACE_OUTER_BOUND('',#3076,.T.);
#2162=FACE_OUTER_BOUND('',#3077,.T.);
#2163=FACE_OUTER_BOUND('',#3078,.T.);
#2164=FACE_OUTER_BOUND('',#3079,.T.);
#2165=FACE_OUTER_BOUND('',#3080,.T.);
#2166=FACE_OUTER_BOUND('',#3081,.T.);
#2167=FACE_OUTER_BOUND('',#3082,.T.);
#2168=FACE_OUTER_BOUND('',#3083,.T.);
#2169=FACE_OUTER_BOUND('',#3084,.T.);
#2170=FACE_OUTER_BOUND('',#3085,.T.);
#2171=FACE_OUTER_BOUND('',#3086,.T.);
#2172=FACE_OUTER_BOUND('',#3087,.T.);
#2173=FACE_OUTER_BOUND('',#3088,.T.);
#2174=FACE_OUTER_BOUND('',#3089,.T.);
#2175=FACE_OUTER_BOUND('',#3090,.T.);
#2176=FACE_OUTER_BOUND('',#3091,.T.);
#2177=FACE_OUTER_BOUND('',#3092,.T.);
#2178=FACE_OUTER_BOUND('',#3093,.T.);
#2179=FACE_OUTER_BOUND('',#3094,.T.);
#2180=FACE_OUTER_BOUND('',#3095,.T.);
#2181=FACE_OUTER_BOUND('',#3096,.T.);
#2182=FACE_OUTER_BOUND('',#3097,.T.);
#2183=FACE_OUTER_BOUND('',#3098,.T.);
#2184=FACE_OUTER_BOUND('',#3099,.T.);
#2185=FACE_OUTER_BOUND('',#3100,.T.);
#2186=FACE_OUTER_BOUND('',#3101,.T.);
#2187=FACE_OUTER_BOUND('',#3102,.T.);
#2188=FACE_OUTER_BOUND('',#3103,.T.);
#2189=FACE_OUTER_BOUND('',#3104,.T.);
#2190=FACE_OUTER_BOUND('',#3105,.T.);
#2191=FACE_OUTER_BOUND('',#3106,.T.);
#2192=FACE_OUTER_BOUND('',#3107,.T.);
#2193=FACE_OUTER_BOUND('',#3108,.T.);
#2194=FACE_OUTER_BOUND('',#3109,.T.);
#2195=FACE_OUTER_BOUND('',#3110,.T.);
#2196=FACE_OUTER_BOUND('',#3111,.T.);
#2197=FACE_OUTER_BOUND('',#3112,.T.);
#2198=FACE_OUTER_BOUND('',#3113,.T.);
#2199=FACE_OUTER_BOUND('',#3114,.T.);
#2200=FACE_OUTER_BOUND('',#3115,.T.);
#2201=FACE_OUTER_BOUND('',#3116,.T.);
#2202=FACE_OUTER_BOUND('',#3117,.T.);
#2203=FACE_OUTER_BOUND('',#3118,.T.);
#2204=FACE_OUTER_BOUND('',#3119,.T.);
#2205=FACE_OUTER_BOUND('',#3120,.T.);
#2206=FACE_OUTER_BOUND('',#3121,.T.);
#2207=FACE_OUTER_BOUND('',#3123,.T.);
#2208=FACE_OUTER_BOUND('',#3124,.T.);
#2209=FACE_OUTER_BOUND('',#3125,.T.);
#2210=FACE_OUTER_BOUND('',#3126,.T.);
#2211=FACE_OUTER_BOUND('',#3127,.T.);
#2212=FACE_OUTER_BOUND('',#3128,.T.);
#2213=FACE_OUTER_BOUND('',#3129,.T.);
#2214=FACE_OUTER_BOUND('',#3130,.T.);
#2215=FACE_OUTER_BOUND('',#3131,.T.);
#2216=FACE_OUTER_BOUND('',#3132,.T.);
#2217=FACE_OUTER_BOUND('',#3133,.T.);
#2218=FACE_OUTER_BOUND('',#3135,.T.);
#2219=FACE_OUTER_BOUND('',#3136,.T.);
#2220=FACE_OUTER_BOUND('',#3138,.T.);
#2221=FACE_OUTER_BOUND('',#3139,.T.);
#2222=FACE_OUTER_BOUND('',#3141,.T.);
#2995=EDGE_LOOP('',(#10847,#10848,#10849,#10850));
#2996=EDGE_LOOP('',(#10851,#10852,#10853,#10854));
#2997=EDGE_LOOP('',(#10855,#10856,#10857,#10858));
#2998=EDGE_LOOP('',(#10859,#10860,#10861,#10862));
#2999=EDGE_LOOP('',(#10863,#10864,#10865,#10866));
#3000=EDGE_LOOP('',(#10867,#10868,#10869,#10870));
#3001=EDGE_LOOP('',(#10871,#10872,#10873,#10874));
#3002=EDGE_LOOP('',(#10875,#10876,#10877,#10878));
#3003=EDGE_LOOP('',(#10879,#10880,#10881,#10882));
#3004=EDGE_LOOP('',(#10883,#10884,#10885,#10886));
#3005=EDGE_LOOP('',(#10887,#10888,#10889,#10890));
#3006=EDGE_LOOP('',(#10891,#10892,#10893,#10894));
#3007=EDGE_LOOP('',(#10895,#10896,#10897,#10898));
#3008=EDGE_LOOP('',(#10899,#10900,#10901,#10902));
#3009=EDGE_LOOP('',(#10903,#10904,#10905,#10906));
#3010=EDGE_LOOP('',(#10907,#10908,#10909,#10910));
#3011=EDGE_LOOP('',(#10911,#10912,#10913,#10914));
#3012=EDGE_LOOP('',(#10915,#10916,#10917,#10918));
#3013=EDGE_LOOP('',(#10919,#10920,#10921,#10922));
#3014=EDGE_LOOP('',(#10923,#10924,#10925,#10926));
#3015=EDGE_LOOP('',(#10927,#10928,#10929,#10930));
#3016=EDGE_LOOP('',(#10931,#10932,#10933,#10934));
#3017=EDGE_LOOP('',(#10935,#10936,#10937,#10938));
#3018=EDGE_LOOP('',(#10939,#10940,#10941,#10942));
#3019=EDGE_LOOP('',(#10943,#10944,#10945,#10946));
#3020=EDGE_LOOP('',(#10947,#10948,#10949,#10950));
#3021=EDGE_LOOP('',(#10951,#10952,#10953,#10954));
#3022=EDGE_LOOP('',(#10955,#10956,#10957,#10958));
#3023=EDGE_LOOP('',(#10959,#10960,#10961,#10962));
#3024=EDGE_LOOP('',(#10963,#10964,#10965,#10966));
#3025=EDGE_LOOP('',(#10967,#10968,#10969,#10970));
#3026=EDGE_LOOP('',(#10971,#10972,#10973,#10974));
#3027=EDGE_LOOP('',(#10975,#10976,#10977,#10978));
#3028=EDGE_LOOP('',(#10979,#10980,#10981,#10982));
#3029=EDGE_LOOP('',(#10983,#10984,#10985,#10986));
#3030=EDGE_LOOP('',(#10987,#10988,#10989,#10990));
#3031=EDGE_LOOP('',(#10991,#10992,#10993,#10994));
#3032=EDGE_LOOP('',(#10995,#10996,#10997,#10998));
#3033=EDGE_LOOP('',(#10999,#11000,#11001,#11002));
#3034=EDGE_LOOP('',(#11003,#11004,#11005,#11006));
#3035=EDGE_LOOP('',(#11007,#11008,#11009,#11010));
#3036=EDGE_LOOP('',(#11011,#11012,#11013,#11014));
#3037=EDGE_LOOP('',(#11015,#11016,#11017,#11018));
#3038=EDGE_LOOP('',(#11019,#11020,#11021,#11022));
#3039=EDGE_LOOP('',(#11023,#11024,#11025,#11026));
#3040=EDGE_LOOP('',(#11027,#11028,#11029,#11030));
#3041=EDGE_LOOP('',(#11031,#11032,#11033,#11034));
#3042=EDGE_LOOP('',(#11035,#11036,#11037,#11038));
#3043=EDGE_LOOP('',(#11039,#11040,#11041,#11042));
#3044=EDGE_LOOP('',(#11043,#11044,#11045,#11046));
#3045=EDGE_LOOP('',(#11047,#11048,#11049,#11050));
#3046=EDGE_LOOP('',(#11051,#11052,#11053,#11054));
#3047=EDGE_LOOP('',(#11055,#11056,#11057,#11058));
#3048=EDGE_LOOP('',(#11059,#11060,#11061,#11062));
#3049=EDGE_LOOP('',(#11063,#11064,#11065,#11066));
#3050=EDGE_LOOP('',(#11067,#11068,#11069,#11070));
#3051=EDGE_LOOP('',(#11071,#11072,#11073,#11074));
#3052=EDGE_LOOP('',(#11075,#11076,#11077,#11078));
#3053=EDGE_LOOP('',(#11079,#11080,#11081,#11082));
#3054=EDGE_LOOP('',(#11083,#11084,#11085,#11086));
#3055=EDGE_LOOP('',(#11087,#11088,#11089,#11090));
#3056=EDGE_LOOP('',(#11091,#11092,#11093,#11094));
#3057=EDGE_LOOP('',(#11095,#11096,#11097,#11098));
#3058=EDGE_LOOP('',(#11099,#11100,#11101));
#3059=EDGE_LOOP('',(#11102,#11103,#11104,#11105,#11106));
#3060=EDGE_LOOP('',(#11107,#11108,#11109,#11110));
#3061=EDGE_LOOP('',(#11111,#11112,#11113,#11114));
#3062=EDGE_LOOP('',(#11115,#11116,#11117,#11118));
#3063=EDGE_LOOP('',(#11119,#11120,#11121,#11122));
#3064=EDGE_LOOP('',(#11123,#11124,#11125,#11126));
#3065=EDGE_LOOP('',(#11127,#11128,#11129,#11130));
#3066=EDGE_LOOP('',(#11131,#11132,#11133,#11134));
#3067=EDGE_LOOP('',(#11135,#11136,#11137,#11138));
#3068=EDGE_LOOP('',(#11139,#11140,#11141,#11142));
#3069=EDGE_LOOP('',(#11143,#11144,#11145,#11146));
#3070=EDGE_LOOP('',(#11147,#11148,#11149,#11150));
#3071=EDGE_LOOP('',(#11151,#11152,#11153,#11154));
#3072=EDGE_LOOP('',(#11155,#11156,#11157,#11158));
#3073=EDGE_LOOP('',(#11159,#11160,#11161,#11162));
#3074=EDGE_LOOP('',(#11163,#11164,#11165,#11166));
#3075=EDGE_LOOP('',(#11167,#11168,#11169,#11170));
#3076=EDGE_LOOP('',(#11171,#11172,#11173,#11174));
#3077=EDGE_LOOP('',(#11175,#11176,#11177,#11178));
#3078=EDGE_LOOP('',(#11179,#11180,#11181,#11182));
#3079=EDGE_LOOP('',(#11183,#11184,#11185,#11186));
#3080=EDGE_LOOP('',(#11187,#11188,#11189,#11190));
#3081=EDGE_LOOP('',(#11191,#11192,#11193,#11194));
#3082=EDGE_LOOP('',(#11195,#11196,#11197,#11198));
#3083=EDGE_LOOP('',(#11199,#11200,#11201,#11202));
#3084=EDGE_LOOP('',(#11203,#11204,#11205,#11206));
#3085=EDGE_LOOP('',(#11207,#11208,#11209,#11210));
#3086=EDGE_LOOP('',(#11211,#11212,#11213,#11214));
#3087=EDGE_LOOP('',(#11215,#11216,#11217,#11218));
#3088=EDGE_LOOP('',(#11219,#11220,#11221,#11222));
#3089=EDGE_LOOP('',(#11223,#11224,#11225,#11226));
#3090=EDGE_LOOP('',(#11227,#11228,#11229,#11230));
#3091=EDGE_LOOP('',(#11231,#11232,#11233,#11234));
#3092=EDGE_LOOP('',(#11235,#11236,#11237,#11238));
#3093=EDGE_LOOP('',(#11239,#11240,#11241,#11242));
#3094=EDGE_LOOP('',(#11243,#11244,#11245,#11246));
#3095=EDGE_LOOP('',(#11247,#11248,#11249,#11250));
#3096=EDGE_LOOP('',(#11251,#11252,#11253,#11254));
#3097=EDGE_LOOP('',(#11255,#11256,#11257,#11258));
#3098=EDGE_LOOP('',(#11259,#11260,#11261,#11262));
#3099=EDGE_LOOP('',(#11263,#11264,#11265,#11266));
#3100=EDGE_LOOP('',(#11267,#11268,#11269,#11270));
#3101=EDGE_LOOP('',(#11271,#11272,#11273,#11274));
#3102=EDGE_LOOP('',(#11275,#11276,#11277,#11278));
#3103=EDGE_LOOP('',(#11279,#11280,#11281,#11282));
#3104=EDGE_LOOP('',(#11283,#11284,#11285,#11286));
#3105=EDGE_LOOP('',(#11287,#11288,#11289,#11290));
#3106=EDGE_LOOP('',(#11291,#11292,#11293,#11294));
#3107=EDGE_LOOP('',(#11295,#11296,#11297,#11298));
#3108=EDGE_LOOP('',(#11299,#11300,#11301,#11302));
#3109=EDGE_LOOP('',(#11303,#11304,#11305,#11306));
#3110=EDGE_LOOP('',(#11307,#11308,#11309,#11310));
#3111=EDGE_LOOP('',(#11311,#11312,#11313,#11314));
#3112=EDGE_LOOP('',(#11315,#11316,#11317,#11318));
#3113=EDGE_LOOP('',(#11319,#11320,#11321,#11322));
#3114=EDGE_LOOP('',(#11323,#11324,#11325,#11326));
#3115=EDGE_LOOP('',(#11327,#11328,#11329,#11330));
#3116=EDGE_LOOP('',(#11331,#11332,#11333,#11334));
#3117=EDGE_LOOP('',(#11335,#11336,#11337,#11338));
#3118=EDGE_LOOP('',(#11339,#11340,#11341,#11342));
#3119=EDGE_LOOP('',(#11343,#11344,#11345,#11346));
#3120=EDGE_LOOP('',(#11347,#11348,#11349,#11350));
#3121=EDGE_LOOP('',(#11351));
#3122=EDGE_LOOP('',(#11352,#11353,#11354,#11355));
#3123=EDGE_LOOP('',(#11356,#11357,#11358,#11359));
#3124=EDGE_LOOP('',(#11360));
#3125=EDGE_LOOP('',(#11361,#11362,#11363,#11364,#11365,#11366,#11367,#11368,
#11369,#11370,#11371,#11372,#11373,#11374,#11375,#11376,#11377,#11378,#11379,
#11380,#11381,#11382,#11383,#11384,#11385,#11386,#11387,#11388,#11389,#11390,
#11391,#11392,#11393,#11394,#11395,#11396,#11397,#11398,#11399,#11400,#11401,
#11402,#11403,#11404,#11405,#11406,#11407,#11408,#11409,#11410,#11411,#11412,
#11413,#11414,#11415,#11416,#11417,#11418,#11419,#11420,#11421,#11422,#11423,
#11424,#11425,#11426,#11427,#11428,#11429,#11430,#11431,#11432,#11433,#11434,
#11435,#11436,#11437,#11438,#11439,#11440,#11441,#11442,#11443,#11444,#11445,
#11446,#11447,#11448,#11449,#11450,#11451,#11452,#11453,#11454,#11455,#11456,
#11457,#11458,#11459,#11460,#11461,#11462,#11463,#11464,#11465,#11466,#11467,
#11468,#11469,#11470,#11471,#11472,#11473,#11474,#11475,#11476,#11477,#11478,
#11479,#11480,#11481,#11482,#11483,#11484,#11485,#11486,#11487,#11488,#11489));
#3126=EDGE_LOOP('',(#11490,#11491,#11492,#11493));
#3127=EDGE_LOOP('',(#11494,#11495,#11496,#11497,#11498,#11499,#11500,#11501,
#11502,#11503,#11504,#11505,#11506,#11507,#11508,#11509,#11510,#11511,#11512,
#11513,#11514,#11515,#11516,#11517,#11518,#11519,#11520,#11521,#11522,#11523,
#11524,#11525,#11526,#11527,#11528,#11529,#11530,#11531,#11532,#11533,#11534,
#11535,#11536,#11537,#11538,#11539,#11540,#11541,#11542,#11543,#11544,#11545,
#11546,#11547,#11548,#11549,#11550,#11551,#11552,#11553,#11554,#11555,#11556,
#11557,#11558,#11559,#11560,#11561,#11562,#11563,#11564,#11565,#11566,#11567,
#11568,#11569,#11570,#11571,#11572,#11573,#11574,#11575,#11576,#11577,#11578,
#11579,#11580,#11581,#11582,#11583,#11584,#11585,#11586,#11587,#11588,#11589,
#11590,#11591,#11592,#11593,#11594,#11595,#11596,#11597,#11598,#11599,#11600,
#11601,#11602,#11603,#11604,#11605,#11606,#11607,#11608,#11609,#11610,#11611,
#11612,#11613,#11614,#11615,#11616,#11617,#11618,#11619,#11620,#11621,#11622,
#11623));
#3128=EDGE_LOOP('',(#11624,#11625,#11626,#11627));
#3129=EDGE_LOOP('',(#11628,#11629,#11630,#11631));
#3130=EDGE_LOOP('',(#11632,#11633,#11634,#11635));
#3131=EDGE_LOOP('',(#11636,#11637,#11638,#11639));
#3132=EDGE_LOOP('',(#11640,#11641,#11642,#11643));
#3133=EDGE_LOOP('',(#11644,#11645,#11646,#11647));
#3134=EDGE_LOOP('',(#11648,#11649,#11650,#11651));
#3135=EDGE_LOOP('',(#11652));
#3136=EDGE_LOOP('',(#11653));
#3137=EDGE_LOOP('',(#11654,#11655,#11656,#11657,#11658));
#3138=EDGE_LOOP('',(#11659,#11660,#11661,#11662));
#3139=EDGE_LOOP('',(#11663));
#3140=EDGE_LOOP('',(#11664));
#3141=EDGE_LOOP('',(#11665,#11666,#11667,#11668));
#3931=LINE('',#23707,#4865);
#3932=LINE('',#23737,#4866);
#3933=LINE('',#23824,#4867);
#3934=LINE('',#23914,#4868);
#3935=LINE('',#24001,#4869);
#3936=LINE('',#24088,#4870);
#3937=LINE('',#24175,#4871);
#3938=LINE('',#24262,#4872);
#3939=LINE('',#24349,#4873);
#3940=LINE('',#24421,#4874);
#3941=LINE('',#24472,#4875);
#3942=LINE('',#24520,#4876);
#3943=LINE('',#24568,#4877);
#3944=LINE('',#24619,#4878);
#3945=LINE('',#24670,#4879);
#3946=LINE('',#24718,#4880);
#3947=LINE('',#24769,#4881);
#3948=LINE('',#24820,#4882);
#3949=LINE('',#24868,#4883);
#3950=LINE('',#24916,#4884);
#3951=LINE('',#24967,#4885);
#3952=LINE('',#25018,#4886);
#3953=LINE('',#25066,#4887);
#3954=LINE('',#25117,#4888);
#3955=LINE('',#25168,#4889);
#3956=LINE('',#25216,#4890);
#3957=LINE('',#25264,#4891);
#3958=LINE('',#25315,#4892);
#3959=LINE('',#25366,#4893);
#3960=LINE('',#25414,#4894);
#3961=LINE('',#25465,#4895);
#3962=LINE('',#25516,#4896);
#3963=LINE('',#25564,#4897);
#3964=LINE('',#25612,#4898);
#3965=LINE('',#25663,#4899);
#3966=LINE('',#25714,#4900);
#3967=LINE('',#25762,#4901);
#3968=LINE('',#25813,#4902);
#3969=LINE('',#25864,#4903);
#3970=LINE('',#25912,#4904);
#3971=LINE('',#25960,#4905);
#3972=LINE('',#26011,#4906);
#3973=LINE('',#26062,#4907);
#3974=LINE('',#26110,#4908);
#3975=LINE('',#26161,#4909);
#3976=LINE('',#26212,#4910);
#3977=LINE('',#26260,#4911);
#3978=LINE('',#26308,#4912);
#3979=LINE('',#26359,#4913);
#3980=LINE('',#26410,#4914);
#3981=LINE('',#26458,#4915);
#3982=LINE('',#26509,#4916);
#3983=LINE('',#26560,#4917);
#3984=LINE('',#26608,#4918);
#3985=LINE('',#26656,#4919);
#3986=LINE('',#26707,#4920);
#3987=LINE('',#26773,#4921);
#3988=LINE('',#26863,#4922);
#3989=LINE('',#26950,#4923);
#3990=LINE('',#27037,#4924);
#3991=LINE('',#27124,#4925);
#3992=LINE('',#27211,#4926);
#3993=LINE('',#27298,#4927);
#3994=LINE('',#27388,#4928);
#3995=LINE('',#27398,#4929);
#3996=LINE('',#27434,#4930);
#3997=LINE('',#27472,#4931);
#3998=LINE('',#27508,#4932);
#3999=LINE('',#27546,#4933);
#4000=LINE('',#27582,#4934);
#4001=LINE('',#27620,#4935);
#4002=LINE('',#27657,#4936);
#4003=LINE('',#27692,#4937);
#4004=LINE('',#27719,#4938);
#4005=LINE('',#27743,#4939);
#4006=LINE('',#27767,#4940);
#4007=LINE('',#27791,#4941);
#4008=LINE('',#27817,#4942);
#4009=LINE('',#27841,#4943);
#4010=LINE('',#27865,#4944);
#4011=LINE('',#27891,#4945);
#4012=LINE('',#27915,#4946);
#4013=LINE('',#27939,#4947);
#4014=LINE('',#27963,#4948);
#4015=LINE('',#27989,#4949);
#4016=LINE('',#28013,#4950);
#4017=LINE('',#28037,#4951);
#4018=LINE('',#28063,#4952);
#4019=LINE('',#28087,#4953);
#4020=LINE('',#28111,#4954);
#4021=LINE('',#28135,#4955);
#4022=LINE('',#28161,#4956);
#4023=LINE('',#28185,#4957);
#4024=LINE('',#28209,#4958);
#4025=LINE('',#28235,#4959);
#4026=LINE('',#28259,#4960);
#4027=LINE('',#28283,#4961);
#4028=LINE('',#28307,#4962);
#4029=LINE('',#28333,#4963);
#4030=LINE('',#28357,#4964);
#4031=LINE('',#28381,#4965);
#4032=LINE('',#28407,#4966);
#4033=LINE('',#28431,#4967);
#4034=LINE('',#28455,#4968);
#4035=LINE('',#28479,#4969);
#4036=LINE('',#28505,#4970);
#4037=LINE('',#28529,#4971);
#4038=LINE('',#28553,#4972);
#4039=LINE('',#28579,#4973);
#4040=LINE('',#28603,#4974);
#4041=LINE('',#28627,#4975);
#4042=LINE('',#28651,#4976);
#4043=LINE('',#28677,#4977);
#4044=LINE('',#28701,#4978);
#4045=LINE('',#28725,#4979);
#4046=LINE('',#28751,#4980);
#4047=LINE('',#28775,#4981);
#4048=LINE('',#28799,#4982);
#4049=LINE('',#28824,#4983);
#4050=LINE('',#28851,#4984);
#4051=LINE('',#28888,#4985);
#4052=LINE('',#28924,#4986);
#4053=LINE('',#28962,#4987);
#4054=LINE('',#28998,#4988);
#4055=LINE('',#29036,#4989);
#4056=LINE('',#29073,#4990);
#4057=LINE('',#29189,#4991);
#4058=LINE('',#33323,#4992);
#4059=LINE('',#33325,#4993);
#4060=LINE('',#33327,#4994);
#4061=LINE('',#33328,#4995);
#4062=LINE('',#33333,#4996);
#4063=LINE('',#33334,#4997);
#4064=LINE('',#33337,#4998);
#4065=LINE('',#33338,#4999);
#4066=LINE('',#33341,#5000);
#4067=LINE('',#33342,#5001);
#4068=LINE('',#33349,#5002);
#4069=LINE('',#33359,#5003);
#4865=VECTOR('',#17562,0.6);
#4866=VECTOR('',#17567,0.6);
#4867=VECTOR('',#17570,0.6);
#4868=VECTOR('',#17573,0.6);
#4869=VECTOR('',#17576,0.6);
#4870=VECTOR('',#17579,0.6);
#4871=VECTOR('',#17582,0.6);
#4872=VECTOR('',#17585,0.6);
#4873=VECTOR('',#17588,0.6);
#4874=VECTOR('',#17591,0.6);
#4875=VECTOR('',#17594,0.6);
#4876=VECTOR('',#17597,0.6);
#4877=VECTOR('',#17600,0.6);
#4878=VECTOR('',#17603,0.6);
#4879=VECTOR('',#17606,0.6);
#4880=VECTOR('',#17609,0.6);
#4881=VECTOR('',#17612,0.6);
#4882=VECTOR('',#17615,0.6);
#4883=VECTOR('',#17618,0.6);
#4884=VECTOR('',#17621,0.6);
#4885=VECTOR('',#17624,0.6);
#4886=VECTOR('',#17627,0.6);
#4887=VECTOR('',#17630,0.6);
#4888=VECTOR('',#17633,0.6);
#4889=VECTOR('',#17636,0.6);
#4890=VECTOR('',#17639,0.6);
#4891=VECTOR('',#17642,0.6);
#4892=VECTOR('',#17645,0.6);
#4893=VECTOR('',#17648,0.6);
#4894=VECTOR('',#17651,0.6);
#4895=VECTOR('',#17654,0.6);
#4896=VECTOR('',#17657,0.6);
#4897=VECTOR('',#17660,0.6);
#4898=VECTOR('',#17663,0.6);
#4899=VECTOR('',#17666,0.6);
#4900=VECTOR('',#17669,0.6);
#4901=VECTOR('',#17672,0.6);
#4902=VECTOR('',#17675,0.6);
#4903=VECTOR('',#17678,0.6);
#4904=VECTOR('',#17681,0.6);
#4905=VECTOR('',#17684,0.6);
#4906=VECTOR('',#17687,0.6);
#4907=VECTOR('',#17690,0.6);
#4908=VECTOR('',#17693,0.6);
#4909=VECTOR('',#17696,0.6);
#4910=VECTOR('',#17699,0.6);
#4911=VECTOR('',#17702,0.6);
#4912=VECTOR('',#17705,0.6);
#4913=VECTOR('',#17708,0.6);
#4914=VECTOR('',#17711,0.6);
#4915=VECTOR('',#17714,0.6);
#4916=VECTOR('',#17717,0.6);
#4917=VECTOR('',#17720,0.6);
#4918=VECTOR('',#17723,0.6);
#4919=VECTOR('',#17726,0.6);
#4920=VECTOR('',#17729,0.6);
#4921=VECTOR('',#17732,0.6);
#4922=VECTOR('',#17735,0.6);
#4923=VECTOR('',#17738,0.6);
#4924=VECTOR('',#17741,0.6);
#4925=VECTOR('',#17744,0.6);
#4926=VECTOR('',#17747,0.6);
#4927=VECTOR('',#17750,0.6);
#4928=VECTOR('',#17753,0.415875);
#4929=VECTOR('',#17758,0.415875);
#4930=VECTOR('',#17763,0.415875);
#4931=VECTOR('',#17766,0.415875);
#4932=VECTOR('',#17769,0.415875);
#4933=VECTOR('',#17772,0.415875);
#4934=VECTOR('',#17775,0.415875);
#4935=VECTOR('',#17778,0.415875);
#4936=VECTOR('',#17781,0.415875);
#4937=VECTOR('',#17784,0.415875);
#4938=VECTOR('',#17787,0.415875);
#4939=VECTOR('',#17790,0.415875);
#4940=VECTOR('',#17793,0.415875);
#4941=VECTOR('',#17796,0.415875);
#4942=VECTOR('',#17799,0.415875);
#4943=VECTOR('',#17802,0.415875);
#4944=VECTOR('',#17805,0.415875);
#4945=VECTOR('',#17808,0.415875);
#4946=VECTOR('',#17811,0.415875);
#4947=VECTOR('',#17814,0.415875);
#4948=VECTOR('',#17817,0.415875);
#4949=VECTOR('',#17820,0.415875);
#4950=VECTOR('',#17823,0.415875);
#4951=VECTOR('',#17826,0.415875);
#4952=VECTOR('',#17829,0.415875);
#4953=VECTOR('',#17832,0.415875);
#4954=VECTOR('',#17835,0.415875);
#4955=VECTOR('',#17838,0.415875);
#4956=VECTOR('',#17841,0.415875);
#4957=VECTOR('',#17844,0.415875);
#4958=VECTOR('',#17847,0.415875);
#4959=VECTOR('',#17850,0.415875);
#4960=VECTOR('',#17853,0.415875);
#4961=VECTOR('',#17856,0.415875);
#4962=VECTOR('',#17859,0.415875);
#4963=VECTOR('',#17862,0.415875);
#4964=VECTOR('',#17865,0.415875);
#4965=VECTOR('',#17868,0.415875);
#4966=VECTOR('',#17871,0.415875);
#4967=VECTOR('',#17874,0.415875);
#4968=VECTOR('',#17877,0.415875);
#4969=VECTOR('',#17880,0.415875);
#4970=VECTOR('',#17883,0.415875);
#4971=VECTOR('',#17886,0.415875);
#4972=VECTOR('',#17889,0.415875);
#4973=VECTOR('',#17892,0.415875);
#4974=VECTOR('',#17895,0.415875);
#4975=VECTOR('',#17898,0.415875);
#4976=VECTOR('',#17901,0.415875);
#4977=VECTOR('',#17904,0.415875);
#4978=VECTOR('',#17907,0.415875);
#4979=VECTOR('',#17910,0.415875);
#4980=VECTOR('',#17913,0.415875);
#4981=VECTOR('',#17916,0.415875);
#4982=VECTOR('',#17919,0.415875);
#4983=VECTOR('',#17922,0.415875);
#4984=VECTOR('',#17925,0.415875);
#4985=VECTOR('',#17928,0.415875);
#4986=VECTOR('',#17931,0.415875);
#4987=VECTOR('',#17934,0.415875);
#4988=VECTOR('',#17937,0.415875);
#4989=VECTOR('',#17940,0.415875);
#4990=VECTOR('',#17943,0.415875);
#4991=VECTOR('',#17952,0.6);
#4992=VECTOR('',#17961,1.);
#4993=VECTOR('',#17962,1.);
#4994=VECTOR('',#17963,1.);
#4995=VECTOR('',#17964,1.);
#4996=VECTOR('',#17969,1.);
#4997=VECTOR('',#17970,1.);
#4998=VECTOR('',#17973,1.);
#4999=VECTOR('',#17974,1.);
#5000=VECTOR('',#17977,1.);
#5001=VECTOR('',#17978,1.);
#5002=VECTOR('',#17987,1.);
#5003=VECTOR('',#18002,1.35);
#5513=CIRCLE('',#14548,0.5941);
#5514=CIRCLE('',#14612,0.415875);
#5515=CIRCLE('',#14614,0.415875);
#5516=CIRCLE('',#14677,0.6);
#5517=CIRCLE('',#14678,0.415875);
#5518=CIRCLE('',#14680,0.6);
#5519=CIRCLE('',#14685,1.);
#5520=CIRCLE('',#14689,1.);
#5521=CIRCLE('',#14691,1.);
#5522=CIRCLE('',#14692,1.);
#5523=CIRCLE('',#14695,1.35);
#5524=CIRCLE('',#14696,0.5941);
#5525=CIRCLE('',#14698,1.35);
#6368=VERTEX_POINT('',#23705);
#6369=VERTEX_POINT('',#23706);
#6370=VERTEX_POINT('',#23708);
#6371=VERTEX_POINT('',#23728);
#6372=VERTEX_POINT('',#23735);
#6373=VERTEX_POINT('',#23736);
#6374=VERTEX_POINT('',#23822);
#6375=VERTEX_POINT('',#23823);
#6376=VERTEX_POINT('',#23912);
#6377=VERTEX_POINT('',#23913);
#6378=VERTEX_POINT('',#23999);
#6379=VERTEX_POINT('',#24000);
#6380=VERTEX_POINT('',#24086);
#6381=VERTEX_POINT('',#24087);
#6382=VERTEX_POINT('',#24173);
#6383=VERTEX_POINT('',#24174);
#6384=VERTEX_POINT('',#24260);
#6385=VERTEX_POINT('',#24261);
#6386=VERTEX_POINT('',#24347);
#6387=VERTEX_POINT('',#24348);
#6388=VERTEX_POINT('',#24419);
#6389=VERTEX_POINT('',#24420);
#6390=VERTEX_POINT('',#24470);
#6391=VERTEX_POINT('',#24471);
#6392=VERTEX_POINT('',#24518);
#6393=VERTEX_POINT('',#24519);
#6394=VERTEX_POINT('',#24566);
#6395=VERTEX_POINT('',#24567);
#6396=VERTEX_POINT('',#24617);
#6397=VERTEX_POINT('',#24618);
#6398=VERTEX_POINT('',#24668);
#6399=VERTEX_POINT('',#24669);
#6400=VERTEX_POINT('',#24716);
#6401=VERTEX_POINT('',#24717);
#6402=VERTEX_POINT('',#24767);
#6403=VERTEX_POINT('',#24768);
#6404=VERTEX_POINT('',#24818);
#6405=VERTEX_POINT('',#24819);
#6406=VERTEX_POINT('',#24866);
#6407=VERTEX_POINT('',#24867);
#6408=VERTEX_POINT('',#24914);
#6409=VERTEX_POINT('',#24915);
#6410=VERTEX_POINT('',#24965);
#6411=VERTEX_POINT('',#24966);
#6412=VERTEX_POINT('',#25016);
#6413=VERTEX_POINT('',#25017);
#6414=VERTEX_POINT('',#25064);
#6415=VERTEX_POINT('',#25065);
#6416=VERTEX_POINT('',#25115);
#6417=VERTEX_POINT('',#25116);
#6418=VERTEX_POINT('',#25166);
#6419=VERTEX_POINT('',#25167);
#6420=VERTEX_POINT('',#25214);
#6421=VERTEX_POINT('',#25215);
#6422=VERTEX_POINT('',#25262);
#6423=VERTEX_POINT('',#25263);
#6424=VERTEX_POINT('',#25313);
#6425=VERTEX_POINT('',#25314);
#6426=VERTEX_POINT('',#25364);
#6427=VERTEX_POINT('',#25365);
#6428=VERTEX_POINT('',#25412);
#6429=VERTEX_POINT('',#25413);
#6430=VERTEX_POINT('',#25463);
#6431=VERTEX_POINT('',#25464);
#6432=VERTEX_POINT('',#25514);
#6433=VERTEX_POINT('',#25515);
#6434=VERTEX_POINT('',#25562);
#6435=VERTEX_POINT('',#25563);
#6436=VERTEX_POINT('',#25610);
#6437=VERTEX_POINT('',#25611);
#6438=VERTEX_POINT('',#25661);
#6439=VERTEX_POINT('',#25662);
#6440=VERTEX_POINT('',#25712);
#6441=VERTEX_POINT('',#25713);
#6442=VERTEX_POINT('',#25760);
#6443=VERTEX_POINT('',#25761);
#6444=VERTEX_POINT('',#25811);
#6445=VERTEX_POINT('',#25812);
#6446=VERTEX_POINT('',#25862);
#6447=VERTEX_POINT('',#25863);
#6448=VERTEX_POINT('',#25910);
#6449=VERTEX_POINT('',#25911);
#6450=VERTEX_POINT('',#25958);
#6451=VERTEX_POINT('',#25959);
#6452=VERTEX_POINT('',#26009);
#6453=VERTEX_POINT('',#26010);
#6454=VERTEX_POINT('',#26060);
#6455=VERTEX_POINT('',#26061);
#6456=VERTEX_POINT('',#26108);
#6457=VERTEX_POINT('',#26109);
#6458=VERTEX_POINT('',#26159);
#6459=VERTEX_POINT('',#26160);
#6460=VERTEX_POINT('',#26210);
#6461=VERTEX_POINT('',#26211);
#6462=VERTEX_POINT('',#26258);
#6463=VERTEX_POINT('',#26259);
#6464=VERTEX_POINT('',#26306);
#6465=VERTEX_POINT('',#26307);
#6466=VERTEX_POINT('',#26357);
#6467=VERTEX_POINT('',#26358);
#6468=VERTEX_POINT('',#26408);
#6469=VERTEX_POINT('',#26409);
#6470=VERTEX_POINT('',#26456);
#6471=VERTEX_POINT('',#26457);
#6472=VERTEX_POINT('',#26507);
#6473=VERTEX_POINT('',#26508);
#6474=VERTEX_POINT('',#26558);
#6475=VERTEX_POINT('',#26559);
#6476=VERTEX_POINT('',#26606);
#6477=VERTEX_POINT('',#26607);
#6478=VERTEX_POINT('',#26654);
#6479=VERTEX_POINT('',#26655);
#6480=VERTEX_POINT('',#26705);
#6481=VERTEX_POINT('',#26706);
#6482=VERTEX_POINT('',#26771);
#6483=VERTEX_POINT('',#26772);
#6484=VERTEX_POINT('',#26861);
#6485=VERTEX_POINT('',#26862);
#6486=VERTEX_POINT('',#26948);
#6487=VERTEX_POINT('',#26949);
#6488=VERTEX_POINT('',#27035);
#6489=VERTEX_POINT('',#27036);
#6490=VERTEX_POINT('',#27122);
#6491=VERTEX_POINT('',#27123);
#6492=VERTEX_POINT('',#27209);
#6493=VERTEX_POINT('',#27210);
#6494=VERTEX_POINT('',#27296);
#6495=VERTEX_POINT('',#27297);
#6496=VERTEX_POINT('',#27386);
#6497=VERTEX_POINT('',#27387);
#6498=VERTEX_POINT('',#27389);
#6499=VERTEX_POINT('',#27396);
#6500=VERTEX_POINT('',#27397);
#6501=VERTEX_POINT('',#27416);
#6502=VERTEX_POINT('',#27432);
#6503=VERTEX_POINT('',#27433);
#6504=VERTEX_POINT('',#27470);
#6505=VERTEX_POINT('',#27471);
#6506=VERTEX_POINT('',#27506);
#6507=VERTEX_POINT('',#27507);
#6508=VERTEX_POINT('',#27544);
#6509=VERTEX_POINT('',#27545);
#6510=VERTEX_POINT('',#27580);
#6511=VERTEX_POINT('',#27581);
#6512=VERTEX_POINT('',#27618);
#6513=VERTEX_POINT('',#27619);
#6514=VERTEX_POINT('',#27655);
#6515=VERTEX_POINT('',#27656);
#6516=VERTEX_POINT('',#27690);
#6517=VERTEX_POINT('',#27691);
#6518=VERTEX_POINT('',#27717);
#6519=VERTEX_POINT('',#27718);
#6520=VERTEX_POINT('',#27741);
#6521=VERTEX_POINT('',#27742);
#6522=VERTEX_POINT('',#27765);
#6523=VERTEX_POINT('',#27766);
#6524=VERTEX_POINT('',#27789);
#6525=VERTEX_POINT('',#27790);
#6526=VERTEX_POINT('',#27815);
#6527=VERTEX_POINT('',#27816);
#6528=VERTEX_POINT('',#27839);
#6529=VERTEX_POINT('',#27840);
#6530=VERTEX_POINT('',#27863);
#6531=VERTEX_POINT('',#27864);
#6532=VERTEX_POINT('',#27889);
#6533=VERTEX_POINT('',#27890);
#6534=VERTEX_POINT('',#27913);
#6535=VERTEX_POINT('',#27914);
#6536=VERTEX_POINT('',#27937);
#6537=VERTEX_POINT('',#27938);
#6538=VERTEX_POINT('',#27961);
#6539=VERTEX_POINT('',#27962);
#6540=VERTEX_POINT('',#27987);
#6541=VERTEX_POINT('',#27988);
#6542=VERTEX_POINT('',#28011);
#6543=VERTEX_POINT('',#28012);
#6544=VERTEX_POINT('',#28035);
#6545=VERTEX_POINT('',#28036);
#6546=VERTEX_POINT('',#28061);
#6547=VERTEX_POINT('',#28062);
#6548=VERTEX_POINT('',#28085);
#6549=VERTEX_POINT('',#28086);
#6550=VERTEX_POINT('',#28109);
#6551=VERTEX_POINT('',#28110);
#6552=VERTEX_POINT('',#28133);
#6553=VERTEX_POINT('',#28134);
#6554=VERTEX_POINT('',#28159);
#6555=VERTEX_POINT('',#28160);
#6556=VERTEX_POINT('',#28183);
#6557=VERTEX_POINT('',#28184);
#6558=VERTEX_POINT('',#28207);
#6559=VERTEX_POINT('',#28208);
#6560=VERTEX_POINT('',#28233);
#6561=VERTEX_POINT('',#28234);
#6562=VERTEX_POINT('',#28257);
#6563=VERTEX_POINT('',#28258);
#6564=VERTEX_POINT('',#28281);
#6565=VERTEX_POINT('',#28282);
#6566=VERTEX_POINT('',#28305);
#6567=VERTEX_POINT('',#28306);
#6568=VERTEX_POINT('',#28331);
#6569=VERTEX_POINT('',#28332);
#6570=VERTEX_POINT('',#28355);
#6571=VERTEX_POINT('',#28356);
#6572=VERTEX_POINT('',#28379);
#6573=VERTEX_POINT('',#28380);
#6574=VERTEX_POINT('',#28405);
#6575=VERTEX_POINT('',#28406);
#6576=VERTEX_POINT('',#28429);
#6577=VERTEX_POINT('',#28430);
#6578=VERTEX_POINT('',#28453);
#6579=VERTEX_POINT('',#28454);
#6580=VERTEX_POINT('',#28477);
#6581=VERTEX_POINT('',#28478);
#6582=VERTEX_POINT('',#28503);
#6583=VERTEX_POINT('',#28504);
#6584=VERTEX_POINT('',#28527);
#6585=VERTEX_POINT('',#28528);
#6586=VERTEX_POINT('',#28551);
#6587=VERTEX_POINT('',#28552);
#6588=VERTEX_POINT('',#28577);
#6589=VERTEX_POINT('',#28578);
#6590=VERTEX_POINT('',#28601);
#6591=VERTEX_POINT('',#28602);
#6592=VERTEX_POINT('',#28625);
#6593=VERTEX_POINT('',#28626);
#6594=VERTEX_POINT('',#28649);
#6595=VERTEX_POINT('',#28650);
#6596=VERTEX_POINT('',#28675);
#6597=VERTEX_POINT('',#28676);
#6598=VERTEX_POINT('',#28699);
#6599=VERTEX_POINT('',#28700);
#6600=VERTEX_POINT('',#28723);
#6601=VERTEX_POINT('',#28724);
#6602=VERTEX_POINT('',#28749);
#6603=VERTEX_POINT('',#28750);
#6604=VERTEX_POINT('',#28773);
#6605=VERTEX_POINT('',#28774);
#6606=VERTEX_POINT('',#28797);
#6607=VERTEX_POINT('',#28798);
#6608=VERTEX_POINT('',#28822);
#6609=VERTEX_POINT('',#28823);
#6610=VERTEX_POINT('',#28849);
#6611=VERTEX_POINT('',#28850);
#6612=VERTEX_POINT('',#28886);
#6613=VERTEX_POINT('',#28887);
#6614=VERTEX_POINT('',#28922);
#6615=VERTEX_POINT('',#28923);
#6616=VERTEX_POINT('',#28960);
#6617=VERTEX_POINT('',#28961);
#6618=VERTEX_POINT('',#28996);
#6619=VERTEX_POINT('',#28997);
#6620=VERTEX_POINT('',#29034);
#6621=VERTEX_POINT('',#29035);
#6622=VERTEX_POINT('',#29071);
#6623=VERTEX_POINT('',#29072);
#6624=VERTEX_POINT('',#29108);
#6625=VERTEX_POINT('',#29110);
#6626=VERTEX_POINT('',#29148);
#6627=VERTEX_POINT('',#29188);
#6628=VERTEX_POINT('',#31184);
#6629=VERTEX_POINT('',#33269);
#6630=VERTEX_POINT('',#33321);
#6631=VERTEX_POINT('',#33322);
#6632=VERTEX_POINT('',#33324);
#6633=VERTEX_POINT('',#33326);
#6634=VERTEX_POINT('',#33330);
#6635=VERTEX_POINT('',#33332);
#6636=VERTEX_POINT('',#33336);
#6637=VERTEX_POINT('',#33340);
#6638=VERTEX_POINT('',#33346);
#6639=VERTEX_POINT('',#33348);
#6640=VERTEX_POINT('',#33353);
#6641=VERTEX_POINT('',#33357);
#7923=EDGE_CURVE('',#6368,#6369,#3931,.T.);
#7924=EDGE_CURVE('',#6368,#6370,#478,.T.);
#7925=EDGE_CURVE('',#6370,#6371,#5513,.F.);
#7926=EDGE_CURVE('',#6371,#6369,#479,.T.);
#7927=EDGE_CURVE('',#6372,#6373,#3932,.T.);
#7928=EDGE_CURVE('',#6372,#6368,#480,.T.);
#7929=EDGE_CURVE('',#6369,#6373,#481,.T.);
#7930=EDGE_CURVE('',#6374,#6375,#3933,.T.);
#7931=EDGE_CURVE('',#6374,#6372,#482,.T.);
#7932=EDGE_CURVE('',#6373,#6375,#483,.T.);
#7933=EDGE_CURVE('',#6376,#6377,#3934,.T.);
#7934=EDGE_CURVE('',#6376,#6374,#484,.T.);
#7935=EDGE_CURVE('',#6375,#6377,#485,.T.);
#7936=EDGE_CURVE('',#6378,#6379,#3935,.T.);
#7937=EDGE_CURVE('',#6378,#6376,#486,.T.);
#7938=EDGE_CURVE('',#6377,#6379,#487,.T.);
#7939=EDGE_CURVE('',#6380,#6381,#3936,.T.);
#7940=EDGE_CURVE('',#6380,#6378,#488,.T.);
#7941=EDGE_CURVE('',#6379,#6381,#489,.T.);
#7942=EDGE_CURVE('',#6382,#6383,#3937,.T.);
#7943=EDGE_CURVE('',#6382,#6380,#490,.T.);
#7944=EDGE_CURVE('',#6381,#6383,#491,.T.);
#7945=EDGE_CURVE('',#6384,#6385,#3938,.T.);
#7946=EDGE_CURVE('',#6384,#6382,#492,.T.);
#7947=EDGE_CURVE('',#6383,#6385,#493,.T.);
#7948=EDGE_CURVE('',#6386,#6387,#3939,.T.);
#7949=EDGE_CURVE('',#6386,#6384,#494,.T.);
#7950=EDGE_CURVE('',#6385,#6387,#495,.T.);
#7951=EDGE_CURVE('',#6388,#6389,#3940,.T.);
#7952=EDGE_CURVE('',#6388,#6386,#496,.T.);
#7953=EDGE_CURVE('',#6387,#6389,#497,.T.);
#7954=EDGE_CURVE('',#6390,#6391,#3941,.T.);
#7955=EDGE_CURVE('',#6390,#6388,#498,.T.);
#7956=EDGE_CURVE('',#6389,#6391,#499,.T.);
#7957=EDGE_CURVE('',#6392,#6393,#3942,.T.);
#7958=EDGE_CURVE('',#6392,#6390,#500,.T.);
#7959=EDGE_CURVE('',#6391,#6393,#501,.T.);
#7960=EDGE_CURVE('',#6394,#6395,#3943,.T.);
#7961=EDGE_CURVE('',#6394,#6392,#502,.T.);
#7962=EDGE_CURVE('',#6393,#6395,#503,.T.);
#7963=EDGE_CURVE('',#6396,#6397,#3944,.T.);
#7964=EDGE_CURVE('',#6396,#6394,#504,.T.);
#7965=EDGE_CURVE('',#6395,#6397,#505,.T.);
#7966=EDGE_CURVE('',#6398,#6399,#3945,.T.);
#7967=EDGE_CURVE('',#6398,#6396,#506,.T.);
#7968=EDGE_CURVE('',#6397,#6399,#507,.T.);
#7969=EDGE_CURVE('',#6400,#6401,#3946,.T.);
#7970=EDGE_CURVE('',#6400,#6398,#508,.T.);
#7971=EDGE_CURVE('',#6399,#6401,#509,.T.);
#7972=EDGE_CURVE('',#6402,#6403,#3947,.T.);
#7973=EDGE_CURVE('',#6402,#6400,#510,.T.);
#7974=EDGE_CURVE('',#6401,#6403,#511,.T.);
#7975=EDGE_CURVE('',#6404,#6405,#3948,.T.);
#7976=EDGE_CURVE('',#6404,#6402,#512,.T.);
#7977=EDGE_CURVE('',#6403,#6405,#513,.T.);
#7978=EDGE_CURVE('',#6406,#6407,#3949,.T.);
#7979=EDGE_CURVE('',#6406,#6404,#514,.T.);
#7980=EDGE_CURVE('',#6405,#6407,#515,.T.);
#7981=EDGE_CURVE('',#6408,#6409,#3950,.T.);
#7982=EDGE_CURVE('',#6408,#6406,#516,.T.);
#7983=EDGE_CURVE('',#6407,#6409,#517,.T.);
#7984=EDGE_CURVE('',#6410,#6411,#3951,.T.);
#7985=EDGE_CURVE('',#6410,#6408,#518,.T.);
#7986=EDGE_CURVE('',#6409,#6411,#519,.T.);
#7987=EDGE_CURVE('',#6412,#6413,#3952,.T.);
#7988=EDGE_CURVE('',#6412,#6410,#520,.T.);
#7989=EDGE_CURVE('',#6411,#6413,#521,.T.);
#7990=EDGE_CURVE('',#6414,#6415,#3953,.T.);
#7991=EDGE_CURVE('',#6414,#6412,#522,.T.);
#7992=EDGE_CURVE('',#6413,#6415,#523,.T.);
#7993=EDGE_CURVE('',#6416,#6417,#3954,.T.);
#7994=EDGE_CURVE('',#6416,#6414,#524,.T.);
#7995=EDGE_CURVE('',#6415,#6417,#525,.T.);
#7996=EDGE_CURVE('',#6418,#6419,#3955,.T.);
#7997=EDGE_CURVE('',#6418,#6416,#526,.T.);
#7998=EDGE_CURVE('',#6417,#6419,#527,.T.);
#7999=EDGE_CURVE('',#6420,#6421,#3956,.T.);
#8000=EDGE_CURVE('',#6420,#6418,#528,.T.);
#8001=EDGE_CURVE('',#6419,#6421,#529,.T.);
#8002=EDGE_CURVE('',#6422,#6423,#3957,.T.);
#8003=EDGE_CURVE('',#6422,#6420,#530,.T.);
#8004=EDGE_CURVE('',#6421,#6423,#531,.T.);
#8005=EDGE_CURVE('',#6424,#6425,#3958,.T.);
#8006=EDGE_CURVE('',#6424,#6422,#532,.T.);
#8007=EDGE_CURVE('',#6423,#6425,#533,.T.);
#8008=EDGE_CURVE('',#6426,#6427,#3959,.T.);
#8009=EDGE_CURVE('',#6426,#6424,#534,.T.);
#8010=EDGE_CURVE('',#6425,#6427,#535,.T.);
#8011=EDGE_CURVE('',#6428,#6429,#3960,.T.);
#8012=EDGE_CURVE('',#6428,#6426,#536,.T.);
#8013=EDGE_CURVE('',#6427,#6429,#537,.T.);
#8014=EDGE_CURVE('',#6430,#6431,#3961,.T.);
#8015=EDGE_CURVE('',#6430,#6428,#538,.T.);
#8016=EDGE_CURVE('',#6429,#6431,#539,.T.);
#8017=EDGE_CURVE('',#6432,#6433,#3962,.T.);
#8018=EDGE_CURVE('',#6432,#6430,#540,.T.);
#8019=EDGE_CURVE('',#6431,#6433,#541,.T.);
#8020=EDGE_CURVE('',#6434,#6435,#3963,.T.);
#8021=EDGE_CURVE('',#6434,#6432,#542,.T.);
#8022=EDGE_CURVE('',#6433,#6435,#543,.T.);
#8023=EDGE_CURVE('',#6436,#6437,#3964,.T.);
#8024=EDGE_CURVE('',#6436,#6434,#544,.T.);
#8025=EDGE_CURVE('',#6435,#6437,#545,.T.);
#8026=EDGE_CURVE('',#6438,#6439,#3965,.T.);
#8027=EDGE_CURVE('',#6438,#6436,#546,.T.);
#8028=EDGE_CURVE('',#6437,#6439,#547,.T.);
#8029=EDGE_CURVE('',#6440,#6441,#3966,.T.);
#8030=EDGE_CURVE('',#6440,#6438,#548,.T.);
#8031=EDGE_CURVE('',#6439,#6441,#549,.T.);
#8032=EDGE_CURVE('',#6442,#6443,#3967,.T.);
#8033=EDGE_CURVE('',#6442,#6440,#550,.T.);
#8034=EDGE_CURVE('',#6441,#6443,#551,.T.);
#8035=EDGE_CURVE('',#6444,#6445,#3968,.T.);
#8036=EDGE_CURVE('',#6444,#6442,#552,.T.);
#8037=EDGE_CURVE('',#6443,#6445,#553,.T.);
#8038=EDGE_CURVE('',#6446,#6447,#3969,.T.);
#8039=EDGE_CURVE('',#6446,#6444,#554,.T.);
#8040=EDGE_CURVE('',#6445,#6447,#555,.T.);
#8041=EDGE_CURVE('',#6448,#6449,#3970,.T.);
#8042=EDGE_CURVE('',#6448,#6446,#556,.T.);
#8043=EDGE_CURVE('',#6447,#6449,#557,.T.);
#8044=EDGE_CURVE('',#6450,#6451,#3971,.T.);
#8045=EDGE_CURVE('',#6450,#6448,#558,.T.);
#8046=EDGE_CURVE('',#6449,#6451,#559,.T.);
#8047=EDGE_CURVE('',#6452,#6453,#3972,.T.);
#8048=EDGE_CURVE('',#6452,#6450,#560,.T.);
#8049=EDGE_CURVE('',#6451,#6453,#561,.T.);
#8050=EDGE_CURVE('',#6454,#6455,#3973,.T.);
#8051=EDGE_CURVE('',#6454,#6452,#562,.T.);
#8052=EDGE_CURVE('',#6453,#6455,#563,.T.);
#8053=EDGE_CURVE('',#6456,#6457,#3974,.T.);
#8054=EDGE_CURVE('',#6456,#6454,#564,.T.);
#8055=EDGE_CURVE('',#6455,#6457,#565,.T.);
#8056=EDGE_CURVE('',#6458,#6459,#3975,.T.);
#8057=EDGE_CURVE('',#6458,#6456,#566,.T.);
#8058=EDGE_CURVE('',#6457,#6459,#567,.T.);
#8059=EDGE_CURVE('',#6460,#6461,#3976,.T.);
#8060=EDGE_CURVE('',#6460,#6458,#568,.T.);
#8061=EDGE_CURVE('',#6459,#6461,#569,.T.);
#8062=EDGE_CURVE('',#6462,#6463,#3977,.T.);
#8063=EDGE_CURVE('',#6462,#6460,#570,.T.);
#8064=EDGE_CURVE('',#6461,#6463,#571,.T.);
#8065=EDGE_CURVE('',#6464,#6465,#3978,.T.);
#8066=EDGE_CURVE('',#6464,#6462,#572,.T.);
#8067=EDGE_CURVE('',#6463,#6465,#573,.T.);
#8068=EDGE_CURVE('',#6466,#6467,#3979,.T.);
#8069=EDGE_CURVE('',#6466,#6464,#574,.T.);
#8070=EDGE_CURVE('',#6465,#6467,#575,.T.);
#8071=EDGE_CURVE('',#6468,#6469,#3980,.T.);
#8072=EDGE_CURVE('',#6468,#6466,#576,.T.);
#8073=EDGE_CURVE('',#6467,#6469,#577,.T.);
#8074=EDGE_CURVE('',#6470,#6471,#3981,.T.);
#8075=EDGE_CURVE('',#6470,#6468,#578,.T.);
#8076=EDGE_CURVE('',#6469,#6471,#579,.T.);
#8077=EDGE_CURVE('',#6472,#6473,#3982,.T.);
#8078=EDGE_CURVE('',#6472,#6470,#580,.T.);
#8079=EDGE_CURVE('',#6471,#6473,#581,.T.);
#8080=EDGE_CURVE('',#6474,#6475,#3983,.T.);
#8081=EDGE_CURVE('',#6474,#6472,#582,.T.);
#8082=EDGE_CURVE('',#6473,#6475,#583,.T.);
#8083=EDGE_CURVE('',#6476,#6477,#3984,.T.);
#8084=EDGE_CURVE('',#6476,#6474,#584,.T.);
#8085=EDGE_CURVE('',#6475,#6477,#585,.T.);
#8086=EDGE_CURVE('',#6478,#6479,#3985,.T.);
#8087=EDGE_CURVE('',#6478,#6476,#586,.T.);
#8088=EDGE_CURVE('',#6477,#6479,#587,.T.);
#8089=EDGE_CURVE('',#6480,#6481,#3986,.T.);
#8090=EDGE_CURVE('',#6480,#6478,#588,.T.);
#8091=EDGE_CURVE('',#6479,#6481,#589,.T.);
#8092=EDGE_CURVE('',#6482,#6483,#3987,.T.);
#8093=EDGE_CURVE('',#6482,#6480,#590,.T.);
#8094=EDGE_CURVE('',#6481,#6483,#591,.T.);
#8095=EDGE_CURVE('',#6484,#6485,#3988,.T.);
#8096=EDGE_CURVE('',#6484,#6482,#592,.T.);
#8097=EDGE_CURVE('',#6483,#6485,#593,.T.);
#8098=EDGE_CURVE('',#6486,#6487,#3989,.T.);
#8099=EDGE_CURVE('',#6486,#6484,#594,.T.);
#8100=EDGE_CURVE('',#6485,#6487,#595,.T.);
#8101=EDGE_CURVE('',#6488,#6489,#3990,.T.);
#8102=EDGE_CURVE('',#6488,#6486,#596,.T.);
#8103=EDGE_CURVE('',#6487,#6489,#597,.T.);
#8104=EDGE_CURVE('',#6490,#6491,#3991,.T.);
#8105=EDGE_CURVE('',#6490,#6488,#598,.T.);
#8106=EDGE_CURVE('',#6489,#6491,#599,.T.);
#8107=EDGE_CURVE('',#6492,#6493,#3992,.T.);
#8108=EDGE_CURVE('',#6492,#6490,#600,.T.);
#8109=EDGE_CURVE('',#6491,#6493,#601,.T.);
#8110=EDGE_CURVE('',#6494,#6495,#3993,.T.);
#8111=EDGE_CURVE('',#6494,#6492,#602,.T.);
#8112=EDGE_CURVE('',#6493,#6495,#603,.T.);
#8113=EDGE_CURVE('',#6496,#6497,#3994,.T.);
#8114=EDGE_CURVE('',#6496,#6498,#604,.T.);
#8115=EDGE_CURVE('',#6497,#6498,#5514,.T.);
#8116=EDGE_CURVE('',#6499,#6500,#3995,.T.);
#8117=EDGE_CURVE('',#6499,#6496,#605,.T.);
#8118=EDGE_CURVE('',#6501,#6497,#5515,.T.);
#8119=EDGE_CURVE('',#6500,#6501,#606,.T.);
#8120=EDGE_CURVE('',#6502,#6503,#3996,.T.);
#8121=EDGE_CURVE('',#6502,#6499,#607,.T.);
#8122=EDGE_CURVE('',#6503,#6500,#608,.T.);
#8123=EDGE_CURVE('',#6504,#6505,#3997,.T.);
#8124=EDGE_CURVE('',#6504,#6502,#609,.T.);
#8125=EDGE_CURVE('',#6505,#6503,#610,.T.);
#8126=EDGE_CURVE('',#6506,#6507,#3998,.T.);
#8127=EDGE_CURVE('',#6506,#6504,#611,.T.);
#8128=EDGE_CURVE('',#6507,#6505,#612,.T.);
#8129=EDGE_CURVE('',#6508,#6509,#3999,.T.);
#8130=EDGE_CURVE('',#6508,#6506,#613,.T.);
#8131=EDGE_CURVE('',#6509,#6507,#614,.T.);
#8132=EDGE_CURVE('',#6510,#6511,#4000,.T.);
#8133=EDGE_CURVE('',#6510,#6508,#615,.T.);
#8134=EDGE_CURVE('',#6511,#6509,#616,.T.);
#8135=EDGE_CURVE('',#6512,#6513,#4001,.T.);
#8136=EDGE_CURVE('',#6512,#6510,#617,.T.);
#8137=EDGE_CURVE('',#6513,#6511,#618,.T.);
#8138=EDGE_CURVE('',#6514,#6515,#4002,.T.);
#8139=EDGE_CURVE('',#6514,#6512,#619,.T.);
#8140=EDGE_CURVE('',#6515,#6513,#620,.T.);
#8141=EDGE_CURVE('',#6516,#6517,#4003,.T.);
#8142=EDGE_CURVE('',#6516,#6514,#621,.T.);
#8143=EDGE_CURVE('',#6517,#6515,#622,.T.);
#8144=EDGE_CURVE('',#6518,#6519,#4004,.T.);
#8145=EDGE_CURVE('',#6518,#6516,#623,.T.);
#8146=EDGE_CURVE('',#6519,#6517,#624,.T.);
#8147=EDGE_CURVE('',#6520,#6521,#4005,.T.);
#8148=EDGE_CURVE('',#6520,#6518,#625,.T.);
#8149=EDGE_CURVE('',#6521,#6519,#626,.T.);
#8150=EDGE_CURVE('',#6522,#6523,#4006,.T.);
#8151=EDGE_CURVE('',#6522,#6520,#627,.T.);
#8152=EDGE_CURVE('',#6523,#6521,#628,.T.);
#8153=EDGE_CURVE('',#6524,#6525,#4007,.T.);
#8154=EDGE_CURVE('',#6524,#6522,#629,.T.);
#8155=EDGE_CURVE('',#6525,#6523,#630,.T.);
#8156=EDGE_CURVE('',#6526,#6527,#4008,.T.);
#8157=EDGE_CURVE('',#6526,#6524,#631,.T.);
#8158=EDGE_CURVE('',#6527,#6525,#632,.T.);
#8159=EDGE_CURVE('',#6528,#6529,#4009,.T.);
#8160=EDGE_CURVE('',#6528,#6526,#633,.T.);
#8161=EDGE_CURVE('',#6529,#6527,#634,.T.);
#8162=EDGE_CURVE('',#6530,#6531,#4010,.T.);
#8163=EDGE_CURVE('',#6530,#6528,#635,.T.);
#8164=EDGE_CURVE('',#6531,#6529,#636,.T.);
#8165=EDGE_CURVE('',#6532,#6533,#4011,.T.);
#8166=EDGE_CURVE('',#6532,#6530,#637,.T.);
#8167=EDGE_CURVE('',#6533,#6531,#638,.T.);
#8168=EDGE_CURVE('',#6534,#6535,#4012,.T.);
#8169=EDGE_CURVE('',#6534,#6532,#639,.T.);
#8170=EDGE_CURVE('',#6535,#6533,#640,.T.);
#8171=EDGE_CURVE('',#6536,#6537,#4013,.T.);
#8172=EDGE_CURVE('',#6536,#6534,#641,.T.);
#8173=EDGE_CURVE('',#6537,#6535,#642,.T.);
#8174=EDGE_CURVE('',#6538,#6539,#4014,.T.);
#8175=EDGE_CURVE('',#6538,#6536,#643,.T.);
#8176=EDGE_CURVE('',#6539,#6537,#644,.T.);
#8177=EDGE_CURVE('',#6540,#6541,#4015,.T.);
#8178=EDGE_CURVE('',#6540,#6538,#645,.T.);
#8179=EDGE_CURVE('',#6541,#6539,#646,.T.);
#8180=EDGE_CURVE('',#6542,#6543,#4016,.T.);
#8181=EDGE_CURVE('',#6542,#6540,#647,.T.);
#8182=EDGE_CURVE('',#6543,#6541,#648,.T.);
#8183=EDGE_CURVE('',#6544,#6545,#4017,.T.);
#8184=EDGE_CURVE('',#6544,#6542,#649,.T.);
#8185=EDGE_CURVE('',#6545,#6543,#650,.T.);
#8186=EDGE_CURVE('',#6546,#6547,#4018,.T.);
#8187=EDGE_CURVE('',#6546,#6544,#651,.T.);
#8188=EDGE_CURVE('',#6547,#6545,#652,.T.);
#8189=EDGE_CURVE('',#6548,#6549,#4019,.T.);
#8190=EDGE_CURVE('',#6548,#6546,#653,.T.);
#8191=EDGE_CURVE('',#6549,#6547,#654,.T.);
#8192=EDGE_CURVE('',#6550,#6551,#4020,.T.);
#8193=EDGE_CURVE('',#6550,#6548,#655,.T.);
#8194=EDGE_CURVE('',#6551,#6549,#656,.T.);
#8195=EDGE_CURVE('',#6552,#6553,#4021,.T.);
#8196=EDGE_CURVE('',#6552,#6550,#657,.T.);
#8197=EDGE_CURVE('',#6553,#6551,#658,.T.);
#8198=EDGE_CURVE('',#6554,#6555,#4022,.T.);
#8199=EDGE_CURVE('',#6554,#6552,#659,.T.);
#8200=EDGE_CURVE('',#6555,#6553,#660,.T.);
#8201=EDGE_CURVE('',#6556,#6557,#4023,.T.);
#8202=EDGE_CURVE('',#6556,#6554,#661,.T.);
#8203=EDGE_CURVE('',#6557,#6555,#662,.T.);
#8204=EDGE_CURVE('',#6558,#6559,#4024,.T.);
#8205=EDGE_CURVE('',#6558,#6556,#663,.T.);
#8206=EDGE_CURVE('',#6559,#6557,#664,.T.);
#8207=EDGE_CURVE('',#6560,#6561,#4025,.T.);
#8208=EDGE_CURVE('',#6560,#6558,#665,.T.);
#8209=EDGE_CURVE('',#6561,#6559,#666,.T.);
#8210=EDGE_CURVE('',#6562,#6563,#4026,.T.);
#8211=EDGE_CURVE('',#6562,#6560,#667,.T.);
#8212=EDGE_CURVE('',#6563,#6561,#668,.T.);
#8213=EDGE_CURVE('',#6564,#6565,#4027,.T.);
#8214=EDGE_CURVE('',#6564,#6562,#669,.T.);
#8215=EDGE_CURVE('',#6565,#6563,#670,.T.);
#8216=EDGE_CURVE('',#6566,#6567,#4028,.T.);
#8217=EDGE_CURVE('',#6566,#6564,#671,.T.);
#8218=EDGE_CURVE('',#6567,#6565,#672,.T.);
#8219=EDGE_CURVE('',#6568,#6569,#4029,.T.);
#8220=EDGE_CURVE('',#6568,#6566,#673,.T.);
#8221=EDGE_CURVE('',#6569,#6567,#674,.T.);
#8222=EDGE_CURVE('',#6570,#6571,#4030,.T.);
#8223=EDGE_CURVE('',#6570,#6568,#675,.T.);
#8224=EDGE_CURVE('',#6571,#6569,#676,.T.);
#8225=EDGE_CURVE('',#6572,#6573,#4031,.T.);
#8226=EDGE_CURVE('',#6572,#6570,#677,.T.);
#8227=EDGE_CURVE('',#6573,#6571,#678,.T.);
#8228=EDGE_CURVE('',#6574,#6575,#4032,.T.);
#8229=EDGE_CURVE('',#6574,#6572,#679,.T.);
#8230=EDGE_CURVE('',#6575,#6573,#680,.T.);
#8231=EDGE_CURVE('',#6576,#6577,#4033,.T.);
#8232=EDGE_CURVE('',#6576,#6574,#681,.T.);
#8233=EDGE_CURVE('',#6577,#6575,#682,.T.);
#8234=EDGE_CURVE('',#6578,#6579,#4034,.T.);
#8235=EDGE_CURVE('',#6578,#6576,#683,.T.);
#8236=EDGE_CURVE('',#6579,#6577,#684,.T.);
#8237=EDGE_CURVE('',#6580,#6581,#4035,.T.);
#8238=EDGE_CURVE('',#6580,#6578,#685,.T.);
#8239=EDGE_CURVE('',#6581,#6579,#686,.T.);
#8240=EDGE_CURVE('',#6582,#6583,#4036,.T.);
#8241=EDGE_CURVE('',#6582,#6580,#687,.T.);
#8242=EDGE_CURVE('',#6583,#6581,#688,.T.);
#8243=EDGE_CURVE('',#6584,#6585,#4037,.T.);
#8244=EDGE_CURVE('',#6584,#6582,#689,.T.);
#8245=EDGE_CURVE('',#6585,#6583,#690,.T.);
#8246=EDGE_CURVE('',#6586,#6587,#4038,.T.);
#8247=EDGE_CURVE('',#6586,#6584,#691,.T.);
#8248=EDGE_CURVE('',#6587,#6585,#692,.T.);
#8249=EDGE_CURVE('',#6588,#6589,#4039,.T.);
#8250=EDGE_CURVE('',#6588,#6586,#693,.T.);
#8251=EDGE_CURVE('',#6589,#6587,#694,.T.);
#8252=EDGE_CURVE('',#6590,#6591,#4040,.T.);
#8253=EDGE_CURVE('',#6590,#6588,#695,.T.);
#8254=EDGE_CURVE('',#6591,#6589,#696,.T.);
#8255=EDGE_CURVE('',#6592,#6593,#4041,.T.);
#8256=EDGE_CURVE('',#6592,#6590,#697,.T.);
#8257=EDGE_CURVE('',#6593,#6591,#698,.T.);
#8258=EDGE_CURVE('',#6594,#6595,#4042,.T.);
#8259=EDGE_CURVE('',#6594,#6592,#699,.T.);
#8260=EDGE_CURVE('',#6595,#6593,#700,.T.);
#8261=EDGE_CURVE('',#6596,#6597,#4043,.T.);
#8262=EDGE_CURVE('',#6596,#6594,#701,.T.);
#8263=EDGE_CURVE('',#6597,#6595,#702,.T.);
#8264=EDGE_CURVE('',#6598,#6599,#4044,.T.);
#8265=EDGE_CURVE('',#6598,#6596,#703,.T.);
#8266=EDGE_CURVE('',#6599,#6597,#704,.T.);
#8267=EDGE_CURVE('',#6600,#6601,#4045,.T.);
#8268=EDGE_CURVE('',#6600,#6598,#705,.T.);
#8269=EDGE_CURVE('',#6601,#6599,#706,.T.);
#8270=EDGE_CURVE('',#6602,#6603,#4046,.T.);
#8271=EDGE_CURVE('',#6602,#6600,#707,.T.);
#8272=EDGE_CURVE('',#6603,#6601,#708,.T.);
#8273=EDGE_CURVE('',#6604,#6605,#4047,.T.);
#8274=EDGE_CURVE('',#6604,#6602,#709,.T.);
#8275=EDGE_CURVE('',#6605,#6603,#710,.T.);
#8276=EDGE_CURVE('',#6606,#6607,#4048,.T.);
#8277=EDGE_CURVE('',#6606,#6604,#711,.T.);
#8278=EDGE_CURVE('',#6607,#6605,#712,.T.);
#8279=EDGE_CURVE('',#6608,#6609,#4049,.T.);
#8280=EDGE_CURVE('',#6608,#6606,#713,.T.);
#8281=EDGE_CURVE('',#6609,#6607,#714,.T.);
#8282=EDGE_CURVE('',#6610,#6611,#4050,.T.);
#8283=EDGE_CURVE('',#6610,#6608,#715,.T.);
#8284=EDGE_CURVE('',#6611,#6609,#716,.T.);
#8285=EDGE_CURVE('',#6612,#6613,#4051,.T.);
#8286=EDGE_CURVE('',#6612,#6610,#717,.T.);
#8287=EDGE_CURVE('',#6613,#6611,#718,.T.);
#8288=EDGE_CURVE('',#6614,#6615,#4052,.T.);
#8289=EDGE_CURVE('',#6614,#6612,#719,.T.);
#8290=EDGE_CURVE('',#6615,#6613,#720,.T.);
#8291=EDGE_CURVE('',#6616,#6617,#4053,.T.);
#8292=EDGE_CURVE('',#6616,#6614,#721,.T.);
#8293=EDGE_CURVE('',#6617,#6615,#722,.T.);
#8294=EDGE_CURVE('',#6618,#6619,#4054,.T.);
#8295=EDGE_CURVE('',#6618,#6616,#723,.T.);
#8296=EDGE_CURVE('',#6619,#6617,#724,.T.);
#8297=EDGE_CURVE('',#6620,#6621,#4055,.T.);
#8298=EDGE_CURVE('',#6620,#6618,#725,.T.);
#8299=EDGE_CURVE('',#6621,#6619,#726,.T.);
#8300=EDGE_CURVE('',#6622,#6623,#4056,.T.);
#8301=EDGE_CURVE('',#6622,#6620,#727,.T.);
#8302=EDGE_CURVE('',#6623,#6621,#728,.T.);
#8303=EDGE_CURVE('',#6624,#6624,#5516,.T.);
#8304=EDGE_CURVE('',#6625,#6371,#729,.T.);
#8305=EDGE_CURVE('',#6370,#6626,#730,.T.);
#8306=EDGE_CURVE('',#6626,#6625,#5517,.T.);
#8307=EDGE_CURVE('',#6624,#6627,#4057,.T.);
#8308=EDGE_CURVE('',#6627,#6627,#5518,.T.);
#8309=EDGE_CURVE('',#6628,#6501,#731,.T.);
#8310=EDGE_CURVE('',#6495,#6628,#732,.T.);
#8311=EDGE_CURVE('',#6625,#6623,#733,.T.);
#8312=EDGE_CURVE('',#6626,#6622,#734,.T.);
#8313=EDGE_CURVE('',#6498,#6629,#735,.T.);
#8314=EDGE_CURVE('',#6629,#6494,#736,.T.);
#8315=EDGE_CURVE('',#6630,#6631,#4058,.T.);
#8316=EDGE_CURVE('',#6630,#6632,#4059,.T.);
#8317=EDGE_CURVE('',#6633,#6632,#4060,.T.);
#8318=EDGE_CURVE('',#6631,#6633,#4061,.T.);
#8319=EDGE_CURVE('',#6631,#6634,#5519,.T.);
#8320=EDGE_CURVE('',#6633,#6635,#4062,.T.);
#8321=EDGE_CURVE('',#6635,#6634,#4063,.T.);
#8322=EDGE_CURVE('',#6632,#6636,#4064,.T.);
#8323=EDGE_CURVE('',#6635,#6636,#4065,.T.);
#8324=EDGE_CURVE('',#6634,#6637,#4066,.T.);
#8325=EDGE_CURVE('',#6636,#6637,#4067,.T.);
#8326=EDGE_CURVE('',#6637,#6630,#5520,.T.);
#8327=EDGE_CURVE('',#6638,#6638,#5521,.T.);
#8328=EDGE_CURVE('',#6638,#6639,#4068,.T.);
#8329=EDGE_CURVE('',#6639,#6639,#5522,.T.);
#8330=EDGE_CURVE('',#6640,#6640,#5523,.T.);
#8331=EDGE_CURVE('',#6629,#6628,#5524,.F.);
#8332=EDGE_CURVE('',#6641,#6641,#5525,.T.);
#8333=EDGE_CURVE('',#6641,#6640,#4069,.T.);
#10847=ORIENTED_EDGE('',*,*,#7923,.F.);
#10848=ORIENTED_EDGE('',*,*,#7924,.T.);
#10849=ORIENTED_EDGE('',*,*,#7925,.T.);
#10850=ORIENTED_EDGE('',*,*,#7926,.T.);
#10851=ORIENTED_EDGE('',*,*,#7927,.F.);
#10852=ORIENTED_EDGE('',*,*,#7928,.T.);
#10853=ORIENTED_EDGE('',*,*,#7923,.T.);
#10854=ORIENTED_EDGE('',*,*,#7929,.T.);
#10855=ORIENTED_EDGE('',*,*,#7930,.F.);
#10856=ORIENTED_EDGE('',*,*,#7931,.T.);
#10857=ORIENTED_EDGE('',*,*,#7927,.T.);
#10858=ORIENTED_EDGE('',*,*,#7932,.T.);
#10859=ORIENTED_EDGE('',*,*,#7933,.F.);
#10860=ORIENTED_EDGE('',*,*,#7934,.T.);
#10861=ORIENTED_EDGE('',*,*,#7930,.T.);
#10862=ORIENTED_EDGE('',*,*,#7935,.T.);
#10863=ORIENTED_EDGE('',*,*,#7936,.F.);
#10864=ORIENTED_EDGE('',*,*,#7937,.T.);
#10865=ORIENTED_EDGE('',*,*,#7933,.T.);
#10866=ORIENTED_EDGE('',*,*,#7938,.T.);
#10867=ORIENTED_EDGE('',*,*,#7939,.F.);
#10868=ORIENTED_EDGE('',*,*,#7940,.T.);
#10869=ORIENTED_EDGE('',*,*,#7936,.T.);
#10870=ORIENTED_EDGE('',*,*,#7941,.T.);
#10871=ORIENTED_EDGE('',*,*,#7942,.F.);
#10872=ORIENTED_EDGE('',*,*,#7943,.T.);
#10873=ORIENTED_EDGE('',*,*,#7939,.T.);
#10874=ORIENTED_EDGE('',*,*,#7944,.T.);
#10875=ORIENTED_EDGE('',*,*,#7945,.F.);
#10876=ORIENTED_EDGE('',*,*,#7946,.T.);
#10877=ORIENTED_EDGE('',*,*,#7942,.T.);
#10878=ORIENTED_EDGE('',*,*,#7947,.T.);
#10879=ORIENTED_EDGE('',*,*,#7948,.F.);
#10880=ORIENTED_EDGE('',*,*,#7949,.T.);
#10881=ORIENTED_EDGE('',*,*,#7945,.T.);
#10882=ORIENTED_EDGE('',*,*,#7950,.T.);
#10883=ORIENTED_EDGE('',*,*,#7951,.F.);
#10884=ORIENTED_EDGE('',*,*,#7952,.T.);
#10885=ORIENTED_EDGE('',*,*,#7948,.T.);
#10886=ORIENTED_EDGE('',*,*,#7953,.T.);
#10887=ORIENTED_EDGE('',*,*,#7954,.F.);
#10888=ORIENTED_EDGE('',*,*,#7955,.T.);
#10889=ORIENTED_EDGE('',*,*,#7951,.T.);
#10890=ORIENTED_EDGE('',*,*,#7956,.T.);
#10891=ORIENTED_EDGE('',*,*,#7957,.F.);
#10892=ORIENTED_EDGE('',*,*,#7958,.T.);
#10893=ORIENTED_EDGE('',*,*,#7954,.T.);
#10894=ORIENTED_EDGE('',*,*,#7959,.T.);
#10895=ORIENTED_EDGE('',*,*,#7960,.F.);
#10896=ORIENTED_EDGE('',*,*,#7961,.T.);
#10897=ORIENTED_EDGE('',*,*,#7957,.T.);
#10898=ORIENTED_EDGE('',*,*,#7962,.T.);
#10899=ORIENTED_EDGE('',*,*,#7963,.F.);
#10900=ORIENTED_EDGE('',*,*,#7964,.T.);
#10901=ORIENTED_EDGE('',*,*,#7960,.T.);
#10902=ORIENTED_EDGE('',*,*,#7965,.T.);
#10903=ORIENTED_EDGE('',*,*,#7966,.F.);
#10904=ORIENTED_EDGE('',*,*,#7967,.T.);
#10905=ORIENTED_EDGE('',*,*,#7963,.T.);
#10906=ORIENTED_EDGE('',*,*,#7968,.T.);
#10907=ORIENTED_EDGE('',*,*,#7969,.F.);
#10908=ORIENTED_EDGE('',*,*,#7970,.T.);
#10909=ORIENTED_EDGE('',*,*,#7966,.T.);
#10910=ORIENTED_EDGE('',*,*,#7971,.T.);
#10911=ORIENTED_EDGE('',*,*,#7972,.F.);
#10912=ORIENTED_EDGE('',*,*,#7973,.T.);
#10913=ORIENTED_EDGE('',*,*,#7969,.T.);
#10914=ORIENTED_EDGE('',*,*,#7974,.T.);
#10915=ORIENTED_EDGE('',*,*,#7975,.F.);
#10916=ORIENTED_EDGE('',*,*,#7976,.T.);
#10917=ORIENTED_EDGE('',*,*,#7972,.T.);
#10918=ORIENTED_EDGE('',*,*,#7977,.T.);
#10919=ORIENTED_EDGE('',*,*,#7978,.F.);
#10920=ORIENTED_EDGE('',*,*,#7979,.T.);
#10921=ORIENTED_EDGE('',*,*,#7975,.T.);
#10922=ORIENTED_EDGE('',*,*,#7980,.T.);
#10923=ORIENTED_EDGE('',*,*,#7981,.F.);
#10924=ORIENTED_EDGE('',*,*,#7982,.T.);
#10925=ORIENTED_EDGE('',*,*,#7978,.T.);
#10926=ORIENTED_EDGE('',*,*,#7983,.T.);
#10927=ORIENTED_EDGE('',*,*,#7984,.F.);
#10928=ORIENTED_EDGE('',*,*,#7985,.T.);
#10929=ORIENTED_EDGE('',*,*,#7981,.T.);
#10930=ORIENTED_EDGE('',*,*,#7986,.T.);
#10931=ORIENTED_EDGE('',*,*,#7987,.F.);
#10932=ORIENTED_EDGE('',*,*,#7988,.T.);
#10933=ORIENTED_EDGE('',*,*,#7984,.T.);
#10934=ORIENTED_EDGE('',*,*,#7989,.T.);
#10935=ORIENTED_EDGE('',*,*,#7990,.F.);
#10936=ORIENTED_EDGE('',*,*,#7991,.T.);
#10937=ORIENTED_EDGE('',*,*,#7987,.T.);
#10938=ORIENTED_EDGE('',*,*,#7992,.T.);
#10939=ORIENTED_EDGE('',*,*,#7993,.F.);
#10940=ORIENTED_EDGE('',*,*,#7994,.T.);
#10941=ORIENTED_EDGE('',*,*,#7990,.T.);
#10942=ORIENTED_EDGE('',*,*,#7995,.T.);
#10943=ORIENTED_EDGE('',*,*,#7996,.F.);
#10944=ORIENTED_EDGE('',*,*,#7997,.T.);
#10945=ORIENTED_EDGE('',*,*,#7993,.T.);
#10946=ORIENTED_EDGE('',*,*,#7998,.T.);
#10947=ORIENTED_EDGE('',*,*,#7999,.F.);
#10948=ORIENTED_EDGE('',*,*,#8000,.T.);
#10949=ORIENTED_EDGE('',*,*,#7996,.T.);
#10950=ORIENTED_EDGE('',*,*,#8001,.T.);
#10951=ORIENTED_EDGE('',*,*,#8002,.F.);
#10952=ORIENTED_EDGE('',*,*,#8003,.T.);
#10953=ORIENTED_EDGE('',*,*,#7999,.T.);
#10954=ORIENTED_EDGE('',*,*,#8004,.T.);
#10955=ORIENTED_EDGE('',*,*,#8005,.F.);
#10956=ORIENTED_EDGE('',*,*,#8006,.T.);
#10957=ORIENTED_EDGE('',*,*,#8002,.T.);
#10958=ORIENTED_EDGE('',*,*,#8007,.T.);
#10959=ORIENTED_EDGE('',*,*,#8008,.F.);
#10960=ORIENTED_EDGE('',*,*,#8009,.T.);
#10961=ORIENTED_EDGE('',*,*,#8005,.T.);
#10962=ORIENTED_EDGE('',*,*,#8010,.T.);
#10963=ORIENTED_EDGE('',*,*,#8011,.F.);
#10964=ORIENTED_EDGE('',*,*,#8012,.T.);
#10965=ORIENTED_EDGE('',*,*,#8008,.T.);
#10966=ORIENTED_EDGE('',*,*,#8013,.T.);
#10967=ORIENTED_EDGE('',*,*,#8014,.F.);
#10968=ORIENTED_EDGE('',*,*,#8015,.T.);
#10969=ORIENTED_EDGE('',*,*,#8011,.T.);
#10970=ORIENTED_EDGE('',*,*,#8016,.T.);
#10971=ORIENTED_EDGE('',*,*,#8017,.F.);
#10972=ORIENTED_EDGE('',*,*,#8018,.T.);
#10973=ORIENTED_EDGE('',*,*,#8014,.T.);
#10974=ORIENTED_EDGE('',*,*,#8019,.T.);
#10975=ORIENTED_EDGE('',*,*,#8020,.F.);
#10976=ORIENTED_EDGE('',*,*,#8021,.T.);
#10977=ORIENTED_EDGE('',*,*,#8017,.T.);
#10978=ORIENTED_EDGE('',*,*,#8022,.T.);
#10979=ORIENTED_EDGE('',*,*,#8023,.F.);
#10980=ORIENTED_EDGE('',*,*,#8024,.T.);
#10981=ORIENTED_EDGE('',*,*,#8020,.T.);
#10982=ORIENTED_EDGE('',*,*,#8025,.T.);
#10983=ORIENTED_EDGE('',*,*,#8026,.F.);
#10984=ORIENTED_EDGE('',*,*,#8027,.T.);
#10985=ORIENTED_EDGE('',*,*,#8023,.T.);
#10986=ORIENTED_EDGE('',*,*,#8028,.T.);
#10987=ORIENTED_EDGE('',*,*,#8029,.F.);
#10988=ORIENTED_EDGE('',*,*,#8030,.T.);
#10989=ORIENTED_EDGE('',*,*,#8026,.T.);
#10990=ORIENTED_EDGE('',*,*,#8031,.T.);
#10991=ORIENTED_EDGE('',*,*,#8032,.F.);
#10992=ORIENTED_EDGE('',*,*,#8033,.T.);
#10993=ORIENTED_EDGE('',*,*,#8029,.T.);
#10994=ORIENTED_EDGE('',*,*,#8034,.T.);
#10995=ORIENTED_EDGE('',*,*,#8035,.F.);
#10996=ORIENTED_EDGE('',*,*,#8036,.T.);
#10997=ORIENTED_EDGE('',*,*,#8032,.T.);
#10998=ORIENTED_EDGE('',*,*,#8037,.T.);
#10999=ORIENTED_EDGE('',*,*,#8038,.F.);
#11000=ORIENTED_EDGE('',*,*,#8039,.T.);
#11001=ORIENTED_EDGE('',*,*,#8035,.T.);
#11002=ORIENTED_EDGE('',*,*,#8040,.T.);
#11003=ORIENTED_EDGE('',*,*,#8041,.F.);
#11004=ORIENTED_EDGE('',*,*,#8042,.T.);
#11005=ORIENTED_EDGE('',*,*,#8038,.T.);
#11006=ORIENTED_EDGE('',*,*,#8043,.T.);
#11007=ORIENTED_EDGE('',*,*,#8044,.F.);
#11008=ORIENTED_EDGE('',*,*,#8045,.T.);
#11009=ORIENTED_EDGE('',*,*,#8041,.T.);
#11010=ORIENTED_EDGE('',*,*,#8046,.T.);
#11011=ORIENTED_EDGE('',*,*,#8047,.F.);
#11012=ORIENTED_EDGE('',*,*,#8048,.T.);
#11013=ORIENTED_EDGE('',*,*,#8044,.T.);
#11014=ORIENTED_EDGE('',*,*,#8049,.T.);
#11015=ORIENTED_EDGE('',*,*,#8050,.F.);
#11016=ORIENTED_EDGE('',*,*,#8051,.T.);
#11017=ORIENTED_EDGE('',*,*,#8047,.T.);
#11018=ORIENTED_EDGE('',*,*,#8052,.T.);
#11019=ORIENTED_EDGE('',*,*,#8053,.F.);
#11020=ORIENTED_EDGE('',*,*,#8054,.T.);
#11021=ORIENTED_EDGE('',*,*,#8050,.T.);
#11022=ORIENTED_EDGE('',*,*,#8055,.T.);
#11023=ORIENTED_EDGE('',*,*,#8056,.F.);
#11024=ORIENTED_EDGE('',*,*,#8057,.T.);
#11025=ORIENTED_EDGE('',*,*,#8053,.T.);
#11026=ORIENTED_EDGE('',*,*,#8058,.T.);
#11027=ORIENTED_EDGE('',*,*,#8059,.F.);
#11028=ORIENTED_EDGE('',*,*,#8060,.T.);
#11029=ORIENTED_EDGE('',*,*,#8056,.T.);
#11030=ORIENTED_EDGE('',*,*,#8061,.T.);
#11031=ORIENTED_EDGE('',*,*,#8062,.F.);
#11032=ORIENTED_EDGE('',*,*,#8063,.T.);
#11033=ORIENTED_EDGE('',*,*,#8059,.T.);
#11034=ORIENTED_EDGE('',*,*,#8064,.T.);
#11035=ORIENTED_EDGE('',*,*,#8065,.F.);
#11036=ORIENTED_EDGE('',*,*,#8066,.T.);
#11037=ORIENTED_EDGE('',*,*,#8062,.T.);
#11038=ORIENTED_EDGE('',*,*,#8067,.T.);
#11039=ORIENTED_EDGE('',*,*,#8068,.F.);
#11040=ORIENTED_EDGE('',*,*,#8069,.T.);
#11041=ORIENTED_EDGE('',*,*,#8065,.T.);
#11042=ORIENTED_EDGE('',*,*,#8070,.T.);
#11043=ORIENTED_EDGE('',*,*,#8071,.F.);
#11044=ORIENTED_EDGE('',*,*,#8072,.T.);
#11045=ORIENTED_EDGE('',*,*,#8068,.T.);
#11046=ORIENTED_EDGE('',*,*,#8073,.T.);
#11047=ORIENTED_EDGE('',*,*,#8074,.F.);
#11048=ORIENTED_EDGE('',*,*,#8075,.T.);
#11049=ORIENTED_EDGE('',*,*,#8071,.T.);
#11050=ORIENTED_EDGE('',*,*,#8076,.T.);
#11051=ORIENTED_EDGE('',*,*,#8077,.F.);
#11052=ORIENTED_EDGE('',*,*,#8078,.T.);
#11053=ORIENTED_EDGE('',*,*,#8074,.T.);
#11054=ORIENTED_EDGE('',*,*,#8079,.T.);
#11055=ORIENTED_EDGE('',*,*,#8080,.F.);
#11056=ORIENTED_EDGE('',*,*,#8081,.T.);
#11057=ORIENTED_EDGE('',*,*,#8077,.T.);
#11058=ORIENTED_EDGE('',*,*,#8082,.T.);
#11059=ORIENTED_EDGE('',*,*,#8083,.F.);
#11060=ORIENTED_EDGE('',*,*,#8084,.T.);
#11061=ORIENTED_EDGE('',*,*,#8080,.T.);
#11062=ORIENTED_EDGE('',*,*,#8085,.T.);
#11063=ORIENTED_EDGE('',*,*,#8086,.F.);
#11064=ORIENTED_EDGE('',*,*,#8087,.T.);
#11065=ORIENTED_EDGE('',*,*,#8083,.T.);
#11066=ORIENTED_EDGE('',*,*,#8088,.T.);
#11067=ORIENTED_EDGE('',*,*,#8089,.F.);
#11068=ORIENTED_EDGE('',*,*,#8090,.T.);
#11069=ORIENTED_EDGE('',*,*,#8086,.T.);
#11070=ORIENTED_EDGE('',*,*,#8091,.T.);
#11071=ORIENTED_EDGE('',*,*,#8092,.F.);
#11072=ORIENTED_EDGE('',*,*,#8093,.T.);
#11073=ORIENTED_EDGE('',*,*,#8089,.T.);
#11074=ORIENTED_EDGE('',*,*,#8094,.T.);
#11075=ORIENTED_EDGE('',*,*,#8095,.F.);
#11076=ORIENTED_EDGE('',*,*,#8096,.T.);
#11077=ORIENTED_EDGE('',*,*,#8092,.T.);
#11078=ORIENTED_EDGE('',*,*,#8097,.T.);
#11079=ORIENTED_EDGE('',*,*,#8098,.F.);
#11080=ORIENTED_EDGE('',*,*,#8099,.T.);
#11081=ORIENTED_EDGE('',*,*,#8095,.T.);
#11082=ORIENTED_EDGE('',*,*,#8100,.T.);
#11083=ORIENTED_EDGE('',*,*,#8101,.F.);
#11084=ORIENTED_EDGE('',*,*,#8102,.T.);
#11085=ORIENTED_EDGE('',*,*,#8098,.T.);
#11086=ORIENTED_EDGE('',*,*,#8103,.T.);
#11087=ORIENTED_EDGE('',*,*,#8104,.F.);
#11088=ORIENTED_EDGE('',*,*,#8105,.T.);
#11089=ORIENTED_EDGE('',*,*,#8101,.T.);
#11090=ORIENTED_EDGE('',*,*,#8106,.T.);
#11091=ORIENTED_EDGE('',*,*,#8107,.F.);
#11092=ORIENTED_EDGE('',*,*,#8108,.T.);
#11093=ORIENTED_EDGE('',*,*,#8104,.T.);
#11094=ORIENTED_EDGE('',*,*,#8109,.T.);
#11095=ORIENTED_EDGE('',*,*,#8110,.F.);
#11096=ORIENTED_EDGE('',*,*,#8111,.T.);
#11097=ORIENTED_EDGE('',*,*,#8107,.T.);
#11098=ORIENTED_EDGE('',*,*,#8112,.T.);
#11099=ORIENTED_EDGE('',*,*,#8113,.F.);
#11100=ORIENTED_EDGE('',*,*,#8114,.T.);
#11101=ORIENTED_EDGE('',*,*,#8115,.F.);
#11102=ORIENTED_EDGE('',*,*,#8116,.F.);
#11103=ORIENTED_EDGE('',*,*,#8117,.T.);
#11104=ORIENTED_EDGE('',*,*,#8113,.T.);
#11105=ORIENTED_EDGE('',*,*,#8118,.F.);
#11106=ORIENTED_EDGE('',*,*,#8119,.F.);
#11107=ORIENTED_EDGE('',*,*,#8120,.F.);
#11108=ORIENTED_EDGE('',*,*,#8121,.T.);
#11109=ORIENTED_EDGE('',*,*,#8116,.T.);
#11110=ORIENTED_EDGE('',*,*,#8122,.F.);
#11111=ORIENTED_EDGE('',*,*,#8123,.F.);
#11112=ORIENTED_EDGE('',*,*,#8124,.T.);
#11113=ORIENTED_EDGE('',*,*,#8120,.T.);
#11114=ORIENTED_EDGE('',*,*,#8125,.F.);
#11115=ORIENTED_EDGE('',*,*,#8126,.F.);
#11116=ORIENTED_EDGE('',*,*,#8127,.T.);
#11117=ORIENTED_EDGE('',*,*,#8123,.T.);
#11118=ORIENTED_EDGE('',*,*,#8128,.F.);
#11119=ORIENTED_EDGE('',*,*,#8129,.F.);
#11120=ORIENTED_EDGE('',*,*,#8130,.T.);
#11121=ORIENTED_EDGE('',*,*,#8126,.T.);
#11122=ORIENTED_EDGE('',*,*,#8131,.F.);
#11123=ORIENTED_EDGE('',*,*,#8132,.F.);
#11124=ORIENTED_EDGE('',*,*,#8133,.T.);
#11125=ORIENTED_EDGE('',*,*,#8129,.T.);
#11126=ORIENTED_EDGE('',*,*,#8134,.F.);
#11127=ORIENTED_EDGE('',*,*,#8135,.F.);
#11128=ORIENTED_EDGE('',*,*,#8136,.T.);
#11129=ORIENTED_EDGE('',*,*,#8132,.T.);
#11130=ORIENTED_EDGE('',*,*,#8137,.F.);
#11131=ORIENTED_EDGE('',*,*,#8138,.F.);
#11132=ORIENTED_EDGE('',*,*,#8139,.T.);
#11133=ORIENTED_EDGE('',*,*,#8135,.T.);
#11134=ORIENTED_EDGE('',*,*,#8140,.F.);
#11135=ORIENTED_EDGE('',*,*,#8141,.F.);
#11136=ORIENTED_EDGE('',*,*,#8142,.T.);
#11137=ORIENTED_EDGE('',*,*,#8138,.T.);
#11138=ORIENTED_EDGE('',*,*,#8143,.F.);
#11139=ORIENTED_EDGE('',*,*,#8144,.F.);
#11140=ORIENTED_EDGE('',*,*,#8145,.T.);
#11141=ORIENTED_EDGE('',*,*,#8141,.T.);
#11142=ORIENTED_EDGE('',*,*,#8146,.F.);
#11143=ORIENTED_EDGE('',*,*,#8147,.F.);
#11144=ORIENTED_EDGE('',*,*,#8148,.T.);
#11145=ORIENTED_EDGE('',*,*,#8144,.T.);
#11146=ORIENTED_EDGE('',*,*,#8149,.F.);
#11147=ORIENTED_EDGE('',*,*,#8150,.F.);
#11148=ORIENTED_EDGE('',*,*,#8151,.T.);
#11149=ORIENTED_EDGE('',*,*,#8147,.T.);
#11150=ORIENTED_EDGE('',*,*,#8152,.F.);
#11151=ORIENTED_EDGE('',*,*,#8153,.F.);
#11152=ORIENTED_EDGE('',*,*,#8154,.T.);
#11153=ORIENTED_EDGE('',*,*,#8150,.T.);
#11154=ORIENTED_EDGE('',*,*,#8155,.F.);
#11155=ORIENTED_EDGE('',*,*,#8156,.F.);
#11156=ORIENTED_EDGE('',*,*,#8157,.T.);
#11157=ORIENTED_EDGE('',*,*,#8153,.T.);
#11158=ORIENTED_EDGE('',*,*,#8158,.F.);
#11159=ORIENTED_EDGE('',*,*,#8159,.F.);
#11160=ORIENTED_EDGE('',*,*,#8160,.T.);
#11161=ORIENTED_EDGE('',*,*,#8156,.T.);
#11162=ORIENTED_EDGE('',*,*,#8161,.F.);
#11163=ORIENTED_EDGE('',*,*,#8162,.F.);
#11164=ORIENTED_EDGE('',*,*,#8163,.T.);
#11165=ORIENTED_EDGE('',*,*,#8159,.T.);
#11166=ORIENTED_EDGE('',*,*,#8164,.F.);
#11167=ORIENTED_EDGE('',*,*,#8165,.F.);
#11168=ORIENTED_EDGE('',*,*,#8166,.T.);
#11169=ORIENTED_EDGE('',*,*,#8162,.T.);
#11170=ORIENTED_EDGE('',*,*,#8167,.F.);
#11171=ORIENTED_EDGE('',*,*,#8168,.F.);
#11172=ORIENTED_EDGE('',*,*,#8169,.T.);
#11173=ORIENTED_EDGE('',*,*,#8165,.T.);
#11174=ORIENTED_EDGE('',*,*,#8170,.F.);
#11175=ORIENTED_EDGE('',*,*,#8171,.F.);
#11176=ORIENTED_EDGE('',*,*,#8172,.T.);
#11177=ORIENTED_EDGE('',*,*,#8168,.T.);
#11178=ORIENTED_EDGE('',*,*,#8173,.F.);
#11179=ORIENTED_EDGE('',*,*,#8174,.F.);
#11180=ORIENTED_EDGE('',*,*,#8175,.T.);
#11181=ORIENTED_EDGE('',*,*,#8171,.T.);
#11182=ORIENTED_EDGE('',*,*,#8176,.F.);
#11183=ORIENTED_EDGE('',*,*,#8177,.F.);
#11184=ORIENTED_EDGE('',*,*,#8178,.T.);
#11185=ORIENTED_EDGE('',*,*,#8174,.T.);
#11186=ORIENTED_EDGE('',*,*,#8179,.F.);
#11187=ORIENTED_EDGE('',*,*,#8180,.F.);
#11188=ORIENTED_EDGE('',*,*,#8181,.T.);
#11189=ORIENTED_EDGE('',*,*,#8177,.T.);
#11190=ORIENTED_EDGE('',*,*,#8182,.F.);
#11191=ORIENTED_EDGE('',*,*,#8183,.F.);
#11192=ORIENTED_EDGE('',*,*,#8184,.T.);
#11193=ORIENTED_EDGE('',*,*,#8180,.T.);
#11194=ORIENTED_EDGE('',*,*,#8185,.F.);
#11195=ORIENTED_EDGE('',*,*,#8186,.F.);
#11196=ORIENTED_EDGE('',*,*,#8187,.T.);
#11197=ORIENTED_EDGE('',*,*,#8183,.T.);
#11198=ORIENTED_EDGE('',*,*,#8188,.F.);
#11199=ORIENTED_EDGE('',*,*,#8189,.F.);
#11200=ORIENTED_EDGE('',*,*,#8190,.T.);
#11201=ORIENTED_EDGE('',*,*,#8186,.T.);
#11202=ORIENTED_EDGE('',*,*,#8191,.F.);
#11203=ORIENTED_EDGE('',*,*,#8192,.F.);
#11204=ORIENTED_EDGE('',*,*,#8193,.T.);
#11205=ORIENTED_EDGE('',*,*,#8189,.T.);
#11206=ORIENTED_EDGE('',*,*,#8194,.F.);
#11207=ORIENTED_EDGE('',*,*,#8195,.F.);
#11208=ORIENTED_EDGE('',*,*,#8196,.T.);
#11209=ORIENTED_EDGE('',*,*,#8192,.T.);
#11210=ORIENTED_EDGE('',*,*,#8197,.F.);
#11211=ORIENTED_EDGE('',*,*,#8198,.F.);
#11212=ORIENTED_EDGE('',*,*,#8199,.T.);
#11213=ORIENTED_EDGE('',*,*,#8195,.T.);
#11214=ORIENTED_EDGE('',*,*,#8200,.F.);
#11215=ORIENTED_EDGE('',*,*,#8201,.F.);
#11216=ORIENTED_EDGE('',*,*,#8202,.T.);
#11217=ORIENTED_EDGE('',*,*,#8198,.T.);
#11218=ORIENTED_EDGE('',*,*,#8203,.F.);
#11219=ORIENTED_EDGE('',*,*,#8204,.F.);
#11220=ORIENTED_EDGE('',*,*,#8205,.T.);
#11221=ORIENTED_EDGE('',*,*,#8201,.T.);
#11222=ORIENTED_EDGE('',*,*,#8206,.F.);
#11223=ORIENTED_EDGE('',*,*,#8207,.F.);
#11224=ORIENTED_EDGE('',*,*,#8208,.T.);
#11225=ORIENTED_EDGE('',*,*,#8204,.T.);
#11226=ORIENTED_EDGE('',*,*,#8209,.F.);
#11227=ORIENTED_EDGE('',*,*,#8210,.F.);
#11228=ORIENTED_EDGE('',*,*,#8211,.T.);
#11229=ORIENTED_EDGE('',*,*,#8207,.T.);
#11230=ORIENTED_EDGE('',*,*,#8212,.F.);
#11231=ORIENTED_EDGE('',*,*,#8213,.F.);
#11232=ORIENTED_EDGE('',*,*,#8214,.T.);
#11233=ORIENTED_EDGE('',*,*,#8210,.T.);
#11234=ORIENTED_EDGE('',*,*,#8215,.F.);
#11235=ORIENTED_EDGE('',*,*,#8216,.F.);
#11236=ORIENTED_EDGE('',*,*,#8217,.T.);
#11237=ORIENTED_EDGE('',*,*,#8213,.T.);
#11238=ORIENTED_EDGE('',*,*,#8218,.F.);
#11239=ORIENTED_EDGE('',*,*,#8219,.F.);
#11240=ORIENTED_EDGE('',*,*,#8220,.T.);
#11241=ORIENTED_EDGE('',*,*,#8216,.T.);
#11242=ORIENTED_EDGE('',*,*,#8221,.F.);
#11243=ORIENTED_EDGE('',*,*,#8222,.F.);
#11244=ORIENTED_EDGE('',*,*,#8223,.T.);
#11245=ORIENTED_EDGE('',*,*,#8219,.T.);
#11246=ORIENTED_EDGE('',*,*,#8224,.F.);
#11247=ORIENTED_EDGE('',*,*,#8225,.F.);
#11248=ORIENTED_EDGE('',*,*,#8226,.T.);
#11249=ORIENTED_EDGE('',*,*,#8222,.T.);
#11250=ORIENTED_EDGE('',*,*,#8227,.F.);
#11251=ORIENTED_EDGE('',*,*,#8228,.F.);
#11252=ORIENTED_EDGE('',*,*,#8229,.T.);
#11253=ORIENTED_EDGE('',*,*,#8225,.T.);
#11254=ORIENTED_EDGE('',*,*,#8230,.F.);
#11255=ORIENTED_EDGE('',*,*,#8231,.F.);
#11256=ORIENTED_EDGE('',*,*,#8232,.T.);
#11257=ORIENTED_EDGE('',*,*,#8228,.T.);
#11258=ORIENTED_EDGE('',*,*,#8233,.F.);
#11259=ORIENTED_EDGE('',*,*,#8234,.F.);
#11260=ORIENTED_EDGE('',*,*,#8235,.T.);
#11261=ORIENTED_EDGE('',*,*,#8231,.T.);
#11262=ORIENTED_EDGE('',*,*,#8236,.F.);
#11263=ORIENTED_EDGE('',*,*,#8237,.F.);
#11264=ORIENTED_EDGE('',*,*,#8238,.T.);
#11265=ORIENTED_EDGE('',*,*,#8234,.T.);
#11266=ORIENTED_EDGE('',*,*,#8239,.F.);
#11267=ORIENTED_EDGE('',*,*,#8240,.F.);
#11268=ORIENTED_EDGE('',*,*,#8241,.T.);
#11269=ORIENTED_EDGE('',*,*,#8237,.T.);
#11270=ORIENTED_EDGE('',*,*,#8242,.F.);
#11271=ORIENTED_EDGE('',*,*,#8243,.F.);
#11272=ORIENTED_EDGE('',*,*,#8244,.T.);
#11273=ORIENTED_EDGE('',*,*,#8240,.T.);
#11274=ORIENTED_EDGE('',*,*,#8245,.F.);
#11275=ORIENTED_EDGE('',*,*,#8246,.F.);
#11276=ORIENTED_EDGE('',*,*,#8247,.T.);
#11277=ORIENTED_EDGE('',*,*,#8243,.T.);
#11278=ORIENTED_EDGE('',*,*,#8248,.F.);
#11279=ORIENTED_EDGE('',*,*,#8249,.F.);
#11280=ORIENTED_EDGE('',*,*,#8250,.T.);
#11281=ORIENTED_EDGE('',*,*,#8246,.T.);
#11282=ORIENTED_EDGE('',*,*,#8251,.F.);
#11283=ORIENTED_EDGE('',*,*,#8252,.F.);
#11284=ORIENTED_EDGE('',*,*,#8253,.T.);
#11285=ORIENTED_EDGE('',*,*,#8249,.T.);
#11286=ORIENTED_EDGE('',*,*,#8254,.F.);
#11287=ORIENTED_EDGE('',*,*,#8255,.F.);
#11288=ORIENTED_EDGE('',*,*,#8256,.T.);
#11289=ORIENTED_EDGE('',*,*,#8252,.T.);
#11290=ORIENTED_EDGE('',*,*,#8257,.F.);
#11291=ORIENTED_EDGE('',*,*,#8258,.F.);
#11292=ORIENTED_EDGE('',*,*,#8259,.T.);
#11293=ORIENTED_EDGE('',*,*,#8255,.T.);
#11294=ORIENTED_EDGE('',*,*,#8260,.F.);
#11295=ORIENTED_EDGE('',*,*,#8261,.F.);
#11296=ORIENTED_EDGE('',*,*,#8262,.T.);
#11297=ORIENTED_EDGE('',*,*,#8258,.T.);
#11298=ORIENTED_EDGE('',*,*,#8263,.F.);
#11299=ORIENTED_EDGE('',*,*,#8264,.F.);
#11300=ORIENTED_EDGE('',*,*,#8265,.T.);
#11301=ORIENTED_EDGE('',*,*,#8261,.T.);
#11302=ORIENTED_EDGE('',*,*,#8266,.F.);
#11303=ORIENTED_EDGE('',*,*,#8267,.F.);
#11304=ORIENTED_EDGE('',*,*,#8268,.T.);
#11305=ORIENTED_EDGE('',*,*,#8264,.T.);
#11306=ORIENTED_EDGE('',*,*,#8269,.F.);
#11307=ORIENTED_EDGE('',*,*,#8270,.F.);
#11308=ORIENTED_EDGE('',*,*,#8271,.T.);
#11309=ORIENTED_EDGE('',*,*,#8267,.T.);
#11310=ORIENTED_EDGE('',*,*,#8272,.F.);
#11311=ORIENTED_EDGE('',*,*,#8273,.F.);
#11312=ORIENTED_EDGE('',*,*,#8274,.T.);
#11313=ORIENTED_EDGE('',*,*,#8270,.T.);
#11314=ORIENTED_EDGE('',*,*,#8275,.F.);
#11315=ORIENTED_EDGE('',*,*,#8276,.F.);
#11316=ORIENTED_EDGE('',*,*,#8277,.T.);
#11317=ORIENTED_EDGE('',*,*,#8273,.T.);
#11318=ORIENTED_EDGE('',*,*,#8278,.F.);
#11319=ORIENTED_EDGE('',*,*,#8279,.F.);
#11320=ORIENTED_EDGE('',*,*,#8280,.T.);
#11321=ORIENTED_EDGE('',*,*,#8276,.T.);
#11322=ORIENTED_EDGE('',*,*,#8281,.F.);
#11323=ORIENTED_EDGE('',*,*,#8282,.F.);
#11324=ORIENTED_EDGE('',*,*,#8283,.T.);
#11325=ORIENTED_EDGE('',*,*,#8279,.T.);
#11326=ORIENTED_EDGE('',*,*,#8284,.F.);
#11327=ORIENTED_EDGE('',*,*,#8285,.F.);
#11328=ORIENTED_EDGE('',*,*,#8286,.T.);
#11329=ORIENTED_EDGE('',*,*,#8282,.T.);
#11330=ORIENTED_EDGE('',*,*,#8287,.F.);
#11331=ORIENTED_EDGE('',*,*,#8288,.F.);
#11332=ORIENTED_EDGE('',*,*,#8289,.T.);
#11333=ORIENTED_EDGE('',*,*,#8285,.T.);
#11334=ORIENTED_EDGE('',*,*,#8290,.F.);
#11335=ORIENTED_EDGE('',*,*,#8291,.F.);
#11336=ORIENTED_EDGE('',*,*,#8292,.T.);
#11337=ORIENTED_EDGE('',*,*,#8288,.T.);
#11338=ORIENTED_EDGE('',*,*,#8293,.F.);
#11339=ORIENTED_EDGE('',*,*,#8294,.F.);
#11340=ORIENTED_EDGE('',*,*,#8295,.T.);
#11341=ORIENTED_EDGE('',*,*,#8291,.T.);
#11342=ORIENTED_EDGE('',*,*,#8296,.F.);
#11343=ORIENTED_EDGE('',*,*,#8297,.F.);
#11344=ORIENTED_EDGE('',*,*,#8298,.T.);
#11345=ORIENTED_EDGE('',*,*,#8294,.T.);
#11346=ORIENTED_EDGE('',*,*,#8299,.F.);
#11347=ORIENTED_EDGE('',*,*,#8300,.F.);
#11348=ORIENTED_EDGE('',*,*,#8301,.T.);
#11349=ORIENTED_EDGE('',*,*,#8297,.T.);
#11350=ORIENTED_EDGE('',*,*,#8302,.F.);
#11351=ORIENTED_EDGE('',*,*,#8303,.T.);
#11352=ORIENTED_EDGE('',*,*,#8304,.T.);
#11353=ORIENTED_EDGE('',*,*,#7925,.F.);
#11354=ORIENTED_EDGE('',*,*,#8305,.T.);
#11355=ORIENTED_EDGE('',*,*,#8306,.T.);
#11356=ORIENTED_EDGE('',*,*,#8303,.F.);
#11357=ORIENTED_EDGE('',*,*,#8307,.T.);
#11358=ORIENTED_EDGE('',*,*,#8308,.T.);
#11359=ORIENTED_EDGE('',*,*,#8307,.F.);
#11360=ORIENTED_EDGE('',*,*,#8308,.F.);
#11361=ORIENTED_EDGE('',*,*,#8309,.F.);
#11362=ORIENTED_EDGE('',*,*,#8310,.F.);
#11363=ORIENTED_EDGE('',*,*,#8112,.F.);
#11364=ORIENTED_EDGE('',*,*,#8109,.F.);
#11365=ORIENTED_EDGE('',*,*,#8106,.F.);
#11366=ORIENTED_EDGE('',*,*,#8103,.F.);
#11367=ORIENTED_EDGE('',*,*,#8100,.F.);
#11368=ORIENTED_EDGE('',*,*,#8097,.F.);
#11369=ORIENTED_EDGE('',*,*,#8094,.F.);
#11370=ORIENTED_EDGE('',*,*,#8091,.F.);
#11371=ORIENTED_EDGE('',*,*,#8088,.F.);
#11372=ORIENTED_EDGE('',*,*,#8085,.F.);
#11373=ORIENTED_EDGE('',*,*,#8082,.F.);
#11374=ORIENTED_EDGE('',*,*,#8079,.F.);
#11375=ORIENTED_EDGE('',*,*,#8076,.F.);
#11376=ORIENTED_EDGE('',*,*,#8073,.F.);
#11377=ORIENTED_EDGE('',*,*,#8070,.F.);
#11378=ORIENTED_EDGE('',*,*,#8067,.F.);
#11379=ORIENTED_EDGE('',*,*,#8064,.F.);
#11380=ORIENTED_EDGE('',*,*,#8061,.F.);
#11381=ORIENTED_EDGE('',*,*,#8058,.F.);
#11382=ORIENTED_EDGE('',*,*,#8055,.F.);
#11383=ORIENTED_EDGE('',*,*,#8052,.F.);
#11384=ORIENTED_EDGE('',*,*,#8049,.F.);
#11385=ORIENTED_EDGE('',*,*,#8046,.F.);
#11386=ORIENTED_EDGE('',*,*,#8043,.F.);
#11387=ORIENTED_EDGE('',*,*,#8040,.F.);
#11388=ORIENTED_EDGE('',*,*,#8037,.F.);
#11389=ORIENTED_EDGE('',*,*,#8034,.F.);
#11390=ORIENTED_EDGE('',*,*,#8031,.F.);
#11391=ORIENTED_EDGE('',*,*,#8028,.F.);
#11392=ORIENTED_EDGE('',*,*,#8025,.F.);
#11393=ORIENTED_EDGE('',*,*,#8022,.F.);
#11394=ORIENTED_EDGE('',*,*,#8019,.F.);
#11395=ORIENTED_EDGE('',*,*,#8016,.F.);
#11396=ORIENTED_EDGE('',*,*,#8013,.F.);
#11397=ORIENTED_EDGE('',*,*,#8010,.F.);
#11398=ORIENTED_EDGE('',*,*,#8007,.F.);
#11399=ORIENTED_EDGE('',*,*,#8004,.F.);
#11400=ORIENTED_EDGE('',*,*,#8001,.F.);
#11401=ORIENTED_EDGE('',*,*,#7998,.F.);
#11402=ORIENTED_EDGE('',*,*,#7995,.F.);
#11403=ORIENTED_EDGE('',*,*,#7992,.F.);
#11404=ORIENTED_EDGE('',*,*,#7989,.F.);
#11405=ORIENTED_EDGE('',*,*,#7986,.F.);
#11406=ORIENTED_EDGE('',*,*,#7983,.F.);
#11407=ORIENTED_EDGE('',*,*,#7980,.F.);
#11408=ORIENTED_EDGE('',*,*,#7977,.F.);
#11409=ORIENTED_EDGE('',*,*,#7974,.F.);
#11410=ORIENTED_EDGE('',*,*,#7971,.F.);
#11411=ORIENTED_EDGE('',*,*,#7968,.F.);
#11412=ORIENTED_EDGE('',*,*,#7965,.F.);
#11413=ORIENTED_EDGE('',*,*,#7962,.F.);
#11414=ORIENTED_EDGE('',*,*,#7959,.F.);
#11415=ORIENTED_EDGE('',*,*,#7956,.F.);
#11416=ORIENTED_EDGE('',*,*,#7953,.F.);
#11417=ORIENTED_EDGE('',*,*,#7950,.F.);
#11418=ORIENTED_EDGE('',*,*,#7947,.F.);
#11419=ORIENTED_EDGE('',*,*,#7944,.F.);
#11420=ORIENTED_EDGE('',*,*,#7941,.F.);
#11421=ORIENTED_EDGE('',*,*,#7938,.F.);
#11422=ORIENTED_EDGE('',*,*,#7935,.F.);
#11423=ORIENTED_EDGE('',*,*,#7932,.F.);
#11424=ORIENTED_EDGE('',*,*,#7929,.F.);
#11425=ORIENTED_EDGE('',*,*,#7926,.F.);
#11426=ORIENTED_EDGE('',*,*,#8304,.F.);
#11427=ORIENTED_EDGE('',*,*,#8311,.T.);
#11428=ORIENTED_EDGE('',*,*,#8302,.T.);
#11429=ORIENTED_EDGE('',*,*,#8299,.T.);
#11430=ORIENTED_EDGE('',*,*,#8296,.T.);
#11431=ORIENTED_EDGE('',*,*,#8293,.T.);
#11432=ORIENTED_EDGE('',*,*,#8290,.T.);
#11433=ORIENTED_EDGE('',*,*,#8287,.T.);
#11434=ORIENTED_EDGE('',*,*,#8284,.T.);
#11435=ORIENTED_EDGE('',*,*,#8281,.T.);
#11436=ORIENTED_EDGE('',*,*,#8278,.T.);
#11437=ORIENTED_EDGE('',*,*,#8275,.T.);
#11438=ORIENTED_EDGE('',*,*,#8272,.T.);
#11439=ORIENTED_EDGE('',*,*,#8269,.T.);
#11440=ORIENTED_EDGE('',*,*,#8266,.T.);
#11441=ORIENTED_EDGE('',*,*,#8263,.T.);
#11442=ORIENTED_EDGE('',*,*,#8260,.T.);
#11443=ORIENTED_EDGE('',*,*,#8257,.T.);
#11444=ORIENTED_EDGE('',*,*,#8254,.T.);
#11445=ORIENTED_EDGE('',*,*,#8251,.T.);
#11446=ORIENTED_EDGE('',*,*,#8248,.T.);
#11447=ORIENTED_EDGE('',*,*,#8245,.T.);
#11448=ORIENTED_EDGE('',*,*,#8242,.T.);
#11449=ORIENTED_EDGE('',*,*,#8239,.T.);
#11450=ORIENTED_EDGE('',*,*,#8236,.T.);
#11451=ORIENTED_EDGE('',*,*,#8233,.T.);
#11452=ORIENTED_EDGE('',*,*,#8230,.T.);
#11453=ORIENTED_EDGE('',*,*,#8227,.T.);
#11454=ORIENTED_EDGE('',*,*,#8224,.T.);
#11455=ORIENTED_EDGE('',*,*,#8221,.T.);
#11456=ORIENTED_EDGE('',*,*,#8218,.T.);
#11457=ORIENTED_EDGE('',*,*,#8215,.T.);
#11458=ORIENTED_EDGE('',*,*,#8212,.T.);
#11459=ORIENTED_EDGE('',*,*,#8209,.T.);
#11460=ORIENTED_EDGE('',*,*,#8206,.T.);
#11461=ORIENTED_EDGE('',*,*,#8203,.T.);
#11462=ORIENTED_EDGE('',*,*,#8200,.T.);
#11463=ORIENTED_EDGE('',*,*,#8197,.T.);
#11464=ORIENTED_EDGE('',*,*,#8194,.T.);
#11465=ORIENTED_EDGE('',*,*,#8191,.T.);
#11466=ORIENTED_EDGE('',*,*,#8188,.T.);
#11467=ORIENTED_EDGE('',*,*,#8185,.T.);
#11468=ORIENTED_EDGE('',*,*,#8182,.T.);
#11469=ORIENTED_EDGE('',*,*,#8179,.T.);
#11470=ORIENTED_EDGE('',*,*,#8176,.T.);
#11471=ORIENTED_EDGE('',*,*,#8173,.T.);
#11472=ORIENTED_EDGE('',*,*,#8170,.T.);
#11473=ORIENTED_EDGE('',*,*,#8167,.T.);
#11474=ORIENTED_EDGE('',*,*,#8164,.T.);
#11475=ORIENTED_EDGE('',*,*,#8161,.T.);
#11476=ORIENTED_EDGE('',*,*,#8158,.T.);
#11477=ORIENTED_EDGE('',*,*,#8155,.T.);
#11478=ORIENTED_EDGE('',*,*,#8152,.T.);
#11479=ORIENTED_EDGE('',*,*,#8149,.T.);
#11480=ORIENTED_EDGE('',*,*,#8146,.T.);
#11481=ORIENTED_EDGE('',*,*,#8143,.T.);
#11482=ORIENTED_EDGE('',*,*,#8140,.T.);
#11483=ORIENTED_EDGE('',*,*,#8137,.T.);
#11484=ORIENTED_EDGE('',*,*,#8134,.T.);
#11485=ORIENTED_EDGE('',*,*,#8131,.T.);
#11486=ORIENTED_EDGE('',*,*,#8128,.T.);
#11487=ORIENTED_EDGE('',*,*,#8125,.T.);
#11488=ORIENTED_EDGE('',*,*,#8122,.T.);
#11489=ORIENTED_EDGE('',*,*,#8119,.T.);
#11490=ORIENTED_EDGE('',*,*,#8300,.T.);
#11491=ORIENTED_EDGE('',*,*,#8311,.F.);
#11492=ORIENTED_EDGE('',*,*,#8306,.F.);
#11493=ORIENTED_EDGE('',*,*,#8312,.T.);
#11494=ORIENTED_EDGE('',*,*,#8313,.F.);
#11495=ORIENTED_EDGE('',*,*,#8114,.F.);
#11496=ORIENTED_EDGE('',*,*,#8117,.F.);
#11497=ORIENTED_EDGE('',*,*,#8121,.F.);
#11498=ORIENTED_EDGE('',*,*,#8124,.F.);
#11499=ORIENTED_EDGE('',*,*,#8127,.F.);
#11500=ORIENTED_EDGE('',*,*,#8130,.F.);
#11501=ORIENTED_EDGE('',*,*,#8133,.F.);
#11502=ORIENTED_EDGE('',*,*,#8136,.F.);
#11503=ORIENTED_EDGE('',*,*,#8139,.F.);
#11504=ORIENTED_EDGE('',*,*,#8142,.F.);
#11505=ORIENTED_EDGE('',*,*,#8145,.F.);
#11506=ORIENTED_EDGE('',*,*,#8148,.F.);
#11507=ORIENTED_EDGE('',*,*,#8151,.F.);
#11508=ORIENTED_EDGE('',*,*,#8154,.F.);
#11509=ORIENTED_EDGE('',*,*,#8157,.F.);
#11510=ORIENTED_EDGE('',*,*,#8160,.F.);
#11511=ORIENTED_EDGE('',*,*,#8163,.F.);
#11512=ORIENTED_EDGE('',*,*,#8166,.F.);
#11513=ORIENTED_EDGE('',*,*,#8169,.F.);
#11514=ORIENTED_EDGE('',*,*,#8172,.F.);
#11515=ORIENTED_EDGE('',*,*,#8175,.F.);
#11516=ORIENTED_EDGE('',*,*,#8178,.F.);
#11517=ORIENTED_EDGE('',*,*,#8181,.F.);
#11518=ORIENTED_EDGE('',*,*,#8184,.F.);
#11519=ORIENTED_EDGE('',*,*,#8187,.F.);
#11520=ORIENTED_EDGE('',*,*,#8190,.F.);
#11521=ORIENTED_EDGE('',*,*,#8193,.F.);
#11522=ORIENTED_EDGE('',*,*,#8196,.F.);
#11523=ORIENTED_EDGE('',*,*,#8199,.F.);
#11524=ORIENTED_EDGE('',*,*,#8202,.F.);
#11525=ORIENTED_EDGE('',*,*,#8205,.F.);
#11526=ORIENTED_EDGE('',*,*,#8208,.F.);
#11527=ORIENTED_EDGE('',*,*,#8211,.F.);
#11528=ORIENTED_EDGE('',*,*,#8214,.F.);
#11529=ORIENTED_EDGE('',*,*,#8217,.F.);
#11530=ORIENTED_EDGE('',*,*,#8220,.F.);
#11531=ORIENTED_EDGE('',*,*,#8223,.F.);
#11532=ORIENTED_EDGE('',*,*,#8226,.F.);
#11533=ORIENTED_EDGE('',*,*,#8229,.F.);
#11534=ORIENTED_EDGE('',*,*,#8232,.F.);
#11535=ORIENTED_EDGE('',*,*,#8235,.F.);
#11536=ORIENTED_EDGE('',*,*,#8238,.F.);
#11537=ORIENTED_EDGE('',*,*,#8241,.F.);
#11538=ORIENTED_EDGE('',*,*,#8244,.F.);
#11539=ORIENTED_EDGE('',*,*,#8247,.F.);
#11540=ORIENTED_EDGE('',*,*,#8250,.F.);
#11541=ORIENTED_EDGE('',*,*,#8253,.F.);
#11542=ORIENTED_EDGE('',*,*,#8256,.F.);
#11543=ORIENTED_EDGE('',*,*,#8259,.F.);
#11544=ORIENTED_EDGE('',*,*,#8262,.F.);
#11545=ORIENTED_EDGE('',*,*,#8265,.F.);
#11546=ORIENTED_EDGE('',*,*,#8268,.F.);
#11547=ORIENTED_EDGE('',*,*,#8271,.F.);
#11548=ORIENTED_EDGE('',*,*,#8274,.F.);
#11549=ORIENTED_EDGE('',*,*,#8277,.F.);
#11550=ORIENTED_EDGE('',*,*,#8280,.F.);
#11551=ORIENTED_EDGE('',*,*,#8283,.F.);
#11552=ORIENTED_EDGE('',*,*,#8286,.F.);
#11553=ORIENTED_EDGE('',*,*,#8289,.F.);
#11554=ORIENTED_EDGE('',*,*,#8292,.F.);
#11555=ORIENTED_EDGE('',*,*,#8295,.F.);
#11556=ORIENTED_EDGE('',*,*,#8298,.F.);
#11557=ORIENTED_EDGE('',*,*,#8301,.F.);
#11558=ORIENTED_EDGE('',*,*,#8312,.F.);
#11559=ORIENTED_EDGE('',*,*,#8305,.F.);
#11560=ORIENTED_EDGE('',*,*,#7924,.F.);
#11561=ORIENTED_EDGE('',*,*,#7928,.F.);
#11562=ORIENTED_EDGE('',*,*,#7931,.F.);
#11563=ORIENTED_EDGE('',*,*,#7934,.F.);
#11564=ORIENTED_EDGE('',*,*,#7937,.F.);
#11565=ORIENTED_EDGE('',*,*,#7940,.F.);
#11566=ORIENTED_EDGE('',*,*,#7943,.F.);
#11567=ORIENTED_EDGE('',*,*,#7946,.F.);
#11568=ORIENTED_EDGE('',*,*,#7949,.F.);
#11569=ORIENTED_EDGE('',*,*,#7952,.F.);
#11570=ORIENTED_EDGE('',*,*,#7955,.F.);
#11571=ORIENTED_EDGE('',*,*,#7958,.F.);
#11572=ORIENTED_EDGE('',*,*,#7961,.F.);
#11573=ORIENTED_EDGE('',*,*,#7964,.F.);
#11574=ORIENTED_EDGE('',*,*,#7967,.F.);
#11575=ORIENTED_EDGE('',*,*,#7970,.F.);
#11576=ORIENTED_EDGE('',*,*,#7973,.F.);
#11577=ORIENTED_EDGE('',*,*,#7976,.F.);
#11578=ORIENTED_EDGE('',*,*,#7979,.F.);
#11579=ORIENTED_EDGE('',*,*,#7982,.F.);
#11580=ORIENTED_EDGE('',*,*,#7985,.F.);
#11581=ORIENTED_EDGE('',*,*,#7988,.F.);
#11582=ORIENTED_EDGE('',*,*,#7991,.F.);
#11583=ORIENTED_EDGE('',*,*,#7994,.F.);
#11584=ORIENTED_EDGE('',*,*,#7997,.F.);
#11585=ORIENTED_EDGE('',*,*,#8000,.F.);
#11586=ORIENTED_EDGE('',*,*,#8003,.F.);
#11587=ORIENTED_EDGE('',*,*,#8006,.F.);
#11588=ORIENTED_EDGE('',*,*,#8009,.F.);
#11589=ORIENTED_EDGE('',*,*,#8012,.F.);
#11590=ORIENTED_EDGE('',*,*,#8015,.F.);
#11591=ORIENTED_EDGE('',*,*,#8018,.F.);
#11592=ORIENTED_EDGE('',*,*,#8021,.F.);
#11593=ORIENTED_EDGE('',*,*,#8024,.F.);
#11594=ORIENTED_EDGE('',*,*,#8027,.F.);
#11595=ORIENTED_EDGE('',*,*,#8030,.F.);
#11596=ORIENTED_EDGE('',*,*,#8033,.F.);
#11597=ORIENTED_EDGE('',*,*,#8036,.F.);
#11598=ORIENTED_EDGE('',*,*,#8039,.F.);
#11599=ORIENTED_EDGE('',*,*,#8042,.F.);
#11600=ORIENTED_EDGE('',*,*,#8045,.F.);
#11601=ORIENTED_EDGE('',*,*,#8048,.F.);
#11602=ORIENTED_EDGE('',*,*,#8051,.F.);
#11603=ORIENTED_EDGE('',*,*,#8054,.F.);
#11604=ORIENTED_EDGE('',*,*,#8057,.F.);
#11605=ORIENTED_EDGE('',*,*,#8060,.F.);
#11606=ORIENTED_EDGE('',*,*,#8063,.F.);
#11607=ORIENTED_EDGE('',*,*,#8066,.F.);
#11608=ORIENTED_EDGE('',*,*,#8069,.F.);
#11609=ORIENTED_EDGE('',*,*,#8072,.F.);
#11610=ORIENTED_EDGE('',*,*,#8075,.F.);
#11611=ORIENTED_EDGE('',*,*,#8078,.F.);
#11612=ORIENTED_EDGE('',*,*,#8081,.F.);
#11613=ORIENTED_EDGE('',*,*,#8084,.F.);
#11614=ORIENTED_EDGE('',*,*,#8087,.F.);
#11615=ORIENTED_EDGE('',*,*,#8090,.F.);
#11616=ORIENTED_EDGE('',*,*,#8093,.F.);
#11617=ORIENTED_EDGE('',*,*,#8096,.F.);
#11618=ORIENTED_EDGE('',*,*,#8099,.F.);
#11619=ORIENTED_EDGE('',*,*,#8102,.F.);
#11620=ORIENTED_EDGE('',*,*,#8105,.F.);
#11621=ORIENTED_EDGE('',*,*,#8108,.F.);
#11622=ORIENTED_EDGE('',*,*,#8111,.F.);
#11623=ORIENTED_EDGE('',*,*,#8314,.F.);
#11624=ORIENTED_EDGE('',*,*,#8315,.F.);
#11625=ORIENTED_EDGE('',*,*,#8316,.T.);
#11626=ORIENTED_EDGE('',*,*,#8317,.F.);
#11627=ORIENTED_EDGE('',*,*,#8318,.F.);
#11628=ORIENTED_EDGE('',*,*,#8319,.F.);
#11629=ORIENTED_EDGE('',*,*,#8318,.T.);
#11630=ORIENTED_EDGE('',*,*,#8320,.T.);
#11631=ORIENTED_EDGE('',*,*,#8321,.T.);
#11632=ORIENTED_EDGE('',*,*,#8320,.F.);
#11633=ORIENTED_EDGE('',*,*,#8317,.T.);
#11634=ORIENTED_EDGE('',*,*,#8322,.T.);
#11635=ORIENTED_EDGE('',*,*,#8323,.F.);
#11636=ORIENTED_EDGE('',*,*,#8324,.F.);
#11637=ORIENTED_EDGE('',*,*,#8321,.F.);
#11638=ORIENTED_EDGE('',*,*,#8323,.T.);
#11639=ORIENTED_EDGE('',*,*,#8325,.T.);
#11640=ORIENTED_EDGE('',*,*,#8326,.F.);
#11641=ORIENTED_EDGE('',*,*,#8325,.F.);
#11642=ORIENTED_EDGE('',*,*,#8322,.F.);
#11643=ORIENTED_EDGE('',*,*,#8316,.F.);
#11644=ORIENTED_EDGE('',*,*,#8327,.F.);
#11645=ORIENTED_EDGE('',*,*,#8328,.T.);
#11646=ORIENTED_EDGE('',*,*,#8329,.F.);
#11647=ORIENTED_EDGE('',*,*,#8328,.F.);
#11648=ORIENTED_EDGE('',*,*,#8324,.T.);
#11649=ORIENTED_EDGE('',*,*,#8326,.T.);
#11650=ORIENTED_EDGE('',*,*,#8315,.T.);
#11651=ORIENTED_EDGE('',*,*,#8319,.T.);
#11652=ORIENTED_EDGE('',*,*,#8327,.T.);
#11653=ORIENTED_EDGE('',*,*,#8330,.F.);
#11654=ORIENTED_EDGE('',*,*,#8331,.T.);
#11655=ORIENTED_EDGE('',*,*,#8309,.T.);
#11656=ORIENTED_EDGE('',*,*,#8118,.T.);
#11657=ORIENTED_EDGE('',*,*,#8115,.T.);
#11658=ORIENTED_EDGE('',*,*,#8313,.T.);
#11659=ORIENTED_EDGE('',*,*,#8332,.F.);
#11660=ORIENTED_EDGE('',*,*,#8333,.T.);
#11661=ORIENTED_EDGE('',*,*,#8330,.T.);
#11662=ORIENTED_EDGE('',*,*,#8333,.F.);
#11663=ORIENTED_EDGE('',*,*,#8332,.T.);
#11664=ORIENTED_EDGE('',*,*,#8329,.T.);
#11665=ORIENTED_EDGE('',*,*,#8110,.T.);
#11666=ORIENTED_EDGE('',*,*,#8310,.T.);
#11667=ORIENTED_EDGE('',*,*,#8331,.F.);
#11668=ORIENTED_EDGE('',*,*,#8314,.T.);
#12137=CYLINDRICAL_SURFACE('',#14547,0.5941);
#12138=CYLINDRICAL_SURFACE('',#14549,0.5941);
#12139=CYLINDRICAL_SURFACE('',#14550,0.5941);
#12140=CYLINDRICAL_SURFACE('',#14551,0.5941);
#12141=CYLINDRICAL_SURFACE('',#14552,0.5941);
#12142=CYLINDRICAL_SURFACE('',#14553,0.5941);
#12143=CYLINDRICAL_SURFACE('',#14554,0.5941);
#12144=CYLINDRICAL_SURFACE('',#14555,0.5941);
#12145=CYLINDRICAL_SURFACE('',#14556,0.5941);
#12146=CYLINDRICAL_SURFACE('',#14557,0.5941);
#12147=CYLINDRICAL_SURFACE('',#14558,0.5941);
#12148=CYLINDRICAL_SURFACE('',#14559,0.5941);
#12149=CYLINDRICAL_SURFACE('',#14560,0.5941);
#12150=CYLINDRICAL_SURFACE('',#14561,0.5941);
#12151=CYLINDRICAL_SURFACE('',#14562,0.5941);
#12152=CYLINDRICAL_SURFACE('',#14563,0.5941);
#12153=CYLINDRICAL_SURFACE('',#14564,0.5941);
#12154=CYLINDRICAL_SURFACE('',#14565,0.5941);
#12155=CYLINDRICAL_SURFACE('',#14566,0.5941);
#12156=CYLINDRICAL_SURFACE('',#14567,0.5941);
#12157=CYLINDRICAL_SURFACE('',#14568,0.5941);
#12158=CYLINDRICAL_SURFACE('',#14569,0.5941);
#12159=CYLINDRICAL_SURFACE('',#14570,0.5941);
#12160=CYLINDRICAL_SURFACE('',#14571,0.5941);
#12161=CYLINDRICAL_SURFACE('',#14572,0.5941);
#12162=CYLINDRICAL_SURFACE('',#14573,0.5941);
#12163=CYLINDRICAL_SURFACE('',#14574,0.5941);
#12164=CYLINDRICAL_SURFACE('',#14575,0.5941);
#12165=CYLINDRICAL_SURFACE('',#14576,0.5941);
#12166=CYLINDRICAL_SURFACE('',#14577,0.5941);
#12167=CYLINDRICAL_SURFACE('',#14578,0.5941);
#12168=CYLINDRICAL_SURFACE('',#14579,0.5941);
#12169=CYLINDRICAL_SURFACE('',#14580,0.5941);
#12170=CYLINDRICAL_SURFACE('',#14581,0.5941);
#12171=CYLINDRICAL_SURFACE('',#14582,0.5941);
#12172=CYLINDRICAL_SURFACE('',#14583,0.5941);
#12173=CYLINDRICAL_SURFACE('',#14584,0.5941);
#12174=CYLINDRICAL_SURFACE('',#14585,0.5941);
#12175=CYLINDRICAL_SURFACE('',#14586,0.5941);
#12176=CYLINDRICAL_SURFACE('',#14587,0.5941);
#12177=CYLINDRICAL_SURFACE('',#14588,0.5941);
#12178=CYLINDRICAL_SURFACE('',#14589,0.5941);
#12179=CYLINDRICAL_SURFACE('',#14590,0.5941);
#12180=CYLINDRICAL_SURFACE('',#14591,0.5941);
#12181=CYLINDRICAL_SURFACE('',#14592,0.5941);
#12182=CYLINDRICAL_SURFACE('',#14593,0.5941);
#12183=CYLINDRICAL_SURFACE('',#14594,0.5941);
#12184=CYLINDRICAL_SURFACE('',#14595,0.5941);
#12185=CYLINDRICAL_SURFACE('',#14596,0.5941);
#12186=CYLINDRICAL_SURFACE('',#14597,0.5941);
#12187=CYLINDRICAL_SURFACE('',#14598,0.5941);
#12188=CYLINDRICAL_SURFACE('',#14599,0.5941);
#12189=CYLINDRICAL_SURFACE('',#14600,0.5941);
#12190=CYLINDRICAL_SURFACE('',#14601,0.5941);
#12191=CYLINDRICAL_SURFACE('',#14602,0.5941);
#12192=CYLINDRICAL_SURFACE('',#14603,0.5941);
#12193=CYLINDRICAL_SURFACE('',#14604,0.5941);
#12194=CYLINDRICAL_SURFACE('',#14605,0.5941);
#12195=CYLINDRICAL_SURFACE('',#14606,0.5941);
#12196=CYLINDRICAL_SURFACE('',#14607,0.5941);
#12197=CYLINDRICAL_SURFACE('',#14608,0.5941);
#12198=CYLINDRICAL_SURFACE('',#14609,0.5941);
#12199=CYLINDRICAL_SURFACE('',#14610,0.5941);
#12200=CYLINDRICAL_SURFACE('',#14611,0.415875);
#12201=CYLINDRICAL_SURFACE('',#14613,0.415875);
#12202=CYLINDRICAL_SURFACE('',#14615,0.415875);
#12203=CYLINDRICAL_SURFACE('',#14616,0.415875);
#12204=CYLINDRICAL_SURFACE('',#14617,0.415875);
#12205=CYLINDRICAL_SURFACE('',#14618,0.415875);
#12206=CYLINDRICAL_SURFACE('',#14619,0.415875);
#12207=CYLINDRICAL_SURFACE('',#14620,0.415875);
#12208=CYLINDRICAL_SURFACE('',#14621,0.415875);
#12209=CYLINDRICAL_SURFACE('',#14622,0.415875);
#12210=CYLINDRICAL_SURFACE('',#14623,0.415875);
#12211=CYLINDRICAL_SURFACE('',#14624,0.415875);
#12212=CYLINDRICAL_SURFACE('',#14625,0.415875);
#12213=CYLINDRICAL_SURFACE('',#14626,0.415875);
#12214=CYLINDRICAL_SURFACE('',#14627,0.415875);
#12215=CYLINDRICAL_SURFACE('',#14628,0.415875);
#12216=CYLINDRICAL_SURFACE('',#14629,0.415875);
#12217=CYLINDRICAL_SURFACE('',#14630,0.415875);
#12218=CYLINDRICAL_SURFACE('',#14631,0.415875);
#12219=CYLINDRICAL_SURFACE('',#14632,0.415875);
#12220=CYLINDRICAL_SURFACE('',#14633,0.415875);
#12221=CYLINDRICAL_SURFACE('',#14634,0.415875);
#12222=CYLINDRICAL_SURFACE('',#14635,0.415875);
#12223=CYLINDRICAL_SURFACE('',#14636,0.415875);
#12224=CYLINDRICAL_SURFACE('',#14637,0.415875);
#12225=CYLINDRICAL_SURFACE('',#14638,0.415875);
#12226=CYLINDRICAL_SURFACE('',#14639,0.415875);
#12227=CYLINDRICAL_SURFACE('',#14640,0.415875);
#12228=CYLINDRICAL_SURFACE('',#14641,0.415875);
#12229=CYLINDRICAL_SURFACE('',#14642,0.415875);
#12230=CYLINDRICAL_SURFACE('',#14643,0.415875);
#12231=CYLINDRICAL_SURFACE('',#14644,0.415875);
#12232=CYLINDRICAL_SURFACE('',#14645,0.415875);
#12233=CYLINDRICAL_SURFACE('',#14646,0.415875);
#12234=CYLINDRICAL_SURFACE('',#14647,0.415875);
#12235=CYLINDRICAL_SURFACE('',#14648,0.415875);
#12236=CYLINDRICAL_SURFACE('',#14649,0.415875);
#12237=CYLINDRICAL_SURFACE('',#14650,0.415875);
#12238=CYLINDRICAL_SURFACE('',#14651,0.415875);
#12239=CYLINDRICAL_SURFACE('',#14652,0.415875);
#12240=CYLINDRICAL_SURFACE('',#14653,0.415875);
#12241=CYLINDRICAL_SURFACE('',#14654,0.415875);
#12242=CYLINDRICAL_SURFACE('',#14655,0.415875);
#12243=CYLINDRICAL_SURFACE('',#14656,0.415875);
#12244=CYLINDRICAL_SURFACE('',#14657,0.415875);
#12245=CYLINDRICAL_SURFACE('',#14658,0.415875);
#12246=CYLINDRICAL_SURFACE('',#14659,0.415875);
#12247=CYLINDRICAL_SURFACE('',#14660,0.415875);
#12248=CYLINDRICAL_SURFACE('',#14661,0.415875);
#12249=CYLINDRICAL_SURFACE('',#14662,0.415875);
#12250=CYLINDRICAL_SURFACE('',#14663,0.415875);
#12251=CYLINDRICAL_SURFACE('',#14664,0.415875);
#12252=CYLINDRICAL_SURFACE('',#14665,0.415875);
#12253=CYLINDRICAL_SURFACE('',#14666,0.415875);
#12254=CYLINDRICAL_SURFACE('',#14667,0.415875);
#12255=CYLINDRICAL_SURFACE('',#14668,0.415875);
#12256=CYLINDRICAL_SURFACE('',#14669,0.415875);
#12257=CYLINDRICAL_SURFACE('',#14670,0.415875);
#12258=CYLINDRICAL_SURFACE('',#14671,0.415875);
#12259=CYLINDRICAL_SURFACE('',#14672,0.415875);
#12260=CYLINDRICAL_SURFACE('',#14673,0.415875);
#12261=CYLINDRICAL_SURFACE('',#14674,0.415875);
#12262=CYLINDRICAL_SURFACE('',#14675,0.415875);
#12263=CYLINDRICAL_SURFACE('',#14679,0.6);
#12264=CYLINDRICAL_SURFACE('',#14682,0.415875);
#12265=CYLINDRICAL_SURFACE('',#14690,1.);
#12266=CYLINDRICAL_SURFACE('',#14697,1.35);
#12267=CYLINDRICAL_SURFACE('',#14700,0.5941);
#12792=ADVANCED_FACE('',(#2080),#12137,.T.);
#12793=ADVANCED_FACE('',(#2081),#12138,.T.);
#12794=ADVANCED_FACE('',(#2082),#12139,.T.);
#12795=ADVANCED_FACE('',(#2083),#12140,.T.);
#12796=ADVANCED_FACE('',(#2084),#12141,.T.);
#12797=ADVANCED_FACE('',(#2085),#12142,.T.);
#12798=ADVANCED_FACE('',(#2086),#12143,.T.);
#12799=ADVANCED_FACE('',(#2087),#12144,.T.);
#12800=ADVANCED_FACE('',(#2088),#12145,.T.);
#12801=ADVANCED_FACE('',(#2089),#12146,.T.);
#12802=ADVANCED_FACE('',(#2090),#12147,.T.);
#12803=ADVANCED_FACE('',(#2091),#12148,.T.);
#12804=ADVANCED_FACE('',(#2092),#12149,.T.);
#12805=ADVANCED_FACE('',(#2093),#12150,.T.);
#12806=ADVANCED_FACE('',(#2094),#12151,.T.);
#12807=ADVANCED_FACE('',(#2095),#12152,.T.);
#12808=ADVANCED_FACE('',(#2096),#12153,.T.);
#12809=ADVANCED_FACE('',(#2097),#12154,.T.);
#12810=ADVANCED_FACE('',(#2098),#12155,.T.);
#12811=ADVANCED_FACE('',(#2099),#12156,.T.);
#12812=ADVANCED_FACE('',(#2100),#12157,.T.);
#12813=ADVANCED_FACE('',(#2101),#12158,.T.);
#12814=ADVANCED_FACE('',(#2102),#12159,.T.);
#12815=ADVANCED_FACE('',(#2103),#12160,.T.);
#12816=ADVANCED_FACE('',(#2104),#12161,.T.);
#12817=ADVANCED_FACE('',(#2105),#12162,.T.);
#12818=ADVANCED_FACE('',(#2106),#12163,.T.);
#12819=ADVANCED_FACE('',(#2107),#12164,.T.);
#12820=ADVANCED_FACE('',(#2108),#12165,.T.);
#12821=ADVANCED_FACE('',(#2109),#12166,.T.);
#12822=ADVANCED_FACE('',(#2110),#12167,.T.);
#12823=ADVANCED_FACE('',(#2111),#12168,.T.);
#12824=ADVANCED_FACE('',(#2112),#12169,.T.);
#12825=ADVANCED_FACE('',(#2113),#12170,.T.);
#12826=ADVANCED_FACE('',(#2114),#12171,.T.);
#12827=ADVANCED_FACE('',(#2115),#12172,.T.);
#12828=ADVANCED_FACE('',(#2116),#12173,.T.);
#12829=ADVANCED_FACE('',(#2117),#12174,.T.);
#12830=ADVANCED_FACE('',(#2118),#12175,.T.);
#12831=ADVANCED_FACE('',(#2119),#12176,.T.);
#12832=ADVANCED_FACE('',(#2120),#12177,.T.);
#12833=ADVANCED_FACE('',(#2121),#12178,.T.);
#12834=ADVANCED_FACE('',(#2122),#12179,.T.);
#12835=ADVANCED_FACE('',(#2123),#12180,.T.);
#12836=ADVANCED_FACE('',(#2124),#12181,.T.);
#12837=ADVANCED_FACE('',(#2125),#12182,.T.);
#12838=ADVANCED_FACE('',(#2126),#12183,.T.);
#12839=ADVANCED_FACE('',(#2127),#12184,.T.);
#12840=ADVANCED_FACE('',(#2128),#12185,.T.);
#12841=ADVANCED_FACE('',(#2129),#12186,.T.);
#12842=ADVANCED_FACE('',(#2130),#12187,.T.);
#12843=ADVANCED_FACE('',(#2131),#12188,.T.);
#12844=ADVANCED_FACE('',(#2132),#12189,.T.);
#12845=ADVANCED_FACE('',(#2133),#12190,.T.);
#12846=ADVANCED_FACE('',(#2134),#12191,.T.);
#12847=ADVANCED_FACE('',(#2135),#12192,.T.);
#12848=ADVANCED_FACE('',(#2136),#12193,.T.);
#12849=ADVANCED_FACE('',(#2137),#12194,.T.);
#12850=ADVANCED_FACE('',(#2138),#12195,.T.);
#12851=ADVANCED_FACE('',(#2139),#12196,.T.);
#12852=ADVANCED_FACE('',(#2140),#12197,.T.);
#12853=ADVANCED_FACE('',(#2141),#12198,.T.);
#12854=ADVANCED_FACE('',(#2142),#12199,.T.);
#12855=ADVANCED_FACE('',(#2143),#12200,.T.);
#12856=ADVANCED_FACE('',(#2144),#12201,.T.);
#12857=ADVANCED_FACE('',(#2145),#12202,.T.);
#12858=ADVANCED_FACE('',(#2146),#12203,.T.);
#12859=ADVANCED_FACE('',(#2147),#12204,.T.);
#12860=ADVANCED_FACE('',(#2148),#12205,.T.);
#12861=ADVANCED_FACE('',(#2149),#12206,.T.);
#12862=ADVANCED_FACE('',(#2150),#12207,.T.);
#12863=ADVANCED_FACE('',(#2151),#12208,.T.);
#12864=ADVANCED_FACE('',(#2152),#12209,.T.);
#12865=ADVANCED_FACE('',(#2153),#12210,.T.);
#12866=ADVANCED_FACE('',(#2154),#12211,.T.);
#12867=ADVANCED_FACE('',(#2155),#12212,.T.);
#12868=ADVANCED_FACE('',(#2156),#12213,.T.);
#12869=ADVANCED_FACE('',(#2157),#12214,.T.);
#12870=ADVANCED_FACE('',(#2158),#12215,.T.);
#12871=ADVANCED_FACE('',(#2159),#12216,.T.);
#12872=ADVANCED_FACE('',(#2160),#12217,.T.);
#12873=ADVANCED_FACE('',(#2161),#12218,.T.);
#12874=ADVANCED_FACE('',(#2162),#12219,.T.);
#12875=ADVANCED_FACE('',(#2163),#12220,.T.);
#12876=ADVANCED_FACE('',(#2164),#12221,.T.);
#12877=ADVANCED_FACE('',(#2165),#12222,.T.);
#12878=ADVANCED_FACE('',(#2166),#12223,.T.);
#12879=ADVANCED_FACE('',(#2167),#12224,.T.);
#12880=ADVANCED_FACE('',(#2168),#12225,.T.);
#12881=ADVANCED_FACE('',(#2169),#12226,.T.);
#12882=ADVANCED_FACE('',(#2170),#12227,.T.);
#12883=ADVANCED_FACE('',(#2171),#12228,.T.);
#12884=ADVANCED_FACE('',(#2172),#12229,.T.);
#12885=ADVANCED_FACE('',(#2173),#12230,.T.);
#12886=ADVANCED_FACE('',(#2174),#12231,.T.);
#12887=ADVANCED_FACE('',(#2175),#12232,.T.);
#12888=ADVANCED_FACE('',(#2176),#12233,.T.);
#12889=ADVANCED_FACE('',(#2177),#12234,.T.);
#12890=ADVANCED_FACE('',(#2178),#12235,.T.);
#12891=ADVANCED_FACE('',(#2179),#12236,.T.);
#12892=ADVANCED_FACE('',(#2180),#12237,.T.);
#12893=ADVANCED_FACE('',(#2181),#12238,.T.);
#12894=ADVANCED_FACE('',(#2182),#12239,.T.);
#12895=ADVANCED_FACE('',(#2183),#12240,.T.);
#12896=ADVANCED_FACE('',(#2184),#12241,.T.);
#12897=ADVANCED_FACE('',(#2185),#12242,.T.);
#12898=ADVANCED_FACE('',(#2186),#12243,.T.);
#12899=ADVANCED_FACE('',(#2187),#12244,.T.);
#12900=ADVANCED_FACE('',(#2188),#12245,.T.);
#12901=ADVANCED_FACE('',(#2189),#12246,.T.);
#12902=ADVANCED_FACE('',(#2190),#12247,.T.);
#12903=ADVANCED_FACE('',(#2191),#12248,.T.);
#12904=ADVANCED_FACE('',(#2192),#12249,.T.);
#12905=ADVANCED_FACE('',(#2193),#12250,.T.);
#12906=ADVANCED_FACE('',(#2194),#12251,.T.);
#12907=ADVANCED_FACE('',(#2195),#12252,.T.);
#12908=ADVANCED_FACE('',(#2196),#12253,.T.);
#12909=ADVANCED_FACE('',(#2197),#12254,.T.);
#12910=ADVANCED_FACE('',(#2198),#12255,.T.);
#12911=ADVANCED_FACE('',(#2199),#12256,.T.);
#12912=ADVANCED_FACE('',(#2200),#12257,.T.);
#12913=ADVANCED_FACE('',(#2201),#12258,.T.);
#12914=ADVANCED_FACE('',(#2202),#12259,.T.);
#12915=ADVANCED_FACE('',(#2203),#12260,.T.);
#12916=ADVANCED_FACE('',(#2204),#12261,.T.);
#12917=ADVANCED_FACE('',(#2205),#12262,.T.);
#12918=ADVANCED_FACE('',(#2206,#1204),#1515,.T.);
#12919=ADVANCED_FACE('',(#2207),#12263,.T.);
#12920=ADVANCED_FACE('',(#2208),#1516,.F.);
#12921=ADVANCED_FACE('',(#2209),#13,.F.);
#12922=ADVANCED_FACE('',(#2210),#12264,.T.);
#12923=ADVANCED_FACE('',(#2211),#14,.F.);
#12924=ADVANCED_FACE('',(#2212),#1517,.F.);
#12925=ADVANCED_FACE('',(#2213),#1518,.T.);
#12926=ADVANCED_FACE('',(#2214),#1519,.F.);
#12927=ADVANCED_FACE('',(#2215),#1520,.F.);
#12928=ADVANCED_FACE('',(#2216),#1521,.F.);
#12929=ADVANCED_FACE('',(#2217,#1205),#12265,.T.);
#12930=ADVANCED_FACE('',(#2218),#1522,.T.);
#12931=ADVANCED_FACE('',(#2219,#1206),#1523,.F.);
#12932=ADVANCED_FACE('',(#2220),#12266,.T.);
#12933=ADVANCED_FACE('',(#2221,#1207),#1524,.T.);
#12934=ADVANCED_FACE('',(#2222),#12267,.T.);
#13063=CLOSED_SHELL('',(#12792,#12793,#12794,#12795,#12796,#12797,#12798,
#12799,#12800,#12801,#12802,#12803,#12804,#12805,#12806,#12807,#12808,#12809,
#12810,#12811,#12812,#12813,#12814,#12815,#12816,#12817,#12818,#12819,#12820,
#12821,#12822,#12823,#12824,#12825,#12826,#12827,#12828,#12829,#12830,#12831,
#12832,#12833,#12834,#12835,#12836,#12837,#12838,#12839,#12840,#12841,#12842,
#12843,#12844,#12845,#12846,#12847,#12848,#12849,#12850,#12851,#12852,#12853,
#12854,#12855,#12856,#12857,#12858,#12859,#12860,#12861,#12862,#12863,#12864,
#12865,#12866,#12867,#12868,#12869,#12870,#12871,#12872,#12873,#12874,#12875,
#12876,#12877,#12878,#12879,#12880,#12881,#12882,#12883,#12884,#12885,#12886,
#12887,#12888,#12889,#12890,#12891,#12892,#12893,#12894,#12895,#12896,#12897,
#12898,#12899,#12900,#12901,#12902,#12903,#12904,#12905,#12906,#12907,#12908,
#12909,#12910,#12911,#12912,#12913,#12914,#12915,#12916,#12917,#12918,#12919,
#12920,#12921,#12922,#12923,#12924,#12925,#12926,#12927,#12928,#12929,#12930,
#12931,#12932,#12933,#12934));
#14546=AXIS2_PLACEMENT_3D('',#23703,#17558,#17559);
#14547=AXIS2_PLACEMENT_3D('',#23704,#17560,#17561);
#14548=AXIS2_PLACEMENT_3D('',#23729,#17563,#17564);
#14549=AXIS2_PLACEMENT_3D('',#23734,#17565,#17566);
#14550=AXIS2_PLACEMENT_3D('',#23821,#17568,#17569);
#14551=AXIS2_PLACEMENT_3D('',#23911,#17571,#17572);
#14552=AXIS2_PLACEMENT_3D('',#23998,#17574,#17575);
#14553=AXIS2_PLACEMENT_3D('',#24085,#17577,#17578);
#14554=AXIS2_PLACEMENT_3D('',#24172,#17580,#17581);
#14555=AXIS2_PLACEMENT_3D('',#24259,#17583,#17584);
#14556=AXIS2_PLACEMENT_3D('',#24346,#17586,#17587);
#14557=AXIS2_PLACEMENT_3D('',#24418,#17589,#17590);
#14558=AXIS2_PLACEMENT_3D('',#24469,#17592,#17593);
#14559=AXIS2_PLACEMENT_3D('',#24517,#17595,#17596);
#14560=AXIS2_PLACEMENT_3D('',#24565,#17598,#17599);
#14561=AXIS2_PLACEMENT_3D('',#24616,#17601,#17602);
#14562=AXIS2_PLACEMENT_3D('',#24667,#17604,#17605);
#14563=AXIS2_PLACEMENT_3D('',#24715,#17607,#17608);
#14564=AXIS2_PLACEMENT_3D('',#24766,#17610,#17611);
#14565=AXIS2_PLACEMENT_3D('',#24817,#17613,#17614);
#14566=AXIS2_PLACEMENT_3D('',#24865,#17616,#17617);
#14567=AXIS2_PLACEMENT_3D('',#24913,#17619,#17620);
#14568=AXIS2_PLACEMENT_3D('',#24964,#17622,#17623);
#14569=AXIS2_PLACEMENT_3D('',#25015,#17625,#17626);
#14570=AXIS2_PLACEMENT_3D('',#25063,#17628,#17629);
#14571=AXIS2_PLACEMENT_3D('',#25114,#17631,#17632);
#14572=AXIS2_PLACEMENT_3D('',#25165,#17634,#17635);
#14573=AXIS2_PLACEMENT_3D('',#25213,#17637,#17638);
#14574=AXIS2_PLACEMENT_3D('',#25261,#17640,#17641);
#14575=AXIS2_PLACEMENT_3D('',#25312,#17643,#17644);
#14576=AXIS2_PLACEMENT_3D('',#25363,#17646,#17647);
#14577=AXIS2_PLACEMENT_3D('',#25411,#17649,#17650);
#14578=AXIS2_PLACEMENT_3D('',#25462,#17652,#17653);
#14579=AXIS2_PLACEMENT_3D('',#25513,#17655,#17656);
#14580=AXIS2_PLACEMENT_3D('',#25561,#17658,#17659);
#14581=AXIS2_PLACEMENT_3D('',#25609,#17661,#17662);
#14582=AXIS2_PLACEMENT_3D('',#25660,#17664,#17665);
#14583=AXIS2_PLACEMENT_3D('',#25711,#17667,#17668);
#14584=AXIS2_PLACEMENT_3D('',#25759,#17670,#17671);
#14585=AXIS2_PLACEMENT_3D('',#25810,#17673,#17674);
#14586=AXIS2_PLACEMENT_3D('',#25861,#17676,#17677);
#14587=AXIS2_PLACEMENT_3D('',#25909,#17679,#17680);
#14588=AXIS2_PLACEMENT_3D('',#25957,#17682,#17683);
#14589=AXIS2_PLACEMENT_3D('',#26008,#17685,#17686);
#14590=AXIS2_PLACEMENT_3D('',#26059,#17688,#17689);
#14591=AXIS2_PLACEMENT_3D('',#26107,#17691,#17692);
#14592=AXIS2_PLACEMENT_3D('',#26158,#17694,#17695);
#14593=AXIS2_PLACEMENT_3D('',#26209,#17697,#17698);
#14594=AXIS2_PLACEMENT_3D('',#26257,#17700,#17701);
#14595=AXIS2_PLACEMENT_3D('',#26305,#17703,#17704);
#14596=AXIS2_PLACEMENT_3D('',#26356,#17706,#17707);
#14597=AXIS2_PLACEMENT_3D('',#26407,#17709,#17710);
#14598=AXIS2_PLACEMENT_3D('',#26455,#17712,#17713);
#14599=AXIS2_PLACEMENT_3D('',#26506,#17715,#17716);
#14600=AXIS2_PLACEMENT_3D('',#26557,#17718,#17719);
#14601=AXIS2_PLACEMENT_3D('',#26605,#17721,#17722);
#14602=AXIS2_PLACEMENT_3D('',#26653,#17724,#17725);
#14603=AXIS2_PLACEMENT_3D('',#26704,#17727,#17728);
#14604=AXIS2_PLACEMENT_3D('',#26770,#17730,#17731);
#14605=AXIS2_PLACEMENT_3D('',#26860,#17733,#17734);
#14606=AXIS2_PLACEMENT_3D('',#26947,#17736,#17737);
#14607=AXIS2_PLACEMENT_3D('',#27034,#17739,#17740);
#14608=AXIS2_PLACEMENT_3D('',#27121,#17742,#17743);
#14609=AXIS2_PLACEMENT_3D('',#27208,#17745,#17746);
#14610=AXIS2_PLACEMENT_3D('',#27295,#17748,#17749);
#14611=AXIS2_PLACEMENT_3D('',#27385,#17751,#17752);
#14612=AXIS2_PLACEMENT_3D('',#27394,#17754,#17755);
#14613=AXIS2_PLACEMENT_3D('',#27395,#17756,#17757);
#14614=AXIS2_PLACEMENT_3D('',#27417,#17759,#17760);
#14615=AXIS2_PLACEMENT_3D('',#27431,#17761,#17762);
#14616=AXIS2_PLACEMENT_3D('',#27469,#17764,#17765);
#14617=AXIS2_PLACEMENT_3D('',#27505,#17767,#17768);
#14618=AXIS2_PLACEMENT_3D('',#27543,#17770,#17771);
#14619=AXIS2_PLACEMENT_3D('',#27579,#17773,#17774);
#14620=AXIS2_PLACEMENT_3D('',#27617,#17776,#17777);
#14621=AXIS2_PLACEMENT_3D('',#27654,#17779,#17780);
#14622=AXIS2_PLACEMENT_3D('',#27689,#17782,#17783);
#14623=AXIS2_PLACEMENT_3D('',#27716,#17785,#17786);
#14624=AXIS2_PLACEMENT_3D('',#27740,#17788,#17789);
#14625=AXIS2_PLACEMENT_3D('',#27764,#17791,#17792);
#14626=AXIS2_PLACEMENT_3D('',#27788,#17794,#17795);
#14627=AXIS2_PLACEMENT_3D('',#27814,#17797,#17798);
#14628=AXIS2_PLACEMENT_3D('',#27838,#17800,#17801);
#14629=AXIS2_PLACEMENT_3D('',#27862,#17803,#17804);
#14630=AXIS2_PLACEMENT_3D('',#27888,#17806,#17807);
#14631=AXIS2_PLACEMENT_3D('',#27912,#17809,#17810);
#14632=AXIS2_PLACEMENT_3D('',#27936,#17812,#17813);
#14633=AXIS2_PLACEMENT_3D('',#27960,#17815,#17816);
#14634=AXIS2_PLACEMENT_3D('',#27986,#17818,#17819);
#14635=AXIS2_PLACEMENT_3D('',#28010,#17821,#17822);
#14636=AXIS2_PLACEMENT_3D('',#28034,#17824,#17825);
#14637=AXIS2_PLACEMENT_3D('',#28060,#17827,#17828);
#14638=AXIS2_PLACEMENT_3D('',#28084,#17830,#17831);
#14639=AXIS2_PLACEMENT_3D('',#28108,#17833,#17834);
#14640=AXIS2_PLACEMENT_3D('',#28132,#17836,#17837);
#14641=AXIS2_PLACEMENT_3D('',#28158,#17839,#17840);
#14642=AXIS2_PLACEMENT_3D('',#28182,#17842,#17843);
#14643=AXIS2_PLACEMENT_3D('',#28206,#17845,#17846);
#14644=AXIS2_PLACEMENT_3D('',#28232,#17848,#17849);
#14645=AXIS2_PLACEMENT_3D('',#28256,#17851,#17852);
#14646=AXIS2_PLACEMENT_3D('',#28280,#17854,#17855);
#14647=AXIS2_PLACEMENT_3D('',#28304,#17857,#17858);
#14648=AXIS2_PLACEMENT_3D('',#28330,#17860,#17861);
#14649=AXIS2_PLACEMENT_3D('',#28354,#17863,#17864);
#14650=AXIS2_PLACEMENT_3D('',#28378,#17866,#17867);
#14651=AXIS2_PLACEMENT_3D('',#28404,#17869,#17870);
#14652=AXIS2_PLACEMENT_3D('',#28428,#17872,#17873);
#14653=AXIS2_PLACEMENT_3D('',#28452,#17875,#17876);
#14654=AXIS2_PLACEMENT_3D('',#28476,#17878,#17879);
#14655=AXIS2_PLACEMENT_3D('',#28502,#17881,#17882);
#14656=AXIS2_PLACEMENT_3D('',#28526,#17884,#17885);
#14657=AXIS2_PLACEMENT_3D('',#28550,#17887,#17888);
#14658=AXIS2_PLACEMENT_3D('',#28576,#17890,#17891);
#14659=AXIS2_PLACEMENT_3D('',#28600,#17893,#17894);
#14660=AXIS2_PLACEMENT_3D('',#28624,#17896,#17897);
#14661=AXIS2_PLACEMENT_3D('',#28648,#17899,#17900);
#14662=AXIS2_PLACEMENT_3D('',#28674,#17902,#17903);
#14663=AXIS2_PLACEMENT_3D('',#28698,#17905,#17906);
#14664=AXIS2_PLACEMENT_3D('',#28722,#17908,#17909);
#14665=AXIS2_PLACEMENT_3D('',#28748,#17911,#17912);
#14666=AXIS2_PLACEMENT_3D('',#28772,#17914,#17915);
#14667=AXIS2_PLACEMENT_3D('',#28796,#17917,#17918);
#14668=AXIS2_PLACEMENT_3D('',#28821,#17920,#17921);
#14669=AXIS2_PLACEMENT_3D('',#28848,#17923,#17924);
#14670=AXIS2_PLACEMENT_3D('',#28885,#17926,#17927);
#14671=AXIS2_PLACEMENT_3D('',#28921,#17929,#17930);
#14672=AXIS2_PLACEMENT_3D('',#28959,#17932,#17933);
#14673=AXIS2_PLACEMENT_3D('',#28995,#17935,#17936);
#14674=AXIS2_PLACEMENT_3D('',#29033,#17938,#17939);
#14675=AXIS2_PLACEMENT_3D('',#29070,#17941,#17942);
#14676=AXIS2_PLACEMENT_3D('',#29107,#17944,#17945);
#14677=AXIS2_PLACEMENT_3D('',#29109,#17946,#17947);
#14678=AXIS2_PLACEMENT_3D('',#29186,#17948,#17949);
#14679=AXIS2_PLACEMENT_3D('',#29187,#17950,#17951);
#14680=AXIS2_PLACEMENT_3D('',#29190,#17953,#17954);
#14681=AXIS2_PLACEMENT_3D('',#29191,#17955,#17956);
#14682=AXIS2_PLACEMENT_3D('',#31265,#17957,#17958);
#14683=AXIS2_PLACEMENT_3D('',#33320,#17959,#17960);
#14684=AXIS2_PLACEMENT_3D('',#33329,#17965,#17966);
#14685=AXIS2_PLACEMENT_3D('',#33331,#17967,#17968);
#14686=AXIS2_PLACEMENT_3D('',#33335,#17971,#17972);
#14687=AXIS2_PLACEMENT_3D('',#33339,#17975,#17976);
#14688=AXIS2_PLACEMENT_3D('',#33343,#17979,#17980);
#14689=AXIS2_PLACEMENT_3D('',#33344,#17981,#17982);
#14690=AXIS2_PLACEMENT_3D('',#33345,#17983,#17984);
#14691=AXIS2_PLACEMENT_3D('',#33347,#17985,#17986);
#14692=AXIS2_PLACEMENT_3D('',#33350,#17988,#17989);
#14693=AXIS2_PLACEMENT_3D('',#33351,#17990,#17991);
#14694=AXIS2_PLACEMENT_3D('',#33352,#17992,#17993);
#14695=AXIS2_PLACEMENT_3D('',#33354,#17994,#17995);
#14696=AXIS2_PLACEMENT_3D('',#33355,#17996,#17997);
#14697=AXIS2_PLACEMENT_3D('',#33356,#17998,#17999);
#14698=AXIS2_PLACEMENT_3D('',#33358,#18000,#18001);
#14699=AXIS2_PLACEMENT_3D('',#33360,#18003,#18004);
#14700=AXIS2_PLACEMENT_3D('',#33361,#18005,#18006);
#17558=DIRECTION('axis',(0.,0.,1.));
#17559=DIRECTION('refdir',(1.,0.,0.));
#17560=DIRECTION('center_axis',(1.,0.,0.));
#17561=DIRECTION('ref_axis',(0.,0.975560628713931,0.219730425074181));
#17562=DIRECTION('',(-1.,0.,0.));
#17563=DIRECTION('center_axis',(-1.,0.,0.));
#17564=DIRECTION('ref_axis',(0.,0.,-1.));
#17565=DIRECTION('center_axis',(1.,0.,0.));
#17566=DIRECTION('ref_axis',(0.,0.,-1.));
#17567=DIRECTION('',(-1.,0.,0.));
#17568=DIRECTION('center_axis',(1.,0.,0.));
#17569=DIRECTION('ref_axis',(0.,0.,-1.));
#17570=DIRECTION('',(-1.,0.,0.));
#17571=DIRECTION('center_axis',(1.,0.,0.));
#17572=DIRECTION('ref_axis',(0.,0.,-1.));
#17573=DIRECTION('',(-1.,0.,0.));
#17574=DIRECTION('center_axis',(1.,0.,0.));
#17575=DIRECTION('ref_axis',(0.,0.,-1.));
#17576=DIRECTION('',(-1.,0.,0.));
#17577=DIRECTION('center_axis',(1.,0.,0.));
#17578=DIRECTION('ref_axis',(0.,0.,-1.));
#17579=DIRECTION('',(-1.,0.,0.));
#17580=DIRECTION('center_axis',(1.,0.,0.));
#17581=DIRECTION('ref_axis',(0.,0.,-1.));
#17582=DIRECTION('',(-1.,0.,0.));
#17583=DIRECTION('center_axis',(1.,0.,0.));
#17584=DIRECTION('ref_axis',(0.,0.,-1.));
#17585=DIRECTION('',(-1.,0.,0.));
#17586=DIRECTION('center_axis',(1.,0.,0.));
#17587=DIRECTION('ref_axis',(0.,0.,-1.));
#17588=DIRECTION('',(-1.,0.,0.));
#17589=DIRECTION('center_axis',(1.,0.,0.));
#17590=DIRECTION('ref_axis',(0.,0.,-1.));
#17591=DIRECTION('',(-1.,0.,0.));
#17592=DIRECTION('center_axis',(1.,0.,0.));
#17593=DIRECTION('ref_axis',(0.,0.,-1.));
#17594=DIRECTION('',(-1.,0.,0.));
#17595=DIRECTION('center_axis',(1.,0.,0.));
#17596=DIRECTION('ref_axis',(0.,0.,-1.));
#17597=DIRECTION('',(-1.,0.,0.));
#17598=DIRECTION('center_axis',(1.,0.,0.));
#17599=DIRECTION('ref_axis',(0.,0.,-1.));
#17600=DIRECTION('',(-1.,0.,0.));
#17601=DIRECTION('center_axis',(1.,0.,0.));
#17602=DIRECTION('ref_axis',(0.,0.,-1.));
#17603=DIRECTION('',(-1.,0.,0.));
#17604=DIRECTION('center_axis',(1.,0.,0.));
#17605=DIRECTION('ref_axis',(0.,0.,-1.));
#17606=DIRECTION('',(-1.,0.,0.));
#17607=DIRECTION('center_axis',(1.,0.,0.));
#17608=DIRECTION('ref_axis',(0.,0.,-1.));
#17609=DIRECTION('',(-1.,0.,0.));
#17610=DIRECTION('center_axis',(1.,0.,0.));
#17611=DIRECTION('ref_axis',(0.,0.,-1.));
#17612=DIRECTION('',(-1.,0.,0.));
#17613=DIRECTION('center_axis',(1.,0.,0.));
#17614=DIRECTION('ref_axis',(0.,0.,-1.));
#17615=DIRECTION('',(-1.,0.,0.));
#17616=DIRECTION('center_axis',(1.,0.,0.));
#17617=DIRECTION('ref_axis',(0.,0.,-1.));
#17618=DIRECTION('',(-1.,0.,0.));
#17619=DIRECTION('center_axis',(1.,0.,0.));
#17620=DIRECTION('ref_axis',(0.,0.,-1.));
#17621=DIRECTION('',(-1.,0.,0.));
#17622=DIRECTION('center_axis',(1.,0.,0.));
#17623=DIRECTION('ref_axis',(0.,0.,-1.));
#17624=DIRECTION('',(-1.,0.,0.));
#17625=DIRECTION('center_axis',(1.,0.,0.));
#17626=DIRECTION('ref_axis',(0.,0.,-1.));
#17627=DIRECTION('',(-1.,0.,0.));
#17628=DIRECTION('center_axis',(1.,0.,0.));
#17629=DIRECTION('ref_axis',(0.,0.,-1.));
#17630=DIRECTION('',(-1.,0.,0.));
#17631=DIRECTION('center_axis',(1.,0.,0.));
#17632=DIRECTION('ref_axis',(0.,0.,-1.));
#17633=DIRECTION('',(-1.,0.,0.));
#17634=DIRECTION('center_axis',(1.,0.,0.));
#17635=DIRECTION('ref_axis',(0.,0.,-1.));
#17636=DIRECTION('',(-1.,0.,0.));
#17637=DIRECTION('center_axis',(1.,0.,0.));
#17638=DIRECTION('ref_axis',(0.,0.,-1.));
#17639=DIRECTION('',(-1.,0.,0.));
#17640=DIRECTION('center_axis',(1.,0.,0.));
#17641=DIRECTION('ref_axis',(0.,0.,-1.));
#17642=DIRECTION('',(-1.,0.,0.));
#17643=DIRECTION('center_axis',(1.,0.,0.));
#17644=DIRECTION('ref_axis',(0.,0.,-1.));
#17645=DIRECTION('',(-1.,0.,0.));
#17646=DIRECTION('center_axis',(1.,0.,0.));
#17647=DIRECTION('ref_axis',(0.,0.,-1.));
#17648=DIRECTION('',(-1.,0.,0.));
#17649=DIRECTION('center_axis',(1.,0.,0.));
#17650=DIRECTION('ref_axis',(0.,0.,-1.));
#17651=DIRECTION('',(-1.,0.,0.));
#17652=DIRECTION('center_axis',(1.,0.,0.));
#17653=DIRECTION('ref_axis',(0.,0.,-1.));
#17654=DIRECTION('',(-1.,0.,0.));
#17655=DIRECTION('center_axis',(1.,0.,0.));
#17656=DIRECTION('ref_axis',(0.,0.,-1.));
#17657=DIRECTION('',(-1.,0.,0.));
#17658=DIRECTION('center_axis',(1.,0.,0.));
#17659=DIRECTION('ref_axis',(0.,0.,-1.));
#17660=DIRECTION('',(-1.,0.,0.));
#17661=DIRECTION('center_axis',(1.,0.,0.));
#17662=DIRECTION('ref_axis',(0.,0.,-1.));
#17663=DIRECTION('',(-1.,0.,0.));
#17664=DIRECTION('center_axis',(1.,0.,0.));
#17665=DIRECTION('ref_axis',(0.,0.,-1.));
#17666=DIRECTION('',(-1.,0.,0.));
#17667=DIRECTION('center_axis',(1.,0.,0.));
#17668=DIRECTION('ref_axis',(0.,0.,-1.));
#17669=DIRECTION('',(-1.,0.,0.));
#17670=DIRECTION('center_axis',(1.,0.,0.));
#17671=DIRECTION('ref_axis',(0.,0.,-1.));
#17672=DIRECTION('',(-1.,0.,0.));
#17673=DIRECTION('center_axis',(1.,0.,0.));
#17674=DIRECTION('ref_axis',(0.,0.,-1.));
#17675=DIRECTION('',(-1.,0.,0.));
#17676=DIRECTION('center_axis',(1.,0.,0.));
#17677=DIRECTION('ref_axis',(0.,0.,-1.));
#17678=DIRECTION('',(-1.,0.,0.));
#17679=DIRECTION('center_axis',(1.,0.,0.));
#17680=DIRECTION('ref_axis',(0.,0.,-1.));
#17681=DIRECTION('',(-1.,0.,0.));
#17682=DIRECTION('center_axis',(1.,0.,0.));
#17683=DIRECTION('ref_axis',(0.,0.,-1.));
#17684=DIRECTION('',(-1.,0.,0.));
#17685=DIRECTION('center_axis',(1.,0.,0.));
#17686=DIRECTION('ref_axis',(0.,0.,-1.));
#17687=DIRECTION('',(-1.,0.,0.));
#17688=DIRECTION('center_axis',(1.,0.,0.));
#17689=DIRECTION('ref_axis',(0.,0.,-1.));
#17690=DIRECTION('',(-1.,0.,0.));
#17691=DIRECTION('center_axis',(1.,0.,0.));
#17692=DIRECTION('ref_axis',(0.,0.,-1.));
#17693=DIRECTION('',(-1.,0.,0.));
#17694=DIRECTION('center_axis',(1.,0.,0.));
#17695=DIRECTION('ref_axis',(0.,0.,-1.));
#17696=DIRECTION('',(-1.,0.,0.));
#17697=DIRECTION('center_axis',(1.,0.,0.));
#17698=DIRECTION('ref_axis',(0.,0.,-1.));
#17699=DIRECTION('',(-1.,0.,0.));
#17700=DIRECTION('center_axis',(1.,0.,0.));
#17701=DIRECTION('ref_axis',(0.,0.,-1.));
#17702=DIRECTION('',(-1.,0.,0.));
#17703=DIRECTION('center_axis',(1.,0.,0.));
#17704=DIRECTION('ref_axis',(0.,0.,-1.));
#17705=DIRECTION('',(-1.,0.,0.));
#17706=DIRECTION('center_axis',(1.,0.,0.));
#17707=DIRECTION('ref_axis',(0.,0.,-1.));
#17708=DIRECTION('',(-1.,0.,0.));
#17709=DIRECTION('center_axis',(1.,0.,0.));
#17710=DIRECTION('ref_axis',(0.,0.,-1.));
#17711=DIRECTION('',(-1.,0.,0.));
#17712=DIRECTION('center_axis',(1.,0.,0.));
#17713=DIRECTION('ref_axis',(0.,0.,-1.));
#17714=DIRECTION('',(-1.,0.,0.));
#17715=DIRECTION('center_axis',(1.,0.,0.));
#17716=DIRECTION('ref_axis',(0.,0.,-1.));
#17717=DIRECTION('',(-1.,0.,0.));
#17718=DIRECTION('center_axis',(1.,0.,0.));
#17719=DIRECTION('ref_axis',(0.,0.,-1.));
#17720=DIRECTION('',(-1.,0.,0.));
#17721=DIRECTION('center_axis',(1.,0.,0.));
#17722=DIRECTION('ref_axis',(0.,0.,-1.));
#17723=DIRECTION('',(-1.,0.,0.));
#17724=DIRECTION('center_axis',(1.,0.,0.));
#17725=DIRECTION('ref_axis',(0.,0.,-1.));
#17726=DIRECTION('',(-1.,0.,0.));
#17727=DIRECTION('center_axis',(1.,0.,0.));
#17728=DIRECTION('ref_axis',(0.,0.,-1.));
#17729=DIRECTION('',(-1.,0.,0.));
#17730=DIRECTION('center_axis',(1.,0.,0.));
#17731=DIRECTION('ref_axis',(0.,0.,-1.));
#17732=DIRECTION('',(-1.,0.,0.));
#17733=DIRECTION('center_axis',(1.,0.,0.));
#17734=DIRECTION('ref_axis',(0.,0.,-1.));
#17735=DIRECTION('',(-1.,0.,0.));
#17736=DIRECTION('center_axis',(1.,0.,0.));
#17737=DIRECTION('ref_axis',(0.,0.,-1.));
#17738=DIRECTION('',(-1.,0.,0.));
#17739=DIRECTION('center_axis',(1.,0.,0.));
#17740=DIRECTION('ref_axis',(0.,0.,-1.));
#17741=DIRECTION('',(-1.,0.,0.));
#17742=DIRECTION('center_axis',(1.,0.,0.));
#17743=DIRECTION('ref_axis',(0.,0.,-1.));
#17744=DIRECTION('',(-1.,0.,0.));
#17745=DIRECTION('center_axis',(1.,0.,0.));
#17746=DIRECTION('ref_axis',(0.,0.,-1.));
#17747=DIRECTION('',(-1.,0.,0.));
#17748=DIRECTION('center_axis',(1.,0.,0.));
#17749=DIRECTION('ref_axis',(0.,0.,-1.));
#17750=DIRECTION('',(-1.,0.,0.));
#17751=DIRECTION('center_axis',(1.,0.,0.));
#17752=DIRECTION('ref_axis',(0.,-1.17203152359781E-12,-1.));
#17753=DIRECTION('',(1.,0.,0.));
#17754=DIRECTION('center_axis',(1.,0.,0.));
#17755=DIRECTION('ref_axis',(0.,-1.17203152359781E-12,-1.));
#17756=DIRECTION('center_axis',(1.,0.,0.));
#17757=DIRECTION('ref_axis',(0.,-1.17203152359781E-12,-1.));
#17758=DIRECTION('',(1.,0.,0.));
#17759=DIRECTION('center_axis',(1.,0.,0.));
#17760=DIRECTION('ref_axis',(0.,-1.17203152359781E-12,-1.));
#17761=DIRECTION('center_axis',(1.,0.,0.));
#17762=DIRECTION('ref_axis',(0.,-1.17203152359781E-12,-1.));
#17763=DIRECTION('',(1.,0.,0.));
#17764=DIRECTION('center_axis',(1.,0.,0.));
#17765=DIRECTION('ref_axis',(0.,-1.17203152359781E-12,-1.));
#17766=DIRECTION('',(1.,0.,0.));
#17767=DIRECTION('center_axis',(1.,0.,0.));
#17768=DIRECTION('ref_axis',(0.,-1.17203152359781E-12,-1.));
#17769=DIRECTION('',(1.,0.,0.));
#17770=DIRECTION('center_axis',(1.,0.,0.));
#17771=DIRECTION('ref_axis',(0.,-1.17203152359781E-12,-1.));
#17772=DIRECTION('',(1.,0.,0.));
#17773=DIRECTION('center_axis',(1.,0.,0.));
#17774=DIRECTION('ref_axis',(0.,-1.17203152359781E-12,-1.));
#17775=DIRECTION('',(1.,0.,0.));
#17776=DIRECTION('center_axis',(1.,0.,0.));
#17777=DIRECTION('ref_axis',(0.,-1.17203152359781E-12,-1.));
#17778=DIRECTION('',(1.,0.,0.));
#17779=DIRECTION('center_axis',(1.,0.,0.));
#17780=DIRECTION('ref_axis',(0.,-1.17203152359781E-12,-1.));
#17781=DIRECTION('',(1.,0.,0.));
#17782=DIRECTION('center_axis',(1.,0.,0.));
#17783=DIRECTION('ref_axis',(0.,-1.17203152359781E-12,-1.));
#17784=DIRECTION('',(1.,0.,0.));
#17785=DIRECTION('center_axis',(1.,0.,0.));
#17786=DIRECTION('ref_axis',(0.,-1.17203152359781E-12,-1.));
#17787=DIRECTION('',(1.,0.,0.));
#17788=DIRECTION('center_axis',(1.,0.,0.));
#17789=DIRECTION('ref_axis',(0.,-1.17203152359781E-12,-1.));
#17790=DIRECTION('',(1.,0.,0.));
#17791=DIRECTION('center_axis',(1.,0.,0.));
#17792=DIRECTION('ref_axis',(0.,-1.17203152359781E-12,-1.));
#17793=DIRECTION('',(1.,0.,0.));
#17794=DIRECTION('center_axis',(1.,0.,0.));
#17795=DIRECTION('ref_axis',(0.,-1.17203152359781E-12,-1.));
#17796=DIRECTION('',(1.,0.,0.));
#17797=DIRECTION('center_axis',(1.,0.,0.));
#17798=DIRECTION('ref_axis',(0.,-1.17203152359781E-12,-1.));
#17799=DIRECTION('',(1.,0.,0.));
#17800=DIRECTION('center_axis',(1.,0.,0.));
#17801=DIRECTION('ref_axis',(0.,-1.17203152359781E-12,-1.));
#17802=DIRECTION('',(1.,0.,0.));
#17803=DIRECTION('center_axis',(1.,0.,0.));
#17804=DIRECTION('ref_axis',(0.,-1.17203152359781E-12,-1.));
#17805=DIRECTION('',(1.,0.,0.));
#17806=DIRECTION('center_axis',(1.,0.,0.));
#17807=DIRECTION('ref_axis',(0.,-1.17203152359781E-12,-1.));
#17808=DIRECTION('',(1.,0.,0.));
#17809=DIRECTION('center_axis',(1.,0.,0.));
#17810=DIRECTION('ref_axis',(0.,-1.17203152359781E-12,-1.));
#17811=DIRECTION('',(1.,0.,0.));
#17812=DIRECTION('center_axis',(1.,0.,0.));
#17813=DIRECTION('ref_axis',(0.,-1.17203152359781E-12,-1.));
#17814=DIRECTION('',(1.,0.,0.));
#17815=DIRECTION('center_axis',(1.,0.,0.));
#17816=DIRECTION('ref_axis',(0.,-1.17203152359781E-12,-1.));
#17817=DIRECTION('',(1.,0.,0.));
#17818=DIRECTION('center_axis',(1.,0.,0.));
#17819=DIRECTION('ref_axis',(0.,-1.17203152359781E-12,-1.));
#17820=DIRECTION('',(1.,0.,0.));
#17821=DIRECTION('center_axis',(1.,0.,0.));
#17822=DIRECTION('ref_axis',(0.,-1.17203152359781E-12,-1.));
#17823=DIRECTION('',(1.,0.,0.));
#17824=DIRECTION('center_axis',(1.,0.,0.));
#17825=DIRECTION('ref_axis',(0.,-1.17203152359781E-12,-1.));
#17826=DIRECTION('',(1.,0.,0.));
#17827=DIRECTION('center_axis',(1.,0.,0.));
#17828=DIRECTION('ref_axis',(0.,-1.17203152359781E-12,-1.));
#17829=DIRECTION('',(1.,0.,0.));
#17830=DIRECTION('center_axis',(1.,0.,0.));
#17831=DIRECTION('ref_axis',(0.,-1.17203152359781E-12,-1.));
#17832=DIRECTION('',(1.,0.,0.));
#17833=DIRECTION('center_axis',(1.,0.,0.));
#17834=DIRECTION('ref_axis',(0.,-1.17203152359781E-12,-1.));
#17835=DIRECTION('',(1.,0.,0.));
#17836=DIRECTION('center_axis',(1.,0.,0.));
#17837=DIRECTION('ref_axis',(0.,-1.17203152359781E-12,-1.));
#17838=DIRECTION('',(1.,0.,0.));
#17839=DIRECTION('center_axis',(1.,0.,0.));
#17840=DIRECTION('ref_axis',(0.,-1.17203152359781E-12,-1.));
#17841=DIRECTION('',(1.,0.,0.));
#17842=DIRECTION('center_axis',(1.,0.,0.));
#17843=DIRECTION('ref_axis',(0.,-1.17203152359781E-12,-1.));
#17844=DIRECTION('',(1.,0.,0.));
#17845=DIRECTION('center_axis',(1.,0.,0.));
#17846=DIRECTION('ref_axis',(0.,-1.17203152359781E-12,-1.));
#17847=DIRECTION('',(1.,0.,0.));
#17848=DIRECTION('center_axis',(1.,0.,0.));
#17849=DIRECTION('ref_axis',(0.,-1.17203152359781E-12,-1.));
#17850=DIRECTION('',(1.,0.,0.));
#17851=DIRECTION('center_axis',(1.,0.,0.));
#17852=DIRECTION('ref_axis',(0.,-1.17203152359781E-12,-1.));
#17853=DIRECTION('',(1.,0.,0.));
#17854=DIRECTION('center_axis',(1.,0.,0.));
#17855=DIRECTION('ref_axis',(0.,-1.17203152359781E-12,-1.));
#17856=DIRECTION('',(1.,0.,0.));
#17857=DIRECTION('center_axis',(1.,0.,0.));
#17858=DIRECTION('ref_axis',(0.,-1.17203152359781E-12,-1.));
#17859=DIRECTION('',(1.,0.,0.));
#17860=DIRECTION('center_axis',(1.,0.,0.));
#17861=DIRECTION('ref_axis',(0.,-1.17203152359781E-12,-1.));
#17862=DIRECTION('',(1.,0.,0.));
#17863=DIRECTION('center_axis',(1.,0.,0.));
#17864=DIRECTION('ref_axis',(0.,-1.17203152359781E-12,-1.));
#17865=DIRECTION('',(1.,0.,0.));
#17866=DIRECTION('center_axis',(1.,0.,0.));
#17867=DIRECTION('ref_axis',(0.,-1.17203152359781E-12,-1.));
#17868=DIRECTION('',(1.,0.,0.));
#17869=DIRECTION('center_axis',(1.,0.,0.));
#17870=DIRECTION('ref_axis',(0.,-1.17203152359781E-12,-1.));
#17871=DIRECTION('',(1.,0.,0.));
#17872=DIRECTION('center_axis',(1.,0.,0.));
#17873=DIRECTION('ref_axis',(0.,-1.17203152359781E-12,-1.));
#17874=DIRECTION('',(1.,0.,0.));
#17875=DIRECTION('center_axis',(1.,0.,0.));
#17876=DIRECTION('ref_axis',(0.,-1.17203152359781E-12,-1.));
#17877=DIRECTION('',(1.,0.,0.));
#17878=DIRECTION('center_axis',(1.,0.,0.));
#17879=DIRECTION('ref_axis',(0.,-1.17203152359781E-12,-1.));
#17880=DIRECTION('',(1.,0.,0.));
#17881=DIRECTION('center_axis',(1.,0.,0.));
#17882=DIRECTION('ref_axis',(0.,-1.17203152359781E-12,-1.));
#17883=DIRECTION('',(1.,0.,0.));
#17884=DIRECTION('center_axis',(1.,0.,0.));
#17885=DIRECTION('ref_axis',(0.,-1.17203152359781E-12,-1.));
#17886=DIRECTION('',(1.,0.,0.));
#17887=DIRECTION('center_axis',(1.,0.,0.));
#17888=DIRECTION('ref_axis',(0.,-1.17203152359781E-12,-1.));
#17889=DIRECTION('',(1.,0.,0.));
#17890=DIRECTION('center_axis',(1.,0.,0.));
#17891=DIRECTION('ref_axis',(0.,-1.17203152359781E-12,-1.));
#17892=DIRECTION('',(1.,0.,0.));
#17893=DIRECTION('center_axis',(1.,0.,0.));
#17894=DIRECTION('ref_axis',(0.,-1.17203152359781E-12,-1.));
#17895=DIRECTION('',(1.,0.,0.));
#17896=DIRECTION('center_axis',(1.,0.,0.));
#17897=DIRECTION('ref_axis',(0.,-1.17203152359781E-12,-1.));
#17898=DIRECTION('',(1.,0.,0.));
#17899=DIRECTION('center_axis',(1.,0.,0.));
#17900=DIRECTION('ref_axis',(0.,-1.17203152359781E-12,-1.));
#17901=DIRECTION('',(1.,0.,0.));
#17902=DIRECTION('center_axis',(1.,0.,0.));
#17903=DIRECTION('ref_axis',(0.,-1.17203152359781E-12,-1.));
#17904=DIRECTION('',(1.,0.,0.));
#17905=DIRECTION('center_axis',(1.,0.,0.));
#17906=DIRECTION('ref_axis',(0.,-1.17203152359781E-12,-1.));
#17907=DIRECTION('',(1.,0.,0.));
#17908=DIRECTION('center_axis',(1.,0.,0.));
#17909=DIRECTION('ref_axis',(0.,-1.17203152359781E-12,-1.));
#17910=DIRECTION('',(1.,0.,0.));
#17911=DIRECTION('center_axis',(1.,0.,0.));
#17912=DIRECTION('ref_axis',(0.,-1.17203152359781E-12,-1.));
#17913=DIRECTION('',(1.,0.,0.));
#17914=DIRECTION('center_axis',(1.,0.,0.));
#17915=DIRECTION('ref_axis',(0.,-1.17203152359781E-12,-1.));
#17916=DIRECTION('',(1.,0.,0.));
#17917=DIRECTION('center_axis',(1.,0.,0.));
#17918=DIRECTION('ref_axis',(0.,-1.17203152359781E-12,-1.));
#17919=DIRECTION('',(1.,0.,0.));
#17920=DIRECTION('center_axis',(1.,0.,0.));
#17921=DIRECTION('ref_axis',(0.,-1.17203152359781E-12,-1.));
#17922=DIRECTION('',(1.,0.,0.));
#17923=DIRECTION('center_axis',(1.,0.,0.));
#17924=DIRECTION('ref_axis',(0.,-1.17203152359781E-12,-1.));
#17925=DIRECTION('',(1.,0.,0.));
#17926=DIRECTION('center_axis',(1.,0.,0.));
#17927=DIRECTION('ref_axis',(0.,-1.17203152359781E-12,-1.));
#17928=DIRECTION('',(1.,0.,0.));
#17929=DIRECTION('center_axis',(1.,0.,0.));
#17930=DIRECTION('ref_axis',(0.,-1.17203152359781E-12,-1.));
#17931=DIRECTION('',(1.,0.,0.));
#17932=DIRECTION('center_axis',(1.,0.,0.));
#17933=DIRECTION('ref_axis',(0.,-1.17203152359781E-12,-1.));
#17934=DIRECTION('',(1.,0.,0.));
#17935=DIRECTION('center_axis',(1.,0.,0.));
#17936=DIRECTION('ref_axis',(0.,-1.17203152359781E-12,-1.));
#17937=DIRECTION('',(1.,0.,0.));
#17938=DIRECTION('center_axis',(1.,0.,0.));
#17939=DIRECTION('ref_axis',(0.,-1.17203152359781E-12,-1.));
#17940=DIRECTION('',(1.,0.,0.));
#17941=DIRECTION('center_axis',(1.,0.,0.));
#17942=DIRECTION('ref_axis',(0.,-1.17203152359781E-12,-1.));
#17943=DIRECTION('',(1.,0.,0.));
#17944=DIRECTION('center_axis',(1.,0.,0.));
#17945=DIRECTION('ref_axis',(0.,0.,-1.));
#17946=DIRECTION('center_axis',(1.,0.,0.));
#17947=DIRECTION('ref_axis',(0.,0.,-1.));
#17948=DIRECTION('center_axis',(-1.,0.,0.));
#17949=DIRECTION('ref_axis',(0.,-1.17203152359781E-12,-1.));
#17950=DIRECTION('center_axis',(1.,0.,0.));
#17951=DIRECTION('ref_axis',(0.,0.,-1.));
#17952=DIRECTION('',(-1.,0.,0.));
#17953=DIRECTION('center_axis',(1.,0.,0.));
#17954=DIRECTION('ref_axis',(0.,0.,-1.));
#17955=DIRECTION('center_axis',(1.,0.,0.));
#17956=DIRECTION('ref_axis',(0.,0.,-1.));
#17957=DIRECTION('center_axis',(1.,0.,0.));
#17958=DIRECTION('ref_axis',(0.,-1.17203152359781E-12,-1.));
#17959=DIRECTION('center_axis',(0.,1.,0.));
#17960=DIRECTION('ref_axis',(0.,0.,1.));
#17961=DIRECTION('',(-1.,0.,0.));
#17962=DIRECTION('',(0.,0.,1.));
#17963=DIRECTION('',(1.,0.,0.));
#17964=DIRECTION('',(0.,0.,1.));
#17965=DIRECTION('center_axis',(1.,0.,0.));
#17966=DIRECTION('ref_axis',(0.,0.,-1.));
#17967=DIRECTION('center_axis',(-1.,0.,0.));
#17968=DIRECTION('ref_axis',(0.,0.,-1.));
#17969=DIRECTION('',(0.,-1.,0.));
#17970=DIRECTION('',(0.,0.,-1.));
#17971=DIRECTION('center_axis',(0.,0.,1.));
#17972=DIRECTION('ref_axis',(0.,-1.,0.));
#17973=DIRECTION('',(0.,-1.,0.));
#17974=DIRECTION('',(1.,0.,0.));
#17975=DIRECTION('center_axis',(0.,-1.,0.));
#17976=DIRECTION('ref_axis',(0.,0.,-1.));
#17977=DIRECTION('',(1.,0.,0.));
#17978=DIRECTION('',(0.,0.,-1.));
#17979=DIRECTION('center_axis',(1.,0.,0.));
#17980=DIRECTION('ref_axis',(0.,0.,-1.));
#17981=DIRECTION('center_axis',(1.,0.,0.));
#17982=DIRECTION('ref_axis',(0.,0.,-1.));
#17983=DIRECTION('center_axis',(1.,0.,0.));
#17984=DIRECTION('ref_axis',(0.,0.,-1.));
#17985=DIRECTION('center_axis',(1.,0.,0.));
#17986=DIRECTION('ref_axis',(0.,0.,-1.));
#17987=DIRECTION('',(-1.,0.,0.));
#17988=DIRECTION('center_axis',(-1.,0.,0.));
#17989=DIRECTION('ref_axis',(0.,0.,-1.));
#17990=DIRECTION('center_axis',(1.,0.,0.));
#17991=DIRECTION('ref_axis',(0.,0.,-1.));
#17992=DIRECTION('center_axis',(1.,0.,0.));
#17993=DIRECTION('ref_axis',(0.,0.,-1.));
#17994=DIRECTION('center_axis',(1.,0.,0.));
#17995=DIRECTION('ref_axis',(0.,0.,-1.));
#17996=DIRECTION('center_axis',(-1.,0.,0.));
#17997=DIRECTION('ref_axis',(0.,0.,-1.));
#17998=DIRECTION('center_axis',(1.,0.,0.));
#17999=DIRECTION('ref_axis',(0.,0.,-1.));
#18000=DIRECTION('center_axis',(1.,0.,0.));
#18001=DIRECTION('ref_axis',(0.,0.,-1.));
#18002=DIRECTION('',(-1.,0.,0.));
#18003=DIRECTION('center_axis',(1.,0.,0.));
#18004=DIRECTION('ref_axis',(0.,0.,-1.));
#18005=DIRECTION('center_axis',(1.,0.,0.));
#18006=DIRECTION('ref_axis',(0.,0.,-1.));
#23703=CARTESIAN_POINT('',(0.,0.,0.));
#23704=CARTESIAN_POINT('Origin',(4.,0.,4.));
#23705=CARTESIAN_POINT('',(4.12884541125756,8.40637486662632E-6,4.59405635738975));
#23706=CARTESIAN_POINT('',(4.02115458874249,-9.26662433349265E-6,4.59413599269206));
#23707=CARTESIAN_POINT('',(4.,-7.27562663373442E-17,4.5941));
#23708=CARTESIAN_POINT('',(4.,0.254721014554615,3.46322028700965));
#23709=CARTESIAN_POINT('Ctrl Pts',(4.12884541125756,8.40637486662632E-6,
4.59405635738975));
#23710=CARTESIAN_POINT('Ctrl Pts',(4.12564700130467,0.0398130654959074,
4.59407663624518));
#23711=CARTESIAN_POINT('Ctrl Pts',(4.12244859135178,0.079613792300143,4.59013569217808));
#23712=CARTESIAN_POINT('Ctrl Pts',(4.11925018139889,0.118599576779877,4.58219388355888));
#23713=CARTESIAN_POINT('Ctrl Pts',(4.11129754205509,0.215535206692688,4.56244709042845));
#23714=CARTESIAN_POINT('Ctrl Pts',(4.10334490271129,0.30743256945264,4.51796551073728));
#23715=CARTESIAN_POINT('Ctrl Pts',(4.09539226336748,0.383054411795556,4.45418672179759));
#23716=CARTESIAN_POINT('Ctrl Pts',(4.08743962402367,0.458676254138472,4.3904079328579));
#23717=CARTESIAN_POINT('Ctrl Pts',(4.07948698467986,0.518022576064352,4.30733193466969));
#23718=CARTESIAN_POINT('Ctrl Pts',(4.07153434533606,0.553840407547632,4.21511760274296));
#23719=CARTESIAN_POINT('Ctrl Pts',(4.06358170599225,0.589658239030912,4.12290327081622));
#23720=CARTESIAN_POINT('Ctrl Pts',(4.05562906664845,0.601947580071592,4.02155060515096));
#23721=CARTESIAN_POINT('Ctrl Pts',(4.04767642730464,0.589200356533535,3.92344812692479));
#23722=CARTESIAN_POINT('Ctrl Pts',(4.03972378796084,0.576453132995478,3.82534564869861));
#23723=CARTESIAN_POINT('Ctrl Pts',(4.03177114861703,0.538669344878685,3.73049335791153));
#23724=CARTESIAN_POINT('Ctrl Pts',(4.02381850927322,0.480479105222089,3.65049437695417));
#23725=CARTESIAN_POINT('Ctrl Pts',(4.01587900618215,0.422384984811151,3.57062753914914));
#23726=CARTESIAN_POINT('Ctrl Pts',(4.00793950309107,0.343951772361455,3.50556498199611));
#23727=CARTESIAN_POINT('Ctrl Pts',(4.,0.254721014554615,3.46322028700965));
#23728=CARTESIAN_POINT('',(4.,0.254694598474614,4.53673594206822));
#23729=CARTESIAN_POINT('Origin',(4.,0.,4.));
#23730=CARTESIAN_POINT('Ctrl Pts',(3.99999999999998,0.254694598474614,4.53673594206822));
#23731=CARTESIAN_POINT('Ctrl Pts',(4.00705152958082,0.175425736340139,4.5743509952638));
#23732=CARTESIAN_POINT('Ctrl Pts',(4.01410305916165,0.0876996967667308,
4.59405101338575));
#23733=CARTESIAN_POINT('Ctrl Pts',(4.02115458874249,-9.26662433349265E-6,
4.59413599269206));
#23734=CARTESIAN_POINT('Origin',(4.,0.,4.));
#23735=CARTESIAN_POINT('',(4.42884541125756,-2.46302091461148E-6,4.59415045696459));
#23736=CARTESIAN_POINT('',(4.32115458874249,3.58587963140688E-6,4.59404994535016));
#23737=CARTESIAN_POINT('',(4.,-7.27562663373442E-17,4.5941));
#23738=CARTESIAN_POINT('Ctrl Pts',(4.42884541125756,-2.46302091461148E-6,
4.59415045696459));
#23739=CARTESIAN_POINT('Ctrl Pts',(4.42107867343035,0.0966117732708647,
4.59412799973471));
#23740=CARTESIAN_POINT('Ctrl Pts',(4.41331193560314,0.193236775309615,4.57009608476161));
#23741=CARTESIAN_POINT('Ctrl Pts',(4.40554519777592,0.278573173318151,4.52479781884576));
#23742=CARTESIAN_POINT('Ctrl Pts',(4.39759255843212,0.36595214906825,4.47841531183407));
#23743=CARTESIAN_POINT('Ctrl Pts',(4.38963991908831,0.441495654419193,4.40973622444741));
#23744=CARTESIAN_POINT('Ctrl Pts',(4.3816872797445,0.495967466205845,4.32715751007026));
#23745=CARTESIAN_POINT('Ctrl Pts',(4.3737346404007,0.550439277992498,4.24457879569311));
#23746=CARTESIAN_POINT('Ctrl Pts',(4.36578200105689,0.58383939621486,4.14810045432546));
#23747=CARTESIAN_POINT('Ctrl Pts',(4.35782936171309,0.59208420294366,4.04951827803692));
#23748=CARTESIAN_POINT('Ctrl Pts',(4.34987672236928,0.600329009672459,3.95093610174838));
#23749=CARTESIAN_POINT('Ctrl Pts',(4.34192408302547,0.583418504907695,3.85025009053894));
#23750=CARTESIAN_POINT('Ctrl Pts',(4.33397144368167,0.54342022548472,3.75977047903001));
#23751=CARTESIAN_POINT('Ctrl Pts',(4.32601880433786,0.503421946061746,3.66929086752108));
#23752=CARTESIAN_POINT('Ctrl Pts',(4.31806616499406,0.440335891980562,3.58901765571266));
#23753=CARTESIAN_POINT('Ctrl Pts',(4.31011352565025,0.361875197644003,3.52876534000234));
#23754=CARTESIAN_POINT('Ctrl Pts',(4.30216088630644,0.283414503307443,3.46851302429202));
#23755=CARTESIAN_POINT('Ctrl Pts',(4.29420824696263,0.189579168715509,3.4282816046798));
#23756=CARTESIAN_POINT('Ctrl Pts',(4.28625560761883,0.0918418319479975,
3.41298991457491));
#23757=CARTESIAN_POINT('Ctrl Pts',(4.27830296827502,-0.00589550481951406,
3.39769822447003));
#23758=CARTESIAN_POINT('Ctrl Pts',(4.27035032893122,-0.107534843762603,
3.4073462638725));
#23759=CARTESIAN_POINT('Ctrl Pts',(4.26239768958741,-0.200649373295791,
3.44075443909651));
#23760=CARTESIAN_POINT('Ctrl Pts',(4.25444505024361,-0.293763902828979,
3.47416261432052));
#23761=CARTESIAN_POINT('Ctrl Pts',(4.24649241089979,-0.378353622952266,
3.53133092536608));
#23762=CARTESIAN_POINT('Ctrl Pts',(4.23853977155599,-0.444076322467606,
3.60526974769923));
#23763=CARTESIAN_POINT('Ctrl Pts',(4.23058713221218,-0.509799021982947,
3.67920857003239));
#23764=CARTESIAN_POINT('Ctrl Pts',(4.22263449286838,-0.556654700890342,
3.76991790365313));
#23765=CARTESIAN_POINT('Ctrl Pts',(4.21468185352458,-0.578914549750806,
3.86630733464992));
#23766=CARTESIAN_POINT('Ctrl Pts',(4.20672921418077,-0.601174398611269,
3.96269676564671));
#23767=CARTESIAN_POINT('Ctrl Pts',(4.19877657483696,-0.598838417424802,
4.06476629401955));
#23768=CARTESIAN_POINT('Ctrl Pts',(4.19082393549315,-0.5721923335546,4.16003645884502));
#23769=CARTESIAN_POINT('Ctrl Pts',(4.18287129614934,-0.545546249684398,
4.25530662367048));
#23770=CARTESIAN_POINT('Ctrl Pts',(4.17491865680554,-0.494590063130461,
4.34377742494856));
#23771=CARTESIAN_POINT('Ctrl Pts',(4.16696601746173,-0.425553631634784,
4.41463223618795));
#23772=CARTESIAN_POINT('Ctrl Pts',(4.15901337811793,-0.356517200139107,
4.48548704742733));
#23773=CARTESIAN_POINT('Ctrl Pts',(4.15106073877413,-0.269400523701689,
4.53872586862801));
#23774=CARTESIAN_POINT('Ctrl Pts',(4.14310809943032,-0.174855236950146,
4.56783927594351));
#23775=CARTESIAN_POINT('Ctrl Pts',(4.1383538700394,-0.118334381217266,4.5852437891806));
#23776=CARTESIAN_POINT('Ctrl Pts',(4.13359964064848,-0.0591586432141876,
4.59402621418361));
#23777=CARTESIAN_POINT('Ctrl Pts',(4.12884541125756,8.40637486662632E-6,
4.59405635738975));
#23778=CARTESIAN_POINT('Ctrl Pts',(4.02115458874249,-9.26662433349265E-6,
4.59413599269206));
#23779=CARTESIAN_POINT('Ctrl Pts',(4.02205569850546,-0.0112175303500608,
4.59414685213492));
#23780=CARTESIAN_POINT('Ctrl Pts',(4.02295680826843,-0.0224255152200988,
4.5938373961197));
#23781=CARTESIAN_POINT('Ctrl Pts',(4.0238579180314,-0.0336155370699344,
4.59320407706013));
#23782=CARTESIAN_POINT('Ctrl Pts',(4.03181055737521,-0.132371772633995,
4.58761479340425));
#23783=CARTESIAN_POINT('Ctrl Pts',(4.03976319671902,-0.229728915328813,
4.55680066053817));
#23784=CARTESIAN_POINT('Ctrl Pts',(4.04771583606282,-0.31374319278985,4.50455967689729));
#23785=CARTESIAN_POINT('Ctrl Pts',(4.05566847540663,-0.397757470250888,
4.4523186932564));
#23786=CARTESIAN_POINT('Ctrl Pts',(4.06362111475043,-0.468428882478145,
4.37865085884071));
#23787=CARTESIAN_POINT('Ctrl Pts',(4.07157375409424,-0.517135915630147,
4.29254879227412));
#23788=CARTESIAN_POINT('Ctrl Pts',(4.07952639343804,-0.565842948782149,
4.20644672570752));
#23789=CARTESIAN_POINT('Ctrl Pts',(4.08747903278185,-0.592585602858896,
4.10791042699003));
#23790=CARTESIAN_POINT('Ctrl Pts',(4.09543167212566,-0.594084460855775,
4.00899459728238));
#23791=CARTESIAN_POINT('Ctrl Pts',(4.10338431146947,-0.595583318852653,
3.91007876757474));
#23792=CARTESIAN_POINT('Ctrl Pts',(4.11133695081327,-0.571838380769662,
3.81078340687695));
#23793=CARTESIAN_POINT('Ctrl Pts',(4.11928959015708,-0.525757920758293,
3.72324489380985));
#23794=CARTESIAN_POINT('Ctrl Pts',(4.12724222950088,-0.479677460746923,
3.63570638074275));
#23795=CARTESIAN_POINT('Ctrl Pts',(4.13519486884469,-0.411261478807175,
3.55992471530633));
#23796=CARTESIAN_POINT('Ctrl Pts',(4.1431475081885,-0.328872047298013,3.50516726345229));
#23797=CARTESIAN_POINT('Ctrl Pts',(4.1511001475323,-0.246482615788851,3.45040981159825));
#23798=CARTESIAN_POINT('Ctrl Pts',(4.15905278687611,-0.150119734710276,
3.41667657332659));
#23799=CARTESIAN_POINT('Ctrl Pts',(4.16700542621992,-0.0515665150750243,
3.40809082437526));
#23800=CARTESIAN_POINT('Ctrl Pts',(4.17495806556372,0.0469867045602276,
3.39950507542393));
#23801=CARTESIAN_POINT('Ctrl Pts',(4.18291070490753,0.147730262752155,3.41606681579293));
#23802=CARTESIAN_POINT('Ctrl Pts',(4.19086334425134,0.238347648045887,3.45575171487277));
#23803=CARTESIAN_POINT('Ctrl Pts',(4.19881598359514,0.32896503333962,3.49543661395261));
#23804=CARTESIAN_POINT('Ctrl Pts',(4.20676862293895,0.409456245735157,3.55824467174328));
#23805=CARTESIAN_POINT('Ctrl Pts',(4.21472126228276,0.469979735422806,3.63649644709345));
#23806=CARTESIAN_POINT('Ctrl Pts',(4.22267390162656,0.530503225110456,3.71474822244363));
#23807=CARTESIAN_POINT('Ctrl Pts',(4.23062654097037,0.571058992090217,3.80844371535332));
#23808=CARTESIAN_POINT('Ctrl Pts',(4.23857918031417,0.586688754827568,3.90612753493601));
#23809=CARTESIAN_POINT('Ctrl Pts',(4.24653181965798,0.602318517564919,4.0038113545187));
#23810=CARTESIAN_POINT('Ctrl Pts',(4.25448445900178,0.593022276059861,4.10548350077438));
#23811=CARTESIAN_POINT('Ctrl Pts',(4.26243709834559,0.559936509464549,4.19871308474845));
#23812=CARTESIAN_POINT('Ctrl Pts',(4.2703897376894,0.526850742869238,4.29194266872251));
#23813=CARTESIAN_POINT('Ctrl Pts',(4.27834237703321,0.469975451183674,4.37672969041494));
#23814=CARTESIAN_POINT('Ctrl Pts',(4.28629501637701,0.396264473279151,4.44270782630825));
#23815=CARTESIAN_POINT('Ctrl Pts',(4.29424765572082,0.322553495374627,4.50868596220156));
#23816=CARTESIAN_POINT('Ctrl Pts',(4.30220029506462,0.232006831251144,4.55585521229574));
#23817=CARTESIAN_POINT('Ctrl Pts',(4.31015293440843,0.135695012128791,4.57844846968215));
#23818=CARTESIAN_POINT('Ctrl Pts',(4.31382015251978,0.0912825306677821,
4.58886694826517));
#23819=CARTESIAN_POINT('Ctrl Pts',(4.31748737063114,0.0456441298716245,
4.59405951624442));
#23820=CARTESIAN_POINT('Ctrl Pts',(4.32115458874249,3.58587963140688E-6,
4.59404994535016));
#23821=CARTESIAN_POINT('Origin',(4.,0.,4.));
#23822=CARTESIAN_POINT('',(4.72884541125756,-4.67700812217808E-6,4.59405084457266));
#23823=CARTESIAN_POINT('',(4.62115458874249,3.7232086238465E-6,4.59414939806979));
#23824=CARTESIAN_POINT('',(4.,-7.27562663373442E-17,4.5941));
#23825=CARTESIAN_POINT('Ctrl Pts',(4.72884541125756,-4.67700812217808E-6,
4.59405084457266));
#23826=CARTESIAN_POINT('Ctrl Pts',(4.72446298489983,0.0545367878429411,
4.59403588702548));
#23827=CARTESIAN_POINT('Ctrl Pts',(4.7200805585421,0.10908225468116,4.58659074407712));
#23828=CARTESIAN_POINT('Ctrl Pts',(4.71569813218437,0.16154350694756,4.57176871113812));
#23829=CARTESIAN_POINT('Ctrl Pts',(4.70774549284056,0.256743148594298,4.54487167450041));
#23830=CARTESIAN_POINT('Ctrl Pts',(4.69979285349676,0.345079446524661,4.4936824501733));
#23831=CARTESIAN_POINT('Ctrl Pts',(4.69184021415295,0.415752085200636,4.42445961801412));
#23832=CARTESIAN_POINT('Ctrl Pts',(4.68388757480915,0.486424723876611,4.35523678585494));
#23833=CARTESIAN_POINT('Ctrl Pts',(4.67593493546534,0.539433703298198,4.26798034586369));
#23834=CARTESIAN_POINT('Ctrl Pts',(4.66798229612153,0.568297953762936,4.17335858623793));
#23835=CARTESIAN_POINT('Ctrl Pts',(4.66002965677773,0.597162204227674,4.07873682661218));
#23836=CARTESIAN_POINT('Ctrl Pts',(4.65207701743392,0.601881725735563,3.97674974735193));
#23837=CARTESIAN_POINT('Ctrl Pts',(4.64412437809011,0.581879492504365,3.87986665793328));
#23838=CARTESIAN_POINT('Ctrl Pts',(4.63617173874631,0.561877259273167,3.78298356851463));
#23839=CARTESIAN_POINT('Ctrl Pts',(4.6282190994025,0.517153271302883,3.69120446893757));
#23840=CARTESIAN_POINT('Ctrl Pts',(4.6202664600587,0.453175645250056,3.61575060413089));
#23841=CARTESIAN_POINT('Ctrl Pts',(4.61231382071489,0.389198019197228,3.5402967393242));
#23842=CARTESIAN_POINT('Ctrl Pts',(4.60436118137108,0.305966755061857,3.48116810928789));
#23843=CARTESIAN_POINT('Ctrl Pts',(4.59640854202727,0.213658008474022,3.4455939943611));
#23844=CARTESIAN_POINT('Ctrl Pts',(4.58845590268347,0.121349261886187,3.41001987943431));
#23845=CARTESIAN_POINT('Ctrl Pts',(4.58050326333966,0.0199630328458878,
3.39800027961704));
#23846=CARTESIAN_POINT('Ctrl Pts',(4.57255062399586,-0.0781048312986516,
3.41100475468789));
#23847=CARTESIAN_POINT('Ctrl Pts',(4.56459798465205,-0.17617269544319,3.42400922975875));
#23848=CARTESIAN_POINT('Ctrl Pts',(4.55664534530825,-0.270922194691968,
3.46203777971774));
#23849=CARTESIAN_POINT('Ctrl Pts',(4.54869270596444,-0.350768912290741,
3.52044089639904));
#23850=CARTESIAN_POINT('Ctrl Pts',(4.54074006662063,-0.430615629889515,
3.57884401308035));
#23851=CARTESIAN_POINT('Ctrl Pts',(4.53278742727683,-0.495559565838284,
3.65762169648397));
#23852=CARTESIAN_POINT('Ctrl Pts',(4.52483478793302,-0.537660439465301,
3.74714230187364));
#23853=CARTESIAN_POINT('Ctrl Pts',(4.51688214858921,-0.579761313092318,
3.8366629072633));
#23854=CARTESIAN_POINT('Ctrl Pts',(4.50892950924541,-0.599019124397585,
3.936926434639));
#23855=CARTESIAN_POINT('Ctrl Pts',(4.5009768699016,-0.593079343631488,4.03567430223551));
#23856=CARTESIAN_POINT('Ctrl Pts',(4.49302423055779,-0.587139562865391,
4.13442216983203));
#23857=CARTESIAN_POINT('Ctrl Pts',(4.48507159121399,-0.556002190027932,
4.23165437764937));
#23858=CARTESIAN_POINT('Ctrl Pts',(4.47711895187018,-0.503474193090318,
4.31548296397124));
#23859=CARTESIAN_POINT('Ctrl Pts',(4.46916631252638,-0.450946196152703,
4.39931155029312));
#23860=CARTESIAN_POINT('Ctrl Pts',(4.46121367318257,-0.377027575114933,
4.46973651511953));
#23861=CARTESIAN_POINT('Ctrl Pts',(4.45326103383876,-0.290755888038263,
4.51814744739689));
#23862=CARTESIAN_POINT('Ctrl Pts',(4.44530839449495,-0.204484200961595,
4.56655837967425));
#23863=CARTESIAN_POINT('Ctrl Pts',(4.43735575515115,-0.105859447846027,
4.59295527940255));
#23864=CARTESIAN_POINT('Ctrl Pts',(4.42940311580734,-0.00693984821361558,
4.59411076594835));
#23865=CARTESIAN_POINT('Ctrl Pts',(4.42921721429075,-0.0046274959494805,
4.59413777669183));
#23866=CARTESIAN_POINT('Ctrl Pts',(4.42903131277416,-0.00231498256911503,
4.59415099449182));
#23867=CARTESIAN_POINT('Ctrl Pts',(4.42884541125756,-2.46302091461148E-6,
4.59415045696459));
#23868=CARTESIAN_POINT('Ctrl Pts',(4.32115458874249,3.58587963140688E-6,
4.59404994535016));
#23869=CARTESIAN_POINT('Ctrl Pts',(4.32544000997495,-0.0533308355660028,
4.59403876103764));
#23870=CARTESIAN_POINT('Ctrl Pts',(4.3297254312074,-0.106668183692779,4.58692369872924));
#23871=CARTESIAN_POINT('Ctrl Pts',(4.33401085243985,-0.158055593105036,
4.57274269264177));
#23872=CARTESIAN_POINT('Ctrl Pts',(4.34196349178366,-0.253417405095285,
4.54642639353635));
#23873=CARTESIAN_POINT('Ctrl Pts',(4.34991613112746,-0.342064054954561,
4.49577653064689));
#23874=CARTESIAN_POINT('Ctrl Pts',(4.35786877047127,-0.413157291282808,
4.42698573291487));
#23875=CARTESIAN_POINT('Ctrl Pts',(4.36582140981507,-0.484250527611055,
4.35819493518285));
#23876=CARTESIAN_POINT('Ctrl Pts',(4.37377404915888,-0.537790350408272,
4.27126320260829));
#23877=CARTESIAN_POINT('Ctrl Pts',(4.38172668850269,-0.567230782432438,
4.17681912699824));
#23878=CARTESIAN_POINT('Ctrl Pts',(4.3896793278465,-0.596671214456604,4.0823750513882));
#23879=CARTESIAN_POINT('Ctrl Pts',(4.3976319671903,-0.602012255707717,3.98041863274268));
#23880=CARTESIAN_POINT('Ctrl Pts',(4.40558460653411,-0.582600893642323,
3.88341542999892));
#23881=CARTESIAN_POINT('Ctrl Pts',(4.41353724587791,-0.563189531576929,
3.78641222725516));
#23882=CARTESIAN_POINT('Ctrl Pts',(4.42148988522172,-0.519025766195027,
3.69436224041317));
#23883=CARTESIAN_POINT('Ctrl Pts',(4.42944252456553,-0.455509217992651,
3.61851983504546));
#23884=CARTESIAN_POINT('Ctrl Pts',(4.43739516390933,-0.391992669790276,
3.54267742967776));
#23885=CARTESIAN_POINT('Ctrl Pts',(4.44534780325314,-0.309123338767427,
3.48304260578434));
#23886=CARTESIAN_POINT('Ctrl Pts',(4.45330044259694,-0.217033129998519,
3.44690653227429));
#23887=CARTESIAN_POINT('Ctrl Pts',(4.46125308194075,-0.12494292122961,3.41077045876423));
#23888=CARTESIAN_POINT('Ctrl Pts',(4.46920572128456,-0.0236318347146405,
3.39813313563753));
#23889=CARTESIAN_POINT('Ctrl Pts',(4.47715836062837,0.074513469760962,3.41053964803971));
#23890=CARTESIAN_POINT('Ctrl Pts',(4.48511099997217,0.172658774236564,3.42294616044189));
#23891=CARTESIAN_POINT('Ctrl Pts',(4.49306363931598,0.2676382966728,3.46039650837296));
#23892=CARTESIAN_POINT('Ctrl Pts',(4.50101627865978,0.34783949666059,3.51831187658845));
#23893=CARTESIAN_POINT('Ctrl Pts',(4.50896891800359,0.428040696648381,3.57622724480394));
#23894=CARTESIAN_POINT('Ctrl Pts',(4.51692155734739,0.493463574187728,3.65460763330386));
#23895=CARTESIAN_POINT('Ctrl Pts',(4.5248741966912,0.536109291561612,3.74386997215216));
#23896=CARTESIAN_POINT('Ctrl Pts',(4.53282683603501,0.578755008935497,3.83313231100046));
#23897=CARTESIAN_POINT('Ctrl Pts',(4.54077947537881,0.598623566143919,3.93327660019715));
#23898=CARTESIAN_POINT('Ctrl Pts',(4.54873211472262,0.593285761408823,4.03205883640902));
#23899=CARTESIAN_POINT('Ctrl Pts',(4.55668475406643,0.587947956673727,4.1308410726209));
#23900=CARTESIAN_POINT('Ctrl Pts',(4.56463739341024,0.557403789995114,4.22826125584796));
#23901=CARTESIAN_POINT('Ctrl Pts',(4.57259003275404,0.505387701781775,4.31240844187621));
#23902=CARTESIAN_POINT('Ctrl Pts',(4.58054267209785,0.453371613568435,4.39655562790445));
#23903=CARTESIAN_POINT('Ctrl Pts',(4.58849531144165,0.37988360382037,4.46742981673387));
#23904=CARTESIAN_POINT('Ctrl Pts',(4.59644795078546,0.293908582600447,4.51636567348148));
#23905=CARTESIAN_POINT('Ctrl Pts',(4.60440059012926,0.207933561380525,4.56530153022909));
#23906=CARTESIAN_POINT('Ctrl Pts',(4.61235322947307,0.109471528688745,4.59229905489488));
#23907=CARTESIAN_POINT('Ctrl Pts',(4.62030586881688,0.01056080905581,4.59405743239568));
#23908=CARTESIAN_POINT('Ctrl Pts',(4.62058877545875,0.00704216595801619,
4.59411998479525));
#23909=CARTESIAN_POINT('Ctrl Pts',(4.62087168210062,0.00352295504485493,
4.59415059693914));
#23910=CARTESIAN_POINT('Ctrl Pts',(4.62115458874249,3.7232086238465E-6,
4.59414939806979));
#23911=CARTESIAN_POINT('Origin',(4.,0.,4.));
#23912=CARTESIAN_POINT('',(5.02884541125756,1.1583539301252E-5,4.59413174414479));
#23913=CARTESIAN_POINT('',(4.92115458874249,-9.52916733652962E-6,4.59405847898621));
#23914=CARTESIAN_POINT('',(4.,-7.27562663373442E-17,4.5941));
#23915=CARTESIAN_POINT('Ctrl Pts',(5.02884541125756,1.1583539301252E-5,
4.59413174414479));
#23916=CARTESIAN_POINT('Ctrl Pts',(5.02784729636931,0.0124287555737821,
4.59414271605904));
#23917=CARTESIAN_POINT('Ctrl Pts',(5.02684918148107,0.024845254523583,4.59376142828251));
#23918=CARTESIAN_POINT('Ctrl Pts',(5.02585106659282,0.0372368329321061,
4.59298328977014));
#23919=CARTESIAN_POINT('Ctrl Pts',(5.01789842724901,0.135968707532707,4.58678334723719));
#23920=CARTESIAN_POINT('Ctrl Pts',(5.00994578790521,0.233118536601742,4.55538989360237));
#23921=CARTESIAN_POINT('Ctrl Pts',(5.0019931485614,0.316808430381418,4.50264120614281));
#23922=CARTESIAN_POINT('Ctrl Pts',(4.9940405092176,0.400498324161095,4.44989251868324));
#23923=CARTESIAN_POINT('Ctrl Pts',(4.98608786987379,0.470728282651411,4.37578859739892));
#23924=CARTESIAN_POINT('Ctrl Pts',(4.97813523052998,0.518911736914097,4.289389655942));
#23925=CARTESIAN_POINT('Ctrl Pts',(4.97018259118617,0.567095191176782,4.20299071448508));
#23926=CARTESIAN_POINT('Ctrl Pts',(4.96222995184237,0.593232141211837,4.10429675285556));
#23927=CARTESIAN_POINT('Ctrl Pts',(4.95427731249856,0.594126988899363,4.00537445204741));
#23928=CARTESIAN_POINT('Ctrl Pts',(4.94632467315476,0.595021836586889,3.90645215123927));
#23929=CARTESIAN_POINT('Ctrl Pts',(4.93837203381095,0.570674581926886,3.80730151125251));
#23930=CARTESIAN_POINT('Ctrl Pts',(4.93041939446714,0.524062008404491,3.72004504823011));
#23931=CARTESIAN_POINT('Ctrl Pts',(4.92246675512334,0.477449434882097,3.6327885852077));
#23932=CARTESIAN_POINT('Ctrl Pts',(4.91451411577953,0.408571542497308,3.55742629914966));
#23933=CARTESIAN_POINT('Ctrl Pts',(4.90656147643572,0.325849591692228,3.50317225594031));
#23934=CARTESIAN_POINT('Ctrl Pts',(4.89860883709192,0.243127640887147,3.44891821273095));
#23935=CARTESIAN_POINT('Ctrl Pts',(4.89065619774811,0.146561631661773,3.41577241237029));
#23936=CARTESIAN_POINT('Ctrl Pts',(4.88270355840431,0.0479580738465473,
3.40778738038914));
#23937=CARTESIAN_POINT('Ctrl Pts',(4.8747509190605,-0.0506454839686783,
3.39980234840799));
#23938=CARTESIAN_POINT('Ctrl Pts',(4.86679827971669,-0.151286590373755,
3.41697808480634));
#23939=CARTESIAN_POINT('Ctrl Pts',(4.85884564037289,-0.241660499406316,
3.45721462188069));
#23940=CARTESIAN_POINT('Ctrl Pts',(4.85089300102908,-0.332034408438876,
3.49745115895503));
#23941=CARTESIAN_POINT('Ctrl Pts',(4.84294036168527,-0.41214112009892,3.56074849670536));
#23942=CARTESIAN_POINT('Ctrl Pts',(4.83498772234147,-0.472186497854497,
3.63936767349926));
#23943=CARTESIAN_POINT('Ctrl Pts',(4.82703508299766,-0.532231875610076,
3.71798685029316));
#23944=CARTESIAN_POINT('Ctrl Pts',(4.81908244365386,-0.572215919461187,
3.81192786613063));
#23945=CARTESIAN_POINT('Ctrl Pts',(4.81112980431005,-0.587250035475296,
3.9097051523746));
#23946=CARTESIAN_POINT('Ctrl Pts',(4.80317716496624,-0.602284151489406,
4.00748243861856));
#23947=CARTESIAN_POINT('Ctrl Pts',(4.79522452562244,-0.592368339666514,
4.10909599526903));
#23948=CARTESIAN_POINT('Ctrl Pts',(4.78727188627863,-0.558714943052599,
4.20212218107662));
#23949=CARTESIAN_POINT('Ctrl Pts',(4.77931924693482,-0.525061546438685,
4.2951483668842));
#23950=CARTESIAN_POINT('Ctrl Pts',(4.77136660759101,-0.467670565033749,
4.37958718184891));
#23951=CARTESIAN_POINT('Ctrl Pts',(4.76341396824721,-0.393558827964045,
4.44511483080773));
#23952=CARTESIAN_POINT('Ctrl Pts',(4.7554613289034,-0.319447090894342,4.51064247976655));
#23953=CARTESIAN_POINT('Ctrl Pts',(4.7475086895596,-0.228614598159871,4.55725896271948));
#23954=CARTESIAN_POINT('Ctrl Pts',(4.73955605021579,-0.13216685911108,4.5792647797218));
#23955=CARTESIAN_POINT('Ctrl Pts',(4.73598583722972,-0.0888681559330128,
4.58914394690572));
#23956=CARTESIAN_POINT('Ctrl Pts',(4.73241562424364,-0.0444377444908,4.59406302997518));
#23957=CARTESIAN_POINT('Ctrl Pts',(4.72884541125756,-4.67700812217808E-6,
4.59405084457266));
#23958=CARTESIAN_POINT('Ctrl Pts',(4.62115458874249,3.7232086238465E-6,
4.59414939806979));
#23959=CARTESIAN_POINT('Ctrl Pts',(4.62882432144443,-0.0954043143036648,
4.59411689615543));
#23960=CARTESIAN_POINT('Ctrl Pts',(4.63649405414636,-0.190827729806029,
4.57070400848325));
#23961=CARTESIAN_POINT('Ctrl Pts',(4.6441637868483,-0.275369369969159,4.52648596729292));
#23962=CARTESIAN_POINT('Ctrl Pts',(4.65211642619211,-0.363029422787103,
4.48063689435358));
#23963=CARTESIAN_POINT('Ctrl Pts',(4.66006906553591,-0.438990121848901,
4.4124195181391));
#23964=CARTESIAN_POINT('Ctrl Pts',(4.66802170487971,-0.493964237128006,
4.33017434199545));
#23965=CARTESIAN_POINT('Ctrl Pts',(4.67597434422352,-0.548938352407109,
4.24792916585179));
#23966=CARTESIAN_POINT('Ctrl Pts',(4.68392698356733,-0.582925883903521,
4.15165618977896));
#23967=CARTESIAN_POINT('Ctrl Pts',(4.69187962291114,-0.591771392992132,
4.05312609631255));
#23968=CARTESIAN_POINT('Ctrl Pts',(4.69983226225494,-0.600616902080743,
3.95459600284613));
#23969=CARTESIAN_POINT('Ctrl Pts',(4.70778490159875,-0.584320388761555,
3.85380879198612));
#23970=CARTESIAN_POINT('Ctrl Pts',(4.71573754094256,-0.544874323741249,
3.76308707295491));
#23971=CARTESIAN_POINT('Ctrl Pts',(4.72369018028636,-0.505428258720944,
3.6723653539237));
#23972=CARTESIAN_POINT('Ctrl Pts',(4.73164281963017,-0.442832641999522,
3.59170912672127));
#23973=CARTESIAN_POINT('Ctrl Pts',(4.73959545897397,-0.364740640256699,
3.53097971363863));
#23974=CARTESIAN_POINT('Ctrl Pts',(4.74754809831778,-0.286648638513876,
3.47025030055599));
#23975=CARTESIAN_POINT('Ctrl Pts',(4.75550073766158,-0.193060251749651,
3.42944770159313));
#23976=CARTESIAN_POINT('Ctrl Pts',(4.76345337700539,-0.095417934894009,
3.41356059019365));
#23977=CARTESIAN_POINT('Ctrl Pts',(4.7714060163492,0.00222438196163176,
3.39767347879416));
#23978=CARTESIAN_POINT('Ctrl Pts',(4.77935865569301,0.10392062890869,3.40670185495805));
#23979=CARTESIAN_POINT('Ctrl Pts',(4.78731129503681,0.19723705468272,3.43954187673519));
#23980=CARTESIAN_POINT('Ctrl Pts',(4.79526393438062,0.290553480456751,3.47238189851233));
#23981=CARTESIAN_POINT('Ctrl Pts',(4.80321657372443,0.375490085057754,3.52903356590271));
#23982=CARTESIAN_POINT('Ctrl Pts',(4.81116921306823,0.441662211759978,3.60257044098769));
#23983=CARTESIAN_POINT('Ctrl Pts',(4.81912185241204,0.507834338462201,3.67610731607267));
#23984=CARTESIAN_POINT('Ctrl Pts',(4.82707449175584,0.555241987265645,3.76652939885225));
#23985=CARTESIAN_POINT('Ctrl Pts',(4.83502713109965,0.57808892742485,3.86278135818256));
#23986=CARTESIAN_POINT('Ctrl Pts',(4.84297977044346,0.600935867584054,3.95903331751286));
#23987=CARTESIAN_POINT('Ctrl Pts',(4.85093240978726,0.599222099099018,4.0611151533939));
#23988=CARTESIAN_POINT('Ctrl Pts',(4.85888504913107,0.573157153508111,4.15654597106253));
#23989=CARTESIAN_POINT('Ctrl Pts',(4.86683768847488,0.547092207917203,4.25197678873116));
#23990=CARTESIAN_POINT('Ctrl Pts',(4.87479032781868,0.496676085220424,4.34075658818739));
#23991=CARTESIAN_POINT('Ctrl Pts',(4.88274296716249,0.428072843071251,4.41203082979109));
#23992=CARTESIAN_POINT('Ctrl Pts',(4.89069560650629,0.359469600922078,4.48330507139479));
#23993=CARTESIAN_POINT('Ctrl Pts',(4.8986482458501,0.272679239320511,4.53707375514596));
#23994=CARTESIAN_POINT('Ctrl Pts',(4.90660088519391,0.178313062033339,4.56676292714126));
#23995=CARTESIAN_POINT('Ctrl Pts',(4.9114521197101,0.120748216373203,4.58487378690922));
#23996=CARTESIAN_POINT('Ctrl Pts',(4.9163033542263,0.0603642649825261,4.59402420038378));
#23997=CARTESIAN_POINT('Ctrl Pts',(4.92115458874249,-9.52916733652962E-6,
4.59405847898621));
#23998=CARTESIAN_POINT('Origin',(4.,0.,4.));
#23999=CARTESIAN_POINT('',(5.32884541125756,-1.45357002139801E-5,4.59407911932661));
#24000=CARTESIAN_POINT('',(5.22115458874249,1.46139895546772E-5,4.59411444380891));
#24001=CARTESIAN_POINT('',(4.,-7.27562663373442E-17,4.5941));
#24002=CARTESIAN_POINT('Ctrl Pts',(5.32884541125756,-1.45357002139801E-5,
4.59407911932661));
#24003=CARTESIAN_POINT('Ctrl Pts',(5.32327896849499,0.0692531541268509,
4.59401614001471));
#24004=CARTESIAN_POINT('Ctrl Pts',(5.31771252573242,0.138542285837495,4.5819075943171));
#24005=CARTESIAN_POINT('Ctrl Pts',(5.31214608296985,0.203593590158122,4.55818044906639));
#24006=CARTESIAN_POINT('Ctrl Pts',(5.30419344362604,0.296530782575621,4.5242820624512));
#24007=CARTESIAN_POINT('Ctrl Pts',(5.29624080428224,0.380818089806801,4.46666879957728));
#24008=CARTESIAN_POINT('Ctrl Pts',(5.28828816493843,0.446150240572578,4.39238466650784));
#24009=CARTESIAN_POINT('Ctrl Pts',(5.28033552559462,0.511482391338355,4.3181005334384));
#24010=CARTESIAN_POINT('Ctrl Pts',(5.27238288625081,0.557859385638729,4.22714553017344));
#24011=CARTESIAN_POINT('Ctrl Pts',(5.26443024690701,0.579611004278495,4.13064014464439));
#24012=CARTESIAN_POINT('Ctrl Pts',(5.2564776075632,0.601362622918262,4.03413475911534));
#24013=CARTESIAN_POINT('Ctrl Pts',(5.2485249682194,0.598488865897423,3.93207899132219));
#24014=CARTESIAN_POINT('Ctrl Pts',(5.24057232887559,0.571341089151559,3.8369505488493));
#24015=CARTESIAN_POINT('Ctrl Pts',(5.23261968953179,0.544193312405696,3.74182210637642));
#24016=CARTESIAN_POINT('Ctrl Pts',(5.22466705018798,0.492771515934809,3.65362098922379));
#24017=CARTESIAN_POINT('Ctrl Pts',(5.21671441084417,0.423362714708271,3.58313098523844));
#24018=CARTESIAN_POINT('Ctrl Pts',(5.20876177150037,0.353953913481732,3.51264098125308));
#24019=CARTESIAN_POINT('Ctrl Pts',(5.20080913215656,0.266558107499543,3.45986209043499));
#24020=CARTESIAN_POINT('Ctrl Pts',(5.19285649281275,0.171860624350003,3.43124725102074));
#24021=CARTESIAN_POINT('Ctrl Pts',(5.18490385346895,0.0771631412004631,
3.40263241160649));
#24022=CARTESIAN_POINT('Ctrl Pts',(5.17695121412514,-0.0248360191164267,
3.39818162359609));
#24023=CARTESIAN_POINT('Ctrl Pts',(5.16899857478133,-0.121666070051256,
3.41843905644231));
#24024=CARTESIAN_POINT('Ctrl Pts',(5.16104593543753,-0.218496120986084,
3.43869648928852));
#24025=CARTESIAN_POINT('Ctrl Pts',(5.15309329609372,-0.310157062538852,
3.48366214299137));
#24026=CARTESIAN_POINT('Ctrl Pts',(5.14514065674991,-0.385442096207774,
3.54783835396576));
#24027=CARTESIAN_POINT('Ctrl Pts',(5.13718801740611,-0.460727129876697,
3.61201456494015));
#24028=CARTESIAN_POINT('Ctrl Pts',(5.1292353780623,-0.519636255661773,3.6954013331861));
#24029=CARTESIAN_POINT('Ctrl Pts',(5.1212827387185,-0.554967030609594,3.78780349058054));
#24030=CARTESIAN_POINT('Ctrl Pts',(5.11333009937469,-0.590297805557415,
3.88020564797498));
#24031=CARTESIAN_POINT('Ctrl Pts',(5.10537746003088,-0.60205022966798,3.98162319451792));
#24032=CARTESIAN_POINT('Ctrl Pts',(5.09742482068708,-0.588787409028971,
4.07965645386523));
#24033=CARTESIAN_POINT('Ctrl Pts',(5.08947218134327,-0.575524588389962,
4.17768971321255));
#24034=CARTESIAN_POINT('Ctrl Pts',(5.08151954199946,-0.537246523001379,
4.27233868536424));
#24035=CARTESIAN_POINT('Ctrl Pts',(5.07356690265566,-0.47863322769376,4.35203124438164));
#24036=CARTESIAN_POINT('Ctrl Pts',(5.06561426331185,-0.42001993238614,4.43172380339905));
#24037=CARTESIAN_POINT('Ctrl Pts',(5.05766162396805,-0.341071407159484,
4.49645994928216));
#24038=CARTESIAN_POINT('Ctrl Pts',(5.04970898462424,-0.251440184480074,
4.53832480650817));
#24039=CARTESIAN_POINT('Ctrl Pts',(5.04275446016868,-0.1730583412759,4.5749353153996));
#24040=CARTESIAN_POINT('Ctrl Pts',(5.03579993571312,-0.0865070403179845,
4.59405529558476));
#24041=CARTESIAN_POINT('Ctrl Pts',(5.02884541125756,1.1583539301252E-5,
4.59413174414479));
#24042=CARTESIAN_POINT('Ctrl Pts',(4.92115458874249,-9.52916733652962E-6,
4.59405847898621));
#24043=CARTESIAN_POINT('Ctrl Pts',(4.9242559935701,-0.0386066277022544,
4.59408039337166));
#24044=CARTESIAN_POINT('Ctrl Pts',(4.92735739839772,-0.0771995748988638,
4.59037647703175));
#24045=CARTESIAN_POINT('Ctrl Pts',(4.93045880322533,-0.115049119822012,
4.58290605049323));
#24046=CARTESIAN_POINT('Ctrl Pts',(4.93841144256913,-0.212103131417409,
4.56375034161047));
#24047=CARTESIAN_POINT('Ctrl Pts',(4.94636408191294,-0.304269161635426,
4.51982926360553));
#24048=CARTESIAN_POINT('Ctrl Pts',(4.95431672125675,-0.380278658005779,
4.45651276645759));
#24049=CARTESIAN_POINT('Ctrl Pts',(4.96226936060055,-0.456288154376132,
4.39319626930964));
#24050=CARTESIAN_POINT('Ctrl Pts',(4.97022199994436,-0.516141116898821,
4.31048435301868));
#24051=CARTESIAN_POINT('Ctrl Pts',(4.97817463928816,-0.552519705724467,
4.21848967586497));
#24052=CARTESIAN_POINT('Ctrl Pts',(4.98612727863197,-0.588898294550112,
4.12649499871126));
#24053=CARTESIAN_POINT('Ctrl Pts',(4.99407991797578,-0.601802509678713,
4.0252175606948));
#24054=CARTESIAN_POINT('Ctrl Pts',(5.00203255731958,-0.589654635058918,
3.92703990798411));
#24055=CARTESIAN_POINT('Ctrl Pts',(5.00998519666339,-0.577506760439122,
3.82886225527341));
#24056=CARTESIAN_POINT('Ctrl Pts',(5.0179378360072,-0.540306796070929,3.73378438786847));
#24057=CARTESIAN_POINT('Ctrl Pts',(5.025890475351,-0.482602944251693,3.65343086999412));
#24058=CARTESIAN_POINT('Ctrl Pts',(5.03384311469481,-0.424899092432456,
3.57307735211977));
#24059=CARTESIAN_POINT('Ctrl Pts',(5.04179575403862,-0.346691353162178,
3.50744818377599));
#24060=CARTESIAN_POINT('Ctrl Pts',(5.04974839338242,-0.257541687734669,
3.46456742464414));
#24061=CARTESIAN_POINT('Ctrl Pts',(5.05770103272623,-0.16839202230716,3.42168666551229));
#24062=CARTESIAN_POINT('Ctrl Pts',(5.06565367207003,-0.0683004307224215,
3.40155431559236));
#24063=CARTESIAN_POINT('Ctrl Pts',(5.07360631141384,0.0304955267282049,
3.40663182885918));
#24064=CARTESIAN_POINT('Ctrl Pts',(5.08155895075765,0.129291484178831,3.41170934212599));
#24065=CARTESIAN_POINT('Ctrl Pts',(5.08951159010146,0.226791807495345,3.44199671857955));
#24066=CARTESIAN_POINT('Ctrl Pts',(5.09746422944526,0.311075754224562,3.49379091394262));
#24067=CARTESIAN_POINT('Ctrl Pts',(5.10541686878907,0.395359700953779,3.54558510930568));
#24068=CARTESIAN_POINT('Ctrl Pts',(5.11336950813287,0.466427271095698,3.61888612357825));
#24069=CARTESIAN_POINT('Ctrl Pts',(5.12132214747668,0.515589486279599,3.70473190942573));
#24070=CARTESIAN_POINT('Ctrl Pts',(5.12927478682048,0.564751701463499,3.79057769527322));
#24071=CARTESIAN_POINT('Ctrl Pts',(5.13722742616429,0.592008561689381,3.88896825269562));
#24072=CARTESIAN_POINT('Ctrl Pts',(5.1451800655081,0.594027544563649,3.98787399599556));
#24073=CARTESIAN_POINT('Ctrl Pts',(5.1531327048519,0.596046527437917,4.0867797392955));
#24074=CARTESIAN_POINT('Ctrl Pts',(5.16108534419571,0.572827632960568,4.18620066847299));
#24075=CARTESIAN_POINT('Ctrl Pts',(5.16903798353952,0.527209687216453,4.2739812208502));
#24076=CARTESIAN_POINT('Ctrl Pts',(5.17699062288332,0.481591741472338,4.3617617732274));
#24077=CARTESIAN_POINT('Ctrl Pts',(5.18494326222713,0.413574744461461,4.43790194880433));
#24078=CARTESIAN_POINT('Ctrl Pts',(5.19289590157094,0.331474700441294,4.49309257410834));
#24079=CARTESIAN_POINT('Ctrl Pts',(5.20084854091474,0.24937465642113,4.54828319941234));
#24080=CARTESIAN_POINT('Ctrl Pts',(5.20880118025855,0.153191565391677,4.58252427444343));
#24081=CARTESIAN_POINT('Ctrl Pts',(5.21675381960235,0.0546851202186884,
4.59162936142496));
#24082=CARTESIAN_POINT('Ctrl Pts',(5.21822074264906,0.0365148790664279,
4.59330886194775));
#24083=CARTESIAN_POINT('Ctrl Pts',(5.21968766569578,0.018265586889787,4.59413312238171));
#24084=CARTESIAN_POINT('Ctrl Pts',(5.22115458874249,1.46139895546772E-5,
4.59411444380891));
#24085=CARTESIAN_POINT('Origin',(4.,0.,4.));
#24086=CARTESIAN_POINT('',(5.62884541125756,1.52328526200479E-5,4.59408648697874));
#24087=CARTESIAN_POINT('',(5.52115458874249,-1.55733839743342E-5,4.59409663347568));
#24088=CARTESIAN_POINT('',(4.,-7.27562663373442E-17,4.5941));
#24089=CARTESIAN_POINT('Ctrl Pts',(5.62884541125756,1.52328526200479E-5,
4.59408648697874));
#24090=CARTESIAN_POINT('Ctrl Pts',(5.62666327996447,0.0271682673899915,
4.59411287463303));
#24091=CARTESIAN_POINT('Ctrl Pts',(5.62448114867138,0.054317778225707,4.59228554395034));
#24092=CARTESIAN_POINT('Ctrl Pts',(5.62229901737829,0.0812075234320336,
4.58857548522516));
#24093=CARTESIAN_POINT('Ctrl Pts',(5.61434637803449,0.179205497408217,4.57505441109036));
#24094=CARTESIAN_POINT('Ctrl Pts',(5.60639373869068,0.273753285393806,4.53652709601604));
#24095=CARTESIAN_POINT('Ctrl Pts',(5.59844109934688,0.353291132582354,4.47770402899113));
#24096=CARTESIAN_POINT('Ctrl Pts',(5.59048846000307,0.432828979770902,4.41888096196622));
#24097=CARTESIAN_POINT('Ctrl Pts',(5.58253582065927,0.497356886162411,4.33976214299073));
#24098=CARTESIAN_POINT('Ctrl Pts',(5.57458318131546,0.538985436353474,4.25002092526659));
#24099=CARTESIAN_POINT('Ctrl Pts',(5.56663054197165,0.580613986544537,4.16027970754245));
#24100=CARTESIAN_POINT('Ctrl Pts',(5.55867790262784,0.599343180535155,4.05991609106967));
#24101=CARTESIAN_POINT('Ctrl Pts',(5.55072526328404,0.592883119270616,3.96120089488413));
#24102=CARTESIAN_POINT('Ctrl Pts',(5.54277262394023,0.586423058006077,3.86248569869858));
#24103=CARTESIAN_POINT('Ctrl Pts',(5.53481998459642,0.554773741486382,3.76541892280029));
#24104=CARTESIAN_POINT('Ctrl Pts',(5.52686734525262,0.501804729712613,3.68186830256729));
#24105=CARTESIAN_POINT('Ctrl Pts',(5.51891470590881,0.448835717938844,3.5983176823343));
#24106=CARTESIAN_POINT('Ctrl Pts',(5.51096206656501,0.374547010911001,3.52828321776661));
#24107=CARTESIAN_POINT('Ctrl Pts',(5.5030094272212,0.288021414854312,3.48032757600706));
#24108=CARTESIAN_POINT('Ctrl Pts',(5.4950567878774,0.201495818797622,3.4323719342475));
#24109=CARTESIAN_POINT('Ctrl Pts',(5.48710414853359,0.102733333712086,3.40649511529609));
#24110=CARTESIAN_POINT('Ctrl Pts',(5.47915150918978,0.00380901851787326,
3.40586091270526));
#24111=CARTESIAN_POINT('Ctrl Pts',(5.47119886984597,-0.0951152966763399,
3.40522671011442));
#24112=CARTESIAN_POINT('Ctrl Pts',(5.46324623050217,-0.194201441979227,
3.42983512388417));
#24113=CARTESIAN_POINT('Ctrl Pts',(5.45529359115836,-0.281334786601535,
3.47667744027106));
#24114=CARTESIAN_POINT('Ctrl Pts',(5.44734095181456,-0.368468131223842,
3.52351975665794));
#24115=CARTESIAN_POINT('Ctrl Pts',(5.43938831247075,-0.443648675165568,
3.59259597566196));
#24116=CARTESIAN_POINT('Ctrl Pts',(5.43143567312694,-0.497684572991269,
3.67546058871077));
#24117=CARTESIAN_POINT('Ctrl Pts',(5.42348303378314,-0.551720470816969,
3.75832520175959));
#24118=CARTESIAN_POINT('Ctrl Pts',(5.41553039443933,-0.584611722526643,
3.85497820885321));
#24119=CARTESIAN_POINT('Ctrl Pts',(5.40757775509553,-0.592336924628993,
3.95360246348684));
#24120=CARTESIAN_POINT('Ctrl Pts',(5.39962511575172,-0.600062126731343,
4.05222671812048));
#24121=CARTESIAN_POINT('Ctrl Pts',(5.39167247640791,-0.582621279226368,
4.15282222029412));
#24122=CARTESIAN_POINT('Ctrl Pts',(5.3837198370641,-0.542146763261091,4.24308979978386));
#24123=CARTESIAN_POINT('Ctrl Pts',(5.3757671977203,-0.501672247295815,4.3333573792736));
#24124=CARTESIAN_POINT('Ctrl Pts',(5.36781455837649,-0.438164062870237,
4.41329703607943));
#24125=CARTESIAN_POINT('Ctrl Pts',(5.35986191903269,-0.359386950494509,
4.47313505840055));
#24126=CARTESIAN_POINT('Ctrl Pts',(5.35190927968888,-0.28060983811878,4.53297308072167));
#24127=CARTESIAN_POINT('Ctrl Pts',(5.34395664034507,-0.1865637977929,4.57270946855809));
#24128=CARTESIAN_POINT('Ctrl Pts',(5.33600400100126,-0.0887472388280498,
4.58748590729807));
#24129=CARTESIAN_POINT('Ctrl Pts',(5.33361780442003,-0.0593972924141157,
4.59191959101989));
#24130=CARTESIAN_POINT('Ctrl Pts',(5.3312316078388,-0.0297078841644672,
4.59410611700271));
#24131=CARTESIAN_POINT('Ctrl Pts',(5.32884541125756,-1.45357002139801E-5,
4.59407911932661));
#24132=CARTESIAN_POINT('Ctrl Pts',(5.22115458874249,1.46139895546772E-5,
4.59411444380891));
#24133=CARTESIAN_POINT('Ctrl Pts',(5.22764030503958,-0.0806785298274998,
4.59403186011492));
#24134=CARTESIAN_POINT('Ctrl Pts',(5.23412602133668,-0.161404528346198,
4.57747154641029));
#24135=CARTESIAN_POINT('Ctrl Pts',(5.24061173763377,-0.235476461490165,
4.54549665421293));
#24136=CARTESIAN_POINT('Ctrl Pts',(5.24856437697758,-0.32630179870949,4.50628976108741));
#24137=CARTESIAN_POINT('Ctrl Pts',(5.25651701632139,-0.407122673831612,
4.44390687590439));
#24138=CARTESIAN_POINT('Ctrl Pts',(5.26446965566519,-0.468057634114636,
4.36597515601533));
#24139=CARTESIAN_POINT('Ctrl Pts',(5.272422295009,-0.52899259439766,4.28804343612627));
#24140=CARTESIAN_POINT('Ctrl Pts',(5.28037493435281,-0.570041639841584,
4.19456288153117));
#24141=CARTESIAN_POINT('Ctrl Pts',(5.28832757369661,-0.586185965564114,
4.09696276320888));
#24142=CARTESIAN_POINT('Ctrl Pts',(5.29628021304042,-0.602330291286644,
3.99936264488659));
#24143=CARTESIAN_POINT('Ctrl Pts',(5.30423285238423,-0.59356989728778,3.89764296283709));
#24144=CARTESIAN_POINT('Ctrl Pts',(5.31218549172803,-0.560975861048054,
3.80424033358521));
#24145=CARTESIAN_POINT('Ctrl Pts',(5.32013813107184,-0.528381824808328,
3.71083770433334));
#24146=CARTESIAN_POINT('Ctrl Pts',(5.32809077041564,-0.471954146327742,
3.62575212787907));
#24147=CARTESIAN_POINT('Ctrl Pts',(5.33604340975945,-0.398591877830097,
3.55938647478623));
#24148=CARTESIAN_POINT('Ctrl Pts',(5.34399604910326,-0.325229609332449,
3.49302082169338));
#24149=CARTESIAN_POINT('Ctrl Pts',(5.35194868844707,-0.234932750817741,
3.44537509196196));
#24150=CARTESIAN_POINT('Ctrl Pts',(5.35990132779087,-0.138741323057917,
3.42227462497344));
#24151=CARTESIAN_POINT('Ctrl Pts',(5.36785396713468,-0.042549895298095,
3.39917415798493));
#24152=CARTESIAN_POINT('Ctrl Pts',(5.37580660647848,0.059536101706843,3.40061895373932));
#24153=CARTESIAN_POINT('Ctrl Pts',(5.38375924582229,0.155035264439678,3.42643236627792));
#24154=CARTESIAN_POINT('Ctrl Pts',(5.39171188516609,0.250534427172515,3.45224577881651));
#24155=CARTESIAN_POINT('Ctrl Pts',(5.3996645245099,0.339446755633248,3.5024278081393));
#24156=CARTESIAN_POINT('Ctrl Pts',(5.40761716385371,0.41090150670596,3.57084301769608));
#24157=CARTESIAN_POINT('Ctrl Pts',(5.41556980319751,0.482356257778672,3.63925822725286));
#24158=CARTESIAN_POINT('Ctrl Pts',(5.42352244254132,0.536353431463363,3.72590661704362));
#24159=CARTESIAN_POINT('Ctrl Pts',(5.43147508188513,0.566291137850326,3.82019424128906));
#24160=CARTESIAN_POINT('Ctrl Pts',(5.43942772122893,0.596228844237288,3.91448186553449));
#24161=CARTESIAN_POINT('Ctrl Pts',(5.44738036057274,0.602107083326521,4.01640872423458));
#24162=CARTESIAN_POINT('Ctrl Pts',(5.45533299991655,0.583207160329387,4.11351287069736));
#24163=CARTESIAN_POINT('Ctrl Pts',(5.46328563926035,0.564307237332252,4.21061701716013));
#24164=CARTESIAN_POINT('Ctrl Pts',(5.47123827860416,0.520629152248751,4.30289845138559));
#24165=CARTESIAN_POINT('Ctrl Pts',(5.47919091794796,0.457513145863858,4.37907451119169));
#24166=CARTESIAN_POINT('Ctrl Pts',(5.48714355729177,0.394397139478966,4.45525057099779));
#24167=CARTESIAN_POINT('Ctrl Pts',(5.49509619663558,0.311843211792683,4.51532125638452));
#24168=CARTESIAN_POINT('Ctrl Pts',(5.50304883597938,0.219944704826683,4.5519421079172));
#24169=CARTESIAN_POINT('Ctrl Pts',(5.50908408690042,0.150203009669811,4.5797336395568));
#24170=CARTESIAN_POINT('Ctrl Pts',(5.51511933782146,0.0750795109720808,
4.59401975858331));
#24171=CARTESIAN_POINT('Ctrl Pts',(5.52115458874249,-1.55733839743342E-5,
4.59409663347568));
#24172=CARTESIAN_POINT('Origin',(4.,0.,4.));
#24173=CARTESIAN_POINT('',(5.92884541125757,-1.3134308860685E-5,4.59412454375027));
#24174=CARTESIAN_POINT('',(5.82115458874249,1.31105368646138E-5,4.59407040741879));
#24175=CARTESIAN_POINT('',(4.,-7.27562663373442E-17,4.5941));
#24176=CARTESIAN_POINT('Ctrl Pts',(5.92884541125757,-1.3134308860685E-5,
4.59412454375027));
#24177=CARTESIAN_POINT('Ctrl Pts',(5.92209495209015,0.0839697382976411,
4.5940436242297));
#24178=CARTESIAN_POINT('Ctrl Pts',(5.91534449292274,0.16798613900316,4.57606223573506));
#24179=CARTESIAN_POINT('Ctrl Pts',(5.90859403375532,0.244517407380453,4.54150437939301));
#24180=CARTESIAN_POINT('Ctrl Pts',(5.90064139441152,0.334678026211646,4.50079216098422));
#24181=CARTESIAN_POINT('Ctrl Pts',(5.89268875506771,0.41445008323119,4.43707358099086));
#24182=CARTESIAN_POINT('Ctrl Pts',(5.8847361157239,0.474080337065587,4.35813908232779));
#24183=CARTESIAN_POINT('Ctrl Pts',(5.8767834763801,0.533710590899983,4.27920458366471));
#24184=CARTESIAN_POINT('Ctrl Pts',(5.86883083703629,0.573199041549232,4.18505416633191));
#24185=CARTESIAN_POINT('Ctrl Pts',(5.86087819769249,0.587717699183782,4.08719901244189));
#24186=CARTESIAN_POINT('Ctrl Pts',(5.85292555834868,0.602236356818331,3.98934385855186));
#24187=CARTESIAN_POINT('Ctrl Pts',(5.84497291900487,0.591785221438181,3.88778396810461));
#24188=CARTESIAN_POINT('Ctrl Pts',(5.83702027966107,0.557642080814915,3.79493641494568));
#24189=CARTESIAN_POINT('Ctrl Pts',(5.82906764031726,0.523498940191649,3.70208886178675));
#24190=CARTESIAN_POINT('Ctrl Pts',(5.82111500097346,0.465663794325265,3.61795364591614));
#24191=CARTESIAN_POINT('Ctrl Pts',(5.81316236162965,0.391207780605707,3.55281744653948));
#24192=CARTESIAN_POINT('Ctrl Pts',(5.80520972228584,0.31675176688615,3.48768124716281));
#24193=CARTESIAN_POINT('Ctrl Pts',(5.79725708294203,0.225674885313418,3.44154406428009));
#24194=CARTESIAN_POINT('Ctrl Pts',(5.78930444359823,0.129112523455512,3.42004679519738));
#24195=CARTESIAN_POINT('Ctrl Pts',(5.78135180425442,0.0325501615976049,
3.39854952611466));
#24196=CARTESIAN_POINT('Ctrl Pts',(5.77339916491062,-0.0694976805454773,
3.40169217083197));
#24197=CARTESIAN_POINT('Ctrl Pts',(5.76544652556681,-0.164554263536051,
3.42909049911887));
#24198=CARTESIAN_POINT('Ctrl Pts',(5.75749388622301,-0.259610846526622,
3.45648882740576));
#24199=CARTESIAN_POINT('Ctrl Pts',(5.7495412468792,-0.347676170364685,3.50814283926225));
#24200=CARTESIAN_POINT('Ctrl Pts',(5.74158860753539,-0.417983050247216,
3.57773712775495));
#24201=CARTESIAN_POINT('Ctrl Pts',(5.73363596819158,-0.488289930129746,
3.64733141624764));
#24202=CARTESIAN_POINT('Ctrl Pts',(5.72568332884778,-0.540838366056745,
3.73486598137654));
#24203=CARTESIAN_POINT('Ctrl Pts',(5.71773068950397,-0.569203595796233,
3.82963853060694));
#24204=CARTESIAN_POINT('Ctrl Pts',(5.70977805016017,-0.597568825535722,
3.92441107983734));
#24205=CARTESIAN_POINT('Ctrl Pts',(5.70182541081636,-0.6017508490877,4.02642161316923));
#24206=CARTESIAN_POINT('Ctrl Pts',(5.69387277147255,-0.581238357244447,
4.12319795341528));
#24207=CARTESIAN_POINT('Ctrl Pts',(5.68592013212875,-0.560725865401195,
4.21997429366132));
#24208=CARTESIAN_POINT('Ctrl Pts',(5.67796749278494,-0.515518858162713,
4.31151644082153));
#24209=CARTESIAN_POINT('Ctrl Pts',(5.67001485344113,-0.451144507802385,
4.38663212069642));
#24210=CARTESIAN_POINT('Ctrl Pts',(5.66206221409732,-0.386770157442057,
4.46174780057131));
#24211=CARTESIAN_POINT('Ctrl Pts',(5.65410957475352,-0.303228463959881,
4.52043701316089));
#24212=CARTESIAN_POINT('Ctrl Pts',(5.64615693540972,-0.210733537235404,
4.55552420285805));
#24213=CARTESIAN_POINT('Ctrl Pts',(5.640386427359,-0.143618370026196,4.5809837895275));
#24214=CARTESIAN_POINT('Ctrl Pts',(5.63461591930828,-0.07178924788396,4.59401670649762));
#24215=CARTESIAN_POINT('Ctrl Pts',(5.62884541125756,1.52328526200479E-5,
4.59408648697874));
#24216=CARTESIAN_POINT('Ctrl Pts',(5.52115458874249,-1.55733839743342E-5,
4.59409663347568));
#24217=CARTESIAN_POINT('Ctrl Pts',(5.52307197716526,-0.0238731473664388,
4.59412105649149));
#24218=CARTESIAN_POINT('Ctrl Pts',(5.52498936558803,-0.0477278534282068,
4.59271130989713));
#24219=CARTESIAN_POINT('Ctrl Pts',(5.5269067540108,-0.0714062077139717,
4.58984482465595));
#24220=CARTESIAN_POINT('Ctrl Pts',(5.53485939335461,-0.169615527042917,
4.57795567218339));
#24221=CARTESIAN_POINT('Ctrl Pts',(5.54281203269841,-0.264791079455087,
4.54100634955965));
#24222=CARTESIAN_POINT('Ctrl Pts',(5.55076467204222,-0.345296357402727,
4.48351441471562));
#24223=CARTESIAN_POINT('Ctrl Pts',(5.55871731138603,-0.425801635350366,
4.4260224798716));
#24224=CARTESIAN_POINT('Ctrl Pts',(5.56666995072984,-0.491636638833473,
4.34798793280729));
#24225=CARTESIAN_POINT('Ctrl Pts',(5.57462259007364,-0.534752142022197,
4.2589515597096));
#24226=CARTESIAN_POINT('Ctrl Pts',(5.58257522941745,-0.577867645210921,
4.16991518661191));
#24227=CARTESIAN_POINT('Ctrl Pts',(5.59052786876125,-0.598263648105263,
4.06987698748084));
#24228=CARTESIAN_POINT('Ctrl Pts',(5.59848050810506,-0.59344646156208,3.97106799465478));
#24229=CARTESIAN_POINT('Ctrl Pts',(5.60643314744886,-0.588629275018896,
3.87225900182873));
#24230=CARTESIAN_POINT('Ctrl Pts',(5.61438578679267,-0.558598899038186,
3.77467921530768));
#24231=CARTESIAN_POINT('Ctrl Pts',(5.62233842613648,-0.50702695609161,3.69025909300064));
#24232=CARTESIAN_POINT('Ctrl Pts',(5.63029106548029,-0.455455013145033,
3.6058389706936));
#24233=CARTESIAN_POINT('Ctrl Pts',(5.63824370482409,-0.382341503232591,
3.53457851260056));
#24234=CARTESIAN_POINT('Ctrl Pts',(5.6461963441679,-0.296625548722353,3.48519028027742));
#24235=CARTESIAN_POINT('Ctrl Pts',(5.6541489835117,-0.210909594212113,3.43580204795428));
#24236=CARTESIAN_POINT('Ctrl Pts',(5.66210162285551,-0.112591195104077,
3.40828604140104));
#24237=CARTESIAN_POINT('Ctrl Pts',(5.67005426219932,-0.0136911147678568,
3.40600646716786));
#24238=CARTESIAN_POINT('Ctrl Pts',(5.67800690154312,0.0852089655683624,
3.40372689293467));
#24239=CARTESIAN_POINT('Ctrl Pts',(5.68595954088693,0.184690727132768,3.42668375102154));
#24240=CARTESIAN_POINT('Ctrl Pts',(5.69391218023074,0.272591169676606,3.47207025288287));
#24241=CARTESIAN_POINT('Ctrl Pts',(5.70186481957454,0.360491612220445,3.51745675474419));
#24242=CARTESIAN_POINT('Ctrl Pts',(5.70981745891835,0.436810735743714,3.58527290037998));
#24243=CARTESIAN_POINT('Ctrl Pts',(5.71777009826216,0.492217487918224,3.667227242308));
#24244=CARTESIAN_POINT('Ctrl Pts',(5.72572273760596,0.547624240092733,3.74918158423602));
#24245=CARTESIAN_POINT('Ctrl Pts',(5.73367537694977,0.582118620918482,3.84527412245626));
#24246=CARTESIAN_POINT('Ctrl Pts',(5.74162801629357,0.591483222595687,3.94375623549444));
#24247=CARTESIAN_POINT('Ctrl Pts',(5.74958065563738,0.600847824272892,4.04223834853263));
#24248=CARTESIAN_POINT('Ctrl Pts',(5.75753329498119,0.585082646801554,4.14311003638875));
#24249=CARTESIAN_POINT('Ctrl Pts',(5.76548593432499,0.546115197731279,4.23403836123177));
#24250=CARTESIAN_POINT('Ctrl Pts',(5.7734385736688,0.507147748661005,4.32496668607478));
#24251=CARTESIAN_POINT('Ctrl Pts',(5.78139121301261,0.444978027991796,4.4059516479047));
#24252=CARTESIAN_POINT('Ctrl Pts',(5.78934385235641,0.367207131024688,4.46709173242012));
#24253=CARTESIAN_POINT('Ctrl Pts',(5.79729649170022,0.28943623405758,4.52823181693554));
#24254=CARTESIAN_POINT('Ctrl Pts',(5.80524913104403,0.196064160792572,4.56952702413646));
#24255=CARTESIAN_POINT('Ctrl Pts',(5.81320177038783,0.0985069184831505,
4.58592845199323));
#24256=CARTESIAN_POINT('Ctrl Pts',(5.81585270983939,0.0659871057213339,
4.59139571767544));
#24257=CARTESIAN_POINT('Ctrl Pts',(5.81850364929094,0.0330022532417819,
4.59409688335147));
#24258=CARTESIAN_POINT('Ctrl Pts',(5.82115458874249,1.31105368646138E-5,
4.59407040741879));
#24259=CARTESIAN_POINT('Origin',(4.,0.,4.));
#24260=CARTESIAN_POINT('',(6.22884541125756,-1.27841859475647E-5,4.5940334609955));
#24261=CARTESIAN_POINT('',(6.12115458874249,-9.50793186244619E-6,4.59413936148612));
#24262=CARTESIAN_POINT('',(4.,-7.27562663373442E-17,4.5941));
#24263=CARTESIAN_POINT('Ctrl Pts',(6.22884541125756,-1.27841859475647E-5,
4.5940334609955));
#24264=CARTESIAN_POINT('Ctrl Pts',(6.22547926355963,0.0418951881409122,
4.59406590912705));
#24265=CARTESIAN_POINT('Ctrl Pts',(6.2221131158617,0.0838018877146867,4.58971510200585));
#24266=CARTESIAN_POINT('Ctrl Pts',(6.21874696816377,0.124749109322564,4.58093223526196));
#24267=CARTESIAN_POINT('Ctrl Pts',(6.21079432881996,0.22148832423537,4.56018241146135));
#24268=CARTESIAN_POINT('Ctrl Pts',(6.20284168947616,0.31287214740051,4.51469474440412));
#24269=CARTESIAN_POINT('Ctrl Pts',(6.19488905013236,0.387808805213989,4.4501133836823));
#24270=CARTESIAN_POINT('Ctrl Pts',(6.18693641078855,0.462745463027469,4.38553202296047));
#24271=CARTESIAN_POINT('Ctrl Pts',(6.17898377144474,0.521234955489287,4.30185696857405));
#24272=CARTESIAN_POINT('Ctrl Pts',(6.17103113210093,0.556083161424236,4.20927485003939));
#24273=CARTESIAN_POINT('Ctrl Pts',(6.16307849275713,0.590931367359184,4.11669273150472));
#24274=CARTESIAN_POINT('Ctrl Pts',(6.15512585341332,0.602138286767263,4.0152035488218));
#24275=CARTESIAN_POINT('Ctrl Pts',(6.14717321406952,0.588356486924291,3.9172389266648));
#24276=CARTESIAN_POINT('Ctrl Pts',(6.13922057472571,0.574574687081318,3.81927430450779));
#24277=CARTESIAN_POINT('Ctrl Pts',(6.1312679353819,0.535804167987293,3.7248342428767));
#24278=CARTESIAN_POINT('Ctrl Pts',(6.12331529603809,0.476773096629474,3.64545304401991));
#24279=CARTESIAN_POINT('Ctrl Pts',(6.11536265669429,0.417742025271657,3.56607184516312));
#24280=CARTESIAN_POINT('Ctrl Pts',(6.10741001735048,0.338450401650047,3.50174950908064));
#24281=CARTESIAN_POINT('Ctrl Pts',(6.09945737800668,0.248599092144812,3.46035682177302));
#24282=CARTESIAN_POINT('Ctrl Pts',(6.09150473866287,0.158747782639575,3.41896413446539));
#24283=CARTESIAN_POINT('Ctrl Pts',(6.08355209931906,0.0583367872507115,
3.40050109593262));
#24284=CARTESIAN_POINT('Ctrl Pts',(6.07559945997526,-0.0403606640336046,
3.40722161935946));
#24285=CARTESIAN_POINT('Ctrl Pts',(6.06764682063145,-0.139058115317921,
3.4139421427863));
#24286=CARTESIAN_POINT('Ctrl Pts',(6.05969418128764,-0.23604202249769,3.44584622817275));
#24287=CARTESIAN_POINT('Ctrl Pts',(6.05174154194384,-0.319452991027635,
3.49903499090221));
#24288=CARTESIAN_POINT('Ctrl Pts',(6.04378890260003,-0.40286395955758,3.55222375363166));
#24289=CARTESIAN_POINT('Ctrl Pts',(6.03583626325623,-0.472701989437702,
3.62669719370411));
#24290=CARTESIAN_POINT('Ctrl Pts',(6.02788362391242,-0.520429378860104,
3.71334895258148));
#24291=CARTESIAN_POINT('Ctrl Pts',(6.01993098456861,-0.568156768282506,
3.80000071145885));
#24292=CARTESIAN_POINT('Ctrl Pts',(6.0119783452248,-0.593773517247188,3.89883078914114));
#24293=CARTESIAN_POINT('Ctrl Pts',(6.004025705881,-0.594147126960238,3.99775637428654));
#24294=CARTESIAN_POINT('Ctrl Pts',(5.99607306653719,-0.594520736673288,
4.09668195943193));
#24295=CARTESIAN_POINT('Ctrl Pts',(5.98812042719339,-0.569651207134705,
4.19570305204043));
#24296=CARTESIAN_POINT('Ctrl Pts',(5.98016778784958,-0.52257944308796,4.28271270390554));
#24297=CARTESIAN_POINT('Ctrl Pts',(5.97221514850578,-0.475507679041215,
4.36972235577065));
#24298=CARTESIAN_POINT('Ctrl Pts',(5.96426250916196,-0.406233680486307,
4.44472056689237));
#24299=CARTESIAN_POINT('Ctrl Pts',(5.95630986981816,-0.323226996343023,
4.49853792802592));
#24300=CARTESIAN_POINT('Ctrl Pts',(5.94835723047435,-0.240220312199739,
4.55235528915947));
#24301=CARTESIAN_POINT('Ctrl Pts',(5.94040459113055,-0.143480942468078,
4.58499180030486));
#24302=CARTESIAN_POINT('Ctrl Pts',(5.93245195178675,-0.0448366672808267,
4.59245712746544));
#24303=CARTESIAN_POINT('Ctrl Pts',(5.93124977161035,-0.0299248641651563,
4.59358564190382));
#24304=CARTESIAN_POINT('Ctrl Pts',(5.93004759143396,-0.0149695309183627,
4.59413895459864));
#24305=CARTESIAN_POINT('Ctrl Pts',(5.92884541125757,-1.3134308860685E-5,
4.59412454375027));
#24306=CARTESIAN_POINT('Ctrl Pts',(5.82115458874249,1.31105368646138E-5,
4.59407040741879));
#24307=CARTESIAN_POINT('Ctrl Pts',(5.82645628863475,-0.0659629472043463,
4.59401745734129));
#24308=CARTESIAN_POINT('Ctrl Pts',(5.831757988527,-0.131956164688202,4.58305467757793));
#24309=CARTESIAN_POINT('Ctrl Pts',(5.83705968841925,-0.194280919321303,
4.56148970414564));
#24310=CARTESIAN_POINT('Ctrl Pts',(5.84501232776306,-0.287769103462499,
4.52914187992864));
#24311=CARTESIAN_POINT('Ctrl Pts',(5.85296496710686,-0.373003060391055,
4.47293858298203));
#24312=CARTESIAN_POINT('Ctrl Pts',(5.86091760645067,-0.439561779454174,
4.39975142997742));
#24313=CARTESIAN_POINT('Ctrl Pts',(5.86887024579447,-0.506120498517293,
4.32656427697281));
#24314=CARTESIAN_POINT('Ctrl Pts',(5.87682288513828,-0.554003979714975,
4.2363932679102));
#24315=CARTESIAN_POINT('Ctrl Pts',(5.88477552448209,-0.577357812582609,
4.14026304025204));
#24316=CARTESIAN_POINT('Ctrl Pts',(5.8927281638259,-0.600711645450243,4.04413281259387));
#24317=CARTESIAN_POINT('Ctrl Pts',(5.9006808031697,-0.59953582998783,3.94204336634015));
#24318=CARTESIAN_POINT('Ctrl Pts',(5.90863344251351,-0.573974130801472,
3.84647652011691));
#24319=CARTESIAN_POINT('Ctrl Pts',(5.91658608185731,-0.548412431615114,
3.75090967389367));
#24320=CARTESIAN_POINT('Ctrl Pts',(5.92453872120112,-0.498464848704808,
3.66186542770092));
#24321=CARTESIAN_POINT('Ctrl Pts',(5.93249136054493,-0.430238144626613,
3.59023066587279));
#24322=CARTESIAN_POINT('Ctrl Pts',(5.94044399988873,-0.362011440548417,
3.51859590404466));
#24323=CARTESIAN_POINT('Ctrl Pts',(5.94839663923254,-0.275505615302329,
3.46437062658116));
#24324=CARTESIAN_POINT('Ctrl Pts',(5.95634927857635,-0.181297202577209,
3.43418458862315));
#24325=CARTESIAN_POINT('Ctrl Pts',(5.96430191792015,-0.087088789852092,
3.40399855066514));
#24326=CARTESIAN_POINT('Ctrl Pts',(5.97225455726396,0.0148222103520573,
3.39785175221263));
#24327=CARTESIAN_POINT('Ctrl Pts',(5.98020719660777,0.111975824940657,3.41649576758492));
#24328=CARTESIAN_POINT('Ctrl Pts',(5.98815983595157,0.209129439529257,3.43513978295721));
#24329=CARTESIAN_POINT('Ctrl Pts',(5.99611247529537,0.301525668502307,3.47857461215431));
#24330=CARTESIAN_POINT('Ctrl Pts',(6.00406511463918,0.377867748972965,3.54148967172874));
#24331=CARTESIAN_POINT('Ctrl Pts',(6.01201775398299,0.454209829443624,3.60440473130317));
#24332=CARTESIAN_POINT('Ctrl Pts',(6.0199703933268,0.514497761411887,3.68680002125492));
#24333=CARTESIAN_POINT('Ctrl Pts',(6.02792303267061,0.551360647735685,3.77860175380959));
#24334=CARTESIAN_POINT('Ctrl Pts',(6.03587567201441,0.588223534059482,3.87040348636426));
#24335=CARTESIAN_POINT('Ctrl Pts',(6.04382831135821,0.601661374738811,3.97161166152184));
#24336=CARTESIAN_POINT('Ctrl Pts',(6.05178095070202,0.590030977261751,4.06985190192822));
#24337=CARTESIAN_POINT('Ctrl Pts',(6.05973359004583,0.578400579784692,4.16809214233459));
#24338=CARTESIAN_POINT('Ctrl Pts',(6.06768622938964,0.541701944151245,4.26336444798975));
#24339=CARTESIAN_POINT('Ctrl Pts',(6.07563886873345,0.484422419230229,4.3440210474869));
#24340=CARTESIAN_POINT('Ctrl Pts',(6.08359150807725,0.427142894309213,4.42467764698404));
#24341=CARTESIAN_POINT('Ctrl Pts',(6.09154414742105,0.349282480100627,4.49071854032316));
#24342=CARTESIAN_POINT('Ctrl Pts',(6.09949678676486,0.26035984028865,4.53406826097581));
#24343=CARTESIAN_POINT('Ctrl Pts',(6.10671605409073,0.179637418414302,4.5734203814938));
#24344=CARTESIAN_POINT('Ctrl Pts',(6.11393532141662,0.0897989573399868,
4.59407340590587));
#24345=CARTESIAN_POINT('Ctrl Pts',(6.12115458874249,-9.50793186244619E-6,
4.59413936148612));
#24346=CARTESIAN_POINT('Origin',(4.,0.,4.));
#24347=CARTESIAN_POINT('',(6.52884541125757,2.61457539729726E-5,4.59508370962656));
#24348=CARTESIAN_POINT('',(6.42115458874249,-0.000630941829811112,4.59394485456974));
#24349=CARTESIAN_POINT('',(4.,-7.27562663373442E-17,4.5941));
#24350=CARTESIAN_POINT('Ctrl Pts',(6.52884541125757,2.61457539729726E-5,
4.59508370962656));
#24351=CARTESIAN_POINT('Ctrl Pts',(6.5129582963415,0.196771080344787,4.59506033873941));
#24352=CARTESIAN_POINT('Ctrl Pts',(6.49707118142544,0.393450480974957,4.48779253427891));
#24353=CARTESIAN_POINT('Ctrl Pts',(6.48118406650938,0.500111739713094,4.32240987211318));
#24354=CARTESIAN_POINT('Ctrl Pts',(6.46527878782176,0.606894944490356,4.15683812760557));
#24355=CARTESIAN_POINT('Ctrl Pts',(6.44937350913416,0.623454053851315,3.93301856375293));
#24356=CARTESIAN_POINT('Ctrl Pts',(6.43346823044654,0.541809843535619,3.75368369989414));
#24357=CARTESIAN_POINT('Ctrl Pts',(6.41756295175893,0.460165633219924,3.57434883603535));
#24358=CARTESIAN_POINT('Ctrl Pts',(6.40165767307132,0.280318103227576,3.43949867217041));
#24359=CARTESIAN_POINT('Ctrl Pts',(6.3857523943837,0.085604811340831,3.41110814665827));
#24360=CARTESIAN_POINT('Ctrl Pts',(6.36984711569609,-0.109108480545914,
3.38271762114613));
#24361=CARTESIAN_POINT('Ctrl Pts',(6.35394183700848,-0.318687534327053,
3.46078673398678));
#24362=CARTESIAN_POINT('Ctrl Pts',(6.33803655832087,-0.448733343985475,
3.60951691634857));
#24363=CARTESIAN_POINT('Ctrl Pts',(6.33008391897706,-0.513756248814686,
3.68388200752946));
#24364=CARTESIAN_POINT('Ctrl Pts',(6.32213127963325,-0.558895842613217,
3.77591236609064));
#24365=CARTESIAN_POINT('Ctrl Pts',(6.31417864028945,-0.579995970841135,
3.87270290659392));
#24366=CARTESIAN_POINT('Ctrl Pts',(6.30622600094564,-0.601096099069052,
3.9694934470972));
#24367=CARTESIAN_POINT('Ctrl Pts',(6.29827336160184,-0.598156761726356,
4.07104416954258));
#24368=CARTESIAN_POINT('Ctrl Pts',(6.29032072225803,-0.570614590620327,
4.16591643177432));
#24369=CARTESIAN_POINT('Ctrl Pts',(6.28236808291422,-0.543072419514299,
4.26078869400605));
#24370=CARTESIAN_POINT('Ctrl Pts',(6.27441544357042,-0.490927414644939,
4.34898249602413));
#24371=CARTESIAN_POINT('Ctrl Pts',(6.26646280422661,-0.421087730399527,
4.41916768405122));
#24372=CARTESIAN_POINT('Ctrl Pts',(6.2585101648828,-0.351248046154114,4.48935287207832));
#24373=CARTESIAN_POINT('Ctrl Pts',(6.250557525539,-0.263713682532649,4.54152944611444));
#24374=CARTESIAN_POINT('Ctrl Pts',(6.24260488619519,-0.168899197391682,
4.5696117428605));
#24375=CARTESIAN_POINT('Ctrl Pts',(6.23801839454932,-0.114217245248871,
4.58580752565092));
#24376=CARTESIAN_POINT('Ctrl Pts',(6.23343190290344,-0.0571138332845632,
4.59398924930378));
#24377=CARTESIAN_POINT('Ctrl Pts',(6.22884541125756,-1.27841859475647E-5,
4.5940334609955));
#24378=CARTESIAN_POINT('Ctrl Pts',(6.12115458874249,-9.50793186244619E-6,
4.59413936148612));
#24379=CARTESIAN_POINT('Ctrl Pts',(6.12188796076042,-0.00913273504488762,
4.59414606160884));
#24380=CARTESIAN_POINT('Ctrl Pts',(6.12262133277835,-0.0182556526135436,
4.59394031163173));
#24381=CARTESIAN_POINT('Ctrl Pts',(6.12335470479628,-0.0273686726716501,
4.59352013235631));
#24382=CARTESIAN_POINT('Ctrl Pts',(6.13130734414009,-0.126189680404606,
4.58896373511797));
#24383=CARTESIAN_POINT('Ctrl Pts',(6.13925998348389,-0.223846830455152,
4.55919239267511));
#24384=CARTESIAN_POINT('Ctrl Pts',(6.14721262282769,-0.308403173896691,
4.50784224986958));
#24385=CARTESIAN_POINT('Ctrl Pts',(6.1551652621715,-0.392959517338232,4.45649210706404));
#24386=CARTESIAN_POINT('Ctrl Pts',(6.16311790151532,-0.464415054170765,
4.38356316389581));
#24387=CARTESIAN_POINT('Ctrl Pts',(6.17107054085912,-0.514027768136376,
4.29797916579711));
#24388=CARTESIAN_POINT('Ctrl Pts',(6.17902318020293,-0.563640482101988,
4.2123951676984));
#24389=CARTESIAN_POINT('Ctrl Pts',(6.18697581954673,-0.591410373200678,
4.11415611466921));
#24390=CARTESIAN_POINT('Ctrl Pts',(6.19492845889053,-0.593952774873424,
4.0152594949342));
#24391=CARTESIAN_POINT('Ctrl Pts',(6.20288109823434,-0.59649517654617,3.9163628751992));
#24392=CARTESIAN_POINT('Ctrl Pts',(6.21083373757815,-0.573810088792972,
3.81680868875837));
#24393=CARTESIAN_POINT('Ctrl Pts',(6.21878637692196,-0.528651094032059,
3.72879442104321));
#24394=CARTESIAN_POINT('Ctrl Pts',(6.22673901626577,-0.483492099271145,
3.64078015332805));
#24395=CARTESIAN_POINT('Ctrl Pts',(6.23469165560957,-0.415859197502516,
3.56430580433857));
#24396=CARTESIAN_POINT('Ctrl Pts',(6.24264429495337,-0.334059153459168,
3.50867301156809));
#24397=CARTESIAN_POINT('Ctrl Pts',(6.25059693429718,-0.252259109415819,
3.45304021879761));
#24398=CARTESIAN_POINT('Ctrl Pts',(6.25854957364099,-0.156291923097747,
3.41824898224614));
#24399=CARTESIAN_POINT('Ctrl Pts',(6.2665022129848,-0.057819682214149,3.40864436538418));
#24400=CARTESIAN_POINT('Ctrl Pts',(6.2744548523286,0.0406525586694487,3.39903974852221));
#24401=CARTESIAN_POINT('Ctrl Pts',(6.28240749167241,0.141629854118573,3.41462175134974));
#24402=CARTESIAN_POINT('Ctrl Pts',(6.29036013101621,0.232632044389671,3.453312878872));
#24403=CARTESIAN_POINT('Ctrl Pts',(6.29831277036002,0.323634234660771,3.49200400639426));
#24404=CARTESIAN_POINT('Ctrl Pts',(6.30626540970382,0.404661319753841,3.55380425861124));
#24405=CARTESIAN_POINT('Ctrl Pts',(6.31421804904763,0.466059055789261,3.63148218419904));
#24406=CARTESIAN_POINT('Ctrl Pts',(6.32217068839144,0.527456791824679,3.70916010978684));
#24407=CARTESIAN_POINT('Ctrl Pts',(6.33012332773525,0.569225178802449,3.80271570874544));
#24408=CARTESIAN_POINT('Ctrl Pts',(6.33807596707905,0.585790493249255,3.90010619949006));
#24409=CARTESIAN_POINT('Ctrl Pts',(6.34602860642286,0.602355807696062,3.99749669023468));
#24410=CARTESIAN_POINT('Ctrl Pts',(6.35398124576666,0.593718049611903,4.09872207276531));
#24411=CARTESIAN_POINT('Ctrl Pts',(6.36193388511047,0.56173881546021,4.19248215342453));
#24412=CARTESIAN_POINT('Ctrl Pts',(6.36988652445427,0.529759581308516,4.28624223408375));
#24413=CARTESIAN_POINT('Ctrl Pts',(6.37783916379808,0.474438871089287,4.37253701287156));
#24414=CARTESIAN_POINT('Ctrl Pts',(6.38579180314189,0.401374624788453,4.4390182948332));
#24415=CARTESIAN_POINT('Ctrl Pts',(6.39757939834209,0.293077024234899,4.53755846574697));
#24416=CARTESIAN_POINT('Ctrl Pts',(6.40936699354229,0.145797072855576,4.59256860517148));
#24417=CARTESIAN_POINT('Ctrl Pts',(6.42115458874249,-0.000630941829811112,
4.59394485456974));
#24418=CARTESIAN_POINT('Origin',(4.,0.,4.));
#24419=CARTESIAN_POINT('',(6.82884541125756,0.000528213615369061,4.5937871332276));
#24420=CARTESIAN_POINT('',(6.72115458874249,0.000109070110168276,4.59505938903171));
#24421=CARTESIAN_POINT('',(4.,-7.27562663373442E-17,4.5941));
#24422=CARTESIAN_POINT('Ctrl Pts',(6.82884541125756,0.000528213615369061,
4.5937871332276));
#24423=CARTESIAN_POINT('Ctrl Pts',(6.82429524715479,0.0572034606387535,
4.59426930340541));
#24424=CARTESIAN_POINT('Ctrl Pts',(6.81974508305202,0.113754426020979,4.58681959872387));
#24425=CARTESIAN_POINT('Ctrl Pts',(6.81519491894924,0.167823213394864,4.57092612439125));
#24426=CARTESIAN_POINT('Ctrl Pts',(6.79928964026163,0.356822799356826,4.51536985589957));
#24427=CARTESIAN_POINT('Ctrl Pts',(6.78338436157403,0.515493156338912,4.35664088088147));
#24428=CARTESIAN_POINT('Ctrl Pts',(6.76747908288642,0.570983871223461,4.16762126762428));
#24429=CARTESIAN_POINT('Ctrl Pts',(6.7515738041988,0.626474586108011,3.97860165436708));
#24430=CARTESIAN_POINT('Ctrl Pts',(6.73566852551118,0.578785658895023,3.75929140287077));
#24431=CARTESIAN_POINT('Ctrl Pts',(6.71976324682357,0.449805704301045,3.61038767491097));
#24432=CARTESIAN_POINT('Ctrl Pts',(6.70385796813595,0.320825749707067,3.46148394695116));
#24433=CARTESIAN_POINT('Ctrl Pts',(6.68795268944834,0.110554767732096,3.38298674252784));
#24434=CARTESIAN_POINT('Ctrl Pts',(6.67204741076073,-0.0844443642884844,
3.4109402193496));
#24435=CARTESIAN_POINT('Ctrl Pts',(6.65614213207312,-0.279443496309066,
3.43889369617135));
#24436=CARTESIAN_POINT('Ctrl Pts',(6.64023685338551,-0.459170778375258,
3.57329785423817));
#24437=CARTESIAN_POINT('Ctrl Pts',(6.6243315746979,-0.541132009270427,3.75243704050979));
#24438=CARTESIAN_POINT('Ctrl Pts',(6.60842629601029,-0.623093240165596,
3.9315762267814));
#24439=CARTESIAN_POINT('Ctrl Pts',(6.59252101732267,-0.60728841988974,4.15545044125781));
#24440=CARTESIAN_POINT('Ctrl Pts',(6.57661573863506,-0.500919754058047,
4.32127168369798));
#24441=CARTESIAN_POINT('Ctrl Pts',(6.56069229617589,-0.394429615589227,
4.48728229340579));
#24442=CARTESIAN_POINT('Ctrl Pts',(6.54476885371673,-0.197168666623305,
4.59510713395368));
#24443=CARTESIAN_POINT('Ctrl Pts',(6.52884541125757,2.61457539729726E-5,
4.59508370962656));
#24444=CARTESIAN_POINT('Ctrl Pts',(6.42115458874249,-0.000630941829811112,
4.59394485456974));
#24445=CARTESIAN_POINT('Ctrl Pts',(6.4252722722299,-0.0517816819022344,
4.59442561076518));
#24446=CARTESIAN_POINT('Ctrl Pts',(6.42938995571731,-0.102828462800867,
4.58836159088269));
#24447=CARTESIAN_POINT('Ctrl Pts',(6.43350763920472,-0.152073274319339,
4.5753220992581));
#24448=CARTESIAN_POINT('Ctrl Pts',(6.44941291789233,-0.342290043897387,
4.52495476314113));
#24449=CARTESIAN_POINT('Ctrl Pts',(6.46531819657995,-0.5056209461254,4.37051151428857));
#24450=CARTESIAN_POINT('Ctrl Pts',(6.48122347526756,-0.56632363157735,4.18304963962536));
#24451=CARTESIAN_POINT('Ctrl Pts',(6.49712875395518,-0.627026317029301,
3.99558776496215));
#24452=CARTESIAN_POINT('Ctrl Pts',(6.51303403264279,-0.58510078570519,3.77510726448829));
#24453=CARTESIAN_POINT('Ctrl Pts',(6.5289393113304,-0.460166914262479,3.62276494217392));
#24454=CARTESIAN_POINT('Ctrl Pts',(6.54484459001801,-0.335233042819767,
3.47042261985956));
#24455=CARTESIAN_POINT('Ctrl Pts',(6.56074986870563,-0.127290831258456,
3.38621847570468));
#24456=CARTESIAN_POINT('Ctrl Pts',(6.57665514739324,0.068373869747762,3.4088573345089));
#24457=CARTESIAN_POINT('Ctrl Pts',(6.59256042608085,0.26403857075398,3.43149619331313));
#24458=CARTESIAN_POINT('Ctrl Pts',(6.60846570476847,0.447425761205104,3.56097805507645));
#24459=CARTESIAN_POINT('Ctrl Pts',(6.62437098345608,0.534230294511761,3.73782813427527));
#24460=CARTESIAN_POINT('Ctrl Pts',(6.64027626214369,0.621034827818418,3.91467821347409));
#24461=CARTESIAN_POINT('Ctrl Pts',(6.65618154083131,0.611256703980608,4.1388965101084));
#24462=CARTESIAN_POINT('Ctrl Pts',(6.67208681951892,0.509439333868548,4.30754322537844));
#24463=CARTESIAN_POINT('Ctrl Pts',(6.68799209820653,0.40762196375649,4.47618994064847));
#24464=CARTESIAN_POINT('Ctrl Pts',(6.70389737689414,0.213765347370184,4.58926507455422));
#24465=CARTESIAN_POINT('Ctrl Pts',(6.71980265558175,0.016851802420978,4.59484308232941));
#24466=CARTESIAN_POINT('Ctrl Pts',(6.72025329996867,0.0112726493937942,
4.59500112406784));
#24467=CARTESIAN_POINT('Ctrl Pts',(6.72070394435558,0.00569104238866241,
4.59507287148453));
#24468=CARTESIAN_POINT('Ctrl Pts',(6.72115458874249,0.000109070110168276,
4.59505938903171));
#24469=CARTESIAN_POINT('Origin',(4.,0.,4.));
#24470=CARTESIAN_POINT('',(7.12884541125757,-0.000233413975479213,4.59320261234329));
#24471=CARTESIAN_POINT('',(7.02115458874249,0.000491936389841303,4.5936290357477));
#24472=CARTESIAN_POINT('',(4.,-7.27562663373442E-17,4.5941));
#24473=CARTESIAN_POINT('Ctrl Pts',(7.12884541125757,-0.000233413975479213,
4.59320261234329));
#24474=CARTESIAN_POINT('Ctrl Pts',(7.11972691928047,0.113624805666132,4.59280158872514));
#24475=CARTESIAN_POINT('Ctrl Pts',(7.11060842730338,0.227688545642871,4.56127879346404));
#24476=CARTESIAN_POINT('Ctrl Pts',(7.10148993532628,0.322592019514134,4.50005536307953));
#24477=CARTESIAN_POINT('Ctrl Pts',(7.08558465663867,0.488131036726243,4.39326405099382));
#24478=CARTESIAN_POINT('Ctrl Pts',(7.06967937795105,0.595374147168556,4.19610732087965));
#24479=CARTESIAN_POINT('Ctrl Pts',(7.05377409926343,0.595079946532544,3.99911121186167));
#24480=CARTESIAN_POINT('Ctrl Pts',(7.03786882057582,0.594785745896532,3.80211510284369));
#24481=CARTESIAN_POINT('Ctrl Pts',(7.02196354188821,0.486954234182196,3.60527961492189));
#24482=CARTESIAN_POINT('Ctrl Pts',(7.0060582632006,0.321096900356496,3.49898325846904));
#24483=CARTESIAN_POINT('Ctrl Pts',(6.99015298451299,0.155239566530797,3.3926869020162));
#24484=CARTESIAN_POINT('Ctrl Pts',(6.97424770582538,-0.0686435894062663,
3.37692967703231));
#24485=CARTESIAN_POINT('Ctrl Pts',(6.95834242713776,-0.247754555527299,
3.45894666907189));
#24486=CARTESIAN_POINT('Ctrl Pts',(6.94243714845015,-0.426865521648332,
3.54096366111146));
#24487=CARTESIAN_POINT('Ctrl Pts',(6.92653186976253,-0.561204297953336,
3.72075487017451));
#24488=CARTESIAN_POINT('Ctrl Pts',(6.91062659107492,-0.589088840804576,
3.91576771430201));
#24489=CARTESIAN_POINT('Ctrl Pts',(6.89472131238731,-0.616973383655816,
4.11078055842951));
#24490=CARTESIAN_POINT('Ctrl Pts',(6.8788160336997,-0.538403693053295,4.32101503762147));
#24491=CARTESIAN_POINT('Ctrl Pts',(6.86291075501209,-0.389454440281117,
4.44994049623482));
#24492=CARTESIAN_POINT('Ctrl Pts',(6.85155564042725,-0.283116420949728,
4.54198310574898));
#24493=CARTESIAN_POINT('Ctrl Pts',(6.8402005258424,-0.140907108175025,4.59258385846765));
#24494=CARTESIAN_POINT('Ctrl Pts',(6.82884541125756,0.000528213615369061,
4.5937871332276));
#24495=CARTESIAN_POINT('Ctrl Pts',(6.72115458874249,0.000109070110168276,
4.59505938903171));
#24496=CARTESIAN_POINT('Ctrl Pts',(6.73660922304319,-0.191322006690816,
4.59459701474307));
#24497=CARTESIAN_POINT('Ctrl Pts',(6.75206385734389,-0.38318268672033,4.49389457135631));
#24498=CARTESIAN_POINT('Ctrl Pts',(6.76751849164459,-0.49122657597837,4.33588597251985));
#24499=CARTESIAN_POINT('Ctrl Pts',(6.78342377033221,-0.60242093591639,4.17326997329048));
#24500=CARTESIAN_POINT('Ctrl Pts',(6.79932904901982,-0.624839182280325,
3.94995709318712));
#24501=CARTESIAN_POINT('Ctrl Pts',(6.81523432770743,-0.548195780923551,
3.76848141254984));
#24502=CARTESIAN_POINT('Ctrl Pts',(6.83113960639504,-0.471552379566775,
3.58700573191256));
#24503=CARTESIAN_POINT('Ctrl Pts',(6.84704488508266,-0.295847330489284,
3.44736725074137));
#24504=CARTESIAN_POINT('Ctrl Pts',(6.86295016377027,-0.101752734572189,
3.41368297698799));
#24505=CARTESIAN_POINT('Ctrl Pts',(6.87885544245788,0.0923418613449005,
3.37999870323461));
#24506=CARTESIAN_POINT('Ctrl Pts',(6.8947607211455,0.304826004101594,3.45226863689903));
#24507=CARTESIAN_POINT('Ctrl Pts',(6.91066599983311,0.438133727661537,3.59730899203965));
#24508=CARTESIAN_POINT('Ctrl Pts',(6.92657127852072,0.571441451221483,3.74234934718029));
#24509=CARTESIAN_POINT('Ctrl Pts',(6.94247655720833,0.625572755584675,3.96016012379713));
#24510=CARTESIAN_POINT('Ctrl Pts',(6.95838183589594,0.57567402069499,4.15073208753033));
#24511=CARTESIAN_POINT('Ctrl Pts',(6.97428711458356,0.525775285805305,4.34130405126353));
#24512=CARTESIAN_POINT('Ctrl Pts',(6.99019239327118,0.371846511662747,4.5046372021131));
#24513=CARTESIAN_POINT('Ctrl Pts',(7.00609767195879,0.184564651688987,4.56573572985967));
#24514=CARTESIAN_POINT('Ctrl Pts',(7.01111664422002,0.125467135782336,4.58501560681028));
#24515=CARTESIAN_POINT('Ctrl Pts',(7.01613561648126,0.0630485115161635,
4.59411554829291));
#24516=CARTESIAN_POINT('Ctrl Pts',(7.02115458874249,0.000491936389841303,
4.5936290357477));
#24517=CARTESIAN_POINT('Origin',(4.,0.,4.));
#24518=CARTESIAN_POINT('',(7.42884541125756,-0.000438237927964824,4.59464495791636));
#24519=CARTESIAN_POINT('',(7.32115458874249,-0.000317338366111653,4.59328419319629));
#24520=CARTESIAN_POINT('',(4.,-7.27562663373442E-17,4.5941));
#24521=CARTESIAN_POINT('Ctrl Pts',(7.42884541125756,-0.000438237927964824,
4.59464495791636));
#24522=CARTESIAN_POINT('Ctrl Pts',(7.41515859140615,0.169409178821721,4.5932420274804));
#24523=CARTESIAN_POINT('Ctrl Pts',(7.40147177155473,0.340360224580004,4.51673272682389));
#24524=CARTESIAN_POINT('Ctrl Pts',(7.38778495170331,0.450965110664874,4.38826722161738));
#24525=CARTESIAN_POINT('Ctrl Pts',(7.37187967301569,0.579497637321094,4.23897909740477));
#24526=CARTESIAN_POINT('Ctrl Pts',(7.35597439432808,0.626535888751401,4.01952688559808));
#24527=CARTESIAN_POINT('Ctrl Pts',(7.34006911564046,0.570481892017836,3.83067375781486));
#24528=CARTESIAN_POINT('Ctrl Pts',(7.32416383695285,0.51442789528427,3.64182063003164));
#24529=CARTESIAN_POINT('Ctrl Pts',(7.30825855826524,0.355281650386831,3.48356658627189));
#24530=CARTESIAN_POINT('Ctrl Pts',(7.29235327957763,0.166116376105148,3.42857518785077));
#24531=CARTESIAN_POINT('Ctrl Pts',(7.27644800089002,-0.023048898176535,
3.37358378942964));
#24532=CARTESIAN_POINT('Ctrl Pts',(7.2605427222024,-0.242233201842457,3.42185503634715));
#24533=CARTESIAN_POINT('Ctrl Pts',(7.24463744351479,-0.390796368104757,
3.5512248149675));
#24534=CARTESIAN_POINT('Ctrl Pts',(7.22873216482718,-0.539359534367058,
3.68059459358785));
#24535=CARTESIAN_POINT('Ctrl Pts',(7.21282688613957,-0.617301563225728,
3.89106290391106));
#24536=CARTESIAN_POINT('Ctrl Pts',(7.19692160745195,-0.588834786584626,
4.08599160058025));
#24537=CARTESIAN_POINT('Ctrl Pts',(7.18101632876434,-0.560368009943526,
4.28092029724944));
#24538=CARTESIAN_POINT('Ctrl Pts',(7.16511105007672,-0.425492427802657,
4.46030938026461));
#24539=CARTESIAN_POINT('Ctrl Pts',(7.14920577138911,-0.24613717474127,4.54179097474357));
#24540=CARTESIAN_POINT('Ctrl Pts',(7.1424189846786,-0.169606239833077,4.57655919310821));
#24541=CARTESIAN_POINT('Ctrl Pts',(7.13563219796808,-0.0849767524450092,
4.59350108952231));
#24542=CARTESIAN_POINT('Ctrl Pts',(7.12884541125757,-0.000233413975479213,
4.59320261234329));
#24543=CARTESIAN_POINT('Ctrl Pts',(7.02115458874249,0.000491936389841303,
4.5936290357477));
#24544=CARTESIAN_POINT('Ctrl Pts',(7.03204089516887,-0.135195214358064,
4.59257377495492));
#24545=CARTESIAN_POINT('Ctrl Pts',(7.04292720159524,-0.271531381894462,
4.54641716720817));
#24546=CARTESIAN_POINT('Ctrl Pts',(7.05381350802162,-0.376033620593693,
4.46121547122365));
#24547=CARTESIAN_POINT('Ctrl Pts',(7.06971878670923,-0.528715087097646,
4.33673278019746));
#24548=CARTESIAN_POINT('Ctrl Pts',(7.08562406539685,-0.613443074300594,
4.1289034935015));
#24549=CARTESIAN_POINT('Ctrl Pts',(7.10152934408446,-0.591314251018945,
3.93315398851514));
#24550=CARTESIAN_POINT('Ctrl Pts',(7.11743462277207,-0.569185427737295,
3.73740448352876));
#24551=CARTESIAN_POINT('Ctrl Pts',(7.13333990145968,-0.440199793971044,
3.55373476025198));
#24552=CARTESIAN_POINT('Ctrl Pts',(7.14924518014729,-0.263582002606135,
3.46647820559892));
#24553=CARTESIAN_POINT('Ctrl Pts',(7.16515045883491,-0.0869642112412332,
3.37922165094586));
#24554=CARTESIAN_POINT('Ctrl Pts',(7.18105573752253,0.137285737722324,3.38837826491652));
#24555=CARTESIAN_POINT('Ctrl Pts',(7.19696101621014,0.306201705590428,3.48974370695041));
#24556=CARTESIAN_POINT('Ctrl Pts',(7.21286629489775,0.47511767345854,3.59110914898431));
#24557=CARTESIAN_POINT('Ctrl Pts',(7.22877157358536,0.588699660231196,3.78468341908144));
#24558=CARTESIAN_POINT('Ctrl Pts',(7.24467685227297,0.594795648982816,3.98158540759));
#24559=CARTESIAN_POINT('Ctrl Pts',(7.26058213096058,0.600891637734436,4.17848739609855));
#24560=CARTESIAN_POINT('Ctrl Pts',(7.2764874096482,0.499501628465021,4.37871710301853));
#24561=CARTESIAN_POINT('Ctrl Pts',(7.29239268833581,0.337179610128186,4.49033751492072));
#24562=CARTESIAN_POINT('Ctrl Pts',(7.30197998847137,0.239335998647354,4.5576194790522));
#24563=CARTESIAN_POINT('Ctrl Pts',(7.31156728860693,0.119353510611835,4.59270637405629));
#24564=CARTESIAN_POINT('Ctrl Pts',(7.32115458874249,-0.000317338366111653,
4.59328419319629));
#24565=CARTESIAN_POINT('Origin',(4.,0.,4.));
#24566=CARTESIAN_POINT('',(7.72884541125757,0.000455182276646732,4.59460030787683));
#24567=CARTESIAN_POINT('',(7.62115458874249,-0.000367422317862595,4.59479267874092));
#24568=CARTESIAN_POINT('',(4.,-7.27562663373442E-17,4.5941));
#24569=CARTESIAN_POINT('Ctrl Pts',(7.72884541125757,0.000455182276646732,
4.59460030787683));
#24570=CARTESIAN_POINT('Ctrl Pts',(7.72649554221944,0.0296217258780686,
4.59484761241511));
#24571=CARTESIAN_POINT('Ctrl Pts',(7.72414567318131,0.0587549042441869,
4.59288776399295));
#24572=CARTESIAN_POINT('Ctrl Pts',(7.72179580414318,0.0875427725731367,
4.58860617484604));
#24573=CARTESIAN_POINT('Ctrl Pts',(7.70589052545556,0.282395788279217,4.55962589232715));
#24574=CARTESIAN_POINT('Ctrl Pts',(7.68998524676794,0.461428877889185,4.42427810603975));
#24575=CARTESIAN_POINT('Ctrl Pts',(7.67407996808033,0.542437620895056,4.24470879335187));
#24576=CARTESIAN_POINT('Ctrl Pts',(7.65817468939272,0.623446363900926,4.065139480664));
#24577=CARTESIAN_POINT('Ctrl Pts',(7.64226941070511,0.606430760302702,3.84134864157567));
#24578=CARTESIAN_POINT('Ctrl Pts',(7.6263641320175,0.499203655448083,3.67609156159133));
#24579=CARTESIAN_POINT('Ctrl Pts',(7.61045885332988,0.391976550593464,3.51083448160699));
#24580=CARTESIAN_POINT('Ctrl Pts',(7.59455357464227,0.19453794448245,3.40411116072664));
#24581=CARTESIAN_POINT('Ctrl Pts',(7.57864829595466,-0.00245670798462758,
3.40492443279829));
#24582=CARTESIAN_POINT('Ctrl Pts',(7.56274301726704,-0.199451360451705,
3.40573770486994));
#24583=CARTESIAN_POINT('Ctrl Pts',(7.54683773857943,-0.396002059274846,
3.5140875698936));
#24584=CARTESIAN_POINT('Ctrl Pts',(7.53093245989182,-0.50186103876401,3.68022435377194));
#24585=CARTESIAN_POINT('Ctrl Pts',(7.51502718120421,-0.607720018253171,
3.84636113765028));
#24586=CARTESIAN_POINT('Ctrl Pts',(7.4991219025166,-0.622887278408357,4.07028484038331));
#24587=CARTESIAN_POINT('Ctrl Pts',(7.48321662382898,-0.540398655351294,
4.24917917107494));
#24588=CARTESIAN_POINT('Ctrl Pts',(7.46731134514137,-0.45791003229423,4.42807350176658));
#24589=CARTESIAN_POINT('Ctrl Pts',(7.45140606645375,-0.277765526024924,
4.56193846041682));
#24590=CARTESIAN_POINT('Ctrl Pts',(7.43550078776614,-0.0826798719492015,
4.58930892143267));
#24591=CARTESIAN_POINT('Ctrl Pts',(7.43328232892995,-0.0554694406452989,
4.59312653709876));
#24592=CARTESIAN_POINT('Ctrl Pts',(7.43106387009376,-0.0279683367079049,
4.5948723550368));
#24593=CARTESIAN_POINT('Ctrl Pts',(7.42884541125756,-0.000438237927964824,
4.59464495791636));
#24594=CARTESIAN_POINT('Ctrl Pts',(7.32115458874249,-0.000317338366111653,
4.59328419319629));
#24595=CARTESIAN_POINT('Ctrl Pts',(7.32747256729455,-0.0791797758050172,
4.59366497286126));
#24596=CARTESIAN_POINT('Ctrl Pts',(7.3337905458466,-0.157906876560309,4.57905936436794));
#24597=CARTESIAN_POINT('Ctrl Pts',(7.34010852439865,-0.230073660466993,
4.54880513582638));
#24598=CARTESIAN_POINT('Ctrl Pts',(7.35601380308626,-0.411750885321067,
4.47264122794544));
#24599=CARTESIAN_POINT('Ctrl Pts',(7.37191908177388,-0.551851307624962,
4.29730229529918));
#24600=CARTESIAN_POINT('Ctrl Pts',(7.38782436046149,-0.586046744500155,
4.10329655692985));
#24601=CARTESIAN_POINT('Ctrl Pts',(7.4037296391491,-0.620242181375348,3.90929081856053));
#24602=CARTESIAN_POINT('Ctrl Pts',(7.41963491783671,-0.548532632821828,
3.69661827446815));
#24603=CARTESIAN_POINT('Ctrl Pts',(7.43554019652432,-0.403844087697925,
3.56292915991696));
#24604=CARTESIAN_POINT('Ctrl Pts',(7.45144547521194,-0.259155542574025,
3.42924004536577));
#24605=CARTESIAN_POINT('Ctrl Pts',(7.46735075389955,-0.0414880008797467,
3.37453436035576));
#24606=CARTESIAN_POINT('Ctrl Pts',(7.48325603258717,0.149214809903968,3.42393064079835));
#24607=CARTESIAN_POINT('Ctrl Pts',(7.49916131127478,0.339917620687686,3.47332692124094));
#24608=CARTESIAN_POINT('Ctrl Pts',(7.51506658996239,0.50365570056084,3.62682516713614));
#24609=CARTESIAN_POINT('Ctrl Pts',(7.53097186865001,0.56524745100941,3.81394547807041));
#24610=CARTESIAN_POINT('Ctrl Pts',(7.54687714733762,0.626839201457978,4.00106578900469));
#24611=CARTESIAN_POINT('Ctrl Pts',(7.56278242602523,0.58628462248197,4.22180816497804));
#24612=CARTESIAN_POINT('Ctrl Pts',(7.57868770471284,0.462204660718925,4.3748170457164));
#24613=CARTESIAN_POINT('Ctrl Pts',(7.59284333272272,0.351774041004839,4.51099427596058));
#24614=CARTESIAN_POINT('Ctrl Pts',(7.60699896073261,0.175183620117616,4.59352033541115));
#24615=CARTESIAN_POINT('Ctrl Pts',(7.62115458874249,-0.000367422317862596,
4.59479267874092));
#24616=CARTESIAN_POINT('Origin',(4.,0.,4.));
#24617=CARTESIAN_POINT('',(8.02884541125756,0.000208508845897126,4.59318438507865));
#24618=CARTESIAN_POINT('',(7.92115458874249,0.000504499356536197,4.59443266285439));
#24619=CARTESIAN_POINT('',(4.,-7.27562663373442E-17,4.5941));
#24620=CARTESIAN_POINT('Ctrl Pts',(8.02884541125756,0.000208508845897126,
4.59318438507865));
#24621=CARTESIAN_POINT('Ctrl Pts',(8.02192721434511,0.0865993248636432,
4.5934556945658));
#24622=CARTESIAN_POINT('Ctrl Pts',(8.01500901743265,0.17288466952141,4.57582457789876));
#24623=CARTESIAN_POINT('Ctrl Pts',(8.0080908205202,0.250602156771344,4.53974023855861));
#24624=CARTESIAN_POINT('Ctrl Pts',(7.99218554183259,0.42927852421987,4.4567805482338));
#24625=CARTESIAN_POINT('Ctrl Pts',(7.97628026314498,0.562668370741438,4.27628395749428));
#24626=CARTESIAN_POINT('Ctrl Pts',(7.96037498445736,0.589524722071826,4.08112686462655));
#24627=CARTESIAN_POINT('Ctrl Pts',(7.94446970576975,0.616381073402214,3.88596977175883));
#24628=CARTESIAN_POINT('Ctrl Pts',(7.92856442708213,0.536703929541425,3.67615217676291));
#24629=CARTESIAN_POINT('Ctrl Pts',(7.91265914839452,0.387077664089382,3.54801344261061));
#24630=CARTESIAN_POINT('Ctrl Pts',(7.89675386970691,0.237451398637336,3.41987470845831));
#24631=CARTESIAN_POINT('Ctrl Pts',(7.88084859101929,0.0178760115940344,
3.37341483514963));
#24632=CARTESIAN_POINT('Ctrl Pts',(7.86494331233168,-0.170828768780714,
3.42996623095257));
#24633=CARTESIAN_POINT('Ctrl Pts',(7.84903803364407,-0.359533549155462,
3.48651762675552));
#24634=CARTESIAN_POINT('Ctrl Pts',(7.83313275495647,-0.517367722861657,
3.64608029167009));
#24635=CARTESIAN_POINT('Ctrl Pts',(7.81722747626885,-0.571860514742998,
3.83538980050754));
#24636=CARTESIAN_POINT('Ctrl Pts',(7.80132219758124,-0.626353306624339,
4.02469930934499));
#24637=CARTESIAN_POINT('Ctrl Pts',(7.78541691889362,-0.577504716680827,
4.24375566210532));
#24638=CARTESIAN_POINT('Ctrl Pts',(7.769511640206,-0.447743950807975,4.3919774491103));
#24639=CARTESIAN_POINT('Ctrl Pts',(7.75595623055652,-0.337154229471824,
4.51830073342946));
#24640=CARTESIAN_POINT('Ctrl Pts',(7.74240082090705,-0.16779438404434,4.593173711641));
#24641=CARTESIAN_POINT('Ctrl Pts',(7.72884541125757,0.000455182276646732,
4.59460030787683));
#24642=CARTESIAN_POINT('Ctrl Pts',(7.62115458874249,-0.000367422317862596,
4.59479267874092));
#24643=CARTESIAN_POINT('Ctrl Pts',(7.62290423942022,-0.022065717876263,
4.59494994172972));
#24644=CARTESIAN_POINT('Ctrl Pts',(7.62465389009795,-0.043748134618359,
4.59386587358433));
#24645=CARTESIAN_POINT('Ctrl Pts',(7.62640354077568,-0.0652877816099521,
4.59148835294282));
#24646=CARTESIAN_POINT('Ctrl Pts',(7.64230881946329,-0.261094917625702,
4.56987539392751));
#24647=CARTESIAN_POINT('Ctrl Pts',(7.6582140981509,-0.445103845107109,4.44137409039354));
#24648=CARTESIAN_POINT('Ctrl Pts',(7.67411937683852,-0.532825449416136,
4.2649868044631));
#24649=CARTESIAN_POINT('Ctrl Pts',(7.69002465552613,-0.620547053725161,
4.08859951853267));
#24650=CARTESIAN_POINT('Ctrl Pts',(7.70592993421374,-0.611981334861803,
3.86432625020577));
#24651=CARTESIAN_POINT('Ctrl Pts',(7.72183521290136,-0.511061308497056,
3.69514379608856));
#24652=CARTESIAN_POINT('Ctrl Pts',(7.73774049158897,-0.410141282132307,
3.52596134197134));
#24653=CARTESIAN_POINT('Ctrl Pts',(7.75364577027658,-0.216866948266163,
3.4118697020638));
#24654=CARTESIAN_POINT('Ctrl Pts',(7.76955104896419,-0.0199817042712483,
3.40525493058698));
#24655=CARTESIAN_POINT('Ctrl Pts',(7.78545632765181,0.176903539723664,3.39864015911017));
#24656=CARTESIAN_POINT('Ctrl Pts',(7.80136160633942,0.377399693847348,3.49950225606407));
#24657=CARTESIAN_POINT('Ctrl Pts',(7.81726688502703,0.489447406431712,3.66152961365368));
#24658=CARTESIAN_POINT('Ctrl Pts',(7.83317216371464,0.601495119016078,3.82355697124329));
#24659=CARTESIAN_POINT('Ctrl Pts',(7.84907744240226,0.625094390061116,4.04674958946861));
#24660=CARTESIAN_POINT('Ctrl Pts',(7.86498272108987,0.549409432699027,4.22862686054007));
#24661=CARTESIAN_POINT('Ctrl Pts',(7.88088799977748,0.473724475336938,4.41050413161152));
#24662=CARTESIAN_POINT('Ctrl Pts',(7.89679327846509,0.298755289567731,4.55106605552911));
#24663=CARTESIAN_POINT('Ctrl Pts',(7.91269855715271,0.104840323164387,4.58577254351526));
#24664=CARTESIAN_POINT('Ctrl Pts',(7.9155172343493,0.0704753991278659,4.59192310448195));
#24665=CARTESIAN_POINT('Ctrl Pts',(7.91833591154589,0.0355154700816755,
4.59474920414003));
#24666=CARTESIAN_POINT('Ctrl Pts',(7.92115458874249,0.000504499356536197,
4.59443266285439));
#24667=CARTESIAN_POINT('Origin',(4.,0.,4.));
#24668=CARTESIAN_POINT('',(8.32884541125757,-0.000534402448739424,4.5938336238991));
#24669=CARTESIAN_POINT('',(8.2211545887425,0.000116005647334215,4.59313666129657));
#24670=CARTESIAN_POINT('',(4.,-7.27562663373442E-17,4.5941));
#24671=CARTESIAN_POINT('Ctrl Pts',(8.32884541125757,-0.000534402448739424,
4.5938336238991));
#24672=CARTESIAN_POINT('Ctrl Pts',(8.31735888647079,0.142509087977489,4.59259298046846));
#24673=CARTESIAN_POINT('Ctrl Pts',(8.30587236168401,0.286359812054371,4.54070236535691));
#24674=CARTESIAN_POINT('Ctrl Pts',(8.29438583689723,0.393155811111917,4.44670960845581));
#24675=CARTESIAN_POINT('Ctrl Pts',(8.27848055820962,0.541035187969857,4.31655875596735));
#24676=CARTESIAN_POINT('Ctrl Pts',(8.262575279522,0.617867056310918,4.10568264439756));
#24677=CARTESIAN_POINT('Ctrl Pts',(8.24667000083439,0.588373472681163,3.91090666274675));
#24678=CARTESIAN_POINT('Ctrl Pts',(8.23076472214677,0.558879889051408,3.71613068109593));
#24679=CARTESIAN_POINT('Ctrl Pts',(8.21485944345917,0.423060853450833,3.53745482936408));
#24680=CARTESIAN_POINT('Ctrl Pts',(8.19895416477155,0.243278720997716,3.45691949951456));
#24681=CARTESIAN_POINT('Ctrl Pts',(8.18304888608394,0.0634965885445972,
3.37638416966503));
#24682=CARTESIAN_POINT('Ctrl Pts',(8.16714360739632,-0.160248640761069,
3.39398936169784));
#24683=CARTESIAN_POINT('Ctrl Pts',(8.15123832870871,-0.325222623502191,
3.50165151624576));
#24684=CARTESIAN_POINT('Ctrl Pts',(8.1353330500211,-0.490196606243315,3.60931367079368));
#24685=CARTESIAN_POINT('Ctrl Pts',(8.11942777133349,-0.59639934241989,3.80703278785672));
#24686=CARTESIAN_POINT('Ctrl Pts',(8.10352249264588,-0.595067028646789,
4.00402461368555));
#24687=CARTESIAN_POINT('Ctrl Pts',(8.08761721395827,-0.593734714873688,
4.20101643951437));
#24688=CARTESIAN_POINT('Ctrl Pts',(8.07171193527065,-0.484867351150922,
4.39728097410898));
#24689=CARTESIAN_POINT('Ctrl Pts',(8.05580665658303,-0.3184522251018,4.50270184645125));
#24690=CARTESIAN_POINT('Ctrl Pts',(8.04681957480788,-0.224421408301879,
4.56226861162124));
#24691=CARTESIAN_POINT('Ctrl Pts',(8.03783249303272,-0.112017456676448,
4.59283194056482));
#24692=CARTESIAN_POINT('Ctrl Pts',(8.02884541125756,0.000208508845897126,
4.59318438507865));
#24693=CARTESIAN_POINT('Ctrl Pts',(7.92115458874249,0.000504499356536197,
4.59443266285439));
#24694=CARTESIAN_POINT('Ctrl Pts',(7.93424119023351,-0.162045019349314,
4.59296301969496));
#24695=CARTESIAN_POINT('Ctrl Pts',(7.94732779172453,-0.325694779556815,
4.52375140444135));
#24696=CARTESIAN_POINT('Ctrl Pts',(7.96041439321555,-0.436005268305889,
4.40499428651169));
#24697=CARTESIAN_POINT('Ctrl Pts',(7.97631967190316,-0.570075146335334,
4.26065848946726));
#24698=CARTESIAN_POINT('Ctrl Pts',(7.99222495059077,-0.625354155356748,
4.04313584332371));
#24699=CARTESIAN_POINT('Ctrl Pts',(8.00813022927838,-0.576460513088508,
3.85230354456612));
#24700=CARTESIAN_POINT('Ctrl Pts',(8.024035507966,-0.527566870820267,3.66147124580852));
#24701=CARTESIAN_POINT('Ctrl Pts',(8.03994078665361,-0.374500577262366,
3.49732929443689));
#24702=CARTESIAN_POINT('Ctrl Pts',(8.05584606534123,-0.187543198716277,
3.43524473024767));
#24703=CARTESIAN_POINT('Ctrl Pts',(8.07175134402884,-0.000585820170193818,
3.37316016605846));
#24704=CARTESIAN_POINT('Ctrl Pts',(8.08765662271645,0.220262643364076,3.41313298905166));
#24705=CARTESIAN_POINT('Ctrl Pts',(8.10356190140406,0.37359792075985,3.53680937001953));
#24706=CARTESIAN_POINT('Ctrl Pts',(8.11946718009167,0.526933198155627,3.66048575098741));
#24707=CARTESIAN_POINT('Ctrl Pts',(8.13537245877928,0.612755289412907,3.86786568992997));
#24708=CARTESIAN_POINT('Ctrl Pts',(8.1512777374669,0.591658321059451,4.06372909240644));
#24709=CARTESIAN_POINT('Ctrl Pts',(8.16718301615451,0.570561352705995,4.2595924948829));
#24710=CARTESIAN_POINT('Ctrl Pts',(8.18308829484212,0.44254532474181,4.44393936089328));
#24711=CARTESIAN_POINT('Ctrl Pts',(8.19899357352974,0.266389781296621,4.53212540863836));
#24712=CARTESIAN_POINT('Ctrl Pts',(8.20638057860065,0.184576572093718,4.57308230066594));
#24713=CARTESIAN_POINT('Ctrl Pts',(8.21376758367158,0.0923795717789203,
4.59329710918813));
#24714=CARTESIAN_POINT('Ctrl Pts',(8.2211545887425,0.000116005647334215,
4.59313666129657));
#24715=CARTESIAN_POINT('Origin',(4.,0.,4.));
#24716=CARTESIAN_POINT('',(8.62884541125757,3.48566139269993E-5,4.59507810043999));
#24717=CARTESIAN_POINT('',(8.5211545887425,-0.000547905086566465,4.594005652201));
#24718=CARTESIAN_POINT('',(4.,-7.27562663373442E-17,4.5941));
#24719=CARTESIAN_POINT('Ctrl Pts',(8.62884541125757,3.48566139269993E-5,
4.59507810043999));
#24720=CARTESIAN_POINT('Ctrl Pts',(8.62869583728408,0.00188744051982823,
4.59507966949126));
#24721=CARTESIAN_POINT('Ctrl Pts',(8.62854626331059,0.00374001065808006,
4.59507176912216));
#24722=CARTESIAN_POINT('Ctrl Pts',(8.6283966893371,0.00559249142073073,
4.59505435897699));
#24723=CARTESIAN_POINT('Ctrl Pts',(8.61249141064948,0.202580123064263,4.59320301275402));
#24724=CARTESIAN_POINT('Ctrl Pts',(8.59658613196187,0.398557131004382,4.48381890612783));
#24725=CARTESIAN_POINT('Ctrl Pts',(8.58068085327426,0.503539164298441,4.31712659320126));
#24726=CARTESIAN_POINT('Ctrl Pts',(8.56477557458664,0.608521197592498,4.15043428027469));
#24727=CARTESIAN_POINT('Ctrl Pts',(8.54887029589904,0.622508256240502,3.92643376104774));
#24728=CARTESIAN_POINT('Ctrl Pts',(8.53296501721142,0.539078074654942,3.74797659726896));
#24729=CARTESIAN_POINT('Ctrl Pts',(8.51705973852381,0.455647893069379,3.56951943349019));
#24730=CARTESIAN_POINT('Ctrl Pts',(8.50115445983619,0.274800471250253,3.43660562515959));
#24731=CARTESIAN_POINT('Ctrl Pts',(8.48524918114857,0.0795732942734406,
3.41026356994308));
#24732=CARTESIAN_POINT('Ctrl Pts',(8.46934390246096,-0.115653882703369,
3.38392151472657));
#24733=CARTESIAN_POINT('Ctrl Pts',(8.45343862377335,-0.32526081483786,3.46415121262414));
#24734=CARTESIAN_POINT('Ctrl Pts',(8.43753334508574,-0.453004866631874,
3.61411458059983));
#24735=CARTESIAN_POINT('Ctrl Pts',(8.42162806639813,-0.580748918425883,
3.76407794857552));
#24736=CARTESIAN_POINT('Ctrl Pts',(8.40572278771052,-0.626630089879422,
3.98377498662932));
#24737=CARTESIAN_POINT('Ctrl Pts',(8.3898175090229,-0.569581688133314,4.17233010950212));
#24738=CARTESIAN_POINT('Ctrl Pts',(8.37391223033529,-0.512533286387202,
4.36088523237493));
#24739=CARTESIAN_POINT('Ctrl Pts',(8.35800695164768,-0.352555311441432,
4.51829844006673));
#24740=CARTESIAN_POINT('Ctrl Pts',(8.34210167296007,-0.163102881281137,
4.57229224720906));
#24741=CARTESIAN_POINT('Ctrl Pts',(8.33768291905923,-0.110469810133188,
4.58729263485501));
#24742=CARTESIAN_POINT('Ctrl Pts',(8.3332641651584,-0.0555618361628184,
4.59431088730997));
#24743=CARTESIAN_POINT('Ctrl Pts',(8.32884541125757,-0.000534402448739424,
4.5938336238991));
#24744=CARTESIAN_POINT('Ctrl Pts',(8.2211545887425,0.000116005647334215,
4.59313666129657));
#24745=CARTESIAN_POINT('Ctrl Pts',(8.22967286235919,-0.106277085140544,
4.59295164192424));
#24746=CARTESIAN_POINT('Ctrl Pts',(8.23819113597589,-0.212758691085218,
4.56567285125378));
#24747=CARTESIAN_POINT('Ctrl Pts',(8.24670940959258,-0.303508593564514,
4.51186277431583));
#24748=CARTESIAN_POINT('Ctrl Pts',(8.26261468828019,-0.472956366054245,
4.41138886276846));
#24749=CARTESIAN_POINT('Ctrl Pts',(8.2785199669678,-0.587556852107514,4.21841581019395));
#24750=CARTESIAN_POINT('Ctrl Pts',(8.29442524565541,-0.594690356875377,
4.02154867831793));
#24751=CARTESIAN_POINT('Ctrl Pts',(8.31033052434302,-0.60182386164324,3.82468154644191));
#24752=CARTESIAN_POINT('Ctrl Pts',(8.32623580303064,-0.501490385125681,
3.62392033526436));
#24753=CARTESIAN_POINT('Ctrl Pts',(8.34214108171825,-0.339758814980244,
3.51144609945163));
#24754=CARTESIAN_POINT('Ctrl Pts',(8.35804636040587,-0.178027244834812,
3.3989718636389));
#24755=CARTESIAN_POINT('Ctrl Pts',(8.37395163909348,0.0451024189384938,
3.37478460319097));
#24756=CARTESIAN_POINT('Ctrl Pts',(8.38985691778109,0.227178474572579,3.44999008482693));
#24757=CARTESIAN_POINT('Ctrl Pts',(8.4057621964687,0.40925453020667,3.5251955664629));
#24758=CARTESIAN_POINT('Ctrl Pts',(8.42166747515631,0.550276977701535,3.69979379018275));
#24759=CARTESIAN_POINT('Ctrl Pts',(8.43757275384392,0.585494275335268,3.89361663829603));
#24760=CARTESIAN_POINT('Ctrl Pts',(8.45347803253154,0.620711572969,4.0874394864093));
#24761=CARTESIAN_POINT('Ctrl Pts',(8.46938331121915,0.550123720741606,4.30048695891599));
#24762=CARTESIAN_POINT('Ctrl Pts',(8.48528858990677,0.406141674070155,4.4349366697363));
#24763=CARTESIAN_POINT('Ctrl Pts',(8.49724392285201,0.297916389879728,4.53599689564107));
#24764=CARTESIAN_POINT('Ctrl Pts',(8.50919925579725,0.148224117540273,4.59265016978245));
#24765=CARTESIAN_POINT('Ctrl Pts',(8.5211545887425,-0.000547905086566465,
4.594005652201));
#24766=CARTESIAN_POINT('Origin',(4.,0.,4.));
#24767=CARTESIAN_POINT('',(8.92884541125757,0.000516595407308196,4.59372894893997));
#24768=CARTESIAN_POINT('',(8.82115458874249,0.000142235148737217,4.59503945166131));
#24769=CARTESIAN_POINT('',(4.,-7.27562663373442E-17,4.5941));
#24770=CARTESIAN_POINT('Ctrl Pts',(8.92884541125757,0.000516595407308196,
4.59372894893997));
#24771=CARTESIAN_POINT('Ctrl Pts',(8.92412750940976,0.0592956068199462,
4.59421507565108));
#24772=CARTESIAN_POINT('Ctrl Pts',(8.91940960756194,0.117944888069788,4.58619493689145));
#24773=CARTESIAN_POINT('Ctrl Pts',(8.91469170571413,0.17383025386194,4.56912565303288));
#24774=CARTESIAN_POINT('Ctrl Pts',(8.89878642702651,0.362234410233906,4.51158064138869));
#24775=CARTESIAN_POINT('Ctrl Pts',(8.8828811483389,0.519225559109383,4.35118846702123));
#24776=CARTESIAN_POINT('Ctrl Pts',(8.86697586965128,0.572720006672535,4.16159443076672));
#24777=CARTESIAN_POINT('Ctrl Pts',(8.85107059096367,0.626214454235688,3.97200039451221));
#24778=CARTESIAN_POINT('Ctrl Pts',(8.83516531227606,0.576212200486512,3.75320449637065));
#24779=CARTESIAN_POINT('Ctrl Pts',(8.81926003358845,0.445672164925724,3.60566855627755));
#24780=CARTESIAN_POINT('Ctrl Pts',(8.80335475490084,0.315132129364936,3.45813261618446));
#24781=CARTESIAN_POINT('Ctrl Pts',(8.78744947621322,0.104054311992536,3.38185663413984));
#24782=CARTESIAN_POINT('Ctrl Pts',(8.77154419752561,-0.0906432834200916,
3.41186331412789));
#24783=CARTESIAN_POINT('Ctrl Pts',(8.755638918838,-0.285340878832719,3.44186999411594));
#24784=CARTESIAN_POINT('Ctrl Pts',(8.73973364015038,-0.463658252285575,
3.57815933613666));
#24785=CARTESIAN_POINT('Ctrl Pts',(8.72382836146277,-0.543719609875046,
3.75815304026071));
#24786=CARTESIAN_POINT('Ctrl Pts',(8.70792308277515,-0.623780967464517,
3.93814674438476));
#24787=CARTESIAN_POINT('Ctrl Pts',(8.69201780408754,-0.605586309190603,
4.16184481061213));
#24788=CARTESIAN_POINT('Ctrl Pts',(8.67611252539993,-0.497489852380174,
4.32653455081593));
#24789=CARTESIAN_POINT('Ctrl Pts',(8.66035682068581,-0.390409939629295,
4.48967554111606));
#24790=CARTESIAN_POINT('Ctrl Pts',(8.64460111597169,-0.195111159088962,
4.59491282095998));
#24791=CARTESIAN_POINT('Ctrl Pts',(8.62884541125757,3.48566139269993E-5,
4.59507810043999));
#24792=CARTESIAN_POINT('Ctrl Pts',(8.5211545887425,-0.000547905086566465,
4.594005652201));
#24793=CARTESIAN_POINT('Ctrl Pts',(8.52510453448487,-0.0497009834700827,
4.59445349267793));
#24794=CARTESIAN_POINT('Ctrl Pts',(8.52905448022724,-0.0987536084630192,
4.58886509038946));
#24795=CARTESIAN_POINT('Ctrl Pts',(8.53300442596961,-0.146177075786514,
4.57684766499685));
#24796=CARTESIAN_POINT('Ctrl Pts',(8.54890970465722,-0.337137537856201,
4.52845700030318));
#24797=CARTESIAN_POINT('Ctrl Pts',(8.56481498334483,-0.501682220880061,
4.37582372178193));
#24798=CARTESIAN_POINT('Ctrl Pts',(8.58072026203244,-0.564259167724997,
4.18903057354857));
#24799=CARTESIAN_POINT('Ctrl Pts',(8.59662554072005,-0.626836114569933,
4.00223742531521));
#24800=CARTESIAN_POINT('Ctrl Pts',(8.61253081940767,-0.587445325235947,
3.78128440736974));
#24801=CARTESIAN_POINT('Ctrl Pts',(8.62843609809528,-0.464173383698336,
3.62762379780141));
#24802=CARTESIAN_POINT('Ctrl Pts',(8.6443413767829,-0.340901442160722,3.47396318823307));
#24803=CARTESIAN_POINT('Ctrl Pts',(8.66024665547051,-0.133748348419481,
3.38759498704188));
#24804=CARTESIAN_POINT('Ctrl Pts',(8.67615193415812,0.0621699608040676,
3.40817581827756));
#24805=CARTESIAN_POINT('Ctrl Pts',(8.69205721284573,0.25808827002761,3.42875664951325));
#24806=CARTESIAN_POINT('Ctrl Pts',(8.70796249153334,0.44277179473346,3.55628651317581));
#24807=CARTESIAN_POINT('Ctrl Pts',(8.72386777022095,0.531421673692279,3.73220909121499));
#24808=CARTESIAN_POINT('Ctrl Pts',(8.73977304890857,0.620071552651101,3.90813166925417));
#24809=CARTESIAN_POINT('Ctrl Pts',(8.75567832759618,0.612687785862888,4.13244696166997));
#24810=CARTESIAN_POINT('Ctrl Pts',(8.7715836062838,0.512660686655375,4.30215887618246));
#24811=CARTESIAN_POINT('Ctrl Pts',(8.78748888497141,0.412633587447865,4.47187079069495));
#24812=CARTESIAN_POINT('Ctrl Pts',(8.80339416365902,0.21996315582106,4.58697932730413));
#24813=CARTESIAN_POINT('Ctrl Pts',(8.81929944234663,0.0231155027642346,
4.59463151583965));
#24814=CARTESIAN_POINT('Ctrl Pts',(8.81991782447859,0.0154622529370322,
4.59492902566351));
#24815=CARTESIAN_POINT('Ctrl Pts',(8.82053620661054,0.00780268890311657,
4.59506410656044));
#24816=CARTESIAN_POINT('Ctrl Pts',(8.82115458874249,0.000142235148737217,
4.59503945166131));
#24817=CARTESIAN_POINT('Origin',(4.,0.,4.));
#24818=CARTESIAN_POINT('',(9.22884541125756,-0.000264402795292107,4.59322887297718));
#24819=CARTESIAN_POINT('',(9.12115458874249,0.000475196148639644,4.59357609051269));
#24820=CARTESIAN_POINT('',(4.,-7.27562663373442E-17,4.5941));
#24821=CARTESIAN_POINT('Ctrl Pts',(9.22884541125756,-0.000264402795292107,
4.59322887297718));
#24822=CARTESIAN_POINT('Ctrl Pts',(9.21955918153543,0.115675446261185,4.59276508993807));
#24823=CARTESIAN_POINT('Ctrl Pts',(9.21027295181329,0.231857423975292,4.55999255403315));
#24824=CARTESIAN_POINT('Ctrl Pts',(9.20098672209116,0.327844211240712,4.49662776730038));
#24825=CARTESIAN_POINT('Ctrl Pts',(9.18508144340355,0.492248565587605,4.38809775866155));
#24826=CARTESIAN_POINT('Ctrl Pts',(9.16917616471593,0.597407924103304,4.18982173958679));
#24827=CARTESIAN_POINT('Ctrl Pts',(9.15327088602831,0.595037558282966,3.99283966966863));
#24828=CARTESIAN_POINT('Ctrl Pts',(9.1373656073407,0.592667192462628,3.79585759975047));
#24829=CARTESIAN_POINT('Ctrl Pts',(9.12146032865309,0.482767102306254,3.60016947898891));
#24830=CARTESIAN_POINT('Ctrl Pts',(9.10555504996548,0.315798759724268,3.49562701355602));
#24831=CARTESIAN_POINT('Ctrl Pts',(9.08964977127787,0.148830417142278,3.39108454812312));
#24832=CARTESIAN_POINT('Ctrl Pts',(9.07374449259025,-0.0752061778653251,
3.37768773801888));
#24833=CARTESIAN_POINT('Ctrl Pts',(9.05783921390264,-0.253442899077741,
3.46158783167087));
#24834=CARTESIAN_POINT('Ctrl Pts',(9.04193393521502,-0.431679620290152,
3.54548792532286));
#24835=CARTESIAN_POINT('Ctrl Pts',(9.02602865652741,-0.56411646770738,3.72668492273107));
#24836=CARTESIAN_POINT('Ctrl Pts',(9.0101233778398,-0.589944043936388,3.92198082849844));
#24837=CARTESIAN_POINT('Ctrl Pts',(8.99421809915219,-0.615771620165397,
4.11727673426582));
#24838=CARTESIAN_POINT('Ctrl Pts',(8.97831282046457,-0.534989925206181,
4.32667154839236));
#24839=CARTESIAN_POINT('Ctrl Pts',(8.96240754177696,-0.384690495792338,
4.45402003099517));
#24840=CARTESIAN_POINT('Ctrl Pts',(8.95122016493716,-0.278973620993485,
4.54359378149875));
#24841=CARTESIAN_POINT('Ctrl Pts',(8.94003278809737,-0.138863784294423,
4.59257621560968));
#24842=CARTESIAN_POINT('Ctrl Pts',(8.92884541125757,0.000516595407308196,
4.59372894893997));
#24843=CARTESIAN_POINT('Ctrl Pts',(8.82115458874249,0.000142235148737217,
4.59503945166131));
#24844=CARTESIAN_POINT('Ctrl Pts',(8.83644148529816,-0.189230254871984,
4.59442996300828));
#24845=CARTESIAN_POINT('Ctrl Pts',(8.85172838185382,-0.379146468724227,
4.49620311855542));
#24846=CARTESIAN_POINT('Ctrl Pts',(8.86701527840948,-0.487657002993039,
4.34104488491935));
#24847=CARTESIAN_POINT('Ctrl Pts',(8.88292055709709,-0.600556981206626,
4.17961022500168));
#24848=CARTESIAN_POINT('Ctrl Pts',(8.89882583578469,-0.62533206314696,3.95654506470448));
#24849=CARTESIAN_POINT('Ctrl Pts',(8.91473111447231,-0.550606579334316,
3.77427148852754));
#24850=CARTESIAN_POINT('Ctrl Pts',(8.93063639315992,-0.47588109552167,3.5919979123506));
#24851=CARTESIAN_POINT('Ctrl Pts',(8.94654167184753,-0.301655045956043,
3.45051592029392));
#24852=CARTESIAN_POINT('Ctrl Pts',(8.96244695053515,-0.107925661701669,
3.41478805750048));
#24853=CARTESIAN_POINT('Ctrl Pts',(8.97835222922276,0.0858037225526985,
3.37906019470703));
#24854=CARTESIAN_POINT('Ctrl Pts',(8.99425750791037,0.299036441495806,3.4490864611768));
#24855=CARTESIAN_POINT('Ctrl Pts',(9.01016278659798,0.433865051721373,3.5927137579139));
#24856=CARTESIAN_POINT('Ctrl Pts',(9.0260680652856,0.568693661946943,3.736341054651));
#24857=CARTESIAN_POINT('Ctrl Pts',(9.04197334397321,0.625118163454969,3.95356938165542));
#24858=CARTESIAN_POINT('Ctrl Pts',(9.05787862266082,0.577230812276762,4.14465668133936));
#24859=CARTESIAN_POINT('Ctrl Pts',(9.07378390134844,0.529343461098555,4.3357439810233));
#24860=CARTESIAN_POINT('Ctrl Pts',(9.08968918003605,0.377144257234124,4.50069025338676));
#24861=CARTESIAN_POINT('Ctrl Pts',(9.10559445872366,0.190516636080703,4.56375914846174));
#24862=CARTESIAN_POINT('Ctrl Pts',(9.11078116872994,0.129657384941762,4.58432590969837));
#24863=CARTESIAN_POINT('Ctrl Pts',(9.11596787873622,0.0651369761893139,
4.59405891310139));
#24864=CARTESIAN_POINT('Ctrl Pts',(9.12115458874249,0.000475196148639644,
4.59357609051269));
#24865=CARTESIAN_POINT('Origin',(4.,0.,4.));
#24866=CARTESIAN_POINT('',(9.52884541125756,-0.000414715089906426,4.59470005288553));
#24867=CARTESIAN_POINT('',(9.4211545887425,-0.000345133784900094,4.59331940772745));
#24868=CARTESIAN_POINT('',(4.,-7.27562663373442E-17,4.5941));
#24869=CARTESIAN_POINT('Ctrl Pts',(9.52884541125756,-0.000414715089906426,
4.59470005288553));
#24870=CARTESIAN_POINT('Ctrl Pts',(9.5149908536611,0.17147269131647,4.59333531965569));
#24871=CARTESIAN_POINT('Ctrl Pts',(9.50113629606464,0.344448366351018,4.51470554290992));
#24872=CARTESIAN_POINT('Ctrl Pts',(9.48728173846818,0.455032043431697,4.38349290156166));
#24873=CARTESIAN_POINT('Ctrl Pts',(9.47137645978057,0.581984072756561,4.23285845412795));
#24874=CARTESIAN_POINT('Ctrl Pts',(9.45547118109296,0.626706888961734,4.01292269047354));
#24875=CARTESIAN_POINT('Ctrl Pts',(9.43956590240535,0.56866566691212,3.82467080855373));
#24876=CARTESIAN_POINT('Ctrl Pts',(9.42366062371773,0.510624444862503,3.63641892663391));
#24877=CARTESIAN_POINT('Ctrl Pts',(9.40775534503012,0.349819184558098,3.47985092644869));
#24878=CARTESIAN_POINT('Ctrl Pts',(9.39185006634251,0.160084858421151,3.42685620983728));
#24879=CARTESIAN_POINT('Ctrl Pts',(9.37594478765489,-0.0296494677157886,
3.37386149322587));
#24880=CARTESIAN_POINT('Ctrl Pts',(9.36003950896728,-0.248312859685263,
3.42444006018826));
#24881=CARTESIAN_POINT('Ctrl Pts',(9.34413423027966,-0.395504338780113,
3.55536837257802));
#24882=CARTESIAN_POINT('Ctrl Pts',(9.32822895159205,-0.542695817874971,
3.6862966849678));
#24883=CARTESIAN_POINT('Ctrl Pts',(9.31232367290444,-0.618415384095196,
3.89757474278496));
#24884=CARTESIAN_POINT('Ctrl Pts',(9.29641839421683,-0.587895816063128,
4.09219260031737));
#24885=CARTESIAN_POINT('Ctrl Pts',(9.28051311552922,-0.55737624803106,4.28681045784976));
#24886=CARTESIAN_POINT('Ctrl Pts',(9.26460783684159,-0.42061754574671,4.4647681150974));
#24887=CARTESIAN_POINT('Ctrl Pts',(9.24870255815398,-0.240413519515492,
4.54435494461976));
#24888=CARTESIAN_POINT('Ctrl Pts',(9.24208350918851,-0.165420852186184,
4.57747534017911));
#24889=CARTESIAN_POINT('Ctrl Pts',(9.23546446022304,-0.0829041350566004,
4.59355944875842));
#24890=CARTESIAN_POINT('Ctrl Pts',(9.22884541125756,-0.000264402795292107,
4.59322887297718));
#24891=CARTESIAN_POINT('Ctrl Pts',(9.12115458874249,0.000475196148639644,
4.59357609051269));
#24892=CARTESIAN_POINT('Ctrl Pts',(9.13187315742383,-0.133151270259641,
4.59257831599443));
#24893=CARTESIAN_POINT('Ctrl Pts',(9.14259172610516,-0.267381477949042,
4.54795275857003));
#24894=CARTESIAN_POINT('Ctrl Pts',(9.1533102947865,-0.371151898503526,4.46515291500219));
#24895=CARTESIAN_POINT('Ctrl Pts',(9.16921557347411,-0.525136773491911,
4.34228626868117));
#24896=CARTESIAN_POINT('Ctrl Pts',(9.18512085216173,-0.612050485026272,
4.13536145825263));
#24897=CARTESIAN_POINT('Ctrl Pts',(9.20102613084934,-0.591985933785934,
3.93938960239856));
#24898=CARTESIAN_POINT('Ctrl Pts',(9.21693140953695,-0.571921382545595,
3.74341774654449));
#24899=CARTESIAN_POINT('Ctrl Pts',(9.23283668822456,-0.444878568530549,
3.55839884526489));
#24900=CARTESIAN_POINT('Ctrl Pts',(9.24874196691217,-0.269190177198291,
3.46928575052316));
#24901=CARTESIAN_POINT('Ctrl Pts',(9.26464724559978,-0.0935017858660342,
3.38017265578144));
#24902=CARTESIAN_POINT('Ctrl Pts',(9.28055252428739,0.130832182783434,3.38696536757758));
#24903=CARTESIAN_POINT('Ctrl Pts',(9.29645780297501,0.300807061133818,3.48654496003073));
#24904=CARTESIAN_POINT('Ctrl Pts',(9.31236308166262,0.470781939484206,3.58612455248389));
#24905=CARTESIAN_POINT('Ctrl Pts',(9.32826836035024,0.586397727535503,3.77849102559406));
#24906=CARTESIAN_POINT('Ctrl Pts',(9.34417363903785,0.594568546715174,3.97531783326339));
#24907=CARTESIAN_POINT('Ctrl Pts',(9.36007891772546,0.602739365894845,4.17214464093271));
#24908=CARTESIAN_POINT('Ctrl Pts',(9.37598419641307,0.503465216202894,4.37343178316119));
#24909=CARTESIAN_POINT('Ctrl Pts',(9.39188947510069,0.342328587234952,4.48675671999422));
#24910=CARTESIAN_POINT('Ctrl Pts',(9.40164451298129,0.243500144778355,4.55626125828842));
#24911=CARTESIAN_POINT('Ctrl Pts',(9.41139955086189,0.121401365174849,4.59267772446372));
#24912=CARTESIAN_POINT('Ctrl Pts',(9.4211545887425,-0.000345133784900094,
4.59331940772745));
#24913=CARTESIAN_POINT('Origin',(4.,0.,4.));
#24914=CARTESIAN_POINT('',(9.82884541125756,0.000474857175501747,4.59454166667424));
#24915=CARTESIAN_POINT('',(9.7211545887425,-0.000338423355870402,4.59484023865297));
#24916=CARTESIAN_POINT('',(4.,-7.27562663373442E-17,4.5941));
#24917=CARTESIAN_POINT('Ctrl Pts',(9.82884541125756,0.000474857175501747,
4.59454166667424));
#24918=CARTESIAN_POINT('Ctrl Pts',(9.82632780447438,0.0317313679687054,
4.59481419231428));
#24919=CARTESIAN_POINT('Ctrl Pts',(9.82381019769121,0.0629485386443197,
4.59256288124703));
#24920=CARTESIAN_POINT('Ctrl Pts',(9.82129259090804,0.093741277189286,4.58765086492638));
#24921=CARTESIAN_POINT('Ctrl Pts',(9.80538731222043,0.288278045752977,4.55661862072519));
#24922=CARTESIAN_POINT('Ctrl Pts',(9.78948203353282,0.465874751366426,4.41939150759219));
#24923=CARTESIAN_POINT('Ctrl Pts',(9.77357675484521,0.54498650030893,4.23897841027765));
#24924=CARTESIAN_POINT('Ctrl Pts',(9.7576714761576,0.624098249251433,4.05856531296313));
#24925=CARTESIAN_POINT('Ctrl Pts',(9.74176619746998,0.604725041522997,3.83496623146707));
#24926=CARTESIAN_POINT('Ctrl Pts',(9.72586091878237,0.495762234499694,3.67084840431546));
#24927=CARTESIAN_POINT('Ctrl Pts',(9.70995564009475,0.386799427476386,3.50673057716384));
#24928=CARTESIAN_POINT('Ctrl Pts',(9.69405036140714,0.188247021158209,3.40209400435668));
#24929=CARTESIAN_POINT('Ctrl Pts',(9.67814508271953,-0.00872811953311764,
3.40498337331868));
#24930=CARTESIAN_POINT('Ctrl Pts',(9.66223980403192,-0.205703260224436,
3.40787274228067));
#24931=CARTESIAN_POINT('Ctrl Pts',(9.6463345253443,-0.4011011352889,3.51828805301183));
#24932=CARTESIAN_POINT('Ctrl Pts',(9.63042924665669,-0.505203307099277,
3.68553126611098));
#24933=CARTESIAN_POINT('Ctrl Pts',(9.61452396796908,-0.609305478909656,
3.85277447921013));
#24934=CARTESIAN_POINT('Ctrl Pts',(9.59861868928147,-0.622111947465945,
4.07684559467727));
#24935=CARTESIAN_POINT('Ctrl Pts',(9.58271341059386,-0.537742524204099,
4.25486063595701));
#24936=CARTESIAN_POINT('Ctrl Pts',(9.56680813190624,-0.453373100942255,
4.43287567723675));
#24937=CARTESIAN_POINT('Ctrl Pts',(9.55090285321863,-0.271827785862281,
4.5648346443291));
#24938=CARTESIAN_POINT('Ctrl Pts',(9.53499757453102,-0.0764645071000137,
4.59014756226876));
#24939=CARTESIAN_POINT('Ctrl Pts',(9.53294685343987,-0.0512756623106346,
4.5934112419387));
#24940=CARTESIAN_POINT('Ctrl Pts',(9.53089613234871,-0.025857110284879,
4.59490205769144));
#24941=CARTESIAN_POINT('Ctrl Pts',(9.52884541125756,-0.000414715089906426,
4.59470005288553));
#24942=CARTESIAN_POINT('Ctrl Pts',(9.4211545887425,-0.000345133784900094,
4.59331940772745));
#24943=CARTESIAN_POINT('Ctrl Pts',(9.42730482954951,-0.0771024252662454,
4.59372396859559));
#24944=CARTESIAN_POINT('Ctrl Pts',(9.43345507035652,-0.153719688677923,
4.57990840728947));
#24945=CARTESIAN_POINT('Ctrl Pts',(9.43960531116353,-0.224276981305518,
4.55119942103951));
#24946=CARTESIAN_POINT('Ctrl Pts',(9.45551058985114,-0.406746812634079,
4.47695445381419));
#24947=CARTESIAN_POINT('Ctrl Pts',(9.47141586853875,-0.548687367047265,
4.30310178792596));
#24948=CARTESIAN_POINT('Ctrl Pts',(9.48732114722636,-0.58492554696818,4.10946721245096));
#24949=CARTESIAN_POINT('Ctrl Pts',(9.50322642591398,-0.621163726889096,
3.91583263697596));
#24950=CARTESIAN_POINT('Ctrl Pts',(9.5191317046016,-0.55169953231774,3.70241615191419));
#24951=CARTESIAN_POINT('Ctrl Pts',(9.53503698328921,-0.408427982613559,
3.56720957829912));
#24952=CARTESIAN_POINT('Ctrl Pts',(9.55094226197682,-0.265156432909381,
3.43200300468405));
#24953=CARTESIAN_POINT('Ctrl Pts',(9.56684754066442,-0.0480775280723801,
3.37500634251568));
#24954=CARTESIAN_POINT('Ctrl Pts',(9.58275281935204,0.14313528264739,3.42239004773181));
#24955=CARTESIAN_POINT('Ctrl Pts',(9.59865809803965,0.334348093367161,3.46977375294793));
#24956=CARTESIAN_POINT('Ctrl Pts',(9.61456337672728,0.499694809969701,3.62153782554855));
#24957=CARTESIAN_POINT('Ctrl Pts',(9.63046865541489,0.563255215433827,3.80799862400389));
#24958=CARTESIAN_POINT('Ctrl Pts',(9.6463739341025,0.626815620897955,3.99445942245922));
#24959=CARTESIAN_POINT('Ctrl Pts',(9.6622792127901,0.588589715223662,4.21561694676927));
#24960=CARTESIAN_POINT('Ctrl Pts',(9.67818449147771,0.466129217091882,4.36992501817411));
#24961=CARTESIAN_POINT('Ctrl Pts',(9.69250785723264,0.355848439261942,4.50888586187125));
#24962=CARTESIAN_POINT('Ctrl Pts',(9.70683122298757,0.177255492135987,4.59363345408847));
#24963=CARTESIAN_POINT('Ctrl Pts',(9.7211545887425,-0.000338423355870402,
4.59484023865297));
#24964=CARTESIAN_POINT('Origin',(4.,0.,4.));
#24965=CARTESIAN_POINT('',(10.1288454112576,0.000175993811045716,4.59316417414361));
#24966=CARTESIAN_POINT('',(10.0211545887425,0.000517772199431355,4.59437035498519));
#24967=CARTESIAN_POINT('',(4.,-7.27562663373442E-17,4.5941));
#24968=CARTESIAN_POINT('Ctrl Pts',(10.1288454112576,0.000175993811045716,
4.59316417414361));
#24969=CARTESIAN_POINT('Ctrl Pts',(10.1217594766001,0.0886689559287146,
4.59339827721605));
#24970=CARTESIAN_POINT('Ctrl Pts',(10.1146735419426,0.177068724884878,4.57486525982572));
#24971=CARTESIAN_POINT('Ctrl Pts',(10.1075876072851,0.256276603526552,4.53706914692868));
#24972=CARTESIAN_POINT('Ctrl Pts',(10.0916823285975,0.434068729046268,4.45223097977176));
#24973=CARTESIAN_POINT('Ctrl Pts',(10.0757770499098,0.565548899719798,4.27033860735548));
#24974=CARTESIAN_POINT('Ctrl Pts',(10.0598717712222,0.590346983641159,4.0749093118617));
#24975=CARTESIAN_POINT('Ctrl Pts',(10.0439664925346,0.61514506756252,3.87948001636793));
#24976=CARTESIAN_POINT('Ctrl Pts',(10.028061213847,0.533261064731712,3.67051379779667));
#24977=CARTESIAN_POINT('Ctrl Pts',(10.0121559351594,0.382292645022166,3.5439591030842));
#24978=CARTESIAN_POINT('Ctrl Pts',(9.99625065647179,0.231324225312614,3.41740440837173));
#24979=CARTESIAN_POINT('Ctrl Pts',(9.98034537778417,0.011271388724311,3.37326123751805));
#24980=CARTESIAN_POINT('Ctrl Pts',(9.96444009909655,-0.17682691184915,3.43179826703564));
#24981=CARTESIAN_POINT('Ctrl Pts',(9.94853482040894,-0.364925212422603,
3.49033529655323));
#24982=CARTESIAN_POINT('Ctrl Pts',(9.93262954172133,-0.521068976981223,
3.65155252644206));
#24983=CARTESIAN_POINT('Ctrl Pts',(9.91672426303372,-0.573563594737602,
3.84142582527571));
#24984=CARTESIAN_POINT('Ctrl Pts',(9.90081898434611,-0.626058212493981,
4.03129912410937));
#24985=CARTESIAN_POINT('Ctrl Pts',(9.8849137056585,-0.574903683448118,4.24982849188785));
#24986=CARTESIAN_POINT('Ctrl Pts',(9.86900842697089,-0.443588003168223,
4.39667448814241));
#24987=CARTESIAN_POINT('Ctrl Pts',(9.85562075506645,-0.333057953489513,
4.52027659892262));
#24988=CARTESIAN_POINT('Ctrl Pts',(9.842233083162,-0.165735336637852,4.59309247934331));
#24989=CARTESIAN_POINT('Ctrl Pts',(9.82884541125756,0.000474857175501747,
4.59454166667424));
#24990=CARTESIAN_POINT('Ctrl Pts',(9.7211545887425,-0.000338423355870402,
4.59484023865297));
#24991=CARTESIAN_POINT('Ctrl Pts',(9.72273650167518,-0.0199523965301825,
4.59497351934566));
#24992=CARTESIAN_POINT('Ctrl Pts',(9.72431841460787,-0.0395541838993478,
4.59408780127083));
#24993=CARTESIAN_POINT('Ctrl Pts',(9.72590032754056,-0.0590504136254521,
4.592143576127));
#24994=CARTESIAN_POINT('Ctrl Pts',(9.74180560622817,-0.255074455621757,
4.57259544417541));
#24995=CARTESIAN_POINT('Ctrl Pts',(9.75771088491579,-0.4404274490251,4.4460405617726));
#24996=CARTESIAN_POINT('Ctrl Pts',(9.7736161636034,-0.530003140903138,4.2705875768224));
#24997=CARTESIAN_POINT('Ctrl Pts',(9.78952144229101,-0.619578832781174,
4.0951345918722));
#24998=CARTESIAN_POINT('Ctrl Pts',(9.80542672097862,-0.61337722313391,3.87078350437461));
#24999=CARTESIAN_POINT('Ctrl Pts',(9.82133199966623,-0.514245828742901,
3.70054684219675));
#25000=CARTESIAN_POINT('Ctrl Pts',(9.83723727835384,-0.41511443435189,3.53031018001889));
#25001=CARTESIAN_POINT('Ctrl Pts',(9.85314255704146,-0.223053255217129,
3.41418794316076));
#25002=CARTESIAN_POINT('Ctrl Pts',(9.86904783572907,-0.0262486593588972,
3.40549855006092));
#25003=CARTESIAN_POINT('Ctrl Pts',(9.88495311441669,0.170555936499329,3.39680915696108));
#25004=CARTESIAN_POINT('Ctrl Pts',(9.9008583931043,0.372103949081026,3.49555260761951));
#25005=CARTESIAN_POINT('Ctrl Pts',(9.91676367179191,0.485853057801912,3.65639008698476));
#25006=CARTESIAN_POINT('Ctrl Pts',(9.93266895047952,0.5996021665228,3.81722756635002));
#25007=CARTESIAN_POINT('Ctrl Pts',(9.94857422916713,0.625552371382872,4.04015907442209));
#25008=CARTESIAN_POINT('Ctrl Pts',(9.96447950785475,0.551788436173011,4.22282389414861));
#25009=CARTESIAN_POINT('Ctrl Pts',(9.98038478654236,0.478024500963153,4.40548871387512));
#25010=CARTESIAN_POINT('Ctrl Pts',(9.99629006522997,0.304546425683368,4.54788684525607));
#25011=CARTESIAN_POINT('Ctrl Pts',(10.0121953439176,0.111008003250015,4.58463509072946));
#25012=CARTESIAN_POINT('Ctrl Pts',(10.0151817588592,0.0746687445744621,
4.59153503329043));
#25013=CARTESIAN_POINT('Ctrl Pts',(10.0181681738009,0.0376222632219309,
4.59471031472953));
#25014=CARTESIAN_POINT('Ctrl Pts',(10.0211545887425,0.000517772199431355,
4.59437035498519));
#25015=CARTESIAN_POINT('Origin',(4.,0.,4.));
#25016=CARTESIAN_POINT('',(10.4288454112576,-0.000541293539476018,4.59389423388278));
#25017=CARTESIAN_POINT('',(10.3211545887425,8.19078234495683E-5,4.59312629593825));
#25018=CARTESIAN_POINT('',(4.,-7.27562663373442E-17,4.5941));
#25019=CARTESIAN_POINT('Ctrl Pts',(10.4288454112576,-0.000541293539476018,
4.59389423388278));
#25020=CARTESIAN_POINT('Ctrl Pts',(10.4171911487257,0.144553461780974,4.59260897165526));
#25021=CARTESIAN_POINT('Ctrl Pts',(10.4055368861939,0.290497422953868,4.53904330389552));
#25022=CARTESIAN_POINT('Ctrl Pts',(10.3938826236621,0.397841883685798,4.4425412994096));
#25023=CARTESIAN_POINT('Ctrl Pts',(10.3779773449745,0.544341377656434,4.31083916286766));
#25024=CARTESIAN_POINT('Ctrl Pts',(10.3620720662869,0.618946539098701,4.09916502578488));
#25025=CARTESIAN_POINT('Ctrl Pts',(10.3461667875993,0.587401834162399,3.90471069671543));
#25026=CARTESIAN_POINT('Ctrl Pts',(10.3302615089117,0.555857129226098,3.710256367646));
#25027=CARTESIAN_POINT('Ctrl Pts',(10.314356230224,0.418162557911234,3.5330218465899));
#25028=CARTESIAN_POINT('Ctrl Pts',(10.2984509515364,0.237541641988682,3.45438572744188));
#25029=CARTESIAN_POINT('Ctrl Pts',(10.2825456728488,0.0569207260661262,
3.37574960829385));
#25030=CARTESIAN_POINT('Ctrl Pts',(10.2666403941612,-0.16662653446412,3.3957118910539));
#25031=CARTESIAN_POINT('Ctrl Pts',(10.2507351154736,-0.330456695071223,
3.50510674001315));
#25032=CARTESIAN_POINT('Ctrl Pts',(10.234829836786,-0.494286855678321,3.61450158897239));
#25033=CARTESIAN_POINT('Ctrl Pts',(10.2189245580984,-0.59839991636228,3.81332900413083));
#25034=CARTESIAN_POINT('Ctrl Pts',(10.2030192794108,-0.594991564317383,
4.01029584814195));
#25035=CARTESIAN_POINT('Ctrl Pts',(10.1871140007231,-0.591583212272486,
4.20726269215308));
#25036=CARTESIAN_POINT('Ctrl Pts',(10.1712087220355,-0.480653447498727,
4.40236896501689));
#25037=CARTESIAN_POINT('Ctrl Pts',(10.1553034433479,-0.313136524928893,
4.50603012050002));
#25038=CARTESIAN_POINT('Ctrl Pts',(10.1464840993178,-0.220249792163878,
4.56350936438632));
#25039=CARTESIAN_POINT('Ctrl Pts',(10.1376647552877,-0.109964716607974,
4.59287280319057));
#25040=CARTESIAN_POINT('Ctrl Pts',(10.1288454112576,0.000175993811045716,
4.59316417414361));
#25041=CARTESIAN_POINT('Ctrl Pts',(10.0211545887425,0.000517772199431355,
4.59437035498519));
#25042=CARTESIAN_POINT('Ctrl Pts',(10.0340734524885,-0.159991692577292,
4.59289973094197));
#25043=CARTESIAN_POINT('Ctrl Pts',(10.0469923162344,-0.321586704601994,
4.52564765365589));
#25044=CARTESIAN_POINT('Ctrl Pts',(10.0599111799804,-0.431712787135162,
4.40956688772629));
#25045=CARTESIAN_POINT('Ctrl Pts',(10.075816458668,-0.567296385500051,4.2666520796839));
#25046=CARTESIAN_POINT('Ctrl Pts',(10.0917217373556,-0.624864812642908,
4.04972410403331));
#25047=CARTESIAN_POINT('Ctrl Pts',(10.1076270160433,-0.577985082339038,
3.85838710972745));
#25048=CARTESIAN_POINT('Ctrl Pts',(10.1235322947309,-0.531105352035168,
3.6670501154216));
#25049=CARTESIAN_POINT('Ctrl Pts',(10.1394375734185,-0.379777464284567,
3.50130410246047));
#25050=CARTESIAN_POINT('Ctrl Pts',(10.1553428521061,-0.193484782987353,
3.43725262786029));
#25051=CARTESIAN_POINT('Ctrl Pts',(10.1712481307937,-0.00719210169012799,
3.37320115326011));
#25052=CARTESIAN_POINT('Ctrl Pts',(10.1871534094813,0.214065373153706,3.41084421702088));
#25053=CARTESIAN_POINT('Ctrl Pts',(10.2030586881689,0.368695569727689,3.53289771681035));
#25054=CARTESIAN_POINT('Ctrl Pts',(10.2189639668565,0.523325766301663,3.65495121659981));
#25055=CARTESIAN_POINT('Ctrl Pts',(10.2348692455442,0.611328684605784,3.86141515241798));
#25056=CARTESIAN_POINT('Ctrl Pts',(10.2507745242318,0.592297107651237,4.05749001970593));
#25057=CARTESIAN_POINT('Ctrl Pts',(10.2666798029194,0.573265530696689,4.25356488699388));
#25058=CARTESIAN_POINT('Ctrl Pts',(10.282585081607,0.447199458483466,4.43925068575162));
#25059=CARTESIAN_POINT('Ctrl Pts',(10.2984903602946,0.271983097956201,4.5292883529079));
#25060=CARTESIAN_POINT('Ctrl Pts',(10.3060451031106,0.188758241169316,4.57205474716445));
#25061=CARTESIAN_POINT('Ctrl Pts',(10.3135998459265,0.0944446272328244,
4.59324204311815));
#25062=CARTESIAN_POINT('Ctrl Pts',(10.3211545887425,8.19078234495684E-5,
4.59312629593825));
#25063=CARTESIAN_POINT('Origin',(4.,0.,4.));
#25064=CARTESIAN_POINT('',(10.7288454112576,7.37317986114466E-5,4.59506942345298));
#25065=CARTESIAN_POINT('',(10.6211545887425,-0.000548317120500629,4.59406879148573));
#25066=CARTESIAN_POINT('',(4.,-7.27562663373442E-17,4.5941));
#25067=CARTESIAN_POINT('Ctrl Pts',(10.7288454112576,7.37317986114466E-5,
4.59506942345298));
#25068=CARTESIAN_POINT('Ctrl Pts',(10.728528099539,0.00400402563557926,
4.59507627971693));
#25069=CARTESIAN_POINT('Ctrl Pts',(10.7282107878205,0.00793419209028873,
4.59504072157671));
#25070=CARTESIAN_POINT('Ctrl Pts',(10.727893476102,0.0118635052742893,4.59496237136513));
#25071=CARTESIAN_POINT('Ctrl Pts',(10.7119881974144,0.208820685209451,4.59103505989901));
#25072=CARTESIAN_POINT('Ctrl Pts',(10.6960829187267,0.403634001393415,4.47959161118634));
#25073=CARTESIAN_POINT('Ctrl Pts',(10.6801776400391,0.506853420906232,4.31180214209248));
#25074=CARTESIAN_POINT('Ctrl Pts',(10.6642723613515,0.610072840419052,4.14401267299861));
#25075=CARTESIAN_POINT('Ctrl Pts',(10.6483670826639,0.621698363260717,3.91987718352354));
#25076=CARTESIAN_POINT('Ctrl Pts',(10.6324618039763,0.536392041177647,3.74230920804366));
#25077=CARTESIAN_POINT('Ctrl Pts',(10.6165565252887,0.451085719094577,3.56474123256377));
#25078=CARTESIAN_POINT('Ctrl Pts',(10.6006512466011,0.26884755208677,3.43374077107907));
#25079=CARTESIAN_POINT('Ctrl Pts',(10.5847459679135,0.0733535965831807,
3.40945769333085));
#25080=CARTESIAN_POINT('Ctrl Pts',(10.5688406892258,-0.122140358920403,
3.38517461558263));
#25081=CARTESIAN_POINT('Ctrl Pts',(10.5529354105382,-0.33089010291977,3.46760892157089));
#25082=CARTESIAN_POINT('Ctrl Pts',(10.5370301318506,-0.457046584443773,
3.61891026549369));
#25083=CARTESIAN_POINT('Ctrl Pts',(10.521124853163,-0.583203065967777,3.7702116094165));
#25084=CARTESIAN_POINT('Ctrl Pts',(10.5052195744754,-0.626766285016417,
3.99037999127385));
#25085=CARTESIAN_POINT('Ctrl Pts',(10.4893142957878,-0.567733854410369,
4.17832340467295));
#25086=CARTESIAN_POINT('Ctrl Pts',(10.4734090171002,-0.508701423804317,
4.36626681807206));
#25087=CARTESIAN_POINT('Ctrl Pts',(10.4575037384126,-0.347073343543565,
4.52198526301292));
#25088=CARTESIAN_POINT('Ctrl Pts',(10.4415984597249,-0.157062390163684,
4.57397941748279));
#25089=CARTESIAN_POINT('Ctrl Pts',(10.4373474435692,-0.106278015462724,
4.58787593542499));
#25090=CARTESIAN_POINT('Ctrl Pts',(10.4330964274134,-0.0534661480554494,
4.59436304694399));
#25091=CARTESIAN_POINT('Ctrl Pts',(10.4288454112576,-0.000541293539476018,
4.59389423388278));
#25092=CARTESIAN_POINT('Ctrl Pts',(10.3211545887425,8.19078234495684E-5,
4.59312629593825));
#25093=CARTESIAN_POINT('Ctrl Pts',(10.3295051246142,-0.104220686264852,
4.59299835631127));
#25094=CARTESIAN_POINT('Ctrl Pts',(10.3378556604858,-0.208583275928277,
4.56684300569277));
#25095=CARTESIAN_POINT('Ctrl Pts',(10.3462061963575,-0.298097175589899,
4.5150330474864));
#25096=CARTESIAN_POINT('Ctrl Pts',(10.3621114750451,-0.468594439767441,
4.41635053935381));
#25097=CARTESIAN_POINT('Ctrl Pts',(10.3780167537327,-0.585222319281217,
4.22459598753381));
#25098=CARTESIAN_POINT('Ctrl Pts',(10.3939220324203,-0.594430225977177,
4.02781496975607));
#25099=CARTESIAN_POINT('Ctrl Pts',(10.4098273111079,-0.603638132673137,
3.83103395197833));
#25100=CARTESIAN_POINT('Ctrl Pts',(10.4257325897955,-0.505426066551287,
3.62922646824286));
#25101=CARTESIAN_POINT('Ctrl Pts',(10.4416378684831,-0.344888853364916,
3.51505397731042));
#25102=CARTESIAN_POINT('Ctrl Pts',(10.4575431471707,-0.184351640178541,
3.40088148637798));
#25103=CARTESIAN_POINT('Ctrl Pts',(10.4734484258584,0.0385107200723601,
3.37434398824859));
#25104=CARTESIAN_POINT('Ctrl Pts',(10.489353704546,0.221369260089487,3.4476263793543));
#25105=CARTESIAN_POINT('Ctrl Pts',(10.5052589832336,0.40422780010661,3.52090877046001));
#25106=CARTESIAN_POINT('Ctrl Pts',(10.5211642619212,0.54708251988996,3.69401105080081));
#25107=CARTESIAN_POINT('Ctrl Pts',(10.5370695406088,0.584340575799814,3.88745197659776));
#25108=CARTESIAN_POINT('Ctrl Pts',(10.5529748192964,0.621598631709669,4.08089290239472));
#25109=CARTESIAN_POINT('Ctrl Pts',(10.568880097984,0.55326002374602,4.29467247364782));
#25110=CARTESIAN_POINT('Ctrl Pts',(10.5847853766716,0.4107029495177,4.43063215550545));
#25111=CARTESIAN_POINT('Ctrl Pts',(10.5969084473619,0.302045344566967,4.53426120008624));
#25112=CARTESIAN_POINT('Ctrl Pts',(10.6090315180522,0.150270129189204,4.59268036842864));
#25113=CARTESIAN_POINT('Ctrl Pts',(10.6211545887425,-0.000548317120500629,
4.59406879148573));
#25114=CARTESIAN_POINT('Origin',(4.,0.,4.));
#25115=CARTESIAN_POINT('',(11.0288454112576,0.000503618959454472,4.59367252935801));
#25116=CARTESIAN_POINT('',(10.9211545887425,0.000179316795020235,4.59501533910171));
#25117=CARTESIAN_POINT('',(4.,-7.27562663373442E-17,4.5941));
#25118=CARTESIAN_POINT('Ctrl Pts',(11.0288454112576,0.000503618959454472,
4.59367252935801));
#25119=CARTESIAN_POINT('Ctrl Pts',(11.0239597716647,0.0613870506829751,
4.59415995979602));
#25120=CARTESIAN_POINT('Ctrl Pts',(11.0190741320719,0.122135879976345,4.58554712933309));
#25121=CARTESIAN_POINT('Ctrl Pts',(11.014188492479,0.179818659528701,4.56726203449827));
#25122=CARTESIAN_POINT('Ctrl Pts',(10.9982832137914,0.36760588100072,4.50773461262244));
#25123=CARTESIAN_POINT('Ctrl Pts',(10.9823779351038,0.52289792528528,4.34569680405454));
#25124=CARTESIAN_POINT('Ctrl Pts',(10.9664726564162,0.574391255511512,4.15554951523459));
#25125=CARTESIAN_POINT('Ctrl Pts',(10.9505673777285,0.625884585737745,3.96540222641464));
#25126=CARTESIAN_POINT('Ctrl Pts',(10.9346620990409,0.573579201905647,3.74714545734266));
#25127=CARTESIAN_POINT('Ctrl Pts',(10.9187568203533,0.441491523412615,3.60099348269406));
#25128=CARTESIAN_POINT('Ctrl Pts',(10.9028515416657,0.309403844919578,3.45484150804546));
#25129=CARTESIAN_POINT('Ctrl Pts',(10.8869462629781,0.0975338717655902,
3.38079432782024));
#25130=CARTESIAN_POINT('Ctrl Pts',(10.8710409842905,-0.0968366678563846,
3.41285127449999));
#25131=CARTESIAN_POINT('Ctrl Pts',(10.8551357056029,-0.291207207478354,
3.44490822117975));
#25132=CARTESIAN_POINT('Ctrl Pts',(10.8392304269153,-0.468078313568319,
3.58306929476445));
#25133=CARTESIAN_POINT('Ctrl Pts',(10.8233251482276,-0.546238257009186,
3.76389677537701));
#25134=CARTESIAN_POINT('Ctrl Pts',(10.80741986954,-0.624398200450053,3.94472425598957));
#25135=CARTESIAN_POINT('Ctrl Pts',(10.7915145908524,-0.603846981241821,
4.16821814362997));
#25136=CARTESIAN_POINT('Ctrl Pts',(10.7756093121648,-0.494020849794526,
4.33175950034039));
#25137=CARTESIAN_POINT('Ctrl Pts',(10.7600213451957,-0.386385759396791,
4.49203819249975));
#25138=CARTESIAN_POINT('Ctrl Pts',(10.7444333782267,-0.193002309618558,
4.59473260886404));
#25139=CARTESIAN_POINT('Ctrl Pts',(10.7288454112576,7.37317986114466E-5,
4.59506942345298));
#25140=CARTESIAN_POINT('Ctrl Pts',(10.6211545887425,-0.000548317120500629,
4.59406879148573));
#25141=CARTESIAN_POINT('Ctrl Pts',(10.6249367967398,-0.0476013079303647,
4.5945019577127));
#25142=CARTESIAN_POINT('Ctrl Pts',(10.6287190047372,-0.0945611723716044,
4.58938408097059));
#25143=CARTESIAN_POINT('Ctrl Pts',(10.6325012127345,-0.140089514783682,
4.57835619988505));
#25144=CARTESIAN_POINT('Ctrl Pts',(10.6484064914221,-0.331549364363767,
4.53198076994489));
#25145=CARTESIAN_POINT('Ctrl Pts',(10.6643117701097,-0.497693523030948,
4.38109011760241));
#25146=CARTESIAN_POINT('Ctrl Pts',(10.6802170487973,-0.562235622104956,
4.19496684675621));
#25147=CARTESIAN_POINT('Ctrl Pts',(10.6961223274849,-0.626777721178965,
4.00884357591002));
#25148=CARTESIAN_POINT('Ctrl Pts',(10.7120276061725,-0.589717760659791,
3.78748768656011));
#25149=CARTESIAN_POINT('Ctrl Pts',(10.7279328848602,-0.468072106540212,
3.63253643830059));
#25150=CARTESIAN_POINT('Ctrl Pts',(10.7438381635478,-0.346426452420629,
3.47758519004106));
#25151=CARTESIAN_POINT('Ctrl Pts',(10.7597434422354,-0.140195104700642,
3.38903858287192));
#25152=CARTESIAN_POINT('Ctrl Pts',(10.775648720923,0.0559292266755373,3.40755347270721));
#25153=CARTESIAN_POINT('Ctrl Pts',(10.7915539996106,0.252053558051711,3.4260683625425));
#25154=CARTESIAN_POINT('Ctrl Pts',(10.8074592782982,0.438070873084069,3.55164474938222));
#25155=CARTESIAN_POINT('Ctrl Pts',(10.8233645569858,0.528569890453362,3.72662326908837));
#25156=CARTESIAN_POINT('Ctrl Pts',(10.8392698356734,0.619068907822657,3.90160178879453));
#25157=CARTESIAN_POINT('Ctrl Pts',(10.8551751143611,0.614049627528876,4.12598244136713));
#25158=CARTESIAN_POINT('Ctrl Pts',(10.8710803930487,0.515816690734684,4.29673912390739));
#25159=CARTESIAN_POINT('Ctrl Pts',(10.8869856717363,0.417583753940498,4.46749580644764));
#25160=CARTESIAN_POINT('Ctrl Pts',(10.9028909504239,0.226137160645921,4.58462851895556));
#25161=CARTESIAN_POINT('Ctrl Pts',(10.9187962291115,0.0293810870543861,
4.59435487532392));
#25162=CARTESIAN_POINT('Ctrl Pts',(10.9195823489885,0.0196563998352688,
4.59483560139116));
#25163=CARTESIAN_POINT('Ctrl Pts',(10.9203684688655,0.00991874240631306,
4.5950539509358));
#25164=CARTESIAN_POINT('Ctrl Pts',(10.9211545887425,0.000179316795020235,
4.59501533910171));
#25165=CARTESIAN_POINT('Origin',(4.,0.,4.));
#25166=CARTESIAN_POINT('',(11.3288454112576,-0.000294350894641693,4.59325842069974));
#25167=CARTESIAN_POINT('',(11.2211545887425,0.000456638431143918,4.59352536526061));
#25168=CARTESIAN_POINT('',(4.,-7.27562663373442E-17,4.5941));
#25169=CARTESIAN_POINT('Ctrl Pts',(11.3288454112576,-0.000294350894641693,
4.59325842069974));
#25170=CARTESIAN_POINT('Ctrl Pts',(11.3193914437904,0.117725031793324,4.59273125875086));
#25171=CARTESIAN_POINT('Ctrl Pts',(11.3099374763232,0.236024696118704,4.55868066117597));
#25172=CARTESIAN_POINT('Ctrl Pts',(11.300483508856,0.333060002447629,4.49314500997921));
#25173=CARTESIAN_POINT('Ctrl Pts',(11.2845782301684,0.496311419914153,4.38288835848583));
#25174=CARTESIAN_POINT('Ctrl Pts',(11.2686729514808,0.599375291650127,4.18351506848348));
#25175=CARTESIAN_POINT('Ctrl Pts',(11.2527676727932,0.594929048027223,3.98656891995295));
#25176=CARTESIAN_POINT('Ctrl Pts',(11.2368623941056,0.59048280440432,3.78962277142242));
#25177=CARTESIAN_POINT('Ctrl Pts',(11.220957115418,0.478526445422532,3.5951037643637));
#25178=CARTESIAN_POINT('Ctrl Pts',(11.2050518367303,0.310465594643358,3.49232679739763));
#25179=CARTESIAN_POINT('Ctrl Pts',(11.1891465580427,0.142404743864184,3.38954983043155));
#25180=CARTESIAN_POINT('Ctrl Pts',(11.1732412793551,-0.0817605987123653,
3.37851490355812));
#25181=CARTESIAN_POINT('Ctrl Pts',(11.1573360006675,-0.259103191428711,
3.46428878834836));
#25182=CARTESIAN_POINT('Ctrl Pts',(11.1414307219799,-0.436445784145052,
3.5500626731386));
#25183=CARTESIAN_POINT('Ctrl Pts',(11.1255254432923,-0.566965627001181,
3.73264536959251));
#25184=CARTESIAN_POINT('Ctrl Pts',(11.1096201646047,-0.590733529996744,
3.92820262793532));
#25185=CARTESIAN_POINT('Ctrl Pts',(11.0937148859171,-0.614501432992307,
4.12375988627813));
#25186=CARTESIAN_POINT('Ctrl Pts',(11.0778096072294,-0.531517396127296,
4.33229170650985));
#25187=CARTESIAN_POINT('Ctrl Pts',(11.0619043285418,-0.379884178365051,
4.45804909903384));
#25188=CARTESIAN_POINT('Ctrl Pts',(11.0508846894471,-0.274828280424841,
4.54517747360242));
#25189=CARTESIAN_POINT('Ctrl Pts',(11.0398650503523,-0.136819945681758,
4.59257312212411));
#25190=CARTESIAN_POINT('Ctrl Pts',(11.0288454112576,0.000503618959454472,
4.59367252935801));
#25191=CARTESIAN_POINT('Ctrl Pts',(10.9211545887425,0.000179316795020235,
4.59501533910171));
#25192=CARTESIAN_POINT('Ctrl Pts',(10.9362737475531,-0.187135527734918,
4.59427273168419));
#25193=CARTESIAN_POINT('Ctrl Pts',(10.9513929063637,-0.375104412928531,
4.49848156101044));
#25194=CARTESIAN_POINT('Ctrl Pts',(10.9665120651743,-0.484035620954107,
4.34616539940523));
#25195=CARTESIAN_POINT('Ctrl Pts',(10.982417343862,-0.598630701482551,4.1859295668894));
#25196=CARTESIAN_POINT('Ctrl Pts',(10.9983226225496,-0.625755308650954,
3.96313790162893));
#25197=CARTESIAN_POINT('Ctrl Pts',(11.0142279012372,-0.55295497039508,3.7800869107734));
#25198=CARTESIAN_POINT('Ctrl Pts',(11.0301331799248,-0.480154632139201,
3.59703591991786));
#25199=CARTESIAN_POINT('Ctrl Pts',(11.0460384586124,-0.307429348459053,
3.45372560346725));
#25200=CARTESIAN_POINT('Ctrl Pts',(11.0619437373,-0.114087262216405,3.41595799577618));
#25201=CARTESIAN_POINT('Ctrl Pts',(11.0778490159876,0.0792548240262376,
3.37819038808511));
#25202=CARTESIAN_POINT('Ctrl Pts',(11.0937542946752,0.293213712831377,3.4459654891536));
#25203=CARTESIAN_POINT('Ctrl Pts',(11.1096595733629,0.429548534313776,3.58816383989905));
#25204=CARTESIAN_POINT('Ctrl Pts',(11.1255648520505,0.565883355796175,3.7303621906445));
#25205=CARTESIAN_POINT('Ctrl Pts',(11.1414701307381,0.624594109955846,3.94698379106692));
#25206=CARTESIAN_POINT('Ctrl Pts',(11.1573754094257,0.578723302329844,4.13856516675647));
#25207=CARTESIAN_POINT('Ctrl Pts',(11.1732806881133,0.53285249470384,4.33014654244603));
#25208=CARTESIAN_POINT('Ctrl Pts',(11.1891859668009,0.382400125292158,4.49668769340272));
#25209=CARTESIAN_POINT('Ctrl Pts',(11.2050912454885,0.196447557013804,4.56171996888228));
#25210=CARTESIAN_POINT('Ctrl Pts',(11.2104456932399,0.133847376870746,4.58361282144047));
#25211=CARTESIAN_POINT('Ctrl Pts',(11.2158001409912,0.0672239414478651,
4.5940016224088));
#25212=CARTESIAN_POINT('Ctrl Pts',(11.2211545887425,0.000456638431143918,
4.59352536526061));
#25213=CARTESIAN_POINT('Origin',(4.,0.,4.));
#25214=CARTESIAN_POINT('',(11.6288454112576,-0.000389145320547679,4.59475273347735));
#25215=CARTESIAN_POINT('',(11.5211545887425,-0.0003715675665865,4.59335763259963));
#25216=CARTESIAN_POINT('',(4.,-7.27562663373442E-17,4.5941));
#25217=CARTESIAN_POINT('Ctrl Pts',(11.6288454112576,-0.000389145320547679,
4.59475273347735));
#25218=CARTESIAN_POINT('Ctrl Pts',(11.6148231159161,0.173538999407471,4.59343557735163));
#25219=CARTESIAN_POINT('Ctrl Pts',(11.6008008205746,0.348531733704351,4.51264940831536));
#25220=CARTESIAN_POINT('Ctrl Pts',(11.586778525233,0.459048433726307,4.37867598496766));
#25221=CARTESIAN_POINT('Ctrl Pts',(11.5708732465454,0.584405864209301,4.22671194604376));
#25222=CARTESIAN_POINT('Ctrl Pts',(11.5549679678578,0.626808276394098,4.00631705984067));
#25223=CARTESIAN_POINT('Ctrl Pts',(11.5390626891702,0.566786276503563,3.81868733396413));
#25224=CARTESIAN_POINT('Ctrl Pts',(11.5231574104826,0.506764276613028,3.6310576080876));
#25225=CARTESIAN_POINT('Ctrl Pts',(11.507252131795,0.344317864647159,3.47619304253762));
#25226=CARTESIAN_POINT('Ctrl Pts',(11.4913468531074,0.154035560439752,3.4252008940353));
#25227=CARTESIAN_POINT('Ctrl Pts',(11.4754415744198,-0.0362467437676612,
3.37420874553297));
#25228=CARTESIAN_POINT('Ctrl Pts',(11.4595362957322,-0.254364940216614,
3.4270890140783));
#25229=CARTESIAN_POINT('Ctrl Pts',(11.4436310170445,-0.400168380917644,
3.55956131753494));
#25230=CARTESIAN_POINT('Ctrl Pts',(11.4277257383569,-0.545971821618673,
3.69203362099157));
#25231=CARTESIAN_POINT('Ctrl Pts',(11.4118204596693,-0.619460506571779,
3.90409795935952));
#25232=CARTESIAN_POINT('Ctrl Pts',(11.3959151809817,-0.586891540696359,
4.09838336016249));
#25233=CARTESIAN_POINT('Ctrl Pts',(11.3800099022941,-0.554322574820941,
4.29266876096545));
#25234=CARTESIAN_POINT('Ctrl Pts',(11.3641046236065,-0.415695958117004,
4.46917522420345));
#25235=CARTESIAN_POINT('Ctrl Pts',(11.3481993449189,-0.234663168166497,
4.54685844933023));
#25236=CARTESIAN_POINT('Ctrl Pts',(11.3417480336984,-0.161234786808821,
4.57836740127901));
#25237=CARTESIAN_POINT('Ctrl Pts',(11.335296722478,-0.080829826651965,4.59361815176584));
#25238=CARTESIAN_POINT('Ctrl Pts',(11.3288454112576,-0.000294350894641693,
4.59325842069974));
#25239=CARTESIAN_POINT('Ctrl Pts',(11.2211545887425,0.000456638431143918,
4.59352536526061));
#25240=CARTESIAN_POINT('Ctrl Pts',(11.2317054196788,-0.131106980996848,
4.59258691018808));
#25241=CARTESIAN_POINT('Ctrl Pts',(11.2422562506151,-0.263229208150973,
4.54946171071576));
#25242=CARTESIAN_POINT('Ctrl Pts',(11.2528070815514,-0.366229002642205,
4.4690386804108));
#25243=CARTESIAN_POINT('Ctrl Pts',(11.268712360239,-0.521500226874852,4.34780171645731));
#25244=CARTESIAN_POINT('Ctrl Pts',(11.2846176389266,-0.610589908195122,
4.1418043885479));
#25245=CARTESIAN_POINT('Ctrl Pts',(11.3005229176142,-0.592591834014348,
3.94563195463032));
#25246=CARTESIAN_POINT('Ctrl Pts',(11.3164281963018,-0.574593759833574,
3.74945952071274));
#25247=CARTESIAN_POINT('Ctrl Pts',(11.3323334749894,-0.449507930151742,
3.56311198078699));
#25248=CARTESIAN_POINT('Ctrl Pts',(11.3482387536771,-0.274768466013715,
3.47215224147272));
#25249=CARTESIAN_POINT('Ctrl Pts',(11.3641440323647,-0.100029001875688,
3.38119250215845));
#25250=CARTESIAN_POINT('Ctrl Pts',(11.3800493110523,0.12436409671854,3.38562056345565));
#25251=CARTESIAN_POINT('Ctrl Pts',(11.3959545897399,0.295379012183608,3.48340324695247));
#25252=CARTESIAN_POINT('Ctrl Pts',(11.4118598684275,0.466393927648671,3.5811859304493));
#25253=CARTESIAN_POINT('Ctrl Pts',(11.4277651471151,0.584030659984583,3.77232323614575));
#25254=CARTESIAN_POINT('Ctrl Pts',(11.4436704258027,0.594275398502411,3.96905299961855));
#25255=CARTESIAN_POINT('Ctrl Pts',(11.4595757044903,0.60452013702024,4.16578276309136));
#25256=CARTESIAN_POINT('Ctrl Pts',(11.475480983178,0.507372881719984,4.36810498434052));
#25257=CARTESIAN_POINT('Ctrl Pts',(11.4913862618656,0.34743954227408,4.48312185891572));
#25258=CARTESIAN_POINT('Ctrl Pts',(11.5013090374912,0.247662438486696,4.55487707062799));
#25259=CARTESIAN_POINT('Ctrl Pts',(11.5112318131169,0.123448374926332,4.59265218509947));
#25260=CARTESIAN_POINT('Ctrl Pts',(11.5211545887425,-0.0003715675665865,
4.59335763259963));
#25261=CARTESIAN_POINT('Origin',(4.,0.,4.));
#25262=CARTESIAN_POINT('',(11.9288454112576,0.000492284285450728,4.5944814532616));
#25263=CARTESIAN_POINT('',(11.8211545887425,-0.000307672146732893,4.59488449882539));
#25264=CARTESIAN_POINT('',(4.,-7.27562663373442E-17,4.5941));
#25265=CARTESIAN_POINT('Ctrl Pts',(11.9288454112576,0.000492284285450728,
4.5944814532616));
#25266=CARTESIAN_POINT('Ctrl Pts',(11.9261600667293,0.0338400408399785,
4.59477876231094));
#25267=CARTESIAN_POINT('Ctrl Pts',(11.9234747222011,0.0671420792079604,
4.59221542322669));
#25268=CARTESIAN_POINT('Ctrl Pts',(11.9207893776729,0.0999293694653808,
4.5866302815369));
#25269=CARTESIAN_POINT('Ctrl Pts',(11.9048840989853,0.294128282668868,4.55354952256816));
#25270=CARTESIAN_POINT('Ctrl Pts',(11.8889788202977,0.470268877700486,4.41445832512751));
#25271=CARTESIAN_POINT('Ctrl Pts',(11.8730735416101,0.547474845215755,4.2332214826164));
#25272=CARTESIAN_POINT('Ctrl Pts',(11.8571682629225,0.624680812731027,4.05198464010529));
#25273=CARTESIAN_POINT('Ctrl Pts',(11.8412629842349,0.602952152729945,3.82860215252373));
#25274=CARTESIAN_POINT('Ctrl Pts',(11.8253577055472,0.492265746621211,3.66564180763548));
#25275=CARTESIAN_POINT('Ctrl Pts',(11.8094524268596,0.38157934051248,3.50268146274723));
#25276=CARTESIAN_POINT('Ctrl Pts',(11.793547148172,0.181935188296101,3.40014326055229));
#25277=CARTESIAN_POINT('Ctrl Pts',(11.7776418694844,-0.0149985615777061,
3.40510840546499));
#25278=CARTESIAN_POINT('Ctrl Pts',(11.7617365907968,-0.211932311451519,
3.41007355037768));
#25279=CARTESIAN_POINT('Ctrl Pts',(11.7458313121092,-0.406155658982761,
3.52254204239802));
#25280=CARTESIAN_POINT('Ctrl Pts',(11.7299260334216,-0.508489459897291,
3.69087310813977));
#25281=CARTESIAN_POINT('Ctrl Pts',(11.714020754734,-0.610823260811815,3.8592041738815));
#25282=CARTESIAN_POINT('Ctrl Pts',(11.6981154760463,-0.621267515109637,
4.08339781334463));
#25283=CARTESIAN_POINT('Ctrl Pts',(11.6822101973587,-0.53502666307716,4.26051379213839));
#25284=CARTESIAN_POINT('Ctrl Pts',(11.6663049186711,-0.448785811044678,
4.43762977093217));
#25285=CARTESIAN_POINT('Ctrl Pts',(11.6503996399835,-0.265859852681883,
4.56766808905658));
#25286=CARTESIAN_POINT('Ctrl Pts',(11.6344943612959,-0.070240649109886,
4.59092065229643));
#25287=CARTESIAN_POINT('Ctrl Pts',(11.6326113779498,-0.0470818155087989,
4.59367346098309));
#25288=CARTESIAN_POINT('Ctrl Pts',(11.6307283946037,-0.0237450789937817,
4.59492960773286));
#25289=CARTESIAN_POINT('Ctrl Pts',(11.6288454112576,-0.000389145320547679,
4.59475273347735));
#25290=CARTESIAN_POINT('Ctrl Pts',(11.5211545887425,-0.0003715675665865,
4.59335763259963));
#25291=CARTESIAN_POINT('Ctrl Pts',(11.5271370918045,-0.0750233800274846,
4.5937829512795));
#25292=CARTESIAN_POINT('Ctrl Pts',(11.5331195948664,-0.149531931096223,
4.58073359799715));
#25293=CARTESIAN_POINT('Ctrl Pts',(11.5391020979284,-0.218455391669058,
4.55353248138526));
#25294=CARTESIAN_POINT('Ctrl Pts',(11.555007376616,-0.40169756257477,4.48121470137836));
#25295=CARTESIAN_POINT('Ctrl Pts',(11.5709126553036,-0.545462480794654,
4.3088676134633));
#25296=CARTESIAN_POINT('Ctrl Pts',(11.5868179339912,-0.583739378074245,
4.1156257090067));
#25297=CARTESIAN_POINT('Ctrl Pts',(11.6027232126789,-0.622016275353834,
3.92238380455011));
#25298=CARTESIAN_POINT('Ctrl Pts',(11.6186284913665,-0.554805151693135,
3.70824708355197));
#25299=CARTESIAN_POINT('Ctrl Pts',(11.6345337700541,-0.412966511608993,
3.57153806891708));
#25300=CARTESIAN_POINT('Ctrl Pts',(11.6504390487417,-0.271127871524847,
3.43482905428217));
#25301=CARTESIAN_POINT('Ctrl Pts',(11.6663443274293,-0.0546617150172531,
3.37554774601052));
#25302=CARTESIAN_POINT('Ctrl Pts',(11.6822496061169,0.137039856773353,3.42091361287512));
#25303=CARTESIAN_POINT('Ctrl Pts',(11.6981548848045,0.328741428563947,3.46627947973972));
#25304=CARTESIAN_POINT('Ctrl Pts',(11.7140601634921,0.495678415637556,3.61629252174057));
#25305=CARTESIAN_POINT('Ctrl Pts',(11.7299654421798,0.56120041605148,3.80207309651931));
#25306=CARTESIAN_POINT('Ctrl Pts',(11.7458707208674,0.626722416465409,3.98785367129807));
#25307=CARTESIAN_POINT('Ctrl Pts',(11.761775999555,0.590829430219633,4.20940177885472));
#25308=CARTESIAN_POINT('Ctrl Pts',(11.7776812782426,0.470001998091193,4.36499190112672));
#25309=CARTESIAN_POINT('Ctrl Pts',(11.7921723817426,0.359917612963646,4.5067481450567));
#25310=CARTESIAN_POINT('Ctrl Pts',(11.8066634852425,0.179330777996457,4.59375393408315));
#25311=CARTESIAN_POINT('Ctrl Pts',(11.8211545887425,-0.000307672146732893,
4.59488449882539));
#25312=CARTESIAN_POINT('Origin',(4.,0.,4.));
#25313=CARTESIAN_POINT('',(12.2288454112576,0.000142795628640946,4.59314744373127));
#25314=CARTESIAN_POINT('',(12.1211545887425,0.00052868291625318,4.59430727435519));
#25315=CARTESIAN_POINT('',(4.,-7.27562663373442E-17,4.5941));
#25316=CARTESIAN_POINT('Ctrl Pts',(12.2288454112576,0.000142795628640946,
4.59314744373127));
#25317=CARTESIAN_POINT('Ctrl Pts',(12.221591738855,0.0907369315914116,4.59334157666405));
#25318=CARTESIAN_POINT('Ctrl Pts',(12.2143380664525,0.181251971066953,4.57388161006077));
#25319=CARTESIAN_POINT('Ctrl Pts',(12.2070843940499,0.261922584292681,4.53433840020651));
#25320=CARTESIAN_POINT('Ctrl Pts',(12.1911791153623,0.438810719578057,4.44763117963851));
#25321=CARTESIAN_POINT('Ctrl Pts',(12.1752738366747,0.56836661021043,4.26436322928705));
#25322=CARTESIAN_POINT('Ctrl Pts',(12.1593685579871,0.591103672269137,4.06868343852597));
#25323=CARTESIAN_POINT('Ctrl Pts',(12.1434632792995,0.613840734327844,3.87300364776488));
#25324=CARTESIAN_POINT('Ctrl Pts',(12.1275580006119,0.529758967812885,3.66491201659415));
#25325=CARTESIAN_POINT('Ctrl Pts',(12.1116527219243,0.377465162701742,3.53995541841648));
#25326=CARTESIAN_POINT('Ctrl Pts',(12.0957474432367,0.225171357590603,3.41499882023882));
#25327=CARTESIAN_POINT('Ctrl Pts',(12.0798421645491,0.00466551388328543,
3.37317725505421));
#25328=CARTESIAN_POINT('Ctrl Pts',(12.0639368858614,-0.182805413822737,
3.43369341627091));
#25329=CARTESIAN_POINT('Ctrl Pts',(12.0480316071738,-0.37027634152876,3.49420957748762));
#25330=CARTESIAN_POINT('Ctrl Pts',(12.0321263284862,-0.524712353233489,
3.65706346510565));
#25331=CARTESIAN_POINT('Ctrl Pts',(12.0162210497986,-0.575202966010955,
3.84747946371059));
#25332=CARTESIAN_POINT('Ctrl Pts',(12.000315771111,-0.625693578788423,4.03789546231555));
#25333=CARTESIAN_POINT('Ctrl Pts',(11.9844104924234,-0.572238792638624,
4.25587357190742));
#25334=CARTESIAN_POINT('Ctrl Pts',(11.9685052137358,-0.439382783876041,
4.40132746645495));
#25335=CARTESIAN_POINT('Ctrl Pts',(11.9552852795764,-0.328957325572706,
4.52222386487166));
#25336=CARTESIAN_POINT('Ctrl Pts',(11.942065345417,-0.163678510702966,4.59301780268865));
#25337=CARTESIAN_POINT('Ctrl Pts',(11.9288454112576,0.000492284285450728,
4.5944814532616));
#25338=CARTESIAN_POINT('Ctrl Pts',(11.8211545887425,-0.000307672146732893,
4.59488449882539));
#25339=CARTESIAN_POINT('Ctrl Pts',(11.8225687639301,-0.0178384446610953,
4.59499482973335));
#25340=CARTESIAN_POINT('Ctrl Pts',(11.8239829391178,-0.035360185088601,
4.59428731490513));
#25341=CARTESIAN_POINT('Ctrl Pts',(11.8253971143054,-0.0528064866265509,
4.59273302680715));
#25342=CARTESIAN_POINT('Ctrl Pts',(11.8413023929931,-0.249025661204777,
4.57525189322826));
#25343=CARTESIAN_POINT('Ctrl Pts',(11.8572076716807,-0.435702132350142,
4.45065748908313));
#25344=CARTESIAN_POINT('Ctrl Pts',(11.8731129503683,-0.527121962142897,
4.27615829360067));
#25345=CARTESIAN_POINT('Ctrl Pts',(11.8890182290559,-0.618541791935657,
4.10165909811819));
#25346=CARTESIAN_POINT('Ctrl Pts',(11.9049235077435,-0.614704980375792,
3.87725511129838));
#25347=CARTESIAN_POINT('Ctrl Pts',(11.9208287864311,-0.517373229009482,
3.70598315013913));
#25348=CARTESIAN_POINT('Ctrl Pts',(11.9367340651187,-0.420041477643178,
3.53471118897989));
#25349=CARTESIAN_POINT('Ctrl Pts',(11.9526393438063,-0.229214786470442,
3.41657125348121));
#25350=CARTESIAN_POINT('Ctrl Pts',(11.9685446224939,-0.0325126988662629,
3.4058082039356));
#25351=CARTESIAN_POINT('Ctrl Pts',(11.9844499011816,0.164189388737916,3.39504515438998));
#25352=CARTESIAN_POINT('Ctrl Pts',(12.0003551798692,0.366766872773537,3.49165899079743));
#25353=CARTESIAN_POINT('Ctrl Pts',(12.0162604585568,0.482204742918021,3.65128872687397));
#25354=CARTESIAN_POINT('Ctrl Pts',(12.0321657372444,0.597642613062508,3.81091846295053));
#25355=CARTESIAN_POINT('Ctrl Pts',(12.048071015932,0.625940869315854,4.03356409869619));
#25356=CARTESIAN_POINT('Ctrl Pts',(12.0639762946196,0.554106149607013,4.21699617753661));
#25357=CARTESIAN_POINT('Ctrl Pts',(12.0798815733072,0.482271429898174,4.40042825637702));
#25358=CARTESIAN_POINT('Ctrl Pts',(12.0957868519948,0.310303734227154,4.5446467783122));
#25359=CARTESIAN_POINT('Ctrl Pts',(12.1116921306825,0.117163353092859,4.583432699452));
#25360=CARTESIAN_POINT('Ctrl Pts',(12.1148462833691,0.0788619649798074,
4.59112427906975));
#25361=CARTESIAN_POINT('Ctrl Pts',(12.1180004360558,0.0397279339241207,
4.59466958677844));
#25362=CARTESIAN_POINT('Ctrl Pts',(12.1211545887425,0.00052868291625318,
4.59430727435519));
#25363=CARTESIAN_POINT('Origin',(4.,0.,4.));
#25364=CARTESIAN_POINT('',(12.5288454112576,-0.000545899910317726,4.59395595168017));
#25365=CARTESIAN_POINT('',(12.4211545887425,4.74932194801069E-5,4.59311952367199));
#25366=CARTESIAN_POINT('',(4.,-7.27562663373442E-17,4.5941));
#25367=CARTESIAN_POINT('Ctrl Pts',(12.5288454112576,-0.000545899910317726,
4.59395595168017));
#25368=CARTESIAN_POINT('Ctrl Pts',(12.5170234109807,0.14659828900878,4.5926299020853));
#25369=CARTESIAN_POINT('Ctrl Pts',(12.5052014107038,0.29463204299547,4.53735693360054));
#25370=CARTESIAN_POINT('Ctrl Pts',(12.493379410427,0.402483765871145,4.43832383497591));
#25371=CARTESIAN_POINT('Ctrl Pts',(12.4774741317394,0.547587104485886,4.30508504322883));
#25372=CARTESIAN_POINT('Ctrl Pts',(12.4615688530518,0.619957272242066,4.09263639239171));
#25373=CARTESIAN_POINT('Ctrl Pts',(12.4456635743641,0.586364949835353,3.89852531496775));
#25374=CARTESIAN_POINT('Ctrl Pts',(12.4297582956765,0.55277262742864,3.7044142375438));
#25375=CARTESIAN_POINT('Ctrl Pts',(12.4138530169889,0.41321781485904,3.52864073353302));
#25376=CARTESIAN_POINT('Ctrl Pts',(12.3979477383013,0.231778177981285,3.45191255961345));
#25377=CARTESIAN_POINT('Ctrl Pts',(12.3820424596137,0.0503385411035255,
3.37518438569388));
#25378=CARTESIAN_POINT('Ctrl Pts',(12.3661371809261,-0.172985920082391,
3.39750154186552));
#25379=CARTESIAN_POINT('Ctrl Pts',(12.3502319022385,-0.335654061078685,
3.50861693417539));
#25380=CARTESIAN_POINT('Ctrl Pts',(12.3343266235509,-0.498322202074975,
3.61973232648525));
#25381=CARTESIAN_POINT('Ctrl Pts',(12.3184213448632,-0.600334022881645,
3.81964595493332));
#25382=CARTESIAN_POINT('Ctrl Pts',(12.3025160661756,-0.594850011148503,
4.0165659389844));
#25383=CARTESIAN_POINT('Ctrl Pts',(12.286610787488,-0.58936599941536,4.21348592303547));
#25384=CARTESIAN_POINT('Ctrl Pts',(12.2707055088004,-0.476386155142398,
4.40741226268955));
#25385=CARTESIAN_POINT('Ctrl Pts',(12.2548002301128,-0.307786043036728,
4.50930218712431));
#25386=CARTESIAN_POINT('Ctrl Pts',(12.2461486238277,-0.216076754679914,
4.564724762732));
#25387=CARTESIAN_POINT('Ctrl Pts',(12.2374970175426,-0.107910718865932,
4.59291589733543));
#25388=CARTESIAN_POINT('Ctrl Pts',(12.2288454112576,0.000142795628640946,
4.59314744373127));
#25389=CARTESIAN_POINT('Ctrl Pts',(12.1211545887425,0.00052868291625318,
4.59430727435519));
#25390=CARTESIAN_POINT('Ctrl Pts',(12.1339057147434,-0.157940052872902,
4.59284257311225));
#25391=CARTESIAN_POINT('Ctrl Pts',(12.1466568407444,-0.317474678016714,
4.52751565545538));
#25392=CARTESIAN_POINT('Ctrl Pts',(12.1594079667453,-0.427372353356377,
4.41409399619463));
#25393=CARTESIAN_POINT('Ctrl Pts',(12.1753132454329,-0.564454612073754,
4.27261605145303));
#25394=CARTESIAN_POINT('Ctrl Pts',(12.1912185241205,-0.62430606291093,4.0563068416254));
#25395=CARTESIAN_POINT('Ctrl Pts',(12.2071238028081,-0.579445451749542,
3.8644864045766));
#25396=CARTESIAN_POINT('Ctrl Pts',(12.2230290814957,-0.534584840588155,
3.6726659675278));
#25397=CARTESIAN_POINT('Ctrl Pts',(12.2389343601834,-0.38501216742821,3.50533430325784));
#25398=CARTESIAN_POINT('Ctrl Pts',(12.254839638871,-0.199404875886796,3.43932303278057));
#25399=CARTESIAN_POINT('Ctrl Pts',(12.2707449175586,-0.0137975843453769,
3.37331176230329));
#25400=CARTESIAN_POINT('Ctrl Pts',(12.2866501962462,0.207844325577514,3.40862088561871));
#25401=CARTESIAN_POINT('Ctrl Pts',(12.3025554749338,0.363752265741203,3.52903794710619));
#25402=CARTESIAN_POINT('Ctrl Pts',(12.3184607536214,0.519660205904889,3.64945500859368));
#25403=CARTESIAN_POINT('Ctrl Pts',(12.334366032309,0.609834176309377,3.85498000825323));
#25404=CARTESIAN_POINT('Ctrl Pts',(12.3502713109967,0.592870104691008,4.05124456128685));
#25405=CARTESIAN_POINT('Ctrl Pts',(12.3661765896843,0.575906033072638,4.24750911432049));
#25406=CARTESIAN_POINT('Ctrl Pts',(12.3820818683719,0.451803919431404,4.4345132207282));
#25407=CARTESIAN_POINT('Ctrl Pts',(12.3979871470595,0.277546204023914,4.52639250633888));
#25408=CARTESIAN_POINT('Ctrl Pts',(12.4057096276205,0.192938958450368,4.57100260157974));
#25409=CARTESIAN_POINT('Ctrl Pts',(12.4134321081815,0.0965080911524262,
4.59318808505049));
#25410=CARTESIAN_POINT('Ctrl Pts',(12.4211545887425,4.74932194801069E-5,
4.59311952367199));
#25411=CARTESIAN_POINT('Origin',(4.,0.,4.));
#25412=CARTESIAN_POINT('',(12.8288454112576,0.000112157221815526,4.59505491513413));
#25413=CARTESIAN_POINT('',(12.7211545887425,-0.000546355209092884,4.59413239245978));
#25414=CARTESIAN_POINT('',(4.,-7.27562663373442E-17,4.5941));
#25415=CARTESIAN_POINT('Ctrl Pts',(12.8288454112576,0.000112157221815526,
4.59505491513413));
#25416=CARTESIAN_POINT('Ctrl Pts',(12.828360361794,0.00612048155630211,
4.59507046002904));
#25417=CARTESIAN_POINT('Ctrl Pts',(12.8278753123304,0.0121283652366354,
4.59498736156652));
#25418=CARTESIAN_POINT('Ctrl Pts',(12.8273902628668,0.0181332013859869,
4.59480429815638));
#25419=CARTESIAN_POINT('Ctrl Pts',(12.8114849841792,0.215038052543873,4.58880145767424));
#25420=CARTESIAN_POINT('Ctrl Pts',(12.7955797054916,0.408666038032992,4.47531104548453));
#25421=CARTESIAN_POINT('Ctrl Pts',(12.779674426804,0.510111378641258,4.30644305748136));
#25422=CARTESIAN_POINT('Ctrl Pts',(12.7637691481164,0.611556719249521,4.1375750694782));
#25423=CARTESIAN_POINT('Ctrl Pts',(12.7478638694288,0.620819414976937,3.9133295056616));
#25424=CARTESIAN_POINT('Ctrl Pts',(12.7319585907412,0.533646427817818,3.7366704418887));
#25425=CARTESIAN_POINT('Ctrl Pts',(12.7160533120536,0.446473440658691,3.56001137811579));
#25426=CARTESIAN_POINT('Ctrl Pts',(12.700148033366,0.26286477061301,3.43093881438659));
#25427=CARTESIAN_POINT('Ctrl Pts',(12.6842427546783,0.0671257511235207,
3.4087174113557));
#25428=CARTESIAN_POINT('Ctrl Pts',(12.6683374759907,-0.128613268365957,
3.38649600832481));
#25429=CARTESIAN_POINT('Ctrl Pts',(12.6524321973031,-0.336482637299241,
3.47112576599221));
#25430=CARTESIAN_POINT('Ctrl Pts',(12.6365269186155,-0.461037535689932,
3.62374828002683));
#25431=CARTESIAN_POINT('Ctrl Pts',(12.6206216399279,-0.585592434080627,
3.77637079406146));
#25432=CARTESIAN_POINT('Ctrl Pts',(12.6047163612403,-0.626832861928724,
3.9969860644633));
#25433=CARTESIAN_POINT('Ctrl Pts',(12.5888110825527,-0.565822959504995,
4.18429689252621));
#25434=CARTESIAN_POINT('Ctrl Pts',(12.5729058038651,-0.504813057081268,
4.37160772058911));
#25435=CARTESIAN_POINT('Ctrl Pts',(12.5570005251774,-0.341552824385721,
4.52561410631309));
#25436=CARTESIAN_POINT('Ctrl Pts',(12.5410952464898,-0.151004453301302,
4.57560283284656));
#25437=CARTESIAN_POINT('Ctrl Pts',(12.5370119680791,-0.102085973774189,
4.58843617527608));
#25438=CARTESIAN_POINT('Ctrl Pts',(12.5329286896683,-0.0513689988622793,
4.59441396466913));
#25439=CARTESIAN_POINT('Ctrl Pts',(12.5288454112576,-0.000545899910317726,
4.59395595168017));
#25440=CARTESIAN_POINT('Ctrl Pts',(12.4211545887425,4.74932194801069E-5,
4.59311952367199));
#25441=CARTESIAN_POINT('Ctrl Pts',(12.4293373868691,-0.102162877376194,
4.59304687552285));
#25442=CARTESIAN_POINT('Ctrl Pts',(12.4375201849957,-0.204406628577491,
4.5679880979308));
#25443=CARTESIAN_POINT('Ctrl Pts',(12.4457029831223,-0.292652646395614,
4.51814611323009));
#25444=CARTESIAN_POINT('Ctrl Pts',(12.4616082618099,-0.46418046423393,4.42126596969699));
#25445=CARTESIAN_POINT('Ctrl Pts',(12.4775135404976,-0.582822782736806,
4.23075121781716));
#25446=CARTESIAN_POINT('Ctrl Pts',(12.4934188191852,-0.594104068590283,
4.03407817163935));
#25447=CARTESIAN_POINT('Ctrl Pts',(12.5093240978728,-0.605385354443759,
3.83740512546155));
#25448=CARTESIAN_POINT('Ctrl Pts',(12.5252293765604,-0.509305607647849,
3.63457378498577));
#25449=CARTESIAN_POINT('Ctrl Pts',(12.541134655248,-0.34998058313236,3.51871572067214));
#25450=CARTESIAN_POINT('Ctrl Pts',(12.5570399339356,-0.19065555861687,3.4028576563585));
#25451=CARTESIAN_POINT('Ctrl Pts',(12.5729452126232,0.031914743618199,3.37397286820701));
#25452=CARTESIAN_POINT('Ctrl Pts',(12.5888504913108,0.215535456959467,3.44532402892222));
#25453=CARTESIAN_POINT('Ctrl Pts',(12.6047557699985,0.399156170300736,3.51667518963742));
#25454=CARTESIAN_POINT('Ctrl Pts',(12.6206610486861,0.543827294748204,3.68826229921932));
#25455=CARTESIAN_POINT('Ctrl Pts',(12.6365663273737,0.583121970486127,3.88129981619987));
#25456=CARTESIAN_POINT('Ctrl Pts',(12.6524716060613,0.622416646224052,4.07433733318042));
#25457=CARTESIAN_POINT('Ctrl Pts',(12.6683768847489,0.556334873252426,4.28882525755962));
#25458=CARTESIAN_POINT('Ctrl Pts',(12.6842821634365,0.415218606030559,4.42627980869829));
#25459=CARTESIAN_POINT('Ctrl Pts',(12.6965729718718,0.306170972122536,4.53249785050629));
#25460=CARTESIAN_POINT('Ctrl Pts',(12.7088637803072,0.152317016475741,4.59271595401221));
#25461=CARTESIAN_POINT('Ctrl Pts',(12.7211545887425,-0.000546355209092884,
4.59413239245978));
#25462=CARTESIAN_POINT('Origin',(4.,0.,4.));
#25463=CARTESIAN_POINT('',(13.1288454112576,0.000488576923893258,4.59361798633976));
#25464=CARTESIAN_POINT('',(13.0211545887425,0.000215375668158819,4.59498635240753));
#25465=CARTESIAN_POINT('',(4.,-7.27562663373442E-17,4.5941));
#25466=CARTESIAN_POINT('Ctrl Pts',(13.1288454112576,0.000488576923893258,
4.59361798633976));
#25467=CARTESIAN_POINT('Ctrl Pts',(13.1237920339197,0.0634769139372694,
4.59410397103046));
#25468=CARTESIAN_POINT('Ctrl Pts',(13.1187386565818,0.126326538027094,4.58487602541266));
#25469=CARTESIAN_POINT('Ctrl Pts',(13.1136852792439,0.185787091792062,4.56533540718874));
#25470=CARTESIAN_POINT('Ctrl Pts',(13.0977800005563,0.372936519850693,4.50383218710482));
#25471=CARTESIAN_POINT('Ctrl Pts',(13.0818747218686,0.526512210440984,4.34016674272733));
#25472=CARTESIAN_POINT('Ctrl Pts',(13.065969443181,0.575998703695535,4.14948732200047));
#25473=CARTESIAN_POINT('Ctrl Pts',(13.0500641644934,0.625485196950086,3.9588079012736));
#25474=CARTESIAN_POINT('Ctrl Pts',(13.0341588858058,0.570882492868891,3.74111450419737));
#25475=CARTESIAN_POINT('Ctrl Pts',(13.0182536071182,0.437261843116128,3.59636272886105));
#25476=CARTESIAN_POINT('Ctrl Pts',(13.0023483284306,0.303641193363369,3.45161095352474));
#25477=CARTESIAN_POINT('Ctrl Pts',(12.986443049743,0.0910025979390456,3.37980079992835));
#25478=CARTESIAN_POINT('Ctrl Pts',(12.9705377710554,-0.10301929613509,3.41390445256627));
#25479=CARTESIAN_POINT('Ctrl Pts',(12.9546324923678,-0.297041190209231,
3.4480081052042));
#25480=CARTESIAN_POINT('Ctrl Pts',(12.9387272136801,-0.472446382933184,
3.58802556407645));
#25481=CARTESIAN_POINT('Ctrl Pts',(12.9228219349925,-0.54869623058984,3.76966673571907));
#25482=CARTESIAN_POINT('Ctrl Pts',(12.9069166563049,-0.624946078246494,
3.95130790736168));
#25483=CARTESIAN_POINT('Ctrl Pts',(12.8910113776173,-0.602040580835857,
4.17457279177466));
#25484=CARTESIAN_POINT('Ctrl Pts',(12.8751060989297,-0.490496973717212,
4.33694759959386));
#25485=CARTESIAN_POINT('Ctrl Pts',(12.8596858697056,-0.382355015061345,
4.49437060399126));
#25486=CARTESIAN_POINT('Ctrl Pts',(12.8442656404816,-0.190898750836606,
4.59456072668396));
#25487=CARTESIAN_POINT('Ctrl Pts',(12.8288454112576,0.000112157221815526,
4.59505491513413));
#25488=CARTESIAN_POINT('Ctrl Pts',(12.7211545887425,-0.000546355209092884,
4.59413239245978));
#25489=CARTESIAN_POINT('Ctrl Pts',(12.7247690589948,-0.0455002825709059,
4.59454893744622));
#25490=CARTESIAN_POINT('Ctrl Pts',(12.7283835292471,-0.0903685417208244,
4.58988016539195));
#25491=CARTESIAN_POINT('Ctrl Pts',(12.7319979994994,-0.13398639330236,4.5798004937111));
#25492=CARTESIAN_POINT('Ctrl Pts',(12.747903278187,-0.325924363941296,4.53544544968711));
#25493=CARTESIAN_POINT('Ctrl Pts',(12.7638085568746,-0.493649543747071,
4.38631418374101));
#25494=CARTESIAN_POINT('Ctrl Pts',(12.7797138355622,-0.560149626020051,
4.20088146397168));
#25495=CARTESIAN_POINT('Ctrl Pts',(12.7956191142498,-0.626649708293032,
4.01544874420235));
#25496=CARTESIAN_POINT('Ctrl Pts',(12.8115243929374,-0.591924693033219,
3.79371457060979));
#25497=CARTESIAN_POINT('Ctrl Pts',(12.827429671625,-0.471918838153678,3.63748989490844));
#25498=CARTESIAN_POINT('Ctrl Pts',(12.8433349503126,-0.351912983274129,
3.48126521920708));
#25499=CARTESIAN_POINT('Ctrl Pts',(12.8592402290002,-0.146626288774854,
3.39055004139693));
#25500=CARTESIAN_POINT('Ctrl Pts',(12.8751455076879,0.0496822801939141,
3.40699693328572));
#25501=CARTESIAN_POINT('Ctrl Pts',(12.8910507863755,0.245990849162665,3.42344382517451));
#25502=CARTESIAN_POINT('Ctrl Pts',(12.9069560650631,0.433321292600904,3.54705278676224));
#25503=CARTESIAN_POINT('Ctrl Pts',(12.9228613437507,0.525659396179275,3.72106781235173));
#25504=CARTESIAN_POINT('Ctrl Pts',(12.9387666224383,0.617997499757654,3.89508283794124));
#25505=CARTESIAN_POINT('Ctrl Pts',(12.9546719011259,0.615343263476151,4.11950392753251));
#25506=CARTESIAN_POINT('Ctrl Pts',(12.9705771798135,0.518915400343756,4.29128641125856));
#25507=CARTESIAN_POINT('Ctrl Pts',(12.9864824585012,0.422487537211366,4.46306889498459));
#25508=CARTESIAN_POINT('Ctrl Pts',(13.0023877371888,0.232286047228094,4.58221277284539));
#25509=CARTESIAN_POINT('Ctrl Pts',(13.0182930158764,0.0356434078328121,
4.59401221668908));
#25510=CARTESIAN_POINT('Ctrl Pts',(13.0192468734984,0.0238505254767134,
4.59471984273368));
#25511=CARTESIAN_POINT('Ctrl Pts',(13.0202007311205,0.0120344772878951,
4.59504140054066));
#25512=CARTESIAN_POINT('Ctrl Pts',(13.0211545887425,0.000215375668158819,
4.59498635240753));
#25513=CARTESIAN_POINT('Origin',(4.,0.,4.));
#25514=CARTESIAN_POINT('',(13.4288454112576,-0.000323145728561625,4.59329116515504));
#25515=CARTESIAN_POINT('',(13.3211545887425,0.000436239896754628,4.59347700091179));
#25516=CARTESIAN_POINT('',(4.,-7.27562663373442E-17,4.5941));
#25517=CARTESIAN_POINT('Ctrl Pts',(13.4288454112576,-0.000323145728561625,
4.59329116515504));
#25518=CARTESIAN_POINT('Ctrl Pts',(13.4192237060453,0.11977362227264,4.59270025156928));
#25519=CARTESIAN_POINT('Ctrl Pts',(13.4096020008331,0.240190260834984,4.55734300206483));
#25520=CARTESIAN_POINT('Ctrl Pts',(13.3999802956209,0.338238798929947,4.48960747645051));
#25521=CARTESIAN_POINT('Ctrl Pts',(13.3840750169333,0.500319146323361,4.37763642888821));
#25522=CARTESIAN_POINT('Ctrl Pts',(13.3681697382457,0.601276083433826,4.17718801339723));
#25523=CARTESIAN_POINT('Ctrl Pts',(13.3522644595581,0.594754455875995,3.9802996620979));
#25524=CARTESIAN_POINT('Ctrl Pts',(13.3363591808704,0.588232828318166,3.78341131079859));
#25525=CARTESIAN_POINT('Ctrl Pts',(13.3204539021828,0.474232636092054,3.59008302369095));
#25526=CARTESIAN_POINT('Ctrl Pts',(13.3045486234952,0.305097944517489,3.48908297116948));
#25527=CARTESIAN_POINT('Ctrl Pts',(13.2886433448076,0.135963252942929,3.388082918648));
#25528=CARTESIAN_POINT('Ctrl Pts',(13.27273806612,-0.0883059379800925,3.3794111007127));
#25529=CARTESIAN_POINT('Ctrl Pts',(13.2568327874324,-0.264734703826722,
3.46704924928509));
#25530=CARTESIAN_POINT('Ctrl Pts',(13.2409275087448,-0.441163469673367,
3.55468739785749));
#25531=CARTESIAN_POINT('Ctrl Pts',(13.2250222300572,-0.569751810443623,
3.7386355129376));
#25532=CARTESIAN_POINT('Ctrl Pts',(13.2091169513696,-0.591457400179852,
3.9344324022836));
#25533=CARTESIAN_POINT('Ctrl Pts',(13.1932116726819,-0.613162989916079,
4.1302292916296));
#25534=CARTESIAN_POINT('Ctrl Pts',(13.1773063939943,-0.527985828618295,
4.33787495524147));
#25535=CARTESIAN_POINT('Ctrl Pts',(13.1614011153067,-0.375035665205916,
4.46202728915223));
#25536=CARTESIAN_POINT('Ctrl Pts',(13.150549213957,-0.270680367988337,4.54673431669939));
#25537=CARTESIAN_POINT('Ctrl Pts',(13.1396973126073,-0.134776053786733,
4.59257435599745));
#25538=CARTESIAN_POINT('Ctrl Pts',(13.1288454112576,0.000488576923893258,
4.59361798633976));
#25539=CARTESIAN_POINT('Ctrl Pts',(13.0211545887425,0.000215375668158819,
4.59498635240753));
#25540=CARTESIAN_POINT('Ctrl Pts',(13.0361060098081,-0.185045360160338,
4.59412349007018));
#25541=CARTESIAN_POINT('Ctrl Pts',(13.0510574308736,-0.371056311319581,
4.5007301079696));
#25542=CARTESIAN_POINT('Ctrl Pts',(13.0660088519392,-0.480360474535337,
4.35124746348123));
#25543=CARTESIAN_POINT('Ctrl Pts',(13.0819141306268,-0.596637928700896,
4.19222825660313));
#25544=CARTESIAN_POINT('Ctrl Pts',(13.0978194093145,-0.626109048224722,
3.96973483302036));
#25545=CARTESIAN_POINT('Ctrl Pts',(13.1137246880021,-0.555241941841719,
3.78592675992164));
#25546=CARTESIAN_POINT('Ctrl Pts',(13.1296299666897,-0.484374835458714,
3.60211868682292));
#25547=CARTESIAN_POINT('Ctrl Pts',(13.1455352453773,-0.313169503168878,
3.45699596420825));
#25548=CARTESIAN_POINT('Ctrl Pts',(13.1614405240649,-0.120236190459409,
3.4171928066662));
#25549=CARTESIAN_POINT('Ctrl Pts',(13.1773458027525,0.0726971222500488,
3.37738964912416));
#25550=CARTESIAN_POINT('Ctrl Pts',(13.1932510814401,0.287358415379145,3.44290605665475));
#25551=CARTESIAN_POINT('Ctrl Pts',(13.2091563601277,0.425184304693362,3.58365966669054));
#25552=CARTESIAN_POINT('Ctrl Pts',(13.2250616388154,0.563010194007583,3.72441327672633));
#25553=CARTESIAN_POINT('Ctrl Pts',(13.240966917503,0.624000679506934,3.94040408926733));
#25554=CARTESIAN_POINT('Ctrl Pts',(13.2568721961906,0.580151510544767,4.13245826101242));
#25555=CARTESIAN_POINT('Ctrl Pts',(13.2727774748782,0.536302341582597,4.32451243275751));
#25556=CARTESIAN_POINT('Ctrl Pts',(13.2886827535658,0.387613518158899,4.49262996370669));
#25557=CARTESIAN_POINT('Ctrl Pts',(13.3045880322534,0.202356657484476,4.55961839611428));
#25558=CARTESIAN_POINT('Ctrl Pts',(13.3101102177498,0.13803695776657,4.58287624384712));
#25559=CARTESIAN_POINT('Ctrl Pts',(13.3156324032461,0.0693092633201986,
4.59394375907155));
#25560=CARTESIAN_POINT('Ctrl Pts',(13.3211545887425,0.000436239896754628,
4.59347700091179));
#25561=CARTESIAN_POINT('Origin',(4.,0.,4.));
#25562=CARTESIAN_POINT('',(13.7288454112576,-0.000361622974213827,4.59480268714608));
#25563=CARTESIAN_POINT('',(13.6211545887425,-0.000396530615921017,4.59339874939382));
#25564=CARTESIAN_POINT('',(4.,-7.27562663373442E-17,4.5941));
#25565=CARTESIAN_POINT('Ctrl Pts',(13.7288454112576,-0.000361622974213827,
4.59480268714608));
#25566=CARTESIAN_POINT('Ctrl Pts',(13.714655378171,0.175608319374377,4.59354294412002));
#25567=CARTESIAN_POINT('Ctrl Pts',(13.7004653450845,0.352610168065205,4.51056419690263));
#25568=CARTESIAN_POINT('Ctrl Pts',(13.6862753119979,0.463013835099274,4.37381700684221));
#25569=CARTESIAN_POINT('Ctrl Pts',(13.6703700333103,0.586762742631886,4.22054025587244));
#25570=CARTESIAN_POINT('Ctrl Pts',(13.6544647546227,0.626840040937572,3.99971072753873));
#25571=CARTESIAN_POINT('Ctrl Pts',(13.6385594759351,0.564843930165024,3.81272399872504));
#25572=CARTESIAN_POINT('Ctrl Pts',(13.6226541972475,0.502847819392478,3.62573726991136));
#25573=CARTESIAN_POINT('Ctrl Pts',(13.6067489185599,0.338778299541704,3.4725933406177));
#25574=CARTESIAN_POINT('Ctrl Pts',(13.5908436398723,0.147969152919217,3.42360942419035));
#25575=CARTESIAN_POINT('Ctrl Pts',(13.5749383611846,-0.0428399937032757,
3.37462550776301));
#25576=CARTESIAN_POINT('Ctrl Pts',(13.559033082497,-0.260388767097474,3.42980160420198));
#25577=CARTESIAN_POINT('Ctrl Pts',(13.5431278038094,-0.404787974250376,
3.56380318433064));
#25578=CARTESIAN_POINT('Ctrl Pts',(13.5272225251218,-0.549187181403275,
3.6978047644593));
#25579=CARTESIAN_POINT('Ctrl Pts',(13.5113172464342,-0.620436822314871,
3.91063182827765));
#25580=CARTESIAN_POINT('Ctrl Pts',(13.4954119677466,-0.585822076202281,
4.10456319205082));
#25581=CARTESIAN_POINT('Ctrl Pts',(13.479506689059,-0.551207330089691,4.298494555824));
#25582=CARTESIAN_POINT('Ctrl Pts',(13.4636014103714,-0.410728196952908,
4.47353021955202));
#25583=CARTESIAN_POINT('Ctrl Pts',(13.4476961316837,-0.228886751546343,
4.54930121159921));
#25584=CARTESIAN_POINT('Ctrl Pts',(13.4414125582084,-0.15704808052867,4.57923546205676));
#25585=CARTESIAN_POINT('Ctrl Pts',(13.435128984733,-0.0787538239969463,
4.5936770685736));
#25586=CARTESIAN_POINT('Ctrl Pts',(13.4288454112576,-0.000323145728561625,
4.59329116515504));
#25587=CARTESIAN_POINT('Ctrl Pts',(13.3211545887425,0.000436239896754628,
4.59347700091179));
#25588=CARTESIAN_POINT('Ctrl Pts',(13.3315376819337,-0.129062311182503,
4.59259937855127));
#25589=CARTESIAN_POINT('Ctrl Pts',(13.341920775125,-0.259074650003773,4.55094414667863));
#25590=CARTESIAN_POINT('Ctrl Pts',(13.3523038683163,-0.361265427801182,
4.47287234722855));
#25591=CARTESIAN_POINT('Ctrl Pts',(13.3682091470039,-0.517805754487323,
4.35327853206923));
#25592=CARTESIAN_POINT('Ctrl Pts',(13.3841144256915,-0.609061509934468,
4.14823156788458));
#25593=CARTESIAN_POINT('Ctrl Pts',(13.4000197043791,-0.593131911953917,
3.95188034580653));
#25594=CARTESIAN_POINT('Ctrl Pts',(13.4159249830667,-0.577202313973367,
3.75552912372848));
#25595=CARTESIAN_POINT('Ctrl Pts',(13.4318302617543,-0.454087362565127,
3.56787364375704));
#25596=CARTESIAN_POINT('Ctrl Pts',(13.4477355404419,-0.280316234851803,
3.47507736324643));
#25597=CARTESIAN_POINT('Ctrl Pts',(13.4636408191295,-0.106545107138479,
3.38228108273583));
#25598=CARTESIAN_POINT('Ctrl Pts',(13.4795460978172,0.117882196879929,3.38434400168606));
#25599=CARTESIAN_POINT('Ctrl Pts',(13.4954513765048,0.2899181539344,3.48031891499009));
#25600=CARTESIAN_POINT('Ctrl Pts',(13.5113566551924,0.461954110988876,3.57629382829412));
#25601=CARTESIAN_POINT('Ctrl Pts',(13.52726193388,0.581598721079409,3.76618073595195));
#25602=CARTESIAN_POINT('Ctrl Pts',(13.5431672125676,0.593916240998451,3.96279160341967));
#25603=CARTESIAN_POINT('Ctrl Pts',(13.5590724912552,0.606233760917493,4.15940247088739));
#25604=CARTESIAN_POINT('Ctrl Pts',(13.5749777699428,0.511224190665043,4.362737298165));
#25605=CARTESIAN_POINT('Ctrl Pts',(13.5908830486304,0.352511905377589,4.47943333495374));
#25606=CARTESIAN_POINT('Ctrl Pts',(13.6009735620011,0.251822790258117,4.55346680161908));
#25607=CARTESIAN_POINT('Ctrl Pts',(13.6110640753718,0.125494626822297,4.59262991567553));
#25608=CARTESIAN_POINT('Ctrl Pts',(13.6211545887425,-0.000396530615921017,
4.59339874939382));
#25609=CARTESIAN_POINT('Origin',(4.,0.,4.));
#25610=CARTESIAN_POINT('',(14.0288454112576,0.000507412974116619,4.59441995931617));
#25611=CARTESIAN_POINT('',(13.9211545887425,-0.000275297881949146,4.59492513410986));
#25612=CARTESIAN_POINT('',(4.,-7.27562663373442E-17,4.5941));
#25613=CARTESIAN_POINT('Ctrl Pts',(14.0288454112576,0.000507412974116619,
4.59441995931617));
#25614=CARTESIAN_POINT('Ctrl Pts',(14.0259923289843,0.0359476882196221,
4.59474138052009));
#25615=CARTESIAN_POINT('Ctrl Pts',(14.0231392467111,0.0713355155074759,
4.59184535342408));
#25616=CARTESIAN_POINT('Ctrl Pts',(14.0202861644378,0.106106362061302,4.58554453803953));
#25617=CARTESIAN_POINT('Ctrl Pts',(14.0043808857502,0.299945849210873,4.55041893875697));
#25618=CARTESIAN_POINT('Ctrl Pts',(13.9884756070626,0.474610768799237,4.40947910659883));
#25619=CARTESIAN_POINT('Ctrl Pts',(13.972570328375,0.549902379214768,4.22743864981956));
#25620=CARTESIAN_POINT('Ctrl Pts',(13.9566650496873,0.625193989630293,4.04539819304031));
#25621=CARTESIAN_POINT('Ctrl Pts',(13.9407597709997,0.601112290873006,3.82225711163994));
#25622=CARTESIAN_POINT('Ctrl Pts',(13.9248544923121,0.488714580199595,3.66047234987686));
#25623=CARTESIAN_POINT('Ctrl Pts',(13.9089492136245,0.376316869526181,3.49868758811377));
#25624=CARTESIAN_POINT('Ctrl Pts',(13.8930439349369,0.175603146936639,3.39825914598798));
#25625=CARTESIAN_POINT('Ctrl Pts',(13.8771386562493,-0.0212673376532481,
3.40529951534663));
#25626=CARTESIAN_POINT('Ctrl Pts',(13.8612333775617,-0.218137822243141,
3.41233988470529));
#25627=CARTESIAN_POINT('Ctrl Pts',(13.8453280988741,-0.411165068833379,
3.52684906554841));
#25628=CARTESIAN_POINT('Ctrl Pts',(13.8294228201864,-0.511719132099071,
3.69624928651676));
#25629=CARTESIAN_POINT('Ctrl Pts',(13.8135175414988,-0.612273195364761,
3.8656495074851));
#25630=CARTESIAN_POINT('Ctrl Pts',(13.7976122628112,-0.62035407530591,4.08994076857866));
#25631=CARTESIAN_POINT('Ctrl Pts',(13.7817069841236,-0.532251373727382,
4.26613801168402));
#25632=CARTESIAN_POINT('Ctrl Pts',(13.765801705436,-0.44414867214885,4.44233525478938));
#25633=CARTESIAN_POINT('Ctrl Pts',(13.7498964267484,-0.259862389050636,
4.57043847990653));
#25634=CARTESIAN_POINT('Ctrl Pts',(13.7339911480608,-0.0640089891217576,
4.59162810566218));
#25635=CARTESIAN_POINT('Ctrl Pts',(13.7322759024597,-0.0428879079209441,
4.59391322201126));
#25636=CARTESIAN_POINT('Ctrl Pts',(13.7305606568586,-0.0216323041412813,
4.594954960835));
#25637=CARTESIAN_POINT('Ctrl Pts',(13.7288454112576,-0.000361622974213827,
4.59480268714608));
#25638=CARTESIAN_POINT('Ctrl Pts',(13.6211545887425,-0.000396530615921017,
4.59339874939382));
#25639=CARTESIAN_POINT('Ctrl Pts',(13.6269693540594,-0.0729426448807452,
4.59384179797573));
#25640=CARTESIAN_POINT('Ctrl Pts',(13.6327841193764,-0.145343639818557,
4.58153501668255));
#25641=CARTESIAN_POINT('Ctrl Pts',(13.6385988846933,-0.212609537044371,
4.5558040579697));
#25642=CARTESIAN_POINT('Ctrl Pts',(13.6545041633809,-0.396603693856438,
4.48542149789704));
#25643=CARTESIAN_POINT('Ctrl Pts',(13.6704094420685,-0.542177007158105,
4.31459913145184));
#25644=CARTESIAN_POINT('Ctrl Pts',(13.6863147207561,-0.582488370180261,
4.12177136240739));
#25645=CARTESIAN_POINT('Ctrl Pts',(13.7022199994437,-0.622799733202417,
3.92894359336294));
#25646=CARTESIAN_POINT('Ctrl Pts',(13.7181252781313,-0.557849145945042,
3.71411042171923));
#25647=CARTESIAN_POINT('Ctrl Pts',(13.734030556819,-0.417459170243993,3.57591415105311));
#25648=CARTESIAN_POINT('Ctrl Pts',(13.7499358355066,-0.277069194542941,
3.43771788038699));
#25649=CARTESIAN_POINT('Ctrl Pts',(13.7658411141942,-0.0612398303982075,
3.37615851069845));
#25650=CARTESIAN_POINT('Ctrl Pts',(13.7817463928818,0.130929209162332,3.41950150018632));
#25651=CARTESIAN_POINT('Ctrl Pts',(13.7976516715694,0.323098248722867,3.46284448967418));
#25652=CARTESIAN_POINT('Ctrl Pts',(13.813556950257,0.491606963699209,3.61108983833845));
#25653=CARTESIAN_POINT('Ctrl Pts',(13.8294622289446,0.559083281190044,3.79616955381596));
#25654=CARTESIAN_POINT('Ctrl Pts',(13.8453675076322,0.62655959868088,3.98124926929349));
#25655=CARTESIAN_POINT('Ctrl Pts',(13.8612727863198,0.593003518686204,4.20316335158427));
#25656=CARTESIAN_POINT('Ctrl Pts',(13.8771780650075,0.4738225734989,4.36001824251097));
#25657=CARTESIAN_POINT('Ctrl Pts',(13.8918369062525,0.363981395029584,4.50458099992985));
#25658=CARTESIAN_POINT('Ctrl Pts',(13.9064957474975,0.181409709145346,4.59388191268165));
#25659=CARTESIAN_POINT('Ctrl Pts',(13.9211545887425,-0.000275297881949146,
4.59492513410986));
#25660=CARTESIAN_POINT('Origin',(4.,0.,4.));
#25661=CARTESIAN_POINT('',(14.3288454112576,0.000109044058801022,4.5931342436645));
#25662=CARTESIAN_POINT('',(14.2211545887425,0.000537210645871958,4.59424369460725));
#25663=CARTESIAN_POINT('',(4.,-7.27562663373442E-17,4.5941));
#25664=CARTESIAN_POINT('Ctrl Pts',(14.3288454112576,0.000109044058801022,
4.5931342436645));
#25665=CARTESIAN_POINT('Ctrl Pts',(14.32142400111,0.0928032711674493,4.59328573107644));
#25666=CARTESIAN_POINT('Ctrl Pts',(14.3140025909624,0.185434358886594,4.57287353691408));
#25667=CARTESIAN_POINT('Ctrl Pts',(14.3065811808148,0.267539471941071,4.53154830171049));
#25668=CARTESIAN_POINT('Ctrl Pts',(14.2906759021272,0.443503969097433,4.44298165875801));
#25669=CARTESIAN_POINT('Ctrl Pts',(14.2747706234396,0.571121189235106,4.25835848700565));
#25670=CARTESIAN_POINT('Ctrl Pts',(14.258865344752,0.591794703906212,4.06244993615984));
#25671=CARTESIAN_POINT('Ctrl Pts',(14.2429600660644,0.612468218577319,3.86654138531401));
#25672=CARTESIAN_POINT('Ctrl Pts',(14.2270547873768,0.526198027781844,3.65934745537473));
#25673=CARTESIAN_POINT('Ctrl Pts',(14.2111495086891,0.372595753342289,3.53600283331781));
#25674=CARTESIAN_POINT('Ctrl Pts',(14.1952442300015,0.218993478902743,3.4126582112609));
#25675=CARTESIAN_POINT('Ctrl Pts',(14.1793389513139,-0.00194087918087354,
3.37316289708635));
#25676=CARTESIAN_POINT('Ctrl Pts',(14.1634336726263,-0.18876361063844,3.43565146815417));
#25677=CARTESIAN_POINT('Ctrl Pts',(14.1475283939387,-0.375586342096006,
3.49814003922198));
#25678=CARTESIAN_POINT('Ctrl Pts',(14.1316231152511,-0.528297446927522,
3.66261249553216));
#25679=CARTESIAN_POINT('Ctrl Pts',(14.1157178365635,-0.576778446468407,
3.85355004340287));
#25680=CARTESIAN_POINT('Ctrl Pts',(14.0998125578759,-0.625259446009293,
4.04448759127359));
#25681=CARTESIAN_POINT('Ctrl Pts',(14.0839072791882,-0.569510340259543,
4.26189023070484));
#25682=CARTESIAN_POINT('Ctrl Pts',(14.0680020005006,-0.435128760029281,
4.40593586721696));
#25683=CARTESIAN_POINT('Ctrl Pts',(14.0549498040863,-0.324852491748397,
4.52414265738481));
#25684=CARTESIAN_POINT('Ctrl Pts',(14.0418976076719,-0.161623710204441,
4.5929495310973));
#25685=CARTESIAN_POINT('Ctrl Pts',(14.0288454112576,0.000507412974116619,
4.59441995931617));
#25686=CARTESIAN_POINT('Ctrl Pts',(13.9211545887425,-0.000275297881949146,
4.59492513410986));
#25687=CARTESIAN_POINT('Ctrl Pts',(13.9224010261851,-0.015723926578741,
4.59501383895544));
#25688=CARTESIAN_POINT('Ctrl Pts',(13.9236474636277,-0.0311661445373128,
4.59446443570748));
#25689=CARTESIAN_POINT('Ctrl Pts',(13.9248939010703,-0.0465566941337027,
4.59325663951544));
#25690=CARTESIAN_POINT('Ctrl Pts',(13.9407991797579,-0.242949206199084,
4.5778444460306));
#25691=CARTESIAN_POINT('Ctrl Pts',(13.9567044584455,-0.430928419949921,
4.4552243594983));
#25692=CARTESIAN_POINT('Ctrl Pts',(13.9726097371331,-0.524182233176515,
4.28169833602613));
#25693=CARTESIAN_POINT('Ctrl Pts',(13.9885150158207,-0.617436046403107,
4.10817231255396));
#25694=CARTESIAN_POINT('Ctrl Pts',(14.0044202945084,-0.615964459105464,
3.88374035214192));
#25695=CARTESIAN_POINT('Ctrl Pts',(14.020325573196,-0.52044316191294,3.71145211607799));
#25696=CARTESIAN_POINT('Ctrl Pts',(14.0362308518836,-0.424921864720413,
3.53916388001405));
#25697=CARTESIAN_POINT('Ctrl Pts',(14.0521361305712,-0.235350857633014,
3.41901936829824));
#25698=CARTESIAN_POINT('Ctrl Pts',(14.0680414092588,-0.0387731270173405,
3.40618385781531));
#25699=CARTESIAN_POINT('Ctrl Pts',(14.0839466879464,0.157804603598333,3.39334834733239));
#25700=CARTESIAN_POINT('Ctrl Pts',(14.0998519666341,0.361389057742269,3.48782183808236));
#25701=CARTESIAN_POINT('Ctrl Pts',(14.1157572453217,0.478502867019537,3.64622609995664));
#25702=CARTESIAN_POINT('Ctrl Pts',(14.1316625240093,0.595616676296804,3.80463036183091));
#25703=CARTESIAN_POINT('Ctrl Pts',(14.1475678026969,0.626259840707404,4.02696539482948));
#25704=CARTESIAN_POINT('Ctrl Pts',(14.1634730813845,0.556362315559365,4.21114435801894));
#25705=CARTESIAN_POINT('Ctrl Pts',(14.1793783600721,0.486464790411328,4.3953233212084));
#25706=CARTESIAN_POINT('Ctrl Pts',(14.1952836387597,0.316026575704654,4.54134621458875));
#25707=CARTESIAN_POINT('Ctrl Pts',(14.2111889174473,0.123305688986428,4.58216550323889));
#25708=CARTESIAN_POINT('Ctrl Pts',(14.2145108078791,0.0830550475387342,
4.59069079896363));
#25709=CARTESIAN_POINT('Ctrl Pts',(14.2178326983108,0.0418324306113591,
4.59462708830176));
#25710=CARTESIAN_POINT('Ctrl Pts',(14.2211545887425,0.000537210645871958,
4.59424369460725));
#25711=CARTESIAN_POINT('Origin',(4.,0.,4.));
#25712=CARTESIAN_POINT('',(14.6288454112575,-0.000548182068839831,4.59401855345973));
#25713=CARTESIAN_POINT('',(14.5211545887425,1.28950532977596E-5,4.59311636453746));
#25714=CARTESIAN_POINT('',(4.,-7.27562663373442E-17,4.5941));
#25715=CARTESIAN_POINT('Ctrl Pts',(14.6288454112575,-0.000548182068839831,
4.59401855345973));
#25716=CARTESIAN_POINT('Ctrl Pts',(14.6168556732357,0.148643716013534,4.59265593252186));
#25717=CARTESIAN_POINT('Ctrl Pts',(14.6048659352138,0.29876355451001,4.53564313143304));
#25718=CARTESIAN_POINT('Ctrl Pts',(14.5928761971919,0.407080942069735,4.43405768361063));
#25719=CARTESIAN_POINT('Ctrl Pts',(14.5769709185042,0.55077200793829,4.29929703619113));
#25720=CARTESIAN_POINT('Ctrl Pts',(14.5610656398166,0.620899143473568,4.08609746938767));
#25721=CARTESIAN_POINT('Ctrl Pts',(14.545160361129,0.585262934872208,3.89235120454656));
#25722=CARTESIAN_POINT('Ctrl Pts',(14.5292550824414,0.549626726270847,3.69860493970543));
#25723=CARTESIAN_POINT('Ctrl Pts',(14.5133498037538,0.408227173532835,3.52431197682665));
#25724=CARTESIAN_POINT('Ctrl Pts',(14.4974445250662,0.225988969153725,3.44950027073699));
#25725=CARTESIAN_POINT('Ctrl Pts',(14.4815392463786,0.04375076477463,3.37468856464734));
#25726=CARTESIAN_POINT('Ctrl Pts',(14.465633967691,-0.179326091245555,3.39935811534679));
#25727=CARTESIAN_POINT('Ctrl Pts',(14.4497286890033,-0.340814144225853,
3.51218170883678));
#25728=CARTESIAN_POINT('Ctrl Pts',(14.4338234103157,-0.50230219720616,3.62500530232677));
#25729=CARTESIAN_POINT('Ctrl Pts',(14.4179181316281,-0.602201447146573,
3.82598293860731));
#25730=CARTESIAN_POINT('Ctrl Pts',(14.4020128529405,-0.594642384863179,
4.02283418976097));
#25731=CARTESIAN_POINT('Ctrl Pts',(14.3861075742529,-0.587083322579785,
4.21968544091462));
#25732=CARTESIAN_POINT('Ctrl Pts',(14.3702022955653,-0.47206594807259,4.4124103069414));
#25733=CARTESIAN_POINT('Ctrl Pts',(14.3542970168777,-0.302401373731467,
4.51251768287848));
#25734=CARTESIAN_POINT('Ctrl Pts',(14.3458131483376,-0.211902365642262,
4.565914912441));
#25735=CARTESIAN_POINT('Ctrl Pts',(14.3373292797976,-0.10585540495725,4.59296106912451));
#25736=CARTESIAN_POINT('Ctrl Pts',(14.3288454112576,0.000109044058801022,
4.5931342436645));
#25737=CARTESIAN_POINT('Ctrl Pts',(14.2211545887425,0.000537210645871958,
4.59424369460725));
#25738=CARTESIAN_POINT('Ctrl Pts',(14.2337379769984,-0.155889919212927,
4.59279139152499));
#25739=CARTESIAN_POINT('Ctrl Pts',(14.2463213652543,-0.313358837143528,
4.52935553548989));
#25740=CARTESIAN_POINT('Ctrl Pts',(14.2589047535102,-0.422984449084643,
4.4185751090669));
#25741=CARTESIAN_POINT('Ctrl Pts',(14.2748100321978,-0.561550141707708,
4.27854974232482));
#25742=CARTESIAN_POINT('Ctrl Pts',(14.2907153108854,-0.623677968224056,
4.06288332492072));
#25743=CARTESIAN_POINT('Ctrl Pts',(14.306620589573,-0.580841459108965,3.87060075163287));
#25744=CARTESIAN_POINT('Ctrl Pts',(14.3225258682606,-0.538004949993874,
3.67831817834502));
#25745=CARTESIAN_POINT('Ctrl Pts',(14.3384311469482,-0.390204105247342,
3.50941944917344));
#25746=CARTESIAN_POINT('Ctrl Pts',(14.3543364256359,-0.205302819838896,
3.44145571503774));
#25747=CARTESIAN_POINT('Ctrl Pts',(14.3702417043235,-0.0204015344304391,
3.37349198090203));
#25748=CARTESIAN_POINT('Ctrl Pts',(14.3861469830111,0.201600191639931,3.40646324180223));
#25749=CARTESIAN_POINT('Ctrl Pts',(14.4020522616987,0.358768557879186,3.52523048963197));
#25750=CARTESIAN_POINT('Ctrl Pts',(14.4179575403863,0.515936924118427,3.6439977374617));
#25751=CARTESIAN_POINT('Ctrl Pts',(14.4338628190739,0.608271930526566,3.84856097222098));
#25752=CARTESIAN_POINT('Ctrl Pts',(14.4497680977615,0.59337724853295,4.04499341086509));
#25753=CARTESIAN_POINT('Ctrl Pts',(14.4656733764491,0.578482566539332,4.2414258495092));
#25754=CARTESIAN_POINT('Ctrl Pts',(14.4815786551367,0.456358196143958,4.42972749203816));
#25755=CARTESIAN_POINT('Ctrl Pts',(14.4974839338244,0.283078481576349,4.52343819058819));
#25756=CARTESIAN_POINT('Ctrl Pts',(14.5053741521304,0.197118668938093,4.56992576768087));
#25757=CARTESIAN_POINT('Ctrl Pts',(14.5132643704364,0.0985699939877532,
4.59313537862966));
#25758=CARTESIAN_POINT('Ctrl Pts',(14.5211545887425,1.28950532977596E-5,
4.59311636453746));
#25759=CARTESIAN_POINT('Origin',(4.,0.,4.));
#25760=CARTESIAN_POINT('',(14.9288454112575,0.000149915246051877,4.59503491979621));
#25761=CARTESIAN_POINT('',(14.8211545887425,-0.000542004001680995,4.59419620878869));
#25762=CARTESIAN_POINT('',(4.,-7.27562663373442E-17,4.5941));
#25763=CARTESIAN_POINT('Ctrl Pts',(14.9288454112575,0.000149915246051877,
4.59503491979621));
#25764=CARTESIAN_POINT('Ctrl Pts',(14.9281926240489,0.00823674021970066,
4.59506221957623));
#25765=CARTESIAN_POINT('Ctrl Pts',(14.9275398368403,0.0163225255999611,
4.59491168338633));
#25766=CARTESIAN_POINT('Ctrl Pts',(14.9268870496317,0.0244008833477238,
4.59458015690877));
#25767=CARTESIAN_POINT('Ctrl Pts',(14.9109817709441,0.221231534471853,4.58650245417764));
#25768=CARTESIAN_POINT('Ctrl Pts',(14.8950764922565,0.413652681988333,4.47097768448731));
#25769=CARTESIAN_POINT('Ctrl Pts',(14.8791712135689,0.513312675625014,4.30104993462962));
#25770=CARTESIAN_POINT('Ctrl Pts',(14.8632659348813,0.612972669261697,4.13112218477192));
#25771=CARTESIAN_POINT('Ctrl Pts',(14.8473606561937,0.619871509018575,3.90679145474687));
#25772=CARTESIAN_POINT('Ctrl Pts',(14.831455377506,0.530841539545133,3.73106092513143));
#25773=CARTESIAN_POINT('Ctrl Pts',(14.8155500988184,0.441811570071688,3.55533039551599));
#25774=CARTESIAN_POINT('Ctrl Pts',(14.7996448201308,0.256852791367914,3.42820006631018));
#25775=CARTESIAN_POINT('Ctrl Pts',(14.7837395414432,0.0608904496539635,
3.40804280624462));
#25776=CARTESIAN_POINT('Ctrl Pts',(14.7678342627556,-0.135071892059981,
3.38788554617906));
#25777=CARTESIAN_POINT('Ctrl Pts',(14.751928984068,-0.342037796784102,3.47470135525375));
#25778=CARTESIAN_POINT('Ctrl Pts',(14.7360237053804,-0.464977277074429,
3.62862808681558));
#25779=CARTESIAN_POINT('Ctrl Pts',(14.7201184266927,-0.587916757364756,
3.78255481837741));
#25780=CARTESIAN_POINT('Ctrl Pts',(14.7042131480052,-0.62682981322129,4.00359247242638));
#25781=CARTESIAN_POINT('Ctrl Pts',(14.6883078693175,-0.56384921567034,4.19024990955517));
#25782=CARTESIAN_POINT('Ctrl Pts',(14.6724025906299,-0.500868618119389,
4.37690734668397));
#25783=CARTESIAN_POINT('Ctrl Pts',(14.6564973119423,-0.335994367160947,
4.52918456689258));
#25784=CARTESIAN_POINT('Ctrl Pts',(14.6405920332547,-0.144929743580805,
4.57716231297912));
#25785=CARTESIAN_POINT('Ctrl Pts',(14.636676492589,-0.097893704910838,4.5889734116427));
#25786=CARTESIAN_POINT('Ctrl Pts',(14.6327609519233,-0.0492704262804658,
4.59446355048005));
#25787=CARTESIAN_POINT('Ctrl Pts',(14.6288454112575,-0.000548182068839831,
4.59401855345973));
#25788=CARTESIAN_POINT('Ctrl Pts',(14.5211545887425,1.28950532977596E-5,
4.59311636453746));
#25789=CARTESIAN_POINT('Ctrl Pts',(14.5291696491241,-0.100103612291989,
4.59309704959697));
#25790=CARTESIAN_POINT('Ctrl Pts',(14.5371847095056,-0.200228812305367,
4.56910822985942));
#25791=CARTESIAN_POINT('Ctrl Pts',(14.5451997698872,-0.287175610734119,
4.52120162576233));
#25792=CARTESIAN_POINT('Ctrl Pts',(14.5611050485748,-0.459714929737158,
4.42613460781534));
#25793=CARTESIAN_POINT('Ctrl Pts',(14.5770103272624,-0.580358509003398,
4.23688081735026));
#25794=CARTESIAN_POINT('Ctrl Pts',(14.59291560595,-0.593711920942704,4.04033758828107));
#25795=CARTESIAN_POINT('Ctrl Pts',(14.6088208846377,-0.607065332882009,
3.84379435921188));
#25796=CARTESIAN_POINT('Ctrl Pts',(14.6247261633253,-0.513128577494387,
3.63996169153858));
#25797=CARTESIAN_POINT('Ctrl Pts',(14.6406314420129,-0.35503343871745,3.52243092280774));
#25798=CARTESIAN_POINT('Ctrl Pts',(14.6565367207005,-0.196938299940509,
3.40490015407689));
#25799=CARTESIAN_POINT('Ctrl Pts',(14.6724419993881,0.025315222225754,3.37367128428849));
#25800=CARTESIAN_POINT('Ctrl Pts',(14.6883472780757,0.209677713173688,3.44308328926485));
#25801=CARTESIAN_POINT('Ctrl Pts',(14.7042525567633,0.394040204121622,3.51249529424121));
#25802=CARTESIAN_POINT('Ctrl Pts',(14.720157835451,0.540511663851219,3.68254817398232));
#25803=CARTESIAN_POINT('Ctrl Pts',(14.7360631141386,0.581838594751101,3.87516084045512));
#25804=CARTESIAN_POINT('Ctrl Pts',(14.7519683928262,0.623165525650983,4.06777350692792));
#25805=CARTESIAN_POINT('Ctrl Pts',(14.7678736715138,0.559347927721136,4.2829459601324));
#25806=CARTESIAN_POINT('Ctrl Pts',(14.7837789502014,0.419688142031033,4.42188011275284));
#25807=CARTESIAN_POINT('Ctrl Pts',(14.7962374963817,0.310293146587505,4.53070672248707));
#25808=CARTESIAN_POINT('Ctrl Pts',(14.8086960425621,0.154364940471616,4.59275708529138));
#25809=CARTESIAN_POINT('Ctrl Pts',(14.8211545887425,-0.000542004001680995,
4.59419620878869));
#25810=CARTESIAN_POINT('Origin',(4.,0.,4.));
#25811=CARTESIAN_POINT('',(15.2288454112576,0.000471544078774977,4.59356550157774));
#25812=CARTESIAN_POINT('',(15.1211545887425,0.000250233060073018,4.59495282954609));
#25813=CARTESIAN_POINT('',(4.,-7.27562663373442E-17,4.5941));
#25814=CARTESIAN_POINT('Ctrl Pts',(15.2288454112576,0.000471544078774977,
4.59356550157774));
#25815=CARTESIAN_POINT('Ctrl Pts',(15.2236242961746,0.0655651715058866,
4.59404721416646));
#25816=CARTESIAN_POINT('Ctrl Pts',(15.2184031810917,0.130516835945995,4.58418155789741));
#25817=CARTESIAN_POINT('Ctrl Pts',(15.2131820660088,0.191734887706884,4.56334598510492));
#25818=CARTESIAN_POINT('Ctrl Pts',(15.1972767873211,0.378225734681762,4.49987379829874));
#25819=CARTESIAN_POINT('Ctrl Pts',(15.1813715086335,0.530068013118856,4.33459889729257));
#25820=CARTESIAN_POINT('Ctrl Pts',(15.1654662299459,0.577542172676889,4.143408524424));
#25821=CARTESIAN_POINT('Ctrl Pts',(15.1495609512583,0.625016332234921,3.95221815155542));
#25822=CARTESIAN_POINT('Ctrl Pts',(15.1336556725707,0.568122372913892,3.73511230682445));
#25823=CARTESIAN_POINT('Ctrl Pts',(15.1177503938831,0.432983593849097,3.59177680914072));
#25824=CARTESIAN_POINT('Ctrl Pts',(15.1018451151955,0.297844814784303,3.44844131145699));
#25825=CARTESIAN_POINT('Ctrl Pts',(15.0859398365078,0.0844612159757424,
3.37887616082051));
#25826=CARTESIAN_POINT('Ctrl Pts',(15.0700345578202,-0.109190481519281,
3.41502273134472));
#25827=CARTESIAN_POINT('Ctrl Pts',(15.0541292791326,-0.302842179014298,
3.45116930186893));
#25828=CARTESIAN_POINT('Ctrl Pts',(15.038224000445,-0.47676197519578,3.59302759355383));
#25829=CARTESIAN_POINT('Ctrl Pts',(15.0223187217574,-0.551093257596978,
3.77546228038711));
#25830=CARTESIAN_POINT('Ctrl Pts',(15.0064134430698,-0.625424539998176,
3.95789696722038));
#25831=CARTESIAN_POINT('Ctrl Pts',(14.9905081643822,-0.600167308619091,
4.18090804920204));
#25832=CARTESIAN_POINT('Ctrl Pts',(14.9746028856946,-0.486918615563658,
4.34209827230691));
#25833=CARTESIAN_POINT('Ctrl Pts',(14.9593503942156,-0.378317895025423,
4.49667289829699));
#25834=CARTESIAN_POINT('Ctrl Pts',(14.9440979027365,-0.188800216398263,
4.59439705548643));
#25835=CARTESIAN_POINT('Ctrl Pts',(14.9288454112575,0.000149915246051877,
4.59503491979621));
#25836=CARTESIAN_POINT('Ctrl Pts',(14.8211545887425,-0.000542004001680995,
4.59419620878869));
#25837=CARTESIAN_POINT('Ctrl Pts',(14.8246013212497,-0.0433979515083632,
4.5945943510493));
#25838=CARTESIAN_POINT('Ctrl Pts',(14.828048053757,-0.0861757330942537,
4.59035339483295));
#25839=CARTESIAN_POINT('Ctrl Pts',(14.8314947862642,-0.127868389248254,
4.58118038604969));
#25840=CARTESIAN_POINT('Ctrl Pts',(14.8474000649518,-0.320263161387096,
4.5388506546897));
#25841=CARTESIAN_POINT('Ctrl Pts',(14.8633053436395,-0.489550732214419,
4.39149533993331));
#25842=CARTESIAN_POINT('Ctrl Pts',(14.8792106223271,-0.558001411172811,
4.20677376822741));
#25843=CARTESIAN_POINT('Ctrl Pts',(14.8951159010147,-0.6264520901312,4.0220521965215));
#25844=CARTESIAN_POINT('Ctrl Pts',(14.9110211797023,-0.594065877220663,
3.79996436786608));
#25845=CARTESIAN_POINT('Ctrl Pts',(14.9269264583899,-0.475713151262041,
3.64248361741852));
#25846=CARTESIAN_POINT('Ctrl Pts',(14.9428317370775,-0.357360425303418,
3.48500286697096));
#25847=CARTESIAN_POINT('Ctrl Pts',(14.9587370157651,-0.153041186296697,
3.39212919473125));
#25848=CARTESIAN_POINT('Ctrl Pts',(14.9746422944528,0.0434298152403689,
3.40650626183085));
#25849=CARTESIAN_POINT('Ctrl Pts',(14.9905475731404,0.239900816777435,3.42088332893044));
#25850=CARTESIAN_POINT('Ctrl Pts',(15.006452851828,0.428523580844854,3.54251113536931));
#25851=CARTESIAN_POINT('Ctrl Pts',(15.0223581305156,0.522690514153935,3.71554333807889));
#25852=CARTESIAN_POINT('Ctrl Pts',(15.0382634092032,0.616857447463019,3.88857554078846));
#25853=CARTESIAN_POINT('Ctrl Pts',(15.0541686878908,0.616568550013756,4.11301213976874));
#25854=CARTESIAN_POINT('Ctrl Pts',(15.0700739665784,0.521956471292605,4.28580134389743));
#25855=CARTESIAN_POINT('Ctrl Pts',(15.085979245266,0.427344392571456,4.45859054802613));
#25856=CARTESIAN_POINT('Ctrl Pts',(15.1018845239536,0.238409132578427,4.57973235730324));
#25857=CARTESIAN_POINT('Ctrl Pts',(15.1177898026413,0.0419017695106382,
4.59360357799603));
#25858=CARTESIAN_POINT('Ctrl Pts',(15.1189113980083,0.0280446248267054,
4.59458173733358));
#25859=CARTESIAN_POINT('Ctrl Pts',(15.1200329933754,0.0141498265549413,
4.59502647517791));
#25860=CARTESIAN_POINT('Ctrl Pts',(15.1211545887425,0.000250233060073018,
4.59495282954609));
#25861=CARTESIAN_POINT('Origin',(4.,0.,4.));
#25862=CARTESIAN_POINT('',(15.5288454112575,-0.000350670266729247,4.59332700645389));
#25863=CARTESIAN_POINT('',(15.4211545887425,0.000414092275955974,4.59343115273787));
#25864=CARTESIAN_POINT('',(4.,-7.27562663373442E-17,4.5941));
#25865=CARTESIAN_POINT('Ctrl Pts',(15.5288454112575,-0.000350670266729247,
4.59332700645389));
#25866=CARTESIAN_POINT('Ctrl Pts',(15.5190559683003,0.121821298278883,4.59267222728074));
#25867=CARTESIAN_POINT('Ctrl Pts',(15.509266525343,0.244354036528086,4.55597946496206));
#25868=CARTESIAN_POINT('Ctrl Pts',(15.4994770823858,0.343380025451582,4.48601555964668));
#25869=CARTESIAN_POINT('Ctrl Pts',(15.4835718036982,0.504271299656008,4.37234255322809));
#25870=CARTESIAN_POINT('Ctrl Pts',(15.4676665250105,0.603110088323456,4.17084127710728));
#25871=CARTESIAN_POINT('Ctrl Pts',(15.4517612463229,0.594513801222153,3.97403259246294));
#25872=CARTESIAN_POINT('Ctrl Pts',(15.4358559676353,0.58591751412085,3.7772239078186));
#25873=CARTESIAN_POINT('Ctrl Pts',(15.4199506889477,0.469886151250777,3.58510781465072));
#25874=CARTESIAN_POINT('Ctrl Pts',(15.4040454102601,0.299696405559752,3.48589589518039));
#25875=CARTESIAN_POINT('Ctrl Pts',(15.3881401315725,0.129506659868722,3.38668397571006));
#25876=CARTESIAN_POINT('Ctrl Pts',(15.3722348528849,-0.0948414686432761,
3.38037622993726));
#25877=CARTESIAN_POINT('Ctrl Pts',(15.3563295741973,-0.270336810750117,
3.46986890786216));
#25878=CARTESIAN_POINT('Ctrl Pts',(15.3404242955096,-0.445832152856957,
3.55936158578705));
#25879=CARTESIAN_POINT('Ctrl Pts',(15.324519016822,-0.572474708558633,3.74465468740961));
#25880=CARTESIAN_POINT('Ctrl Pts',(15.3086137381344,-0.592115574081638,
3.94066945956945));
#25881=CARTESIAN_POINT('Ctrl Pts',(15.2927084594468,-0.611756439604643,
4.13668423172929));
#25882=CARTESIAN_POINT('Ctrl Pts',(15.2768031807592,-0.524395614948954,
4.3434206744264));
#25883=CARTESIAN_POINT('Ctrl Pts',(15.2608979020716,-0.370145494864779,
4.46595415947185));
#25884=CARTESIAN_POINT('Ctrl Pts',(15.2502137384669,-0.266529987624151,
4.54826443060822));
#25885=CARTESIAN_POINT('Ctrl Pts',(15.2395295748622,-0.13273198696893,4.59257975504152));
#25886=CARTESIAN_POINT('Ctrl Pts',(15.2288454112576,0.000471544078774977,
4.59356550157774));
#25887=CARTESIAN_POINT('Ctrl Pts',(15.1211545887425,0.000250233060073018,
4.59495282954609));
#25888=CARTESIAN_POINT('Ctrl Pts',(15.135938272063,-0.18295950063263,4.59398211075496));
#25889=CARTESIAN_POINT('Ctrl Pts',(15.1507219553836,-0.367002343096231,
4.50294888365168));
#25890=CARTESIAN_POINT('Ctrl Pts',(15.1655056387041,-0.476631971954554,
4.35629051265579));
#25891=CARTESIAN_POINT('Ctrl Pts',(15.1814109173917,-0.594578884209397,
4.19850559451431));
#25892=CARTESIAN_POINT('Ctrl Pts',(15.1973161960793,-0.626393242576541,
3.97633512612291));
#25893=CARTESIAN_POINT('Ctrl Pts',(15.2132214747669,-0.557467239648298,
3.79179038730953));
#25894=CARTESIAN_POINT('Ctrl Pts',(15.2291267534545,-0.488541236720055,
3.60724564849615));
#25895=CARTESIAN_POINT('Ctrl Pts',(15.2450320321422,-0.318874872496425,
3.46032663926078));
#25896=CARTESIAN_POINT('Ctrl Pts',(15.2609373108298,-0.126371763436977,
3.41849235301362));
#25897=CARTESIAN_POINT('Ctrl Pts',(15.2768425895174,0.0661313456224706,
3.37665806676646));
#25898=CARTESIAN_POINT('Ctrl Pts',(15.292747868205,0.281471199517752,3.4399085035075));
#25899=CARTESIAN_POINT('Ctrl Pts',(15.3086531468926,0.420772847618048,3.57920173859056));
#25900=CARTESIAN_POINT('Ctrl Pts',(15.3245584255802,0.560074495718348,3.71849497367363));
#25901=CARTESIAN_POINT('Ctrl Pts',(15.3404637042678,0.623337938023671,3.9338310070987));
#25902=CARTESIAN_POINT('Ctrl Pts',(15.3563689829554,0.581515278282945,4.12633664243329));
#25903=CARTESIAN_POINT('Ctrl Pts',(15.3722742616431,0.53969261854222,4.31884227776789));
#25904=CARTESIAN_POINT('Ctrl Pts',(15.3881795403307,0.392783856755445,4.48851751501199));
#25905=CARTESIAN_POINT('Ctrl Pts',(15.4040848190183,0.208243281137944,4.55745466359042));
#25906=CARTESIAN_POINT('Ctrl Pts',(15.4097747422597,0.142226097106806,4.58211610408423));
#25907=CARTESIAN_POINT('Ctrl Pts',(15.4154646655011,0.0713929250243718,
4.593885435962));
#25908=CARTESIAN_POINT('Ctrl Pts',(15.4211545887425,0.000414092275955974,
4.59343115273787));
#25909=CARTESIAN_POINT('Origin',(4.,0.,4.));
#25910=CARTESIAN_POINT('',(15.8288454112575,-0.000332254705457391,4.59484959654372));
#25911=CARTESIAN_POINT('',(15.7211545887425,-0.000419917270904514,4.59344262983929));
#25912=CARTESIAN_POINT('',(4.,-7.27562663373442E-17,4.5941));
#25913=CARTESIAN_POINT('Ctrl Pts',(15.8288454112575,-0.000332254705457391,
4.59484959654372));
#25914=CARTESIAN_POINT('Ctrl Pts',(15.814487640426,0.177680873019276,4.5936575613883));
#25915=CARTESIAN_POINT('Ctrl Pts',(15.8001298695944,0.356683508224643,4.50844978272675));
#25916=CARTESIAN_POINT('Ctrl Pts',(15.7857720987628,0.466927807092597,4.36891650689757));
#25917=CARTESIAN_POINT('Ctrl Pts',(15.7698668200752,0.589054446233417,4.21434406913608));
#25918=CARTESIAN_POINT('Ctrl Pts',(15.7539615413876,0.626802179063893,3.99310442736787));
#25919=CARTESIAN_POINT('Ctrl Pts',(15.7380562627,0.562838843643149,3.80678146521555));
#25920=CARTESIAN_POINT('Ctrl Pts',(15.7221509840123,0.498875508222402,3.62045850306322));
#25921=CARTESIAN_POINT('Ctrl Pts',(15.7062457053247,0.333201104550436,3.46905222052678));
#25922=CARTESIAN_POINT('Ctrl Pts',(15.6903404266371,0.141886309687413,3.42208197707538));
#25923=CARTESIAN_POINT('Ctrl Pts',(15.6744351479495,-0.0494284851756215,
3.37511173362399));
#25924=CARTESIAN_POINT('Ctrl Pts',(15.6585298692619,-0.266383671229707,
3.43257752925765));
#25925=CARTESIAN_POINT('Ctrl Pts',(15.6426245905743,-0.409362605655794,
3.5680935017987));
#25926=CARTESIAN_POINT('Ctrl Pts',(15.6267193118867,-0.552341540081869,
3.70360947433975));
#25927=CARTESIAN_POINT('Ctrl Pts',(15.6108140331991,-0.621344222879956,
3.9171756237882));
#25928=CARTESIAN_POINT('Ctrl Pts',(15.5949087545115,-0.584687541371933,
4.11073140955597));
#25929=CARTESIAN_POINT('Ctrl Pts',(15.5790034758238,-0.548030859863907,
4.30428719532377));
#25930=CARTESIAN_POINT('Ctrl Pts',(15.5630981971362,-0.405714814049763,
4.47783261741089));
#25931=CARTESIAN_POINT('Ctrl Pts',(15.5471929184486,-0.223084911271984,
4.55168296009627));
#25932=CARTESIAN_POINT('Ctrl Pts',(15.5410770827183,-0.152860773312716,
4.58007960584922));
#25933=CARTESIAN_POINT('Ctrl Pts',(15.5349612469879,-0.0766761255292402,
4.5937360717991));
#25934=CARTESIAN_POINT('Ctrl Pts',(15.5288454112575,-0.000350670266729247,
4.59332700645389));
#25935=CARTESIAN_POINT('Ctrl Pts',(15.4211545887425,0.000414092275955974,
4.59343115273787));
#25936=CARTESIAN_POINT('Ctrl Pts',(15.4313699441887,-0.12701715326484,4.59261555920332));
#25937=CARTESIAN_POINT('Ctrl Pts',(15.4415852996349,-0.254917899718674,
4.55240018390688));
#25938=CARTESIAN_POINT('Ctrl Pts',(15.4518006550811,-0.356261725310785,
4.47665348962993));
#25939=CARTESIAN_POINT('Ctrl Pts',(15.4677059337687,-0.514053766693778,
4.35871610717824));
#25940=CARTESIAN_POINT('Ctrl Pts',(15.4836112124564,-0.607465460011524,
4.15464228236211));
#25941=CARTESIAN_POINT('Ctrl Pts',(15.499516491144,-0.593606107615349,3.95813408188558));
#25942=CARTESIAN_POINT('Ctrl Pts',(15.5154217698316,-0.579746755219174,
3.76162588140906));
#25943=CARTESIAN_POINT('Ctrl Pts',(15.5313270485192,-0.458616357109098,
3.57268330527213));
#25944=CARTESIAN_POINT('Ctrl Pts',(15.5472323272068,-0.285832867492734,
3.47806079093568));
#25945=CARTESIAN_POINT('Ctrl Pts',(15.5631376058944,-0.113049377876356,
3.38343827659922));
#25946=CARTESIAN_POINT('Ctrl Pts',(15.579042884582,0.111387203246309,3.38313582406324));
#25947=CARTESIAN_POINT('Ctrl Pts',(15.5949481632696,0.284425092952457,3.47729230673655));
#25948=CARTESIAN_POINT('Ctrl Pts',(15.6108534419572,0.457462982658595,3.57144878940986));
#25949=CARTESIAN_POINT('Ctrl Pts',(15.6267587206449,0.579102180948212,3.76006420729246));
#25950=CARTESIAN_POINT('Ctrl Pts',(15.6426639993325,0.593491114096805,3.95653434015292));
#25951=CARTESIAN_POINT('Ctrl Pts',(15.6585692780201,0.607880047245398,4.15300447301339));
#25952=CARTESIAN_POINT('Ctrl Pts',(15.6744745567077,0.515018715252963,4.35732932085173));
#25953=CARTESIAN_POINT('Ctrl Pts',(15.6903798353953,0.357545113131455,4.47569155781202));
#25954=CARTESIAN_POINT('Ctrl Pts',(15.700638086511,0.255981111243369,4.55203033647815));
#25955=CARTESIAN_POINT('Ctrl Pts',(15.7108963376268,0.127540214881222,4.59261107697802));
#25956=CARTESIAN_POINT('Ctrl Pts',(15.7211545887425,-0.000419917270904514,
4.59344262983929));
#25957=CARTESIAN_POINT('Origin',(4.,0.,4.));
#25958=CARTESIAN_POINT('',(16.1288454112575,0.000520203518568921,4.59435747030618));
#25959=CARTESIAN_POINT('',(16.0211545887425,-0.00024144267326323,4.59496181546483));
#25960=CARTESIAN_POINT('',(4.,-7.27562663373442E-17,4.5941));
#25961=CARTESIAN_POINT('Ctrl Pts',(16.1288454112575,0.000520203518568921,
4.59435747030618));
#25962=CARTESIAN_POINT('Ctrl Pts',(16.1258245912393,0.0380542554257849,
4.59470210862833));
#25963=CARTESIAN_POINT('Ctrl Pts',(16.122803771221,0.0755288363057283,4.59145263304759));
#25964=CARTESIAN_POINT('Ctrl Pts',(16.1197829512027,0.112271568866026,4.58439375503351));
#25965=CARTESIAN_POINT('Ctrl Pts',(16.1038776725151,0.305730099191281,4.54722721702202));
#25966=CARTESIAN_POINT('Ctrl Pts',(16.0879723938275,0.478899942385972,4.40445440507416));
#25967=CARTESIAN_POINT('Ctrl Pts',(16.0720671151398,0.55226883266698,4.22163055421683));
#25968=CARTESIAN_POINT('Ctrl Pts',(16.0561618364522,0.625637722947984,4.03880670335952));
#25969=CARTESIAN_POINT('Ctrl Pts',(16.0402565577646,0.599205660315318,3.81593181359275));
#25970=CARTESIAN_POINT('Ctrl Pts',(16.024351279077,0.485109129681553,3.65534060523843));
#25971=CARTESIAN_POINT('Ctrl Pts',(16.0084460003894,0.371012599047788,3.4947493968841));
#25972=CARTESIAN_POINT('Ctrl Pts',(15.9925407217018,0.169251600412921,3.39644186994223));
#25973=CARTESIAN_POINT('Ctrl Pts',(15.9766354430142,-0.0275337514538456,
3.40555668173602));
#25974=CARTESIAN_POINT('Ctrl Pts',(15.9607301643265,-0.224319103320618,
3.41467149352982));
#25975=CARTESIAN_POINT('Ctrl Pts',(15.9448248856389,-0.416128808419276,
3.53120864405929));
#25976=CARTESIAN_POINT('Ctrl Pts',(15.9289196069513,-0.514891964967956,
3.70165920408156));
#25977=CARTESIAN_POINT('Ctrl Pts',(15.9130143282637,-0.613655121516638,
3.87210976410384));
#25978=CARTESIAN_POINT('Ctrl Pts',(15.8971090495761,-0.619371729515322,
4.09647373361892));
#25979=CARTESIAN_POINT('Ctrl Pts',(15.8812037708885,-0.52941696442075,4.27173266988224));
#25980=CARTESIAN_POINT('Ctrl Pts',(15.8652984922009,-0.439462199326184,
4.44699160614554));
#25981=CARTESIAN_POINT('Ctrl Pts',(15.8493932135132,-0.25383606113837,4.57314550915708));
#25982=CARTESIAN_POINT('Ctrl Pts',(15.8334879348256,-0.0577702193188812,
4.59226984378546));
#25983=CARTESIAN_POINT('Ctrl Pts',(15.8319404269696,-0.0386939468137543,
4.59413055045147));
#25984=CARTESIAN_POINT('Ctrl Pts',(15.8303929191136,-0.0195188482833839,
4.59497807636063));
#25985=CARTESIAN_POINT('Ctrl Pts',(15.8288454112575,-0.000332254705457391,
4.59484959654372));
#25986=CARTESIAN_POINT('Ctrl Pts',(15.7211545887425,-0.000419917270904514,
4.59344262983929));
#25987=CARTESIAN_POINT('Ctrl Pts',(15.7268016163144,-0.0708602278282204,
4.59390038836772));
#25988=CARTESIAN_POINT('Ctrl Pts',(15.7324486438863,-0.141154849878182,
4.58231274148771));
#25989=CARTESIAN_POINT('Ctrl Pts',(15.7380956714582,-0.206740066761224,
4.55801389847688));
#25990=CARTESIAN_POINT('Ctrl Pts',(15.7540009501458,-0.391465772281827,
4.48957437609924));
#25991=CARTESIAN_POINT('Ctrl Pts',(15.7699062288334,-0.538831311072463,
4.32029570526172));
#25992=CARTESIAN_POINT('Ctrl Pts',(15.785811507521,-0.58117266224226,4.12790349002296));
#25993=CARTESIAN_POINT('Ctrl Pts',(15.8017167862086,-0.62351401341206,3.93551127478418));
#25994=CARTESIAN_POINT('Ctrl Pts',(15.8176220648962,-0.560831176961022,
3.72000551514415));
#25995=CARTESIAN_POINT('Ctrl Pts',(15.8335273435838,-0.421905459495345,
3.58033733863277));
#25996=CARTESIAN_POINT('Ctrl Pts',(15.8494326222715,-0.282979742029676,
3.44066916212139));
#25997=CARTESIAN_POINT('Ctrl Pts',(15.8653379009591,-0.0678111435493865,
3.37683856873865));
#25998=CARTESIAN_POINT('Ctrl Pts',(15.8812431796467,0.124804018556085,3.41815386651619));
#25999=CARTESIAN_POINT('Ctrl Pts',(15.8971484583343,0.317419180661557,3.45946916429373));
#26000=CARTESIAN_POINT('Ctrl Pts',(15.9130537370219,0.487480906392202,3.60593035323155));
#26001=CARTESIAN_POINT('Ctrl Pts',(15.9289590157095,0.556904046010802,3.79028865163133));
#26002=CARTESIAN_POINT('Ctrl Pts',(15.9448642943971,0.6263271856294,3.9746469500311));
#26003=CARTESIAN_POINT('Ctrl Pts',(15.9607695730847,0.595111739135951,4.19690235789283));
#26004=CARTESIAN_POINT('Ctrl Pts',(15.9766748517723,0.477590518943614,4.35500459477727));
#26005=CARTESIAN_POINT('Ctrl Pts',(15.9915014307624,0.368039615220995,4.50238430120742));
#26006=CARTESIAN_POINT('Ctrl Pts',(16.0063280097524,0.18349252241573,4.59401752470064));
#26007=CARTESIAN_POINT('Ctrl Pts',(16.0211545887425,-0.00024144267326323,
4.59496181546483));
#26008=CARTESIAN_POINT('Origin',(4.,0.,4.));
#26009=CARTESIAN_POINT('',(16.4288454112575,7.48704377684928E-5,4.59312461313858));
#26010=CARTESIAN_POINT('',(16.3211545887425,0.000543344619121817,4.59417988242975));
#26011=CARTESIAN_POINT('',(4.,-7.27562663373442E-17,4.5941));
#26012=CARTESIAN_POINT('Ctrl Pts',(16.4288454112575,7.48704377684928E-5,
4.59312461313858));
#26013=CARTESIAN_POINT('Ctrl Pts',(16.4212562633649,0.0948679978941589,
4.5932308806522));
#26014=CARTESIAN_POINT('Ctrl Pts',(16.4136671154723,0.189615837117123,4.57184094704105));
#26015=CARTESIAN_POINT('Ctrl Pts',(16.4060779675797,0.273126642574496,4.52869916135151));
#26016=CARTESIAN_POINT('Ctrl Pts',(16.3901726888921,0.448147956300534,4.43828293357696));
#26017=CARTESIAN_POINT('Ctrl Pts',(16.3742674102045,0.573812330828296,4.25232504748949));
#26018=CARTESIAN_POINT('Ctrl Pts',(16.3583621315169,0.592420001795879,4.05620949715111));
#26019=CARTESIAN_POINT('Ctrl Pts',(16.3424568528292,0.611027672763462,3.86009394681272));
#26020=CARTESIAN_POINT('Ctrl Pts',(16.3265515741416,0.522578640170867,3.6538207322234));
#26021=CARTESIAN_POINT('Ctrl Pts',(16.310646295454,0.367684957814641,3.53210178682255));
#26022=CARTESIAN_POINT('Ctrl Pts',(16.2947410167664,0.212791275458425,3.4103828414217));
#26023=CARTESIAN_POINT('Ctrl Pts',(16.2788357380788,-0.00854705666138705,
3.3732181652093));
#26024=CARTESIAN_POINT('Ctrl Pts',(16.2629304593912,-0.19470084048803,3.43767220519428));
#26025=CARTESIAN_POINT('Ctrl Pts',(16.2470251807036,-0.380854624314662,
3.50212624517926));
#26026=CARTESIAN_POINT('Ctrl Pts',(16.231119902016,-0.531823859848111,3.66819900136163));
#26027=CARTESIAN_POINT('Ctrl Pts',(16.2152146233283,-0.578289861113055,
3.85963689006134));
#26028=CARTESIAN_POINT('Ctrl Pts',(16.1993093446407,-0.624755862378002,
4.05107477876107));
#26029=CARTESIAN_POINT('Ctrl Pts',(16.1834040659531,-0.566718629374431,
4.26787779997815));
#26030=CARTESIAN_POINT('Ctrl Pts',(16.1674987872655,-0.430826404144746,
4.41049917854914));
#26031=CARTESIAN_POINT('Ctrl Pts',(16.1546143285962,-0.320743594918802,
4.52603310245269));
#26032=CARTESIAN_POINT('Ctrl Pts',(16.1417298699269,-0.159570744489656,
4.592887512417));
#26033=CARTESIAN_POINT('Ctrl Pts',(16.1288454112575,0.000520203518568921,
4.59435747030618));
#26034=CARTESIAN_POINT('Ctrl Pts',(16.0211545887425,-0.00024144267326323,
4.59496181546483));
#26035=CARTESIAN_POINT('Ctrl Pts',(16.0222332884401,-0.0136089074611732,
4.59503051682625));
#26036=CARTESIAN_POINT('Ctrl Pts',(16.0233119881376,-0.0269720681925484,
4.59461918253551));
#26037=CARTESIAN_POINT('Ctrl Pts',(16.0243906878352,-0.0403017303441999,
4.59371435609144));
#26038=CARTESIAN_POINT('Ctrl Pts',(16.0402959665228,-0.236845765548457,
4.58037281461397));
#26039=CARTESIAN_POINT('Ctrl Pts',(16.0562012452104,-0.426106842065734,
4.45974066575184));
#26040=CARTESIAN_POINT('Ctrl Pts',(16.072106523898,-0.521184280535122,4.2872070887372));
#26041=CARTESIAN_POINT('Ctrl Pts',(16.0880118025856,-0.616261719004504,
4.11467351172257));
#26042=CARTESIAN_POINT('Ctrl Pts',(16.1039170812732,-0.61715551942601,3.89023850655542));
#26043=CARTESIAN_POINT('Ctrl Pts',(16.1198223599609,-0.523455286459661,
3.71695313254649));
#26044=CARTESIAN_POINT('Ctrl Pts',(16.1357276386485,-0.429755053493313,
3.54366775853756));
#26045=CARTESIAN_POINT('Ctrl Pts',(16.1516329173361,-0.241460787139106,
3.42153201568684));
#26046=CARTESIAN_POINT('Ctrl Pts',(16.1675381960237,-0.045029248433429,
3.40662546997421));
#26047=CARTESIAN_POINT('Ctrl Pts',(16.1834434747113,0.151402290272254,3.39171892426158));
#26048=CARTESIAN_POINT('Ctrl Pts',(16.1993487533989,0.355971101329402,3.48404157568705));
#26049=CARTESIAN_POINT('Ctrl Pts',(16.2152540320865,0.474747841293266,3.64120276856532));
#26050=CARTESIAN_POINT('Ctrl Pts',(16.2311593107741,0.593524581257127,3.79836396144359));
#26051=CARTESIAN_POINT('Ctrl Pts',(16.2470645894618,0.626509250127697,4.02036369577466));
#26052=CARTESIAN_POINT('Ctrl Pts',(16.2629698681494,0.558556683425868,4.20526908558792));
#26053=CARTESIAN_POINT('Ctrl Pts',(16.278875146837,0.490604116724039,4.39017447540119));
#26054=CARTESIAN_POINT('Ctrl Pts',(16.2947804255246,0.32171431444981,4.53798552069667));
#26055=CARTESIAN_POINT('Ctrl Pts',(16.3106857042122,0.129434328669215,4.58083364284428));
#26056=CARTESIAN_POINT('Ctrl Pts',(16.314175332389,0.0872479785030607,4.5902345478711));
#26057=CARTESIAN_POINT('Ctrl Pts',(16.3176649605657,0.0439357035691123,
4.5945828907904));
#26058=CARTESIAN_POINT('Ctrl Pts',(16.3211545887425,0.000543344619121817,
4.59417988242975));
#26059=CARTESIAN_POINT('Origin',(4.,0.,4.));
#26060=CARTESIAN_POINT('',(16.7288454112575,-0.000548108868865471,4.59408180714414));
#26061=CARTESIAN_POINT('',(16.6211545887425,-2.1752937549985E-5,4.5931168278739));
#26062=CARTESIAN_POINT('',(4.,-7.27562663373442E-17,4.5941));
#26063=CARTESIAN_POINT('Ctrl Pts',(16.7288454112575,-0.000548108868865471,
4.59408180714414));
#26064=CARTESIAN_POINT('Ctrl Pts',(16.7166879354906,0.15068989439403,4.59268722311157));
#26065=CARTESIAN_POINT('Ctrl Pts',(16.7045304597237,0.302891836883802,4.53390177381835));
#26066=CARTESIAN_POINT('Ctrl Pts',(16.6923729839567,0.411632901649024,4.42974331917764));
#26067=CARTESIAN_POINT('Ctrl Pts',(16.6764677052691,0.553895734249677,4.29347578465895));
#26068=CARTESIAN_POINT('Ctrl Pts',(16.6605624265815,0.621772048174623,4.07954898308531));
#26069=CARTESIAN_POINT('Ctrl Pts',(16.6446571478939,0.58409591167956,3.88618905124272));
#26070=CARTESIAN_POINT('Ctrl Pts',(16.6287518692063,0.546419775184499,3.69282911940014));
#26071=CARTESIAN_POINT('Ctrl Pts',(16.6128465905187,0.403191188269443,3.52003605728863));
#26072=CARTESIAN_POINT('Ctrl Pts',(16.596941311831,0.220174658543969,3.44714912875817));
#26073=CARTESIAN_POINT('Ctrl Pts',(16.5810360331434,0.0371581288184754,
3.37426220022769));
#26074=CARTESIAN_POINT('Ctrl Pts',(16.5651307544558,-0.185646343717467,
3.40128140527831));
#26075=CARTESIAN_POINT('Ctrl Pts',(16.5492254757682,-0.34593637135519,3.51580066803907));
#26076=CARTESIAN_POINT('Ctrl Pts',(16.5333201970806,-0.506226398992903,
3.63031993079982));
#26077=CARTESIAN_POINT('Ctrl Pts',(16.517414918393,-0.604001981732426,3.83233925127069));
#26078=CARTESIAN_POINT('Ctrl Pts',(16.5015096397054,-0.594368708523554,
4.02909990422408));
#26079=CARTESIAN_POINT('Ctrl Pts',(16.4856043610178,-0.584735435314682,
4.22586055717748));
#26080=CARTESIAN_POINT('Ctrl Pts',(16.4696990823301,-0.467693306157413,
4.4173625426134));
#26081=CARTESIAN_POINT('Ctrl Pts',(16.4537938036425,-0.296983115116624,
4.51567625060054));
#26082=CARTESIAN_POINT('Ctrl Pts',(16.4454776728475,-0.20772669247752,4.56707991793767));
#26083=CARTESIAN_POINT('Ctrl Pts',(16.4371615420525,-0.103798720846626,
4.59300816600183));
#26084=CARTESIAN_POINT('Ctrl Pts',(16.4288454112575,7.48704377684928E-5,
4.59312461313858));
#26085=CARTESIAN_POINT('Ctrl Pts',(16.3211545887425,0.000543344619121817,
4.59417988242975));
#26086=CARTESIAN_POINT('Ctrl Pts',(16.3335702392533,-0.153841115924154,
4.59274603025257));
#26087=CARTESIAN_POINT('Ctrl Pts',(16.3459858897642,-0.309239316255332,
4.53116741914846));
#26088=CARTESIAN_POINT('Ctrl Pts',(16.3584015402751,-0.418549561707542,
4.42300972860235));
#26089=CARTESIAN_POINT('Ctrl Pts',(16.3743068189627,-0.558583297016706,
4.28445249321304));
#26090=CARTESIAN_POINT('Ctrl Pts',(16.3902120976503,-0.622980598348072,
4.06945282343469));
#26091=CARTESIAN_POINT('Ctrl Pts',(16.4061173763379,-0.582172949355422,
3.87672947174358));
#26092=CARTESIAN_POINT('Ctrl Pts',(16.4220226550255,-0.541365300362771,
3.68400612005246));
#26093=CARTESIAN_POINT('Ctrl Pts',(16.4379279337131,-0.395352701046104,
3.5135590864486));
#26094=CARTESIAN_POINT('Ctrl Pts',(16.4538332124007,-0.211177959727979,
3.44365043774355));
#26095=CARTESIAN_POINT('Ctrl Pts',(16.4697384910883,-0.0270032184098532,
3.37374178903851));
#26096=CARTESIAN_POINT('Ctrl Pts',(16.485643769776,0.195333664909731,3.40437152523229));
#26097=CARTESIAN_POINT('Ctrl Pts',(16.5015490484636,0.353744999708243,3.52147576730199));
#26098=CARTESIAN_POINT('Ctrl Pts',(16.5174543271512,0.512156334506764,3.63858000937169));
#26099=CARTESIAN_POINT('Ctrl Pts',(16.5333596058388,0.606642120784206,3.84215875731731));
#26100=CARTESIAN_POINT('Ctrl Pts',(16.5492648845264,0.59381848284593,4.03873726278877));
#26101=CARTESIAN_POINT('Ctrl Pts',(16.565170163214,0.580994844907655,4.23531576826023));
#26102=CARTESIAN_POINT('Ctrl Pts',(16.5810754419016,0.460861782753675,4.42489403125753));
#26103=CARTESIAN_POINT('Ctrl Pts',(16.5969807205892,0.288579316114369,4.52042573380721));
#26104=CARTESIAN_POINT('Ctrl Pts',(16.6050386766403,0.201297315476928,4.56882414767653));
#26105=CARTESIAN_POINT('Ctrl Pts',(16.6130966326914,0.100630370301649,4.59308406930439));
#26106=CARTESIAN_POINT('Ctrl Pts',(16.6211545887425,-2.1752937549985E-5,
4.5931168278739));
#26107=CARTESIAN_POINT('Origin',(4.,0.,4.));
#26108=CARTESIAN_POINT('',(17.0288454112575,0.000186802344652959,4.59500977980842));
#26109=CARTESIAN_POINT('',(16.9211545887425,-0.000535257393875686,4.59425998651214));
#26110=CARTESIAN_POINT('',(4.,-7.27562663373442E-17,4.5941));
#26111=CARTESIAN_POINT('Ctrl Pts',(17.0288454112575,0.000186802344652959,
4.59500977980842));
#26112=CARTESIAN_POINT('Ctrl Pts',(17.0280248863039,0.0103527338555297,
4.59505157132578));
#26113=CARTESIAN_POINT('Ctrl Pts',(17.0272043613502,0.0205166685362397,
4.5948136789481));
#26114=CARTESIAN_POINT('Ctrl Pts',(17.0263838363966,0.0306658549750798,
4.59428997251885));
#26115=CARTESIAN_POINT('Ctrl Pts',(17.010478557709,0.227400443050786,4.58413830477164));
#26116=CARTESIAN_POINT('Ctrl Pts',(16.9945732790214,0.418593379366704,4.46659200952389));
#26117=CARTESIAN_POINT('Ctrl Pts',(16.9786680003338,0.516456956272638,4.29562337257973));
#26118=CARTESIAN_POINT('Ctrl Pts',(16.9627627216462,0.614320533178566,4.12465473563558));
#26119=CARTESIAN_POINT('Ctrl Pts',(16.9468574429585,0.618854750674521,3.90026375699502));
#26120=CARTESIAN_POINT('Ctrl Pts',(16.9309521642709,0.527977687913284,3.72548128085037));
#26121=CARTESIAN_POINT('Ctrl Pts',(16.9150468855833,0.437100625152047,3.55069880470573));
#26122=CARTESIAN_POINT('Ctrl Pts',(16.8991416068957,0.25081228213362,3.42552483105699));
#26123=CARTESIAN_POINT('Ctrl Pts',(16.8832363282081,0.054648384762208,3.40743395292956));
#26124=CARTESIAN_POINT('Ctrl Pts',(16.8673310495205,-0.141515512609204,
3.38934307480212));
#26125=CARTESIAN_POINT('Ctrl Pts',(16.8514257708328,-0.347554964333599,
3.47833529219599));
#26126=CARTESIAN_POINT('Ctrl Pts',(16.8355204921452,-0.468865370989487,
3.63354914383413));
#26127=CARTESIAN_POINT('Ctrl Pts',(16.8196152134576,-0.590175777645383,
3.78876299547228));
#26128=CARTESIAN_POINT('Ctrl Pts',(16.80370993477,-0.62675713923276,4.01019848135471));
#26129=CARTESIAN_POINT('Ctrl Pts',(16.7878046560824,-0.561812842140477,
4.19618179452704));
#26130=CARTESIAN_POINT('Ctrl Pts',(16.7718993773948,-0.496868545048197,
4.38216510769936));
#26131=CARTESIAN_POINT('Ctrl Pts',(16.7559940987072,-0.330398589276266,
4.53269624816158));
#26132=CARTESIAN_POINT('Ctrl Pts',(16.7400888200196,-0.138838935752124,
4.57865768466082));
#26133=CARTESIAN_POINT('Ctrl Pts',(16.7363410170989,-0.0937012275068688,
4.58948769960953));
#26134=CARTESIAN_POINT('Ctrl Pts',(16.7325932141782,-0.0471704703862807,
4.59451171761327));
#26135=CARTESIAN_POINT('Ctrl Pts',(16.7288454112575,-0.000548108868865471,
4.59408180714414));
#26136=CARTESIAN_POINT('Ctrl Pts',(16.6211545887425,-2.1752937549985E-5,
4.5931168278739));
#26137=CARTESIAN_POINT('Ctrl Pts',(16.629001911379,-0.0980428491191961,
4.59314873014073));
#26138=CARTESIAN_POINT('Ctrl Pts',(16.6368492340155,-0.196049888122182,
4.57020350190738));
#26139=CARTESIAN_POINT('Ctrl Pts',(16.6446965566521,-0.281666676968544,
4.52419924569128));
#26140=CARTESIAN_POINT('Ctrl Pts',(16.6606018353397,-0.455198332287519,
4.43095591292362));
#26141=CARTESIAN_POINT('Ctrl Pts',(16.6765071140273,-0.577829771800838,
4.24298410528626));
#26142=CARTESIAN_POINT('Ctrl Pts',(16.6924123927149,-0.593253826592341,
4.0465925244149));
#26143=CARTESIAN_POINT('Ctrl Pts',(16.7083176714025,-0.608677881383846,
3.85020094354353));
#26144=CARTESIAN_POINT('Ctrl Pts',(16.7242229500901,-0.516894551453523,
3.64538958943816));
#26145=CARTESIAN_POINT('Ctrl Pts',(16.7401282287778,-0.360046858872914,
3.52619917105016));
#26146=CARTESIAN_POINT('Ctrl Pts',(16.7560335074654,-0.203199166292313,
3.40700875266216));
#26147=CARTESIAN_POINT('Ctrl Pts',(16.771938786153,0.0187128889385656,3.37343926999153));
#26148=CARTESIAN_POINT('Ctrl Pts',(16.7878440648406,0.203796679382533,3.44090440927292));
#26149=CARTESIAN_POINT('Ctrl Pts',(16.8037493435282,0.388880469826499,3.50836954855431));
#26150=CARTESIAN_POINT('Ctrl Pts',(16.8196546222158,0.537135995483554,3.67686930978772));
#26151=CARTESIAN_POINT('Ctrl Pts',(16.8355599009034,0.58049059114602,3.86903573125179));
#26152=CARTESIAN_POINT('Ctrl Pts',(16.851465179591,0.623845186808487,4.06120215271587));
#26153=CARTESIAN_POINT('Ctrl Pts',(16.8673704582787,0.562298852476364,4.2770352344106));
#26154=CARTESIAN_POINT('Ctrl Pts',(16.8832757369663,0.424111061064287,4.41743355636644));
#26155=CARTESIAN_POINT('Ctrl Pts',(16.8959020208917,0.314411738992559,4.5288876912157));
#26156=CARTESIAN_POINT('Ctrl Pts',(16.9085283048171,0.156414067554279,4.59280392009262));
#26157=CARTESIAN_POINT('Ctrl Pts',(16.9211545887425,-0.000535257393875686,
4.59425998651214));
#26158=CARTESIAN_POINT('Origin',(4.,0.,4.));
#26159=CARTESIAN_POINT('',(17.3288454112575,0.000452601584348983,4.59351524744837));
#26160=CARTESIAN_POINT('',(17.2211545887425,0.000283723793354941,4.5949151055343));
#26161=CARTESIAN_POINT('',(4.,-7.27562663373442E-17,4.5941));
#26162=CARTESIAN_POINT('Ctrl Pts',(17.3288454112575,0.000452601584348983,
4.59351524744837));
#26163=CARTESIAN_POINT('Ctrl Pts',(17.3234565584296,0.0676518012035294,
4.59398979695312));
#26164=CARTESIAN_POINT('Ctrl Pts',(17.3180677056016,0.134706745978521,4.58346365752876));
#26165=CARTESIAN_POINT('Ctrl Pts',(17.3126788527736,0.197661386620268,4.56129398922237));
#26166=CARTESIAN_POINT('Ctrl Pts',(17.296773574086,0.383472937993069,4.49585988588324));
#26167=CARTESIAN_POINT('Ctrl Pts',(17.2808682953984,0.533564938357213,4.32899388620009));
#26168=CARTESIAN_POINT('Ctrl Pts',(17.2649630167108,0.579021491014364,4.13731379770915));
#26169=CARTESIAN_POINT('Ctrl Pts',(17.2490577380232,0.624478043671518,3.94563370921821));
#26170=CARTESIAN_POINT('Ctrl Pts',(17.2331524593355,0.565299148621668,3.72913953191949));
#26171=CARTESIAN_POINT('Ctrl Pts',(17.2172471806479,0.428657250819126,3.58723623291525));
#26172=CARTESIAN_POINT('Ctrl Pts',(17.2013419019603,0.292015353016592,3.44533293391101));
#26173=CARTESIAN_POINT('Ctrl Pts',(17.1854366232727,0.0779104524613767,
3.37802051320125));
#26174=CARTESIAN_POINT('Ctrl Pts',(17.1695313445851,-0.115349538542919,
3.41620598662221));
#26175=CARTESIAN_POINT('Ctrl Pts',(17.1536260658975,-0.308609529547215,
3.45439146004317));
#26176=CARTESIAN_POINT('Ctrl Pts',(17.1377207872099,-0.48102461100059,3.59807482759486));
#26177=CARTESIAN_POINT('Ctrl Pts',(17.1218155085223,-0.553429071780215,
3.78128276563952));
#26178=CARTESIAN_POINT('Ctrl Pts',(17.1059102298347,-0.625833532559839,
3.96449070368418));
#26179=CARTESIAN_POINT('Ctrl Pts',(17.090004951147,-0.598227372665711,4.18722321222181));
#26180=CARTESIAN_POINT('Ctrl Pts',(17.0740996724594,-0.483286172800906,
4.34721094636728));
#26181=CARTESIAN_POINT('Ctrl Pts',(17.0590149187255,-0.374274584390508,
4.4989451987145));
#26182=CARTESIAN_POINT('Ctrl Pts',(17.0439301649915,-0.186706445247169,
4.59424147319602));
#26183=CARTESIAN_POINT('Ctrl Pts',(17.0288454112575,0.000186802344652959,
4.59500977980842));
#26184=CARTESIAN_POINT('Ctrl Pts',(16.9211545887425,-0.000535257393875686,
4.59425998651214));
#26185=CARTESIAN_POINT('Ctrl Pts',(16.9244335835047,-0.0412943609811605,
4.59463812105998));
#26186=CARTESIAN_POINT('Ctrl Pts',(16.9277125782669,-0.0819827620002526,
4.59080381827239));
#26187=CARTESIAN_POINT('Ctrl Pts',(16.9309915730291,-0.121736182180322,
4.58249572362891));
#26188=CARTESIAN_POINT('Ctrl Pts',(16.9468968517167,-0.31456638552074,4.54219600671859));
#26189=CARTESIAN_POINT('Ctrl Pts',(16.9628021304043,-0.485397543709551,
4.39663301068103));
#26190=CARTESIAN_POINT('Ctrl Pts',(16.978707409092,-0.555791216176751,4.21264310503418));
#26191=CARTESIAN_POINT('Ctrl Pts',(16.9946126877796,-0.626184888643955,
4.02865319938731));
#26192=CARTESIAN_POINT('Ctrl Pts',(17.0105179664672,-0.596141075389537,
3.80623638413113));
#26193=CARTESIAN_POINT('Ctrl Pts',(17.0264232451548,-0.479454624411006,
3.64751705115182));
#26194=CARTESIAN_POINT('Ctrl Pts',(17.0423285238424,-0.362768173432475,
3.48879771817251));
#26195=CARTESIAN_POINT('Ctrl Pts',(17.05823380253,-0.159439084729831,3.39377586747005));
#26196=CARTESIAN_POINT('Ctrl Pts',(17.0741390812176,0.0371725263090214,
3.40608151284405));
#26197=CARTESIAN_POINT('Ctrl Pts',(17.0900443599052,0.233784137347885,3.41838715821804));
#26198=CARTESIAN_POINT('Ctrl Pts',(17.1059496385929,0.423678270722955,3.5380202996685));
#26199=CARTESIAN_POINT('Ctrl Pts',(17.1218549172805,0.519663574146654,3.71005045990219));
#26200=CARTESIAN_POINT('Ctrl Pts',(17.1377601959681,0.615648877570348,3.88208062013586));
#26201=CARTESIAN_POINT('Ctrl Pts',(17.1536654746557,0.617725351042682,4.10650779915277));
#26202=CARTESIAN_POINT('Ctrl Pts',(17.1695707533433,0.524939565793509,4.28028453107927));
#26203=CARTESIAN_POINT('Ctrl Pts',(17.1854760320309,0.432153780544336,4.45406126300578));
#26204=CARTESIAN_POINT('Ctrl Pts',(17.2013813107185,0.244505736573655,4.5771875478419));
#26205=CARTESIAN_POINT('Ctrl Pts',(17.2172865894061,0.0481554769387473,
4.59312900463441));
#26206=CARTESIAN_POINT('Ctrl Pts',(17.2185759225182,0.0322386925622284,
4.59442127046022));
#26207=CARTESIAN_POINT('Ctrl Pts',(17.2198652556304,0.0162647237884017,
4.5950091984451));
#26208=CARTESIAN_POINT('Ctrl Pts',(17.2211545887425,0.000283723793354941,
4.5949151055343));
#26209=CARTESIAN_POINT('Origin',(4.,0.,4.));
#26210=CARTESIAN_POINT('',(17.6288454112575,-0.000376811216598938,4.5933658344624));
#26211=CARTESIAN_POINT('',(17.5211545887425,0.000390292690419375,4.59338796628294));
#26212=CARTESIAN_POINT('',(4.,-7.27562663373442E-17,4.5941));
#26213=CARTESIAN_POINT('Ctrl Pts',(17.6288454112575,-0.000376811216598938,
4.5933658344624));
#26214=CARTESIAN_POINT('Ctrl Pts',(17.6188882305552,0.123868145157646,4.5926473455414));
#26215=CARTESIAN_POINT('Ctrl Pts',(17.608931049853,0.248515939035854,4.55458993700248));
#26216=CARTESIAN_POINT('Ctrl Pts',(17.5989738691507,0.348483110949462,4.48236965854082));
#26217=CARTESIAN_POINT('Ctrl Pts',(17.5830685904631,0.508167440925656,4.36700731952407));
#26218=CARTESIAN_POINT('Ctrl Pts',(17.5671633117754,0.604877102606476,4.16447556457896));
#26219=CARTESIAN_POINT('Ctrl Pts',(17.5512580330878,0.594207110796467,3.96776840716434));
#26220=CARTESIAN_POINT('Ctrl Pts',(17.5353527544002,0.583537118986457,3.77106124974973));
#26221=CARTESIAN_POINT('Ctrl Pts',(17.5194474757126,0.465487473685617,3.58017868986561));
#26222=CARTESIAN_POINT('Ctrl Pts',(17.503542197025,0.294261577747463,3.48276592343564));
#26223=CARTESIAN_POINT('Ctrl Pts',(17.4876369183374,0.123035681809298,3.38535315700567));
#26224=CARTESIAN_POINT('Ctrl Pts',(17.4717316396498,-0.101366464766187,
3.38141018402985));
#26225=CARTESIAN_POINT('Ctrl Pts',(17.4558263609621,-0.275908889943427,
3.47274745088526));
#26226=CARTESIAN_POINT('Ctrl Pts',(17.4399210822745,-0.450451315120656,
3.56408471774066));
#26227=CARTESIAN_POINT('Ctrl Pts',(17.4240158035869,-0.575134018899647,
3.75070222442727));
#26228=CARTESIAN_POINT('Ctrl Pts',(17.4081105248993,-0.592707978595278,
3.94691310701022));
#26229=CARTESIAN_POINT('Ctrl Pts',(17.3922052462117,-0.610281938290908,
4.14312398959316));
#26230=CARTESIAN_POINT('Ctrl Pts',(17.3762999675241,-0.520747153903178,
4.34892824807245));
#26231=CARTESIAN_POINT('Ctrl Pts',(17.3603946888365,-0.365214210518585,
4.46982927381454));
#26232=CARTESIAN_POINT('Ctrl Pts',(17.3498782629768,-0.262377240481122,
4.54976793433994));
#26233=CARTESIAN_POINT('Ctrl Pts',(17.3393618371172,-0.130687628661636,
4.59258915708319));
#26234=CARTESIAN_POINT('Ctrl Pts',(17.3288454112575,0.000452601584348983,
4.59351524744837));
#26235=CARTESIAN_POINT('Ctrl Pts',(17.2211545887425,0.000283723793354941,
4.5949151055343));
#26236=CARTESIAN_POINT('Ctrl Pts',(17.235770534318,-0.18087770297476,4.59384846352355));
#26237=CARTESIAN_POINT('Ctrl Pts',(17.2503864798935,-0.362942684182573,
4.50513801271133));
#26238=CARTESIAN_POINT('Ctrl Pts',(17.265002425469,-0.47285052735612,4.36129398677095));
#26239=CARTESIAN_POINT('Ctrl Pts',(17.2809077041566,-0.592453796716944,
4.20476088336606));
#26240=CARTESIAN_POINT('Ctrl Pts',(17.2968129828442,-0.626607860139456,
3.98293804780737));
#26241=CARTESIAN_POINT('Ctrl Pts',(17.3127182615318,-0.559630616639302,
3.79767714163318));
#26242=CARTESIAN_POINT('Ctrl Pts',(17.3286235402194,-0.492653373139145,
3.61241623545897));
#26243=CARTESIAN_POINT('Ctrl Pts',(17.3445288189071,-0.324544822716309,
3.46371725866926));
#26244=CARTESIAN_POINT('Ctrl Pts',(17.3604340975947,-0.132493299638714,
3.41985649047097));
#26245=CARTESIAN_POINT('Ctrl Pts',(17.3763393762823,0.0595582234388708,
3.37599572227269));
#26246=CARTESIAN_POINT('Ctrl Pts',(17.3922446549699,0.275552719171213,3.43697316266583));
#26247=CARTESIAN_POINT('Ctrl Pts',(17.4081499336575,0.416314653091553,3.5747905507646));
#26248=CARTESIAN_POINT('Ctrl Pts',(17.4240552123451,0.557076587011893,3.71260793886338));
#26249=CARTESIAN_POINT('Ctrl Pts',(17.4399604910327,0.622605959120231,3.92726527466781));
#26250=CARTESIAN_POINT('Ctrl Pts',(17.4558657697203,0.582814454063527,4.12020099097945));
#26251=CARTESIAN_POINT('Ctrl Pts',(17.4717710484079,0.543022949006823,4.31313670729109));
#26252=CARTESIAN_POINT('Ctrl Pts',(17.4876763270955,0.397910566785078,4.48435080410994));
#26253=CARTESIAN_POINT('Ctrl Pts',(17.5035816057832,0.214106774115907,4.55522901164789));
#26254=CARTESIAN_POINT('Ctrl Pts',(17.5094392667696,0.146414762764002,4.58133232736073));
#26255=CARTESIAN_POINT('Ctrl Pts',(17.515296927756,0.073474912906076,4.59382676872096));
#26256=CARTESIAN_POINT('Ctrl Pts',(17.5211545887425,0.000390292690419375,
4.59338796628294));
#26257=CARTESIAN_POINT('Origin',(4.,0.,4.));
#26258=CARTESIAN_POINT('',(17.9288454112575,-0.000301159635511528,4.59489313984584));
#26259=CARTESIAN_POINT('',(17.8211545887425,-0.000441626631060947,4.59348913571676));
#26260=CARTESIAN_POINT('',(4.,-7.27562663373442E-17,4.5941));
#26261=CARTESIAN_POINT('Ctrl Pts',(17.9288454112575,-0.000301159635511528,
4.59489313984584));
#26262=CARTESIAN_POINT('Ctrl Pts',(17.9143199026809,0.179756887528332,4.59377956832623));
#26263=CARTESIAN_POINT('Ctrl Pts',(17.8997943941043,0.360751589755073,4.50630604003092));
#26264=CARTESIAN_POINT('Ctrl Pts',(17.8852688855277,0.470789914960854,4.36397502945801));
#26265=CARTESIAN_POINT('Ctrl Pts',(17.8693636068401,0.591280720462369,4.20812407407766));
#26266=CARTESIAN_POINT('Ctrl Pts',(17.8534583281524,0.626694694978596,3.98649889312445));
#26267=CARTESIAN_POINT('Ctrl Pts',(17.8375530494648,0.560771239653389,3.80086039350393));
#26268=CARTESIAN_POINT('Ctrl Pts',(17.8216477707772,0.494847784328189,3.61522189388343));
#26269=CARTESIAN_POINT('Ctrl Pts',(17.8057424920896,0.327586899161578,3.46557007559562));
#26270=CARTESIAN_POINT('Ctrl Pts',(17.789837213402,0.135787706397568,3.42061872235194));
#26271=CARTESIAN_POINT('Ctrl Pts',(17.7739319347144,-0.0560114863664412,
3.37566736910827));
#26272=CARTESIAN_POINT('Ctrl Pts',(17.7580266560268,-0.272348986727849,
3.43541648090873));
#26273=CARTESIAN_POINT('Ctrl Pts',(17.7421213773392,-0.41389176700556,3.57243179339102));
#26274=CARTESIAN_POINT('Ctrl Pts',(17.7262160986515,-0.555434547283271,
3.7094471058733));
#26275=CARTESIAN_POINT('Ctrl Pts',(17.710310819964,-0.622182607477285,3.92372861903742));
#26276=CARTESIAN_POINT('Ctrl Pts',(17.6944055412763,-0.583488062224059,
4.11688732754162));
#26277=CARTESIAN_POINT('Ctrl Pts',(17.6785002625887,-0.544793516970831,
4.31004603604583));
#26278=CARTESIAN_POINT('Ctrl Pts',(17.6625949839011,-0.400656366270352,
4.48208193989012));
#26279=CARTESIAN_POINT('Ctrl Pts',(17.6466897052135,-0.217258291784321,
4.55400343026805));
#26280=CARTESIAN_POINT('Ctrl Pts',(17.6407416072282,-0.148672903323923,
4.58089991415997));
#26281=CARTESIAN_POINT('Ctrl Pts',(17.6347935092429,-0.0745967331795002,
4.59379503652584));
#26282=CARTESIAN_POINT('Ctrl Pts',(17.6288454112575,-0.000376811216598938,
4.5933658344624));
#26283=CARTESIAN_POINT('Ctrl Pts',(17.5211545887425,0.000390292690419375,
4.59338796628294));
#26284=CARTESIAN_POINT('Ctrl Pts',(17.5312022064437,-0.12497140465997,4.59263529057266));
#26285=CARTESIAN_POINT('Ctrl Pts',(17.5412498241448,-0.250759050797478,
4.55382993891589));
#26286=CARTESIAN_POINT('Ctrl Pts',(17.551297441846,-0.351218450958555,4.48038168762358));
#26287=CARTESIAN_POINT('Ctrl Pts',(17.5672027205336,-0.510244680247213,
4.36411383780432));
#26288=CARTESIAN_POINT('Ctrl Pts',(17.5831079992212,-0.605801935707933,
4.16103581990878));
#26289=CARTESIAN_POINT('Ctrl Pts',(17.5990132779088,-0.594014368327242,
3.96439246823218));
#26290=CARTESIAN_POINT('Ctrl Pts',(17.6149185565964,-0.58222680094655,3.76774911655557));
#26291=CARTESIAN_POINT('Ctrl Pts',(17.6308238352841,-0.463094410724447,
3.5775404310979));
#26292=CARTESIAN_POINT('Ctrl Pts',(17.6467291139717,-0.291317751175132,
3.48110219315546));
#26293=CARTESIAN_POINT('Ctrl Pts',(17.6626343926593,-0.119541091625818,
3.38466395521302));
#26294=CARTESIAN_POINT('Ctrl Pts',(17.6785396713469,0.104879837250709,3.38199616478582));
#26295=CARTESIAN_POINT('Ctrl Pts',(17.6944449500345,0.278900439380867,3.47432375837312));
#26296=CARTESIAN_POINT('Ctrl Pts',(17.7103502287221,0.452921041511034,3.56665135196042));
#26297=CARTESIAN_POINT('Ctrl Pts',(17.7262555074097,0.576541316894826,3.75397432956222));
#26298=CARTESIAN_POINT('Ctrl Pts',(17.7421607860974,0.593000065018554,3.95028190484542));
#26299=CARTESIAN_POINT('Ctrl Pts',(17.758066064785,0.60945881314228,4.1465894801286));
#26300=CARTESIAN_POINT('Ctrl Pts',(17.7739713434726,0.518756034005955,4.35188165309317));
#26301=CARTESIAN_POINT('Ctrl Pts',(17.7898766221602,0.362538606470845,4.47189694310939));
#26302=CARTESIAN_POINT('Ctrl Pts',(17.8003026110209,0.260137309937395,4.55056755941266));
#26303=CARTESIAN_POINT('Ctrl Pts',(17.8107285998817,0.129585238016204,4.59259583028147));
#26304=CARTESIAN_POINT('Ctrl Pts',(17.8211545887425,-0.000441626631060947,
4.59348913571676));
#26305=CARTESIAN_POINT('Origin',(4.,0.,4.));
#26306=CARTESIAN_POINT('',(18.2288454112575,0.000530626821107938,4.59429426521737));
#26307=CARTESIAN_POINT('',(18.1211545887425,-0.000206261771334874,4.59499421029555));
#26308=CARTESIAN_POINT('',(4.,-7.27562663373442E-17,4.5941));
#26309=CARTESIAN_POINT('Ctrl Pts',(18.2288454112575,0.000530626821107938,
4.59429426521737));
#26310=CARTESIAN_POINT('Ctrl Pts',(18.2256568534942,0.0401596894680921,
4.59466101186164));
#26311=CARTESIAN_POINT('Ctrl Pts',(18.2224682957309,0.0797220295111884,
4.5910372210354));
#26312=CARTESIAN_POINT('Ctrl Pts',(18.2192797379675,0.118424305077702,4.58317806034235));
#26313=CARTESIAN_POINT('Ctrl Pts',(18.2033744592799,0.311480390123117,4.54397471188459));
#26314=CARTESIAN_POINT('Ctrl Pts',(18.1874691805923,0.483135922039688,4.39938477867344));
#26315=CARTESIAN_POINT('Ctrl Pts',(18.1715639019047,0.554573942717995,4.21579784094385));
#26316=CARTESIAN_POINT('Ctrl Pts',(18.1556586232171,0.626011963396302,4.03221090321426));
#26317=CARTESIAN_POINT('Ctrl Pts',(18.1397533445295,0.597232472836345,3.80962696096622));
#26318=CARTESIAN_POINT('Ctrl Pts',(18.1238480658419,0.481449795543417,3.65024714373002));
#26319=CARTESIAN_POINT('Ctrl Pts',(18.1079427871543,0.365667118250483,3.49086732649381));
#26320=CARTESIAN_POINT('Ctrl Pts',(18.0920375084667,0.16288125422457,3.39469163426944));
#26321=CARTESIAN_POINT('Ctrl Pts',(18.076132229779,-0.0337971069360236,
3.40587987606835));
#26322=CARTESIAN_POINT('Ctrl Pts',(18.0602269510914,-0.230475468096606,
3.41706811786726));
#26323=CARTESIAN_POINT('Ctrl Pts',(18.0443216724038,-0.421046326391869,
3.53562029368944));
#26324=CARTESIAN_POINT('Ctrl Pts',(18.0284163937162,-0.518007606080761,
3.70710225992629));
#26325=CARTESIAN_POINT('Ctrl Pts',(18.0125111150286,-0.614968885769652,
3.87858422616314));
#26326=CARTESIAN_POINT('Ctrl Pts',(17.996605836341,-0.618320586852172,4.10299598281466));
#26327=CARTESIAN_POINT('Ctrl Pts',(17.9807005576534,-0.526523749990007,
4.27729714530494));
#26328=CARTESIAN_POINT('Ctrl Pts',(17.9647952789658,-0.434726913127837,
4.45159830779523));
#26329=CARTESIAN_POINT('Ctrl Pts',(17.9488900002781,-0.247781538320971,
4.57578887612429));
#26330=CARTESIAN_POINT('Ctrl Pts',(17.9329847215905,-0.0515250326741526,
4.59284579538505));
#26331=CARTESIAN_POINT('Ctrl Pts',(17.9316049514795,-0.0344999389365885,
4.59432546938787));
#26332=CARTESIAN_POINT('Ctrl Pts',(17.9302251813685,-0.0174047750035579,
4.59499891739512));
#26333=CARTESIAN_POINT('Ctrl Pts',(17.9288454112575,-0.000301159635511528,
4.59489313984584));
#26334=CARTESIAN_POINT('Ctrl Pts',(17.8211545887425,-0.000441626631060947,
4.59348913571676));
#26335=CARTESIAN_POINT('Ctrl Pts',(17.8266338785693,-0.0687761401428734,
4.59395860479535));
#26336=CARTESIAN_POINT('Ctrl Pts',(17.8321131683962,-0.136965594625977,
4.58306684864343));
#26337=CARTESIAN_POINT('Ctrl Pts',(17.837592458223,-0.200847632772524,4.56016175744822));
#26338=CARTESIAN_POINT('Ctrl Pts',(17.8534977369106,-0.386284368546891,
4.49367287470298));
#26339=CARTESIAN_POINT('Ctrl Pts',(17.8694030155983,-0.535425764161732,
4.32595670214462));
#26340=CARTESIAN_POINT('Ctrl Pts',(17.8853082942859,-0.579792400402821,
4.13402141072584));
#26341=CARTESIAN_POINT('Ctrl Pts',(17.9012135729735,-0.624159036643913,
3.94208611930704));
#26342=CARTESIAN_POINT('Ctrl Pts',(17.9171188516611,-0.563750913511241,
3.72593170902781));
#26343=CARTESIAN_POINT('Ctrl Pts',(17.9330241303487,-0.426304885490399,
3.58480714034942));
#26344=CARTESIAN_POINT('Ctrl Pts',(17.9489294090363,-0.288858857469565,
3.44368257167104));
#26345=CARTESIAN_POINT('Ctrl Pts',(17.9648346877239,-0.0743749245605683,
3.37758784459349));
#26346=CARTESIAN_POINT('Ctrl Pts',(17.9807399664116,0.118664965311668,3.41687086155347));
#26347=CARTESIAN_POINT('Ctrl Pts',(17.9966452450992,0.311704855183904,3.45615387851346));
#26348=CARTESIAN_POINT('Ctrl Pts',(18.0125505237868,0.483300702019379,3.60081463951098));
#26349=CARTESIAN_POINT('Ctrl Pts',(18.0284558024744,0.554662952572844,3.78443104318807));
#26350=CARTESIAN_POINT('Ctrl Pts',(18.044361081162,0.62602520312631,3.96804744686516));
#26351=CARTESIAN_POINT('Ctrl Pts',(18.0602663598496,0.597153857397765,4.19061949322182));
#26352=CARTESIAN_POINT('Ctrl Pts',(18.0761716385372,0.481305415899848,4.34995151481781));
#26353=CARTESIAN_POINT('Ctrl Pts',(18.0911659552723,0.372092100044007,4.50015792394613));
#26354=CARTESIAN_POINT('Ctrl Pts',(18.1061602720074,0.185579460002099,4.59416090236354));
#26355=CARTESIAN_POINT('Ctrl Pts',(18.1211545887425,-0.000206261771334874,
4.59499421029555));
#26356=CARTESIAN_POINT('Origin',(4.,0.,4.));
#26357=CARTESIAN_POINT('',(18.5288454112575,4.04073003155148E-5,4.59311858068669));
#26358=CARTESIAN_POINT('',(18.4211545887425,0.000547083855738422,4.59411609730493));
#26359=CARTESIAN_POINT('',(4.,-7.27562663373442E-17,4.5941));
#26360=CARTESIAN_POINT('Ctrl Pts',(18.5288454112575,4.04073003155148E-5,
4.59311858068669));
#26361=CARTESIAN_POINT('Ctrl Pts',(18.5210885256199,0.0969311390001333,
4.59317716754242));
#26362=CARTESIAN_POINT('Ctrl Pts',(18.5133316399822,0.193796352446061,4.57078374547556));
#26363=CARTESIAN_POINT('Ctrl Pts',(18.5055747543446,0.27868347559656,4.52579129559858));
#26364=CARTESIAN_POINT('Ctrl Pts',(18.489669475657,0.452742165355285,4.43353552600749));
#26365=CARTESIAN_POINT('Ctrl Pts',(18.4737641969693,0.576439736070726,4.24626358090446));
#26366=CARTESIAN_POINT('Ctrl Pts',(18.4578589182817,0.592979496483005,4.04996281465819));
#26367=CARTESIAN_POINT('Ctrl Pts',(18.4419536395941,0.609519256895283,3.85366204841193));
#26368=CARTESIAN_POINT('Ctrl Pts',(18.4260483609065,0.518901207004412,3.64833246102244));
#26369=CARTESIAN_POINT('Ctrl Pts',(18.4101430822189,0.362733321586741,3.52825271224048));
#26370=CARTESIAN_POINT('Ctrl Pts',(18.3942378035313,0.206565436169079,3.40817296345854));
#26371=CARTESIAN_POINT('Ctrl Pts',(18.3783325248437,-0.015152284775374,
3.37334305328413));
#26372=CARTESIAN_POINT('Ctrl Pts',(18.3624272461561,-0.200616443892158,
3.43975540293737));
#26373=CARTESIAN_POINT('Ctrl Pts',(18.3465219674685,-0.386080603008964,
3.50616775259061));
#26374=CARTESIAN_POINT('Ctrl Pts',(18.3306166887808,-0.535291200298091,
3.67382236207151));
#26375=CARTESIAN_POINT('Ctrl Pts',(18.3147114100932,-0.579737042064157,
3.86573932758804));
#26376=CARTESIAN_POINT('Ctrl Pts',(18.2988061314056,-0.624182883830224,
4.05765629310458));
#26377=CARTESIAN_POINT('Ctrl Pts',(18.282900852718,-0.563863970073232,4.27383561465674));
#26378=CARTESIAN_POINT('Ctrl Pts',(18.2669955740304,-0.426476194107598,
4.41501689358062));
#26379=CARTESIAN_POINT('Ctrl Pts',(18.2542788531061,-0.316630774880643,
4.52789532589669));
#26380=CARTESIAN_POINT('Ctrl Pts',(18.2415621321818,-0.157519428275204,
4.5928315930404));
#26381=CARTESIAN_POINT('Ctrl Pts',(18.2288454112575,0.000530626821107938,
4.59429426521737));
#26382=CARTESIAN_POINT('Ctrl Pts',(18.1211545887425,-0.000206261771334874,
4.59499421029555));
#26383=CARTESIAN_POINT('Ctrl Pts',(18.122065550695,-0.0114934532352288,
4.59504483693191));
#26384=CARTESIAN_POINT('Ctrl Pts',(18.1229765126475,-0.0227779616248223,
4.59475157188293));
#26385=CARTESIAN_POINT('Ctrl Pts',(18.1238874746001,-0.0340422900297544,
4.59410612569417));
#26386=CARTESIAN_POINT('Ctrl Pts',(18.1397927532877,-0.230716017194119,
4.58283671813918));
#26387=CARTESIAN_POINT('Ctrl Pts',(18.1556980319753,-0.421237934255556,
4.46420590619388));
#26388=CARTESIAN_POINT('Ctrl Pts',(18.1716033106629,-0.518128437217054,
4.29268393984778));
#26389=CARTESIAN_POINT('Ctrl Pts',(18.1875085893505,-0.615018940178556,
4.12116197350168));
#26390=CARTESIAN_POINT('Ctrl Pts',(18.2034138680381,-0.618278029040109,
3.89674885275477));
#26391=CARTESIAN_POINT('Ctrl Pts',(18.2193191467258,-0.526409268077163,
3.72248558851787));
#26392=CARTESIAN_POINT('Ctrl Pts',(18.2352244254134,-0.434540507114227,
3.54822232428098));
#26393=CARTESIAN_POINT('Ctrl Pts',(18.251129704101,-0.24754389632682,3.42410891655409));
#26394=CARTESIAN_POINT('Ctrl Pts',(18.2670349827886,-0.0512803682143169,
3.40713299136011));
#26395=CARTESIAN_POINT('Ctrl Pts',(18.2829402614762,0.144983159898198,3.39015706616613));
#26396=CARTESIAN_POINT('Ctrl Pts',(18.2988455401638,0.35051360533581,3.48031862350507));
#26397=CARTESIAN_POINT('Ctrl Pts',(18.3147508188514,0.470940082829639,3.63621929066782));
#26398=CARTESIAN_POINT('Ctrl Pts',(18.330656097539,0.591366560323475,3.79211995783059));
#26399=CARTESIAN_POINT('Ctrl Pts',(18.3465613762266,0.62668906987352,4.01375973481717));
#26400=CARTESIAN_POINT('Ctrl Pts',(18.3624666549143,0.560689009466533,4.199371012841));
#26401=CARTESIAN_POINT('Ctrl Pts',(18.3783719336019,0.49468894905955,4.38498229086483));
#26402=CARTESIAN_POINT('Ctrl Pts',(18.3942772122895,0.327366318695548,4.53456506992591));
#26403=CARTESIAN_POINT('Ctrl Pts',(18.4101824909771,0.135548591400956,4.57943726620491));
#26404=CARTESIAN_POINT('Ctrl Pts',(18.4138398568989,0.0914407431336166,
4.58975547846199));
#26405=CARTESIAN_POINT('Ctrl Pts',(18.4174972228207,0.0460377050408626,
4.59453706917327));
#26406=CARTESIAN_POINT('Ctrl Pts',(18.4211545887425,0.000547083855738422,
4.59411609730493));
#26407=CARTESIAN_POINT('Origin',(4.,0.,4.));
#26408=CARTESIAN_POINT('',(18.8288454112575,-0.000545657836941327,4.59414547262434));
#26409=CARTESIAN_POINT('',(18.7211545887425,-5.63168744233308E-5,4.59312091231189));
#26410=CARTESIAN_POINT('',(4.,-7.27562663373442E-17,4.5941));
#26411=CARTESIAN_POINT('Ctrl Pts',(18.8288454112575,-0.000545657836941327,
4.59414547262434));
#26412=CARTESIAN_POINT('Ctrl Pts',(18.8165201977456,0.15273698101805,4.59272393327212));
#26413=CARTESIAN_POINT('Ctrl Pts',(18.8041949842336,0.307016766534516,4.53213273669464));
#26414=CARTESIAN_POINT('Ctrl Pts',(18.7918697707216,0.416139138999065,4.42538122089617));
#26415=CARTESIAN_POINT('Ctrl Pts',(18.775964492034,0.556957936451544,4.28762193522949));
#26416=CARTESIAN_POINT('Ctrl Pts',(18.7600592133464,0.622575889387102,4.0729916608594));
#26417=CARTESIAN_POINT('Ctrl Pts',(18.7441539346588,0.582864009884755,3.88003953951897));
#26418=CARTESIAN_POINT('Ctrl Pts',(18.7282486559712,0.543152130382401,3.6870874181785));
#26419=CARTESIAN_POINT('Ctrl Pts',(18.7123433772835,0.3981104184421,3.51581344986768));
#26420=CARTESIAN_POINT('Ctrl Pts',(18.6964380985959,0.214335891977863,3.44485939483061));
#26421=CARTESIAN_POINT('Ctrl Pts',(18.6805328199083,0.0305613655136472,
3.37390533979354));
#26422=CARTESIAN_POINT('Ctrl Pts',(18.6646275412207,-0.191945975474496,
3.40327119803019));
#26423=CARTESIAN_POINT('Ctrl Pts',(18.6487222625331,-0.351020173514001,
3.51947340980541));
#26424=CARTESIAN_POINT('Ctrl Pts',(18.6328169838455,-0.510094371553506,
3.63567562158063));
#26425=CARTESIAN_POINT('Ctrl Pts',(18.6169117051579,-0.605735426644373,
3.83871418689441));
#26426=CARTESIAN_POINT('Ctrl Pts',(18.6010064264702,-0.594029012528289,
4.03536238640794));
#26427=CARTESIAN_POINT('Ctrl Pts',(18.5851011477826,-0.582322598412206,
4.23201058592146));
#26428=CARTESIAN_POINT('Ctrl Pts',(18.569195869095,-0.463268715089173,4.42226841963472));
#26429=CARTESIAN_POINT('Ctrl Pts',(18.5532905904074,-0.29153186902666,4.51877753945177));
#26430=CARTESIAN_POINT('Ctrl Pts',(18.5451421973574,-0.203549800283198,
4.56821988225003));
#26431=CARTESIAN_POINT('Ctrl Pts',(18.5369938043075,-0.101740616897797,
4.59305703682098));
#26432=CARTESIAN_POINT('Ctrl Pts',(18.5288454112575,4.04073003155148E-5,
4.59311858068669));
#26433=CARTESIAN_POINT('Ctrl Pts',(18.4211545887425,0.000547083855738422,
4.59411609730493));
#26434=CARTESIAN_POINT('Ctrl Pts',(18.4334025015083,-0.151793472668411,
4.59270633223614));
#26435=CARTESIAN_POINT('Ctrl Pts',(18.4456504142741,-0.305116246576315,
4.53295143150856));
#26436=CARTESIAN_POINT('Ctrl Pts',(18.4578983270399,-0.414068183831284,
4.42739736222451));
#26437=CARTESIAN_POINT('Ctrl Pts',(18.4738036057275,-0.555554407543751,
4.29032364846819));
#26438=CARTESIAN_POINT('Ctrl Pts',(18.4897088844152,-0.622214030743504,
4.07601460745865));
#26439=CARTESIAN_POINT('Ctrl Pts',(18.5056141631028,-0.583439774593308,
3.88287188415962));
#26440=CARTESIAN_POINT('Ctrl Pts',(18.5215194417904,-0.54466551844311,3.68972916086059));
#26441=CARTESIAN_POINT('Ctrl Pts',(18.537424720478,-0.400457382942952,3.51775275527208));
#26442=CARTESIAN_POINT('Ctrl Pts',(18.5533299991656,-0.217029642971419,
3.44590695711865));
#26443=CARTESIAN_POINT('Ctrl Pts',(18.5692352778532,-0.0336019029998957,
3.37406115896522));
#26444=CARTESIAN_POINT('Ctrl Pts',(18.5851405565408,0.189045441442997,3.40234596824686));
#26445=CARTESIAN_POINT('Ctrl Pts',(18.6010458352284,0.348682149221421,3.51777419717301));
#26446=CARTESIAN_POINT('Ctrl Pts',(18.6169511139161,0.508318856999844,3.63320242609916));
#26447=CARTESIAN_POINT('Ctrl Pts',(18.6328563926037,0.604944928113798,3.83577407466982));
#26448=CARTESIAN_POINT('Ctrl Pts',(18.6487616712913,0.594193758619731,4.03247681196108));
#26449=CARTESIAN_POINT('Ctrl Pts',(18.6646669499789,0.583442589125664,4.22917954925235));
#26450=CARTESIAN_POINT('Ctrl Pts',(18.6805722286665,0.465314179023576,4.42001337526422));
#26451=CARTESIAN_POINT('Ctrl Pts',(18.6964775073541,0.294048096631404,4.51735547060535));
#26452=CARTESIAN_POINT('Ctrl Pts',(18.7047032011502,0.205474838715737,4.56769764225005));
#26453=CARTESIAN_POINT('Ctrl Pts',(18.7129288949463,0.102689258835563,4.59303430424318));
#26454=CARTESIAN_POINT('Ctrl Pts',(18.7211545887425,-5.63168744233308E-5,
4.59312091231189));
#26455=CARTESIAN_POINT('Origin',(4.,0.,4.));
#26456=CARTESIAN_POINT('',(19.1288454112575,0.000222628893785728,4.59497983522242));
#26457=CARTESIAN_POINT('',(19.0211545887425,-0.000526118841417405,4.59432346427954));
#26458=CARTESIAN_POINT('',(4.,-7.27562663373442E-17,4.5941));
#26459=CARTESIAN_POINT('Ctrl Pts',(19.1288454112575,0.000222628893785728,
4.59497983522242));
#26460=CARTESIAN_POINT('Ctrl Pts',(19.1278571485589,0.012468395078646,4.59503853204781));
#26461=CARTESIAN_POINT('Ctrl Pts',(19.1268688858602,0.0247107891953784,
4.59469333777414));
#26462=CARTESIAN_POINT('Ctrl Pts',(19.1258806231615,0.0369274203756033,
4.59393377720877));
#26463=CARTESIAN_POINT('Ctrl Pts',(19.1099753444739,0.233544093050454,4.58170927203582));
#26464=CARTESIAN_POINT('Ctrl Pts',(19.0940700657862,0.423487581379576,4.46215450773496));
#26465=CARTESIAN_POINT('Ctrl Pts',(19.0781647870986,0.519543871337238,4.29016397409385));
#26466=CARTESIAN_POINT('Ctrl Pts',(19.062259508411,0.615600161294901,4.11817344045274));
#26467=CARTESIAN_POINT('Ctrl Pts',(19.0463542297234,0.617769252881104,3.89374713747137));
#26468=CARTESIAN_POINT('Ctrl Pts',(19.0304489510358,0.525055191022736,3.71993212880311));
#26469=CARTESIAN_POINT('Ctrl Pts',(19.0145436723482,0.432341129164367,3.54611712013485));
#26470=CARTESIAN_POINT('Ctrl Pts',(18.9986383936606,0.244743913861428,3.42291340577968));
#26471=CARTESIAN_POINT('Ctrl Pts',(18.982733114973,0.0484002497885746,3.40689091904056));
#26472=CARTESIAN_POINT('Ctrl Pts',(18.9668278362853,-0.147943414284278,
3.39086843230144));
#26473=CARTESIAN_POINT('Ctrl Pts',(18.9509225575977,-0.353033527127044,
3.48202717317836));
#26474=CARTESIAN_POINT('Ctrl Pts',(18.9350172789101,-0.472701385564812,
3.63851090447403));
#26475=CARTESIAN_POINT('Ctrl Pts',(18.9191120002225,-0.592369244002587,
3.79499463576972));
#26476=CARTESIAN_POINT('Ctrl Pts',(18.9032067215349,-0.626614848035354,
4.01680335748416));
#26477=CARTESIAN_POINT('Ctrl Pts',(18.8873014428473,-0.559714065105754,
4.20209188855652));
#26478=CARTESIAN_POINT('Ctrl Pts',(18.8713961641597,-0.492813282176159,
4.38738041962887));
#26479=CARTESIAN_POINT('Ctrl Pts',(18.8554908854721,-0.324766112284209,
4.53614876005914));
#26480=CARTESIAN_POINT('Ctrl Pts',(18.8395856067844,-0.132732706353525,
4.58008878179264));
#26481=CARTESIAN_POINT('Ctrl Pts',(18.8360055416088,-0.0895085590353085,
4.5899790920924));
#26482=CARTESIAN_POINT('Ctrl Pts',(18.8324254764332,-0.0450691735440342,
4.59455838259347));
#26483=CARTESIAN_POINT('Ctrl Pts',(18.8288454112575,-0.000545657836941327,
4.59414547262434));
#26484=CARTESIAN_POINT('Ctrl Pts',(18.7211545887425,-5.63168744233308E-5,
4.59312091231189));
#26485=CARTESIAN_POINT('Ctrl Pts',(18.728834173634,-0.0959805501911411,
4.59320177041728));
#26486=CARTESIAN_POINT('Ctrl Pts',(18.7365137585255,-0.191869914813978,
4.57127401300463));
#26487=CARTESIAN_POINT('Ctrl Pts',(18.744193343417,-0.276126457005151,4.5271386400555));
#26488=CARTESIAN_POINT('Ctrl Pts',(18.7600986221046,-0.450631173567243,
4.43572934949413));
#26489=CARTESIAN_POINT('Ctrl Pts',(18.7760039007922,-0.575236852009173,
4.249060403701));
#26490=CARTESIAN_POINT('Ctrl Pts',(18.7919091794798,-0.592729836422094,
4.05284228527226));
#26491=CARTESIAN_POINT('Ctrl Pts',(18.8078144581674,-0.610222820835014,
3.85662416684351));
#26492=CARTESIAN_POINT('Ctrl Pts',(18.823719736855,-0.520603111218926,3.65085687577915));
#26493=CARTESIAN_POINT('Ctrl Pts',(18.8396250155426,-0.365020286731977,
3.53002004684018));
#26494=CARTESIAN_POINT('Ctrl Pts',(18.8555302942302,-0.209437462245028,
3.40918321790122));
#26495=CARTESIAN_POINT('Ctrl Pts',(18.8714355729179,0.0121084771127808,
3.37327685108765));
#26496=CARTESIAN_POINT('Ctrl Pts',(18.8873408516055,0.197893008823487,3.43878763096633));
#26497=CARTESIAN_POINT('Ctrl Pts',(18.9032461302931,0.383677540534204,3.50429841084501));
#26498=CARTESIAN_POINT('Ctrl Pts',(18.9191514089807,0.533700664597814,3.67122633741595));
#26499=CARTESIAN_POINT('Ctrl Pts',(18.9350566876683,0.579078109400399,3.86292516893752));
#26500=CARTESIAN_POINT('Ctrl Pts',(18.9509619663559,0.624455554202981,4.05462400045908));
#26501=CARTESIAN_POINT('Ctrl Pts',(18.9668672450435,0.56518731974455,4.27109373693126));
#26502=CARTESIAN_POINT('Ctrl Pts',(18.9827725237311,0.428486871854059,4.41294063344238));
#26503=CARTESIAN_POINT('Ctrl Pts',(18.9955665454016,0.318526617336051,4.52704063153052));
#26504=CARTESIAN_POINT('Ctrl Pts',(19.008360567072,0.158464569423419,4.5928566151945));
#26505=CARTESIAN_POINT('Ctrl Pts',(19.0211545887425,-0.000526118841417405,
4.59432346427954));
#26506=CARTESIAN_POINT('Origin',(4.,0.,4.));
#26507=CARTESIAN_POINT('',(19.4288454112575,0.000431836873498515,4.59346738712276));
#26508=CARTESIAN_POINT('',(19.3211545887425,0.000315695961457875,4.59487351203822));
#26509=CARTESIAN_POINT('',(4.,-7.27562663373442E-17,4.5941));
#26510=CARTESIAN_POINT('Ctrl Pts',(19.4288454112575,0.000431836873498515,
4.59346738712276));
#26511=CARTESIAN_POINT('Ctrl Pts',(19.4232888206845,0.0697367837969298,
4.59393182999066));
#26512=CARTESIAN_POINT('Ctrl Pts',(19.4177322301115,0.13889623855249,4.58272225272434));
#26513=CARTESIAN_POINT('Ctrl Pts',(19.4121756395385,0.203565929825556,4.55917964700716));
#26514=CARTESIAN_POINT('Ctrl Pts',(19.3962703608509,0.38867754617092,4.49179089484985));
#26515=CARTESIAN_POINT('Ctrl Pts',(19.3803650821633,0.537002597765565,4.32335233206236));
#26516=CARTESIAN_POINT('Ctrl Pts',(19.3644598034757,0.580436494614329,4.13120381907284));
#26517=CARTESIAN_POINT('Ctrl Pts',(19.3485545247881,0.623870391463095,3.93905530608331));
#26518=CARTESIAN_POINT('Ctrl Pts',(19.3326492461004,0.562413133565966,3.72319684289176));
#26519=CARTESIAN_POINT('Ctrl Pts',(19.3167439674128,0.424283294458304,3.58274150440131));
#26520=CARTESIAN_POINT('Ctrl Pts',(19.3008386887252,0.286153455350651,3.44228616591086));
#26521=CARTESIAN_POINT('Ctrl Pts',(19.2849334100376,0.071351035032473,3.37723395212151));
#26522=CARTESIAN_POINT('Ctrl Pts',(19.26902813135,-0.12149578302492,3.4174540870367));
#26523=CARTESIAN_POINT('Ctrl Pts',(19.2531228526624,-0.314342601082313,
3.45767422195189));
#26524=CARTESIAN_POINT('Ctrl Pts',(19.2372175739748,-0.485233816878921,
3.60316670557164));
#26525=CARTESIAN_POINT('Ctrl Pts',(19.2213122952871,-0.555703413721375,
3.78712754492824));
#26526=CARTESIAN_POINT('Ctrl Pts',(19.2054070165995,-0.626173010563829,
3.97108838428485));
#26527=CARTESIAN_POINT('Ctrl Pts',(19.1895017379119,-0.59622098845213,4.19351757937831));
#26528=CARTESIAN_POINT('Ctrl Pts',(19.1735964592243,-0.479600048885993,
4.35228505390253));
#26529=CARTESIAN_POINT('Ctrl Pts',(19.1586794432354,-0.370225264934164,
4.50118762911129));
#26530=CARTESIAN_POINT('Ctrl Pts',(19.1437624272465,-0.184617181632464,
4.59409385471947));
#26531=CARTESIAN_POINT('Ctrl Pts',(19.1288454112575,0.000222628893785728,
4.59497983522242));
#26532=CARTESIAN_POINT('Ctrl Pts',(19.0211545887425,-0.000526118841417405,
4.59432346427954));
#26533=CARTESIAN_POINT('Ctrl Pts',(19.0242658457596,-0.0391895592568775,
4.59468017342281));
#26534=CARTESIAN_POINT('Ctrl Pts',(19.0273771027768,-0.0777896429211806,
4.59123148246997));
#26535=CARTESIAN_POINT('Ctrl Pts',(19.030488359794,-0.115590453236054,4.58374636034569));
#26536=CARTESIAN_POINT('Ctrl Pts',(19.0463936384816,-0.308834669113126,
4.5454811341878));
#26537=CARTESIAN_POINT('Ctrl Pts',(19.0622989171692,-0.481190439544719,
4.40172662532195));
#26538=CARTESIAN_POINT('Ctrl Pts',(19.0782041958568,-0.553519286527586,
4.21848882245705));
#26539=CARTESIAN_POINT('Ctrl Pts',(19.0941094745444,-0.625848133510457,
4.03525101959215));
#26540=CARTESIAN_POINT('Ctrl Pts',(19.1100147532321,-0.598150057044591,
3.81252992272818));
#26541=CARTESIAN_POINT('Ctrl Pts',(19.1259200319197,-0.483142842019737,
3.65258963701249));
#26542=CARTESIAN_POINT('Ctrl Pts',(19.1418253106073,-0.36813562699489,3.49264935129682));
#26543=CARTESIAN_POINT('Ctrl Pts',(19.1577305892949,-0.165819273411065,
3.39548987672941));
#26544=CARTESIAN_POINT('Ctrl Pts',(19.1736358679825,0.0309111084379188,
3.40572273351557));
#26545=CARTESIAN_POINT('Ctrl Pts',(19.1895411466701,0.227641490286902,3.41595559030173));
#26546=CARTESIAN_POINT('Ctrl Pts',(19.2054464253577,0.418785900401045,3.53358077844144));
#26547=CARTESIAN_POINT('Ctrl Pts',(19.2213517040453,0.516578912360374,3.70458978792342));
#26548=CARTESIAN_POINT('Ctrl Pts',(19.237256982733,0.614371924319703,3.87559879740541));
#26549=CARTESIAN_POINT('Ctrl Pts',(19.2531622614206,0.618813538124218,4.09999162822965));
#26550=CARTESIAN_POINT('Ctrl Pts',(19.2690675401082,0.527864352527146,4.27473658562515));
#26551=CARTESIAN_POINT('Ctrl Pts',(19.2849728187958,0.436915166930073,4.44948154302064));
#26552=CARTESIAN_POINT('Ctrl Pts',(19.3008780974834,0.250575181931413,4.5745786269874));
#26553=CARTESIAN_POINT('Ctrl Pts',(19.316783376171,0.0544038354309166,4.59258854924263));
#26554=CARTESIAN_POINT('Ctrl Pts',(19.3182404470282,0.0364327229714708,
4.59423842494573));
#26555=CARTESIAN_POINT('Ctrl Pts',(19.3196975178853,0.0183791031991185,
4.59498959766064));
#26556=CARTESIAN_POINT('Ctrl Pts',(19.3211545887425,0.000315695961457875,
4.59487351203822));
#26557=CARTESIAN_POINT('Origin',(4.,0.,4.));
#26558=CARTESIAN_POINT('',(19.7288454112575,-0.000401422265437046,4.59340756962635));
#26559=CARTESIAN_POINT('',(19.6211545887425,0.000364945106097663,4.59334757974602));
#26560=CARTESIAN_POINT('',(4.,-7.27562663373442E-17,4.5941));
#26561=CARTESIAN_POINT('Ctrl Pts',(19.7288454112575,-0.000401422265437046,
4.59340756962635));
#26562=CARTESIAN_POINT('Ctrl Pts',(19.7187204928102,0.125914276337785,4.59262579220321));
#26563=CARTESIAN_POINT('Ctrl Pts',(19.7085955743629,0.252675872983383,4.55317429478549));
#26564=CARTESIAN_POINT('Ctrl Pts',(19.6984706559155,0.353547469597214,4.47867015725961));
#26565=CARTESIAN_POINT('Ctrl Pts',(19.6825653772279,0.512007102052776,4.36163128164859));
#26566=CARTESIAN_POINT('Ctrl Pts',(19.6666600985403,0.606576931433326,4.15809158444534));
#26567=CARTESIAN_POINT('Ctrl Pts',(19.6507548198527,0.593834428727047,3.9615078130365));
#26568=CARTESIAN_POINT('Ctrl Pts',(19.6348495411651,0.581091926020768,3.76492404162769));
#26569=CARTESIAN_POINT('Ctrl Pts',(19.6189442624775,0.46103709122769,3.57529619601327));
#26570=CARTESIAN_POINT('Ctrl Pts',(19.6030389837899,0.288794059426421,3.47969339775167));
#26571=CARTESIAN_POINT('Ctrl Pts',(19.5871337051022,0.116551027625133,3.38409059949006));
#26572=CARTESIAN_POINT('Ctrl Pts',(19.5712284264146,-0.107880201184358,
3.38251284858128));
#26573=CARTESIAN_POINT('Ctrl Pts',(19.555323147727,-0.281450319664219,3.47568456171554));
#26574=CARTESIAN_POINT('Ctrl Pts',(19.5394178690394,-0.45502043814407,3.5688562748498));
#26575=CARTESIAN_POINT('Ctrl Pts',(19.5235125903518,-0.577729446294298,
3.75677745202708));
#26576=CARTESIAN_POINT('Ctrl Pts',(19.5076073116642,-0.593234549413986,
3.95316264945144));
#26577=CARTESIAN_POINT('Ctrl Pts',(19.4917020329766,-0.608739652533674,
4.1495478468758));
#26578=CARTESIAN_POINT('Ctrl Pts',(19.475796754289,-0.517040850622822,4.35439706454724));
#26579=CARTESIAN_POINT('Ctrl Pts',(19.4598914756013,-0.360242359119356,
4.47365220261941));
#26580=CARTESIAN_POINT('Ctrl Pts',(19.4495427874867,-0.258222223711561,
4.55124494740629));
#26581=CARTESIAN_POINT('Ctrl Pts',(19.4391940993721,-0.128642866595325,
4.59260240088276));
#26582=CARTESIAN_POINT('Ctrl Pts',(19.4288454112575,0.000431836873498515,
4.59346738712276));
#26583=CARTESIAN_POINT('Ctrl Pts',(19.3211545887425,0.000315695961457875,
4.59487351203822));
#26584=CARTESIAN_POINT('Ctrl Pts',(19.3356027965729,-0.178799726336078,
4.59372241551416));
#26585=CARTESIAN_POINT('Ctrl Pts',(19.3500510044034,-0.35887750705714,4.50729762043595));
#26586=CARTESIAN_POINT('Ctrl Pts',(19.3644992122339,-0.469016560662847,
4.36625733020606));
#26587=CARTESIAN_POINT('Ctrl Pts',(19.3804044909215,-0.590262902253753,
4.21099342837053));
#26588=CARTESIAN_POINT('Ctrl Pts',(19.3963097696091,-0.626752877433238,
3.98954286415574));
#26589=CARTESIAN_POINT('Ctrl Pts',(19.4122150482967,-0.561731832709929,
3.80358636875254));
#26590=CARTESIAN_POINT('Ctrl Pts',(19.4281203269843,-0.49671078798662,3.61762987334934));
#26591=CARTESIAN_POINT('Ctrl Pts',(19.4440256056719,-0.330178723360516,
3.46716744675772));
#26592=CARTESIAN_POINT('Ctrl Pts',(19.4599308843595,-0.138600118749324,
3.42128506802099));
#26593=CARTESIAN_POINT('Ctrl Pts',(19.4758361630471,0.0529784858618673,
3.37540268928427));
#26594=CARTESIAN_POINT('Ctrl Pts',(19.4917414417347,0.269603630458146,3.43410035840244));
#26595=CARTESIAN_POINT('Ctrl Pts',(19.5076467204224,0.411810215621333,3.57042659223364));
#26596=CARTESIAN_POINT('Ctrl Pts',(19.52355199911,0.554016800784528,3.70675282606484));
#26597=CARTESIAN_POINT('Ctrl Pts',(19.5394572777976,0.621804826514621,3.92070762460909));
#26598=CARTESIAN_POINT('Ctrl Pts',(19.5553625564852,0.584048894878601,4.11405198996909));
#26599=CARTESIAN_POINT('Ctrl Pts',(19.5712678351728,0.546292963242583,4.30739635532907));
#26600=CARTESIAN_POINT('Ctrl Pts',(19.5871731138604,0.402993074240464,4.4801302875048));
#26601=CARTESIAN_POINT('Ctrl Pts',(19.6030783925481,0.219946482677819,4.55294168410437));
#26602=CARTESIAN_POINT('Ctrl Pts',(19.6091037912795,0.150602919307179,4.5805248346624));
#26603=CARTESIAN_POINT('Ctrl Pts',(19.615129190011,0.0755552166468998,4.59376787586841));
#26604=CARTESIAN_POINT('Ctrl Pts',(19.6211545887425,0.000364945106097663,
4.59334757974602));
#26605=CARTESIAN_POINT('Origin',(4.,0.,4.));
#26606=CARTESIAN_POINT('',(20.0288454112575,-0.000266600559035268,4.5949350414008));
#26607=CARTESIAN_POINT('',(19.9211545887425,-0.000461335262921832,4.59353843444423));
#26608=CARTESIAN_POINT('',(4.,-7.27562663373442E-17,4.5941));
#26609=CARTESIAN_POINT('Ctrl Pts',(20.0288454112575,-0.000266600559035268,
4.5949350414008));
#26610=CARTESIAN_POINT('Ctrl Pts',(20.0141521649359,0.181839152323842,4.59391190659116));
#26611=CARTESIAN_POINT('Ctrl Pts',(19.9994589186142,0.364814066967773,4.50413264800542));
#26612=CARTESIAN_POINT('Ctrl Pts',(19.9847656722925,0.474598868642052,4.35899217880197));
#26613=CARTESIAN_POINT('Ctrl Pts',(19.9688603936049,0.593439717564554,4.20187920587587));
#26614=CARTESIAN_POINT('Ctrl Pts',(19.9529551149173,0.626517665065843,3.97989492921597));
#26615=CARTESIAN_POINT('Ctrl Pts',(19.9370498362297,0.558641803885684,3.79496194153783));
#26616=CARTESIAN_POINT('Ctrl Pts',(19.9211445575421,0.490765942705524,3.61002895385969));
#26617=CARTESIAN_POINT('Ctrl Pts',(19.9052392788545,0.321936272843916,3.46214725516331));
#26618=CARTESIAN_POINT('Ctrl Pts',(19.8893340001669,0.129673778938228,3.41921955761011));
#26619=CARTESIAN_POINT('Ctrl Pts',(19.8734287214793,-0.0625887149674591,
3.37629186005692));
#26620=CARTESIAN_POINT('Ctrl Pts',(19.8575234427916,-0.278284032917226,
3.43831816364691));
#26621=CARTESIAN_POINT('Ctrl Pts',(19.841618164104,-0.418374827314372,3.57681771754473));
#26622=CARTESIAN_POINT('Ctrl Pts',(19.8257128854164,-0.558465621711518,
3.71531727144255));
#26623=CARTESIAN_POINT('Ctrl Pts',(19.8098076067288,-0.622951892556044,
3.9302900756482));
#26624=CARTESIAN_POINT('Ctrl Pts',(19.7939023280412,-0.58222383973146,4.12303018792675));
#26625=CARTESIAN_POINT('Ctrl Pts',(19.7779970493536,-0.541495786906873,
4.3157703002053));
#26626=CARTESIAN_POINT('Ctrl Pts',(19.762091770666,-0.395553410413165,4.48627772055676));
#26627=CARTESIAN_POINT('Ctrl Pts',(19.7461864919784,-0.211407504401025,
4.55626240372308));
#26628=CARTESIAN_POINT('Ctrl Pts',(19.7404061317381,-0.144484459893097,
4.58169651826758));
#26629=CARTESIAN_POINT('Ctrl Pts',(19.7346257714978,-0.0725156072563085,
4.59385388977766));
#26630=CARTESIAN_POINT('Ctrl Pts',(19.7288454112575,-0.000401422265437046,
4.59340756962635));
#26631=CARTESIAN_POINT('Ctrl Pts',(19.6211545887425,0.000364945106097663,
4.59334757974602));
#26632=CARTESIAN_POINT('Ctrl Pts',(19.6310344686986,-0.122924963130536,
4.59265841784648));
#26633=CARTESIAN_POINT('Ctrl Pts',(19.6409143486547,-0.246598186964828,
4.55523353708024));
#26634=CARTESIAN_POINT('Ctrl Pts',(19.6507942286109,-0.346136160298313,
4.48405653351353));
#26635=CARTESIAN_POINT('Ctrl Pts',(19.6666995072985,-0.506378917588675,
4.36947112529969));
#26636=CARTESIAN_POINT('Ctrl Pts',(19.6826047859861,-0.60407113804621,4.16741144784858));
#26637=CARTESIAN_POINT('Ctrl Pts',(19.6985100646737,-0.5943566574826,3.97065479758251));
#26638=CARTESIAN_POINT('Ctrl Pts',(19.7144153433613,-0.584642176918989,
3.77389814731645));
#26639=CARTESIAN_POINT('Ctrl Pts',(19.7303206220489,-0.467520995334232,
3.58244452423543));
#26640=CARTESIAN_POINT('Ctrl Pts',(19.7462259007365,-0.296770260159971,
3.48420125495101));
#26641=CARTESIAN_POINT('Ctrl Pts',(19.7621311794242,-0.12601952498572,3.38595798566659));
#26642=CARTESIAN_POINT('Ctrl Pts',(19.7780364581118,0.098360763778029,3.38092507017875));
#26643=CARTESIAN_POINT('Ctrl Pts',(19.7939417367994,0.27334477570878,3.47141355644931));
#26644=CARTESIAN_POINT('Ctrl Pts',(19.809847015487,0.448328787639532,3.56190204271987));
#26645=CARTESIAN_POINT('Ctrl Pts',(19.8257522941746,0.573916522737285,3.74791193074883));
#26646=CARTESIAN_POINT('Ctrl Pts',(19.8416575728622,0.592443207149574,3.9440350735258));
#26647=CARTESIAN_POINT('Ctrl Pts',(19.8575628515498,0.610969891561863,4.14015821630277));
#26648=CARTESIAN_POINT('Ctrl Pts',(19.8734681302375,0.522435525288687,4.34639461382776));
#26649=CARTESIAN_POINT('Ctrl Pts',(19.8893734089251,0.367491719635661,4.46804975837363));
#26650=CARTESIAN_POINT('Ctrl Pts',(19.8999671355309,0.264291244586565,4.54907828775811));
#26651=CARTESIAN_POINT('Ctrl Pts',(19.9105608621367,0.131629953687138,4.59258455010229));
#26652=CARTESIAN_POINT('Ctrl Pts',(19.9211545887425,-0.000461335262921832,
4.59353843444423));
#26653=CARTESIAN_POINT('Origin',(4.,0.,4.));
#26654=CARTESIAN_POINT('',(20.3288454112575,0.000547175593784699,4.59423670486774));
#26655=CARTESIAN_POINT('',(20.2211545887425,-0.000159442692484791,4.59503650419094));
#26656=CARTESIAN_POINT('',(4.,-7.27562663373442E-17,4.5941));
#26657=CARTESIAN_POINT('Ctrl Pts',(20.3288454112575,0.000547175593784699,
4.59423670486774));
#26658=CARTESIAN_POINT('Ctrl Pts',(20.3254891157492,0.0422991098545892,
4.59465405164581));
#26659=CARTESIAN_POINT('Ctrl Pts',(20.3221328202408,0.0839734681026259,
4.59066114403672));
#26660=CARTESIAN_POINT('Ctrl Pts',(20.3187765247324,0.124636177719752,4.58197547152207));
#26661=CARTESIAN_POINT('Ctrl Pts',(20.3028712460448,0.317334266145104,4.54081460186972));
#26662=CARTESIAN_POINT('Ctrl Pts',(20.2869659673572,0.48731321493246,4.39426577643889));
#26663=CARTESIAN_POINT('Ctrl Pts',(20.2710606886696,0.556778600406793,4.20989870881916));
#26664=CARTESIAN_POINT('Ctrl Pts',(20.255155409982,0.626243985881127,4.02553164119943));
#26665=CARTESIAN_POINT('Ctrl Pts',(20.2392501312944,0.595195808042437,3.80334633139079));
#26666=CARTESIAN_POINT('Ctrl Pts',(20.2233448526068,0.477757630702126,3.64521515909767));
#26667=CARTESIAN_POINT('Ctrl Pts',(20.2074395739191,0.360319453361808,3.48708398680455));
#26668=CARTESIAN_POINT('Ctrl Pts',(20.1915342952315,0.156491276519859,3.39300695202695));
#26669=CARTESIAN_POINT('Ctrl Pts',(20.1756290165439,-0.04006765138094,3.40625706061923));
#26670=CARTESIAN_POINT('Ctrl Pts',(20.1597237378563,-0.236626579281727,
3.4195071692115));
#26671=CARTESIAN_POINT('Ctrl Pts',(20.1438184591687,-0.425916258241364,
3.54008442117362));
#26672=CARTESIAN_POINT('Ctrl Pts',(20.1279131804811,-0.521059912873915,
3.71258420787224));
#26673=CARTESIAN_POINT('Ctrl Pts',(20.1120079017935,-0.616203567506467,
3.88508399457085));
#26674=CARTESIAN_POINT('Ctrl Pts',(20.0961026231058,-0.617201197811932,
4.10950631600596));
#26675=CARTESIAN_POINT('Ctrl Pts',(20.0801973444182,-0.523575121773085,
4.28282745216878));
#26676=CARTESIAN_POINT('Ctrl Pts',(20.0642920657306,-0.429949045734243,
4.45614858833159));
#26677=CARTESIAN_POINT('Ctrl Pts',(20.048386787043,-0.241699263351099,4.57836853922213));
#26678=CARTESIAN_POINT('Ctrl Pts',(20.0324815083554,-0.0452724969876719,
4.59335768007126));
#26679=CARTESIAN_POINT('Ctrl Pts',(20.0312694759895,-0.030304158296608,
4.59449989984645));
#26680=CARTESIAN_POINT('Ctrl Pts',(20.0300574436235,-0.0152883365109376,
4.5950194388496));
#26681=CARTESIAN_POINT('Ctrl Pts',(20.0288454112575,-0.000266600559035268,
4.5949350414008));
#26682=CARTESIAN_POINT('Ctrl Pts',(19.9211545887425,-0.000461335262921832,
4.59353843444423));
#26683=CARTESIAN_POINT('Ctrl Pts',(19.9264661408243,-0.0666901315043342,
4.5940166992278));
#26684=CARTESIAN_POINT('Ctrl Pts',(19.9317776929061,-0.132775635823809,
4.58379778651276));
#26685=CARTESIAN_POINT('Ctrl Pts',(19.9370892449879,-0.194932679790098,
4.56224768701753));
#26686=CARTESIAN_POINT('Ctrl Pts',(19.9529945236755,-0.381060028529917,
4.49771657954882));
#26687=CARTESIAN_POINT('Ctrl Pts',(19.9688998023631,-0.531961480976676,
4.33158047304464));
#26688=CARTESIAN_POINT('Ctrl Pts',(19.9848050810507,-0.578348134104426,
4.14012389605102));
#26689=CARTESIAN_POINT('Ctrl Pts',(20.0007103597384,-0.624734787232175,
3.94866731905739));
#26690=CARTESIAN_POINT('Ctrl Pts',(20.016615638426,-0.566606641040915,3.73189027157431));
#26691=CARTESIAN_POINT('Ctrl Pts',(20.0325209171136,-0.430656211588969,
3.58932409618151));
#26692=CARTESIAN_POINT('Ctrl Pts',(20.0484261958012,-0.294705782137024,
3.44675792078871));
#26693=CARTESIAN_POINT('Ctrl Pts',(20.0643314744888,-0.080933069424392,
3.37840261748619));
#26694=CARTESIAN_POINT('Ctrl Pts',(20.0802367531764,0.112511319004002,3.41565067076361));
#26695=CARTESIAN_POINT('Ctrl Pts',(20.096142031864,0.305955707432406,3.45289872404102));
#26696=CARTESIAN_POINT('Ctrl Pts',(20.1120473105516,0.479071771576571,3.59575013389837));
#26697=CARTESIAN_POINT('Ctrl Pts',(20.1279525892393,0.552362916535151,3.77860107435498));
#26698=CARTESIAN_POINT('Ctrl Pts',(20.1438578679269,0.625654061493722,3.96145201481158));
#26699=CARTESIAN_POINT('Ctrl Pts',(20.1597631466145,0.599120287266732,4.18430248586742));
#26700=CARTESIAN_POINT('Ctrl Pts',(20.1756684253021,0.484961816589866,4.3448525870839));
#26701=CARTESIAN_POINT('Ctrl Pts',(20.1908304797822,0.376137759761604,4.49790047950022));
#26702=CARTESIAN_POINT('Ctrl Pts',(20.2059925342623,0.187686755696174,4.59433432972249));
#26703=CARTESIAN_POINT('Ctrl Pts',(20.2211545887425,-0.000159442692484791,
4.59503650419094));
#26704=CARTESIAN_POINT('Origin',(4.,0.,4.));
#26705=CARTESIAN_POINT('',(20.6288454112575,1.84392275237588E-6,4.59415158619139));
#26706=CARTESIAN_POINT('',(20.5211545887425,0.00014515264107467,4.59408556636595));
#26707=CARTESIAN_POINT('',(4.,-7.27562663373442E-17,4.5941));
#26708=CARTESIAN_POINT('Ctrl Pts',(20.6288454112575,1.84392275237588E-6,
4.59415158619139));
#26709=CARTESIAN_POINT('Ctrl Pts',(20.6209207878748,0.0985777406598016,
4.59414764832452));
#26710=CARTESIAN_POINT('Ctrl Pts',(20.6129961644921,0.197149291092008,4.56908802213256));
#26711=CARTESIAN_POINT('Ctrl Pts',(20.6050715411094,0.283761277174982,4.52200793915563));
#26712=CARTESIAN_POINT('Ctrl Pts',(20.5971189017656,0.370679463050262,4.47476141372331));
#26713=CARTESIAN_POINT('Ctrl Pts',(20.5891662624218,0.445553373684486,4.40533845822152));
#26714=CARTESIAN_POINT('Ctrl Pts',(20.581213623078,0.499196468040806,4.3222224876916));
#26715=CARTESIAN_POINT('Ctrl Pts',(20.5732609837342,0.552839562397126,4.23910651716169));
#26716=CARTESIAN_POINT('Ctrl Pts',(20.5653083443904,0.585251840475543,4.14229753160364));
#26717=CARTESIAN_POINT('Ctrl Pts',(20.5573557050466,0.592531230276538,4.04364021904617));
#26718=CARTESIAN_POINT('Ctrl Pts',(20.5494030657028,0.599810620077534,3.9449829064887));
#26719=CARTESIAN_POINT('Ctrl Pts',(20.541450426359,0.581957121601108,3.84447726693182));
#26720=CARTESIAN_POINT('Ctrl Pts',(20.5334977870152,0.541038843355354,3.75439549632807));
#26721=CARTESIAN_POINT('Ctrl Pts',(20.5255451476714,0.5001205651096,3.66431372572433));
#26722=CARTESIAN_POINT('Ctrl Pts',(20.5175925083276,0.436137507094518,3.58465582407373));
#26723=CARTESIAN_POINT('Ctrl Pts',(20.5096398689838,0.357128912623608,3.5251911792601));
#26724=CARTESIAN_POINT('Ctrl Pts',(20.50168722964,0.278120318152698,3.46572653444646));
#26725=CARTESIAN_POINT('Ctrl Pts',(20.4937345902962,0.184086187225959,3.42645514646979));
#26726=CARTESIAN_POINT('Ctrl Pts',(20.4857819509524,0.0861162623359374,
3.4121221101222));
#26727=CARTESIAN_POINT('Ctrl Pts',(20.4778293116085,-0.0118536625540841,
3.39778907377461));
#26728=CARTESIAN_POINT('Ctrl Pts',(20.4698766722647,-0.113759381407388,
3.4083943890561));
#26729=CARTESIAN_POINT('Ctrl Pts',(20.4619240329209,-0.206384677702653,
3.44274365129583));
#26730=CARTESIAN_POINT('Ctrl Pts',(20.4539713935771,-0.299009973997917,
3.47709291353557));
#26731=CARTESIAN_POINT('Ctrl Pts',(20.4460187542333,-0.382354847735142,
3.53518612273354));
#26732=CARTESIAN_POINT('Ctrl Pts',(20.4380661148895,-0.447563842371028,
3.60976099223211));
#26733=CARTESIAN_POINT('Ctrl Pts',(20.4301134755457,-0.512772837006921,
3.68433586173069));
#26734=CARTESIAN_POINT('Ctrl Pts',(20.4221608362019,-0.559845952541473,
3.77539239152987));
#26735=CARTESIAN_POINT('Ctrl Pts',(20.4142081968581,-0.580888308445953,
3.87190852591559));
#26736=CARTESIAN_POINT('Ctrl Pts',(20.3983029181705,-0.622973020254908,
4.06494079468701));
#26737=CARTESIAN_POINT('Ctrl Pts',(20.3823976394829,-0.5609346935436,4.27981148180459));
#26738=CARTESIAN_POINT('Ctrl Pts',(20.3664923607953,-0.422206916156273,
4.41936036842645));
#26739=CARTESIAN_POINT('Ctrl Pts',(20.353943377616,-0.312753156865475,4.52946196836027));
#26740=CARTESIAN_POINT('Ctrl Pts',(20.3413943944368,-0.155560747392339,
4.59267627084609));
#26741=CARTESIAN_POINT('Ctrl Pts',(20.3288454112575,0.000547175593784699,
4.59423670486774));
#26742=CARTESIAN_POINT('Ctrl Pts',(20.2211545887425,-0.000159442692484791,
4.59503650419094));
#26743=CARTESIAN_POINT('Ctrl Pts',(20.22189781295,-0.00936741923094289,
4.59507092387091));
#26744=CARTESIAN_POINT('Ctrl Pts',(20.2226410371574,-0.0185739425223631,
4.59487531632137));
#26745=CARTESIAN_POINT('Ctrl Pts',(20.2233842613649,-0.0277695625699301,
4.59444507412072));
#26746=CARTESIAN_POINT('Ctrl Pts',(20.2392895400526,-0.224559303926058,
4.58523772856393));
#26747=CARTESIAN_POINT('Ctrl Pts',(20.2551948187402,-0.416355619511548,
4.46857330607325));
#26748=CARTESIAN_POINT('Ctrl Pts',(20.2711000974278,-0.51503297954037,4.29810345018796));
#26749=CARTESIAN_POINT('Ctrl Pts',(20.2870053761154,-0.613710339569191,
4.12763359430267));
#26750=CARTESIAN_POINT('Ctrl Pts',(20.302910654803,-0.619268744041345,3.90335830502277));
#26751=CARTESIAN_POINT('Ctrl Pts',(20.3188159334906,-0.529271009537506,
3.72809546473432));
#26752=CARTESIAN_POINT('Ctrl Pts',(20.3347212121782,-0.439273275033663,
3.55283262444587));
#26753=CARTESIAN_POINT('Ctrl Pts',(20.3506264908658,-0.253719401553817,
3.42658223314887));
#26754=CARTESIAN_POINT('Ctrl Pts',(20.3665317695535,-0.0575887485100287,
3.40762076142476));
#26755=CARTESIAN_POINT('Ctrl Pts',(20.3824370482411,0.138541904533748,3.38865928970065));
#26756=CARTESIAN_POINT('Ctrl Pts',(20.3983423269287,0.345249337141466,3.47698673754941));
#26757=CARTESIAN_POINT('Ctrl Pts',(20.4142476056163,0.467192899405167,3.63141813202173));
#26758=CARTESIAN_POINT('Ctrl Pts',(20.4301528843039,0.589136461668875,3.78584952649406));
#26759=CARTESIAN_POINT('Ctrl Pts',(20.4460581629915,0.626316153588557,4.00638486758996));
#26760=CARTESIAN_POINT('Ctrl Pts',(20.4619634416791,0.562534942182983,4.19337293359078));
#26761=CARTESIAN_POINT('Ctrl Pts',(20.4699160810229,0.530644336480201,4.28686696659118));
#26762=CARTESIAN_POINT('Ctrl Pts',(20.4778687203667,0.473513504946115,4.3719741808178));
#26763=CARTESIAN_POINT('Ctrl Pts',(20.4858213597105,0.400240502138227,4.43864269813793));
#26764=CARTESIAN_POINT('Ctrl Pts',(20.4937739990544,0.326967499330329,4.50531121545807));
#26765=CARTESIAN_POINT('Ctrl Pts',(20.5017266383982,0.237552325248626,4.55354103587171));
#26766=CARTESIAN_POINT('Ctrl Pts',(20.509679277742,0.141619450488441,4.57712494713439));
#26767=CARTESIAN_POINT('Ctrl Pts',(20.5135043814088,0.0954771353210092,
4.58846846487098));
#26768=CARTESIAN_POINT('Ctrl Pts',(20.5173294850756,0.0478269697500401,
4.59411022582368));
#26769=CARTESIAN_POINT('Ctrl Pts',(20.5211545887425,0.00014515264107467,
4.59408556636595));
#26770=CARTESIAN_POINT('Origin',(4.,0.,4.));
#26771=CARTESIAN_POINT('',(20.9288454112575,-6.4040329070536E-6,4.59405282094147));
#26772=CARTESIAN_POINT('',(20.8211545887425,5.65245430726296E-6,4.59414685459231));
#26773=CARTESIAN_POINT('',(4.,-7.27562663373442E-17,4.5941));
#26774=CARTESIAN_POINT('Ctrl Pts',(20.9288454112575,-6.4040329070536E-6,
4.59405282094147));
#26775=CARTESIAN_POINT('Ctrl Pts',(20.9243050993443,0.0564994875152707,
4.59403151438501));
#26776=CARTESIAN_POINT('Ctrl Pts',(20.9197647874311,0.113011285737041,4.58603249222448));
#26777=CARTESIAN_POINT('Ctrl Pts',(20.9152244755179,0.167207550221224,4.57013805289591));
#26778=CARTESIAN_POINT('Ctrl Pts',(20.9072718361741,0.262135685878584,4.5422979516059));
#26779=CARTESIAN_POINT('Ctrl Pts',(20.8993191968303,0.349959832061366,4.49023494241839));
#26780=CARTESIAN_POINT('Ctrl Pts',(20.8913665574865,0.419942299057043,4.42031443844746));
#26781=CARTESIAN_POINT('Ctrl Pts',(20.8834139181427,0.489924766052721,4.35039393447653));
#26782=CARTESIAN_POINT('Ctrl Pts',(20.8754612787989,0.542065553861293,4.26261593572219));
#26783=CARTESIAN_POINT('Ctrl Pts',(20.8675086394551,0.569989725359365,4.16771249585991));
#26784=CARTESIAN_POINT('Ctrl Pts',(20.8595560001113,0.597913896857441,4.07280905599763));
#26785=CARTESIAN_POINT('Ctrl Pts',(20.8516033607674,0.601621452045013,3.97078017502742));
#26786=CARTESIAN_POINT('Ctrl Pts',(20.8436507214236,0.580659121393648,3.87410027737825));
#26787=CARTESIAN_POINT('Ctrl Pts',(20.8356980820798,0.559696790742287,3.77742037972911));
#26788=CARTESIAN_POINT('Ctrl Pts',(20.827745442736,0.514064574252002,3.686089465401));
#26789=CARTESIAN_POINT('Ctrl Pts',(20.8197928033922,0.44934157601673,3.61127397478397));
#26790=CARTESIAN_POINT('Ctrl Pts',(20.8118401640484,0.384618577781443,3.53645848416692));
#26791=CARTESIAN_POINT('Ctrl Pts',(20.8038875247046,0.300804797801161,3.47815841726095));
#26792=CARTESIAN_POINT('Ctrl Pts',(20.7959348853608,0.208147717693743,3.44350176598286));
#26793=CARTESIAN_POINT('Ctrl Pts',(20.787982246017,0.115490637586335,3.40884511470477));
#26794=CARTESIAN_POINT('Ctrl Pts',(20.7800296066732,0.0139902573517945,
3.39783187905454));
#26795=CARTESIAN_POINT('Ctrl Pts',(20.7720769673294,-0.0839438183138644,
3.41180854931868));
#26796=CARTESIAN_POINT('Ctrl Pts',(20.7641243279856,-0.181877893979523,
3.42578521958283));
#26797=CARTESIAN_POINT('Ctrl Pts',(20.7561716886418,-0.2762456650763,3.46475179576135));
#26798=CARTESIAN_POINT('Ctrl Pts',(20.748219049298,-0.355509010203556,3.52394413563581));
#26799=CARTESIAN_POINT('Ctrl Pts',(20.7402664099542,-0.434772355330821,
3.58313647551028));
#26800=CARTESIAN_POINT('Ctrl Pts',(20.7323137706103,-0.498931274488562,
3.66255457908069));
#26801=CARTESIAN_POINT('Ctrl Pts',(20.7243611312665,-0.54014217617541,3.75248840252759));
#26802=CARTESIAN_POINT('Ctrl Pts',(20.7164084919227,-0.581353077862249,
3.84242222597448));
#26803=CARTESIAN_POINT('Ctrl Pts',(20.7084558525789,-0.599615962078206,
3.94287176929784));
#26804=CARTESIAN_POINT('Ctrl Pts',(20.7005032132351,-0.592696601504336,
4.0415558946729));
#26805=CARTESIAN_POINT('Ctrl Pts',(20.6925505738913,-0.585777240930466,
4.14024002004797));
#26806=CARTESIAN_POINT('Ctrl Pts',(20.6845979345475,-0.553675635566762,
4.23715872747472));
#26807=CARTESIAN_POINT('Ctrl Pts',(20.6766452952037,-0.50031917594212,4.32046203197985));
#26808=CARTESIAN_POINT('Ctrl Pts',(20.6686926558599,-0.446962716317479,
4.40376533648498));
#26809=CARTESIAN_POINT('Ctrl Pts',(20.6607400165161,-0.3723514024319,4.47345323806848));
#26810=CARTESIAN_POINT('Ctrl Pts',(20.6527873771723,-0.285602702553558,
4.52100610813718));
#26811=CARTESIAN_POINT('Ctrl Pts',(20.6448347378285,-0.198854002675205,
4.56855897820588));
#26812=CARTESIAN_POINT('Ctrl Pts',(20.6368820984847,-0.099967916804087,
4.59397681675976));
#26813=CARTESIAN_POINT('Ctrl Pts',(20.6289294591409,-0.00104364331035449,
4.59415068835528));
#26814=CARTESIAN_POINT('Ctrl Pts',(20.6289014431798,-0.000695147863829354,
4.59415130087895));
#26815=CARTESIAN_POINT('Ctrl Pts',(20.6288734272186,-0.000346651943377611,
4.59415160011295));
#26816=CARTESIAN_POINT('Ctrl Pts',(20.6288454112575,1.84392275237588E-6,
4.59415158619139));
#26817=CARTESIAN_POINT('Ctrl Pts',(20.5211545887425,0.00014515264107467,
4.59408556636595));
#26818=CARTESIAN_POINT('Ctrl Pts',(20.5252821244194,-0.0513066296901884,
4.59405895720698));
#26819=CARTESIAN_POINT('Ctrl Pts',(20.5294096600964,-0.102795266482965,
4.58743447362686));
#26820=CARTESIAN_POINT('Ctrl Pts',(20.5335371957734,-0.152465997634008,
4.57425651377355));
#26821=CARTESIAN_POINT('Ctrl Pts',(20.5414898351172,-0.248167995557571,
4.5488661670383));
#26822=CARTESIAN_POINT('Ctrl Pts',(20.549442474461,-0.33712141596603,4.49914747145609));
#26823=CARTESIAN_POINT('Ctrl Pts',(20.5573951138048,-0.408848640915227,
4.43107686705031));
#26824=CARTESIAN_POINT('Ctrl Pts',(20.5653477531486,-0.480575865864423,
4.36300626264453));
#26825=CARTESIAN_POINT('Ctrl Pts',(20.5733003924924,-0.535076895354358,
4.27658374941519));
#26826=CARTESIAN_POINT('Ctrl Pts',(20.5812530318362,-0.565476628275392,
4.18243021985824));
#26827=CARTESIAN_POINT('Ctrl Pts',(20.58920567118,-0.595876361196427,4.08827669030129));
#26828=CARTESIAN_POINT('Ctrl Pts',(20.5971583105238,-0.602174797548561,
3.98639214441672));
#26829=CARTESIAN_POINT('Ctrl Pts',(20.6051109498677,-0.58371402745925,3.88920441471463));
#26830=CARTESIAN_POINT('Ctrl Pts',(20.6130635892115,-0.565253257369939,
3.79201668501254));
#26831=CARTESIAN_POINT('Ctrl Pts',(20.6210162285553,-0.522033280839182,
3.69952577149293));
#26832=CARTESIAN_POINT('Ctrl Pts',(20.6289688678991,-0.459278917219465,
3.62305528060961));
#26833=CARTESIAN_POINT('Ctrl Pts',(20.6369215072429,-0.396524553599749,
3.54658478972629));
#26834=CARTESIAN_POINT('Ctrl Pts',(20.6448741465867,-0.314235802891072,
3.48613472147926));
#26835=CARTESIAN_POINT('Ctrl Pts',(20.6528267859305,-0.222505051509483,
3.44908779917463));
#26836=CARTESIAN_POINT('Ctrl Pts',(20.6607794252743,-0.130774300127894,
3.41204087687));
#26837=CARTESIAN_POINT('Ctrl Pts',(20.6687320646181,-0.029601548073392,
3.39839710050778));
#26838=CARTESIAN_POINT('Ctrl Pts',(20.6766847039619,0.0686601223983595,
3.40982890848785));
#26839=CARTESIAN_POINT('Ctrl Pts',(20.6846373433057,0.1669217928701,3.42126071646792));
#26840=CARTESIAN_POINT('Ctrl Pts',(20.6925899826495,0.262272381759091,3.45776810879028));
#26841=CARTESIAN_POINT('Ctrl Pts',(20.7005426219933,0.343045155251024,3.51488528173127));
#26842=CARTESIAN_POINT('Ctrl Pts',(20.7084952613371,0.423817928742975,3.57200245467228));
#26843=CARTESIAN_POINT('Ctrl Pts',(20.7164479006809,0.490012886837861,3.64972940823193));
#26844=CARTESIAN_POINT('Ctrl Pts',(20.7244005400247,0.533541468465666,3.73856417004634));
#26845=CARTESIAN_POINT('Ctrl Pts',(20.7323531793686,0.577070050093471,3.82739893186076));
#26846=CARTESIAN_POINT('Ctrl Pts',(20.7403058187123,0.597932255254196,3.92734150192994));
#26847=CARTESIAN_POINT('Ctrl Pts',(20.7482584580562,0.593574919799613,4.02617190099588));
#26848=CARTESIAN_POINT('Ctrl Pts',(20.7562110974,0.589217584345031,4.1250023000618));
#26849=CARTESIAN_POINT('Ctrl Pts',(20.7641637367438,0.559640708275147,4.22272052812447));
#26850=CARTESIAN_POINT('Ctrl Pts',(20.7721163760876,0.508461778515953,4.30737953925928));
#26851=CARTESIAN_POINT('Ctrl Pts',(20.7800690154314,0.457282848756759,4.39203855039408));
#26852=CARTESIAN_POINT('Ctrl Pts',(20.7880216547752,0.384501865308254,4.46363834460102));
#26853=CARTESIAN_POINT('Ctrl Pts',(20.795974294119,0.299016600344635,4.51342469267633));
#26854=CARTESIAN_POINT('Ctrl Pts',(20.8039269334628,0.213531335381016,4.56321104075164));
#26855=CARTESIAN_POINT('Ctrl Pts',(20.8118795728066,0.115341788902283,4.59118394269532));
#26856=CARTESIAN_POINT('Ctrl Pts',(20.8198322121504,0.0164533379892873,
4.59392342516246));
#26857=CARTESIAN_POINT('Ctrl Pts',(20.8202730043478,0.0109722321971217,
4.59407526688998));
#26858=CARTESIAN_POINT('Ctrl Pts',(20.8207137965451,0.00548897925183007,
4.59414958726715));
#26859=CARTESIAN_POINT('Ctrl Pts',(20.8211545887425,5.65245430726296E-6,
4.59414685459231));
#26860=CARTESIAN_POINT('Origin',(4.,0.,4.));
#26861=CARTESIAN_POINT('',(21.2288454112575,1.28243205298473E-5,4.59412621697841));
#26862=CARTESIAN_POINT('',(21.1211545887425,-1.09306879613159E-5,4.5940621922514));
#26863=CARTESIAN_POINT('',(4.,-7.27562663373442E-17,4.5941));
#26864=CARTESIAN_POINT('Ctrl Pts',(21.2288454112575,1.28243205298473E-5,
4.59412621697841));
#26865=CARTESIAN_POINT('Ctrl Pts',(21.2276894108138,0.0143945780386088,
4.59413985249388));
#26866=CARTESIAN_POINT('Ctrl Pts',(21.2265334103701,0.028775363636007,4.59362827285675));
#26867=CARTESIAN_POINT('Ctrl Pts',(21.2253774099263,0.043117441953227,4.59258471957415));
#26868=CARTESIAN_POINT('Ctrl Pts',(21.2174247705826,0.141782954511012,4.58540565408365));
#26869=CARTESIAN_POINT('Ctrl Pts',(21.2094721312387,0.238616577754522,4.55305001116024));
#26870=CARTESIAN_POINT('Ctrl Pts',(21.2015194918949,0.321779082392626,4.49947370882601));
#26871=CARTESIAN_POINT('Ctrl Pts',(21.1935668525511,0.404941587030731,4.44589740649178));
#26872=CARTESIAN_POINT('Ctrl Pts',(21.1856142132073,0.474432973063433,4.37110044474674));
#26873=CARTESIAN_POINT('Ctrl Pts',(21.1776615738635,0.521756972098598,4.28422777087894));
#26874=CARTESIAN_POINT('Ctrl Pts',(21.1697089345197,0.569080971133768,4.19735509701114));
#26875=CARTESIAN_POINT('Ctrl Pts',(21.1617562951759,0.594237583171398,4.09840671102057));
#26876=CARTESIAN_POINT('Ctrl Pts',(21.1538036558321,0.594151069756079,3.9994804007435));
#26877=CARTESIAN_POINT('Ctrl Pts',(21.1458510164883,0.59406455634076,3.90055409046644));
#26878=CARTESIAN_POINT('Ctrl Pts',(21.1378983771445,0.568734917472505,3.80164985590287));
#26879=CARTESIAN_POINT('Ctrl Pts',(21.1299457378007,0.521259046500119,3.71486008677882));
#26880=CARTESIAN_POINT('Ctrl Pts',(21.1219930984569,0.473783175527722,3.62807031765475));
#26881=CARTESIAN_POINT('Ctrl Pts',(21.114040459113,0.40416107245118,3.5533950139702));
#26882=CARTESIAN_POINT('Ctrl Pts',(21.1060878197692,0.320904987578411,3.49996424865404));
#26883=CARTESIAN_POINT('Ctrl Pts',(21.0981351804254,0.237648902705652,3.44653348333788));
#26884=CARTESIAN_POINT('Ctrl Pts',(21.0901825410817,0.140758836036697,3.41434725639011));
#26885=CARTESIAN_POINT('Ctrl Pts',(21.0822299017378,0.042080917889342,3.40734077242984));
#26886=CARTESIAN_POINT('Ctrl Pts',(21.074277262394,-0.056597000258024,3.40033428846957));
#26887=CARTESIAN_POINT('Ctrl Pts',(21.0663246230502,-0.157062769883762,
3.41850754749682));
#26888=CARTESIAN_POINT('Ctrl Pts',(21.0583719837064,-0.247033082431791,
3.45963862106718));
#26889=CARTESIAN_POINT('Ctrl Pts',(21.0504193443626,-0.337003394979799,
3.50076969463752));
#26890=CARTESIAN_POINT('Ctrl Pts',(21.0424667050188,-0.416478250450111,
3.56485858275095));
#26891=CARTESIAN_POINT('Ctrl Pts',(21.034514065675,-0.475740765152555,3.644069545988));
#26892=CARTESIAN_POINT('Ctrl Pts',(21.0265614263312,-0.535003279855012,
3.72328050922507));
#26893=CARTESIAN_POINT('Ctrl Pts',(21.0186087869874,-0.574053453789596,
3.81761354758578));
#26894=CARTESIAN_POINT('Ctrl Pts',(21.0106561476436,-0.588116871685884,
3.91553516229212));
#26895=CARTESIAN_POINT('Ctrl Pts',(21.0027035082998,-0.60218028958217,4.01345677699845));
#26896=CARTESIAN_POINT('Ctrl Pts',(20.994750868956,-0.591256951440166,4.11496696805043));
#26897=CARTESIAN_POINT('Ctrl Pts',(20.9867982296121,-0.556682383467722,
4.20765473214191));
#26898=CARTESIAN_POINT('Ctrl Pts',(20.9788455902683,-0.522107815495282,
4.30034249623339));
#26899=CARTESIAN_POINT('Ctrl Pts',(20.9708929509246,-0.463882017692404,
4.38420783336438));
#26900=CARTESIAN_POINT('Ctrl Pts',(20.9629403115808,-0.389123888092725,
4.4489970636758));
#26901=CARTESIAN_POINT('Ctrl Pts',(20.9549876722369,-0.314365758493028,
4.51378629398723));
#26902=CARTESIAN_POINT('Ctrl Pts',(20.9470350328931,-0.223075297096518,
4.5594994174791));
#26903=CARTESIAN_POINT('Ctrl Pts',(20.9390823935493,-0.12641400383229,4.58054738252877));
#26904=CARTESIAN_POINT('Ctrl Pts',(20.9356700661187,-0.0849384674446181,
4.58957866703598));
#26905=CARTESIAN_POINT('Ctrl Pts',(20.9322577386881,-0.0424741039190781,
4.59406883414683));
#26906=CARTESIAN_POINT('Ctrl Pts',(20.9288454112575,-6.4040329070536E-6,
4.59405282094147));
#26907=CARTESIAN_POINT('Ctrl Pts',(20.8211545887425,5.65245430726296E-6,
4.59414685459231));
#26908=CARTESIAN_POINT('Ctrl Pts',(20.8286664358889,-0.0934395423672534,
4.59410028517524));
#26909=CARTESIAN_POINT('Ctrl Pts',(20.8361782830354,-0.18690618531264,4.57167601133058));
#26910=CARTESIAN_POINT('Ctrl Pts',(20.8436901301818,-0.270133012248912,
4.529191754035));
#26911=CARTESIAN_POINT('Ctrl Pts',(20.8516427695256,-0.358243556226857,
4.4842145374498));
#26912=CARTESIAN_POINT('Ctrl Pts',(20.8595954088694,-0.434877288835492,
4.41675404128879));
#26913=CARTESIAN_POINT('Ctrl Pts',(20.8675480482133,-0.490664589397756,
4.33505825661903));
#26914=CARTESIAN_POINT('Ctrl Pts',(20.8755006875571,-0.546451889960021,
4.25336247194927));
#26915=CARTESIAN_POINT('Ctrl Pts',(20.8834533269009,-0.581392758475918,
4.15743139877076));
#26916=CARTESIAN_POINT('Ctrl Pts',(20.8914059662447,-0.591215252505097,
4.05899390323763));
#26917=CARTESIAN_POINT('Ctrl Pts',(20.8993586055885,-0.601037746534278,
3.96055640770449));
#26918=CARTESIAN_POINT('Ctrl Pts',(20.9073112449323,-0.585741866076735,
3.85961248981672));
#26919=CARTESIAN_POINT('Ctrl Pts',(20.9152638842761,-0.547197711916726,
3.76850392583047));
#26920=CARTESIAN_POINT('Ctrl Pts',(20.9232165236199,-0.508653557756717,
3.67739536184422));
#26921=CARTESIAN_POINT('Ctrl Pts',(20.9311691629637,-0.446861129894262,
3.59612215175949));
#26922=CARTESIAN_POINT('Ctrl Pts',(20.9391218023075,-0.369375409551539,
3.53462104847409));
#26923=CARTESIAN_POINT('Ctrl Pts',(20.9470744416513,-0.291889689208826,
3.4731199451887));
#26924=CARTESIAN_POINT('Ctrl Pts',(20.9550270809951,-0.198710676385865,
3.43139094870266));
#26925=CARTESIAN_POINT('Ctrl Pts',(20.9629797203389,-0.101230766359376,
3.41453599926792));
#26926=CARTESIAN_POINT('Ctrl Pts',(20.9709323596827,-0.00375085633288601,
3.39768104983318));
#26927=CARTESIAN_POINT('Ctrl Pts',(20.9788849990265,0.0980299508971346,
3.40570014744973));
#26928=CARTESIAN_POINT('Ctrl Pts',(20.9868376383704,0.191667561123074,3.43761284710704));
#26929=CARTESIAN_POINT('Ctrl Pts',(20.9947902777142,0.285305171349014,3.46952554676435));
#26930=CARTESIAN_POINT('Ctrl Pts',(21.002742917058,0.37079958457088,3.52533184846243));
#26931=CARTESIAN_POINT('Ctrl Pts',(21.0106955564018,0.437697946637459,3.59820867233944));
#26932=CARTESIAN_POINT('Ctrl Pts',(21.0186481957456,0.504596308704037,3.67108549621644));
#26933=CARTESIAN_POINT('Ctrl Pts',(21.0266008350894,0.552898619615334,3.76103284227238));
#26934=CARTESIAN_POINT('Ctrl Pts',(21.0345534744332,0.576699262792956,3.8570534220826));
#26935=CARTESIAN_POINT('Ctrl Pts',(21.042506113777,0.600499905970578,3.95307400189282));
#26936=CARTESIAN_POINT('Ctrl Pts',(21.0504587531208,0.599798881414527,4.05516781545734));
#26937=CARTESIAN_POINT('Ctrl Pts',(21.0584113924646,0.574681899562831,4.15085250374278));
#26938=CARTESIAN_POINT('Ctrl Pts',(21.0663640318084,0.549564917711138,4.24653719202821));
#26939=CARTESIAN_POINT('Ctrl Pts',(21.0743166711522,0.500031978563804,4.33581275503458));
#26940=CARTESIAN_POINT('Ctrl Pts',(21.082269310496,0.432139158218639,4.40776403918836));
#26941=CARTESIAN_POINT('Ctrl Pts',(21.0902219498398,0.364246337873458,4.47971532334216));
#26942=CARTESIAN_POINT('Ctrl Pts',(21.0981745891836,0.277993636330433,4.53434232864337));
#26943=CARTESIAN_POINT('Ctrl Pts',(21.1061272285274,0.183926621270441,4.56496615973523));
#26944=CARTESIAN_POINT('Ctrl Pts',(21.1111363485991,0.124676735433976,4.5842551580617));
#26945=CARTESIAN_POINT('Ctrl Pts',(21.1161454686708,0.0623266393968894,
4.59402126159141));
#26946=CARTESIAN_POINT('Ctrl Pts',(21.1211545887425,-1.09306879613159E-5,
4.5940621922514));
#26947=CARTESIAN_POINT('Origin',(4.,0.,4.));
#26948=CARTESIAN_POINT('',(21.5288454112575,-1.51073027558624E-5,4.59408477831653));
#26949=CARTESIAN_POINT('',(21.4211545887425,1.51733402061755E-5,4.59410821609125));
#26950=CARTESIAN_POINT('',(4.,-7.27562663373442E-17,4.5941));
#26951=CARTESIAN_POINT('Ctrl Pts',(21.5288454112575,-1.51073027558624E-5,
4.59408477831653));
#26952=CARTESIAN_POINT('Ctrl Pts',(21.5231210829395,0.0712153309254728,
4.59401644885886));
#26953=CARTESIAN_POINT('Ctrl Pts',(21.5173967546214,0.142469702059594,4.58119587380047));
#26954=CARTESIAN_POINT('Ctrl Pts',(21.5116724263034,0.209120766622247,4.55613331912479));
#26955=CARTESIAN_POINT('Ctrl Pts',(21.5037197869596,0.301717111362981,4.52131465616629));
#26956=CARTESIAN_POINT('Ctrl Pts',(21.4957671476158,0.385428743083265,4.46286809139133));
#26957=CARTESIAN_POINT('Ctrl Pts',(21.4878145082719,0.450020774675764,4.38793951336988));
#26958=CARTESIAN_POINT('Ctrl Pts',(21.4798618689281,0.514612806268249,4.31301093534845));
#26959=CARTESIAN_POINT('Ctrl Pts',(21.4719092295843,0.560085237732952,4.22160034408054));
#26960=CARTESIAN_POINT('Ctrl Pts',(21.4639565902405,0.58087844500124,4.1248839293359));
#26961=CARTESIAN_POINT('Ctrl Pts',(21.4560039508967,0.601671652269532,4.02816751459124));
#26962=CARTESIAN_POINT('Ctrl Pts',(21.4480513115529,0.597785635341394,3.92614527636987));
#26963=CARTESIAN_POINT('Ctrl Pts',(21.4400986722091,0.569695512712777,3.83129082280931));
#26964=CARTESIAN_POINT('Ctrl Pts',(21.4321460328653,0.541605390084162,3.73643636924876));
#26965=CARTESIAN_POINT('Ctrl Pts',(21.4241933935215,0.489311161755075,3.64874970034904));
#26966=CARTESIAN_POINT('Ctrl Pts',(21.4162407541777,0.419206509371839,3.57895170565158));
#26967=CARTESIAN_POINT('Ctrl Pts',(21.4082881148339,0.349101856988603,3.50915371095413));
#26968=CARTESIAN_POINT('Ctrl Pts',(21.4003354754901,0.261186780551223,3.45724439045894));
#26969=CARTESIAN_POINT('Ctrl Pts',(21.3923828361463,0.16621009553345,3.42957036558731));
#26970=CARTESIAN_POINT('Ctrl Pts',(21.3844301968025,0.0712334105156764,
3.40189634071567));
#26971=CARTESIAN_POINT('Ctrl Pts',(21.3764775574587,-0.0308048830825163,
3.3984576114676));
#26972=CARTESIAN_POINT('Ctrl Pts',(21.3685249181149,-0.127429214135013,
3.41967460932821));
#26973=CARTESIAN_POINT('Ctrl Pts',(21.360572278771,-0.22405354518751,3.44089160718882));
#26974=CARTESIAN_POINT('Ctrl Pts',(21.3526196394272,-0.315263913694308,
3.4867643321581));
#26975=CARTESIAN_POINT('Ctrl Pts',(21.3446670000834,-0.389908609845283,
3.5516842188346));
#26976=CARTESIAN_POINT('Ctrl Pts',(21.3367143607396,-0.464553305996249,
3.6166041055111));
#26977=CARTESIAN_POINT('Ctrl Pts',(21.3287617213958,-0.522632329791381,
3.70057115389483));
#26978=CARTESIAN_POINT('Ctrl Pts',(21.320809082052,-0.557044729551177,3.79331924871262));
#26979=CARTESIAN_POINT('Ctrl Pts',(21.3128564427082,-0.591457129310977,
3.88606734353042));
#26980=CARTESIAN_POINT('Ctrl Pts',(21.3049038033644,-0.602202905035458,
3.9875964847823));
#26981=CARTESIAN_POINT('Ctrl Pts',(21.2969511640206,-0.587968239287942,
4.08549335215105));
#26982=CARTESIAN_POINT('Ctrl Pts',(21.2889985246768,-0.573733573540424,
4.18339021951981));
#26983=CARTESIAN_POINT('Ctrl Pts',(21.281045885333,-0.534518466320906,4.27765481300544));
#26984=CARTESIAN_POINT('Ctrl Pts',(21.2730932459892,-0.47511749858569,4.35676200219639));
#26985=CARTESIAN_POINT('Ctrl Pts',(21.2651406066454,-0.415716530850488,
4.43586919138732));
#26986=CARTESIAN_POINT('Ctrl Pts',(21.2571879673016,-0.336129702599601,
4.49981897628356));
#26987=CARTESIAN_POINT('Ctrl Pts',(21.2492353279577,-0.246087587538132,
4.54079262470289));
#26988=CARTESIAN_POINT('Ctrl Pts',(21.2424386890577,-0.169134048541188,
4.57581031891556));
#26989=CARTESIAN_POINT('Ctrl Pts',(21.2356420501576,-0.0845438791841879,
4.59404604774026));
#26990=CARTESIAN_POINT('Ctrl Pts',(21.2288454112575,1.28243205298473E-5,
4.59412621697841));
#26991=CARTESIAN_POINT('Ctrl Pts',(21.1211545887425,-1.09306879613159E-5,
4.5940621922514));
#26992=CARTESIAN_POINT('Ctrl Pts',(21.1240981080146,-0.0366424819978743,
4.5940862444172));
#26993=CARTESIAN_POINT('Ctrl Pts',(21.1270416272867,-0.0732697079540161,
4.59075208378119));
#26994=CARTESIAN_POINT('Ctrl Pts',(21.1299851465589,-0.109260984540888,
4.58401866488291));
#26995=CARTESIAN_POINT('Ctrl Pts',(21.1379377859027,-0.20650024671525,4.56582668205621));
#26996=CARTESIAN_POINT('Ctrl Pts',(21.1458904252465,-0.299097442487026,
4.52282205952027));
#26997=CARTESIAN_POINT('Ctrl Pts',(21.1538430645903,-0.375731303474415,
4.46026269810429));
#26998=CARTESIAN_POINT('Ctrl Pts',(21.1617957039341,-0.452365164461805,
4.3977033366883));
#26999=CARTESIAN_POINT('Ctrl Pts',(21.1697483432779,-0.513035690664809,
4.31558923639226));
#27000=CARTESIAN_POINT('Ctrl Pts',(21.1777009826217,-0.550325083965727,
4.22395996434209));
#27001=CARTESIAN_POINT('Ctrl Pts',(21.1856536219655,-0.587614477266646,
4.13233069229192));
#27002=CARTESIAN_POINT('Ctrl Pts',(21.1936062613093,-0.601522737665479,
4.03118624848761));
#27003=CARTESIAN_POINT('Ctrl Pts',(21.2015589006531,-0.590349390887683,
3.93289291874755));
#27004=CARTESIAN_POINT('Ctrl Pts',(21.2095115399969,-0.579176044109886,
3.83459958900749));
#27005=CARTESIAN_POINT('Ctrl Pts',(21.2174641793407,-0.542921090155459,
3.73915737333167));
#27006=CARTESIAN_POINT('Ctrl Pts',(21.2254168186845,-0.486017190935348,
3.65823538248142));
#27007=CARTESIAN_POINT('Ctrl Pts',(21.2333694580283,-0.429113291715238,
3.57731339163117));
#27008=CARTESIAN_POINT('Ctrl Pts',(21.2413220973721,-0.351560447229444,
3.51091162560648));
#27009=CARTESIAN_POINT('Ctrl Pts',(21.249274736716,-0.262840548960938,3.46714860467879));
#27010=CARTESIAN_POINT('Ctrl Pts',(21.2572273760598,-0.174120650692433,
3.4233855837511));
#27011=CARTESIAN_POINT('Ctrl Pts',(21.2651800154036,-0.0742336986412151,
3.40226130792041));
#27012=CARTESIAN_POINT('Ctrl Pts',(21.2731326547474,0.0246077668693877,
3.40635850761334));
#27013=CARTESIAN_POINT('Ctrl Pts',(21.2810852940912,0.123449232380002,3.41045570730627));
#27014=CARTESIAN_POINT('Ctrl Pts',(21.289037933435,0.221245211350001,3.43977438252282));
#27015=CARTESIAN_POINT('Ctrl Pts',(21.2969905727788,0.306038813396919,3.49072992590572));
#27016=CARTESIAN_POINT('Ctrl Pts',(21.3049432121226,0.390832415443818,3.54168546928862));
#27017=CARTESIAN_POINT('Ctrl Pts',(21.3128958514664,0.462623640567642,3.61427788083785));
#27018=CARTESIAN_POINT('Ctrl Pts',(21.3208484908102,0.512635033719562,3.69963174955258));
#27019=CARTESIAN_POINT('Ctrl Pts',(21.328801130154,0.562646426871494,3.78498561826733));
#27020=CARTESIAN_POINT('Ctrl Pts',(21.3367537694978,0.590877988051513,3.88310094414759));
#27021=CARTESIAN_POINT('Ctrl Pts',(21.3447064088416,0.59387802439953,3.98198179230066));
#27022=CARTESIAN_POINT('Ctrl Pts',(21.3526590481854,0.596878060747546,4.08086264045372));
#27023=CARTESIAN_POINT('Ctrl Pts',(21.3606116875293,0.574646572263566,4.1805090108796));
#27024=CARTESIAN_POINT('Ctrl Pts',(21.3685643268731,0.529901661201384,4.26873777763737));
#27025=CARTESIAN_POINT('Ctrl Pts',(21.3765169662169,0.485156750139203,4.35696654439514));
#27026=CARTESIAN_POINT('Ctrl Pts',(21.3844696055607,0.417898416498819,4.4337777074848));
#27027=CARTESIAN_POINT('Ctrl Pts',(21.3924222449045,0.336349907607971,4.48978005607163));
#27028=CARTESIAN_POINT('Ctrl Pts',(21.4003748842483,0.254801398717122,4.54578240465847));
#27029=CARTESIAN_POINT('Ctrl Pts',(21.4083275235921,0.158962714575808,4.58097593874246));
#27030=CARTESIAN_POINT('Ctrl Pts',(21.4162801629359,0.0605514396169286,
4.59105776945554));
#27031=CARTESIAN_POINT('Ctrl Pts',(21.4179049715381,0.0404449719157324,
4.59311759444699));
#27032=CARTESIAN_POINT('Ctrl Pts',(21.4195297801403,0.0202311170044278,
4.59412918598148));
#27033=CARTESIAN_POINT('Ctrl Pts',(21.4211545887425,1.51733402061755E-5,
4.59410821609125));
#27034=CARTESIAN_POINT('Origin',(4.,0.,4.));
#27035=CARTESIAN_POINT('',(21.8288454112575,1.47252919898561E-5,4.59408074293421));
#27036=CARTESIAN_POINT('',(21.7211545887425,-1.54601956517634E-5,4.59410286710644));
#27037=CARTESIAN_POINT('',(4.,-7.27562663373442E-17,4.5941));
#27038=CARTESIAN_POINT('Ctrl Pts',(21.8288454112575,1.47252919898561E-5,
4.59408074293421));
#27039=CARTESIAN_POINT('Ctrl Pts',(21.826505394409,0.0291331941223908,4.59410767674242));
#27040=CARTESIAN_POINT('Ctrl Pts',(21.8241653775604,0.0582478076928112,
4.59200528777341));
#27041=CARTESIAN_POINT('Ctrl Pts',(21.8218253607118,0.0870422430987805,
4.58774093918134));
#27042=CARTESIAN_POINT('Ctrl Pts',(21.813872721368,0.184901264939656,4.57324838268129));
#27043=CARTESIAN_POINT('Ctrl Pts',(21.8059200820242,0.279062206656402,4.53378504179028));
#27044=CARTESIAN_POINT('Ctrl Pts',(21.7979674426804,0.358012610677869,4.47417584741217));
#27045=CARTESIAN_POINT('Ctrl Pts',(21.7900148033366,0.436963014699336,4.41456665303406));
#27046=CARTESIAN_POINT('Ctrl Pts',(21.7820621639928,0.500702881025523,4.33481160516884));
#27047=CARTESIAN_POINT('Ctrl Pts',(21.774109524649,0.541439142878506,4.24466184465998));
#27048=CARTESIAN_POINT('Ctrl Pts',(21.7661568853052,0.58217540473149,4.15451208415111));
#27049=CARTESIAN_POINT('Ctrl Pts',(21.7582042459614,0.599908062111268,4.0539676109986));
#27050=CARTESIAN_POINT('Ctrl Pts',(21.7502516066176,0.59246905613922,3.95532135643358));
#27051=CARTESIAN_POINT('Ctrl Pts',(21.7422989672738,0.585030050167171,3.85667510186855));
#27052=CARTESIAN_POINT('Ctrl Pts',(21.73434632793,0.552419380843296,3.759927065891));
#27053=CARTESIAN_POINT('Ctrl Pts',(21.7263936885861,0.498624146640836,3.67690601358098));
#27054=CARTESIAN_POINT('Ctrl Pts',(21.7184410492423,0.444828912438376,3.59388496127097));
#27055=CARTESIAN_POINT('Ctrl Pts',(21.7104884098985,0.369849113357332,3.52459089262848));
#27056=CARTESIAN_POINT('Ctrl Pts',(21.7025357705547,0.28285205103972,3.47749595131133));
#27057=CARTESIAN_POINT('Ctrl Pts',(21.6945831312109,0.195854988722108,3.43040100999418));
#27058=CARTESIAN_POINT('Ctrl Pts',(21.6866304918671,0.0968406631679286,
3.40550519600236));
#27059=CARTESIAN_POINT('Ctrl Pts',(21.6786778525233,-0.00208507577578169,
3.40585236167057));
#27060=CARTESIAN_POINT('Ctrl Pts',(21.6707252131795,-0.101010814719503,
3.40619952733877));
#27061=CARTESIAN_POINT('Ctrl Pts',(21.6627725738357,-0.199847967052756,
3.431789672667));
#27062=CARTESIAN_POINT('Ctrl Pts',(21.6548199344919,-0.28651234476781,3.47949405385809));
#27063=CARTESIAN_POINT('Ctrl Pts',(21.6468672951481,-0.373176722482865,
3.52719843504918));
#27064=CARTESIAN_POINT('Ctrl Pts',(21.6389146558043,-0.44766832557972,3.59701705210314));
#27065=CARTESIAN_POINT('Ctrl Pts',(21.6309620164605,-0.500879541024521,
3.68041362817464));
#27066=CARTESIAN_POINT('Ctrl Pts',(21.6230093771167,-0.55409075646931,3.76381020424612));
#27067=CARTESIAN_POINT('Ctrl Pts',(21.6150567377728,-0.586021584262053,
3.86078473933514));
#27068=CARTESIAN_POINT('Ctrl Pts',(21.607104098429,-0.592768045815946,3.95948077576042));
#27069=CARTESIAN_POINT('Ctrl Pts',(21.5991514590852,-0.599514507369841,
4.05817681218572));
#27070=CARTESIAN_POINT('Ctrl Pts',(21.5911988197414,-0.581076602684875,
4.15859434994728));
#27071=CARTESIAN_POINT('Ctrl Pts',(21.5832461803976,-0.539708616728004,
4.24845597739434));
#27072=CARTESIAN_POINT('Ctrl Pts',(21.5752935410538,-0.498340630771147,
4.33831760484137));
#27073=CARTESIAN_POINT('Ctrl Pts',(21.56734090171,-0.434042563542403,4.41762332197391));
#27074=CARTESIAN_POINT('Ctrl Pts',(21.5593882623662,-0.354675729482573,
4.47667692475034));
#27075=CARTESIAN_POINT('Ctrl Pts',(21.5514356230224,-0.275308895422716,
4.53573052752678));
#27076=CARTESIAN_POINT('Ctrl Pts',(21.5434829836786,-0.180873294531764,
4.57453201594709));
#27077=CARTESIAN_POINT('Ctrl Pts',(21.5355303443348,-0.0829149652056982,
4.58833737958621));
#27078=CARTESIAN_POINT('Ctrl Pts',(21.533302033309,-0.055467269432644,4.59220561033096));
#27079=CARTESIAN_POINT('Ctrl Pts',(21.5310737222833,-0.0277430016607059,
4.5941113769453));
#27080=CARTESIAN_POINT('Ctrl Pts',(21.5288454112575,-1.51073027558624E-5,
4.59408477831653));
#27081=CARTESIAN_POINT('Ctrl Pts',(21.4211545887425,1.51733402061755E-5,
4.59410821609125));
#27082=CARTESIAN_POINT('Ctrl Pts',(21.4274824194841,-0.0787159889745399,
4.59402654867773));
#27083=CARTESIAN_POINT('Ctrl Pts',(21.4338102502257,-0.15747883181342,4.57828382012605));
#27084=CARTESIAN_POINT('Ctrl Pts',(21.4401380809673,-0.230053504748576,
4.54780575811717));
#27085=CARTESIAN_POINT('Ctrl Pts',(21.4480907203111,-0.321263308378747,
4.50950178872359));
#27086=CARTESIAN_POINT('Ctrl Pts',(21.4560433596549,-0.402699049862651,
4.44792372259427));
#27087=CARTESIAN_POINT('Ctrl Pts',(21.4639959989987,-0.464404100671371,
4.37060031698995));
#27088=CARTESIAN_POINT('Ctrl Pts',(21.4719486383425,-0.526109151480106,
4.2932769113856));
#27089=CARTESIAN_POINT('Ctrl Pts',(21.4799012776864,-0.568083511613643,
4.20020816630624));
#27090=CARTESIAN_POINT('Ctrl Pts',(21.4878539170302,-0.585195243866348,
4.10277300340868));
#27091=CARTESIAN_POINT('Ctrl Pts',(21.495806556374,-0.602306976119048,4.00533784051114));
#27092=CARTESIAN_POINT('Ctrl Pts',(21.5037591957178,-0.594556080490919,
3.90353625979537));
#27093=CARTESIAN_POINT('Ctrl Pts',(21.5117118350616,-0.562890209537588,
3.80981489101362));
#27094=CARTESIAN_POINT('Ctrl Pts',(21.5196644744054,-0.53122433858425,3.71609352223184));
#27095=CARTESIAN_POINT('Ctrl Pts',(21.5276171137492,-0.47564349230572,3.63045236538409));
#27096=CARTESIAN_POINT('Ctrl Pts',(21.535569753093,-0.402943186155437,3.56336221830407));
#27097=CARTESIAN_POINT('Ctrl Pts',(21.5435223924368,-0.330242880005154,
3.49627207122406));
#27098=CARTESIAN_POINT('Ctrl Pts',(21.5514750317806,-0.24042311398314,3.44773293391182));
#27099=CARTESIAN_POINT('Ctrl Pts',(21.5594276711244,-0.144465577806233,
3.42367937699355));
#27100=CARTESIAN_POINT('Ctrl Pts',(21.5673803104682,-0.0485080416293372,
3.39962582007528));
#27101=CARTESIAN_POINT('Ctrl Pts',(21.575332949812,0.0535872647024426,3.40005784355098));
#27102=CARTESIAN_POINT('Ctrl Pts',(21.5832855891558,0.149337799479898,3.42492262666669));
#27103=CARTESIAN_POINT('Ctrl Pts',(21.5912382284996,0.245088334257342,3.44978740978241));
#27104=CARTESIAN_POINT('Ctrl Pts',(21.5991908678434,0.33449409748049,3.49908495253815));
#27105=CARTESIAN_POINT('Ctrl Pts',(21.6071435071872,0.406624016913212,3.56678795891296));
#27106=CARTESIAN_POINT('Ctrl Pts',(21.6150961465311,0.478753936345942,3.63449096528778));
#27107=CARTESIAN_POINT('Ctrl Pts',(21.6230487858749,0.533608011988269,3.72059943528167));
#27108=CARTESIAN_POINT('Ctrl Pts',(21.6310014252187,0.564479585995414,3.81458543566408));
#27109=CARTESIAN_POINT('Ctrl Pts',(21.6389540645625,0.595351160002559,3.90857143604649));
#27110=CARTESIAN_POINT('Ctrl Pts',(21.6469067039063,0.602240232374519,4.0104349668174));
#27111=CARTESIAN_POINT('Ctrl Pts',(21.6548593432501,0.584304520186539,4.10772182398666));
#27112=CARTESIAN_POINT('Ctrl Pts',(21.6628119825939,0.566368807998562,4.2050086811559));
#27113=CARTESIAN_POINT('Ctrl Pts',(21.6707646219377,0.523608311250652,4.29771886472347));
#27114=CARTESIAN_POINT('Ctrl Pts',(21.6787172612815,0.461251083056512,4.37451729206089));
#27115=CARTESIAN_POINT('Ctrl Pts',(21.6866699006253,0.398893854862358,4.45131571939834));
#27116=CARTESIAN_POINT('Ctrl Pts',(21.6946225399691,0.316939895221968,4.51220239050563));
#27117=CARTESIAN_POINT('Ctrl Pts',(21.7025751793129,0.225409191891896,4.54973308058009));
#27118=CARTESIAN_POINT('Ctrl Pts',(21.7087683157894,0.15412944274098,4.5789601931952));
#27119=CARTESIAN_POINT('Ctrl Pts',(21.7149614522659,0.0770418275534371,
4.59402294959611));
#27120=CARTESIAN_POINT('Ctrl Pts',(21.7211545887425,-1.54601956517634E-5,
4.59410286710644));
#27121=CARTESIAN_POINT('Origin',(4.,0.,4.));
#27122=CARTESIAN_POINT('',(22.1288454112575,-1.19684274697274E-5,4.59413016891312));
#27123=CARTESIAN_POINT('',(22.0211545887425,1.20066176157995E-5,4.59406577061205));
#27124=CARTESIAN_POINT('',(4.,-7.27562663373442E-17,4.5941));
#27125=CARTESIAN_POINT('Ctrl Pts',(22.1288454112575,-1.19684274697274E-5,
4.59413016891312));
#27126=CARTESIAN_POINT('Ctrl Pts',(22.1219370665346,0.0859328098890183,
4.59405244111828));
#27127=CARTESIAN_POINT('Ctrl Pts',(22.1150287218117,0.171910584533005,4.57519344187135));
#27128=CARTESIAN_POINT('Ctrl Pts',(22.1081203770888,0.24987714748571,4.53905210772026));
#27129=CARTESIAN_POINT('Ctrl Pts',(22.100167737745,0.339629466009183,4.49744749656716));
#27130=CARTESIAN_POINT('Ctrl Pts',(22.0922150984012,0.418765494330909,4.4329406966096));
#27131=CARTESIAN_POINT('Ctrl Pts',(22.0842624590574,0.477609775176754,4.35341854270704));
#27132=CARTESIAN_POINT('Ctrl Pts',(22.0763098197136,0.536454056022584,4.2738963888045));
#27133=CARTESIAN_POINT('Ctrl Pts',(22.0683571803698,0.575006589392542,4.17935888095698));
#27134=CARTESIAN_POINT('Ctrl Pts',(22.060404541026,0.588553803007579,4.081364517074));
#27135=CARTESIAN_POINT('Ctrl Pts',(22.0524519016822,0.60210101662262,3.983370153191));
#27136=CARTESIAN_POINT('Ctrl Pts',(22.0444992623384,0.590642910482727,3.88191893327255));
#27137=CARTESIAN_POINT('Ctrl Pts',(22.0365466229946,0.55558039411957,3.78941465069146));
#27138=CARTESIAN_POINT('Ctrl Pts',(22.0285939836508,0.520517877756421,3.69691036811039));
#27139=CARTESIAN_POINT('Ctrl Pts',(22.020641344307,0.461850951170019,3.61335302286667));
#27140=CARTESIAN_POINT('Ctrl Pts',(22.0126887049632,0.386752445163155,3.5489586384446));
#27141=CARTESIAN_POINT('Ctrl Pts',(22.0047360656194,0.311653939156274,3.48456425402251));
#27142=CARTESIAN_POINT('Ctrl Pts',(21.9967834262756,0.220123853728924,3.43933283042207));
#27143=CARTESIAN_POINT('Ctrl Pts',(21.9888307869318,0.123352988439278,3.41879452521803));
#27144=CARTESIAN_POINT('Ctrl Pts',(21.980878147588,0.0265821231496428,3.398256220014));
#27145=CARTESIAN_POINT('Ctrl Pts',(21.9729255082441,-0.075429522002288,
3.40241103320635));
#27146=CARTESIAN_POINT('Ctrl Pts',(21.9649728689003,-0.170209634025949,
3.43075098229493));
#27147=CARTESIAN_POINT('Ctrl Pts',(21.9570202295565,-0.26498974604961,3.4590909313835));
#27148=CARTESIAN_POINT('Ctrl Pts',(21.9490675902127,-0.352538324945002,
3.5116160163683));
#27149=CARTESIAN_POINT('Ctrl Pts',(21.9411149508689,-0.422151364554475,
3.58190433023263));
#27150=CARTESIAN_POINT('Ctrl Pts',(21.9331623115251,-0.491764404163956,
3.65219264409696));
#27151=CARTESIAN_POINT('Ctrl Pts',(21.9252096721813,-0.543441904487514,
3.74024418684083));
#27152=CARTESIAN_POINT('Ctrl Pts',(21.9172570328375,-0.570865587277161,
3.83529345812586));
#27153=CARTESIAN_POINT('Ctrl Pts',(21.9093043934937,-0.598289270066803,
3.93034272941087));
#27154=CARTESIAN_POINT('Ctrl Pts',(21.9013517541499,-0.601459135322544,
4.03238972923704));
#27155=CARTESIAN_POINT('Ctrl Pts',(21.8933991148061,-0.579987623844179,
4.12895782202339));
#27156=CARTESIAN_POINT('Ctrl Pts',(21.8854464754623,-0.558516112365809,
4.22552591480976));
#27157=CARTESIAN_POINT('Ctrl Pts',(21.8774938361185,-0.512403224153321,
4.31661510055631));
#27158=CARTESIAN_POINT('Ctrl Pts',(21.8695411967747,-0.447286887835617,
4.39108848569571));
#27159=CARTESIAN_POINT('Ctrl Pts',(21.8615885574308,-0.38217055151792,4.46556187083511));
#27160=CARTESIAN_POINT('Ctrl Pts',(21.853635918087,-0.298050767095013,4.52341945536736));
#27161=CARTESIAN_POINT('Ctrl Pts',(21.8456832787432,-0.205212323901057,
4.55758736157894));
#27162=CARTESIAN_POINT('Ctrl Pts',(21.840070656248,-0.139691040693493,4.58170156451555));
#27163=CARTESIAN_POINT('Ctrl Pts',(21.8344580337528,-0.0698270680627233,
4.59401614113532));
#27164=CARTESIAN_POINT('Ctrl Pts',(21.8288454112575,1.47252919898561E-5,
4.59408074293421));
#27165=CARTESIAN_POINT('Ctrl Pts',(21.7211545887425,-1.54601956517634E-5,
4.59410286710644));
#27166=CARTESIAN_POINT('Ctrl Pts',(21.7229140916097,-0.0219078436841643,
4.59412557209431));
#27167=CARTESIAN_POINT('Ctrl Pts',(21.724673594477,-0.0437977792686499,
4.59293892497318));
#27168=CARTESIAN_POINT('Ctrl Pts',(21.7264330973443,-0.0655513867134097,
4.59052415646896));
#27169=CARTESIAN_POINT('Ctrl Pts',(21.7343857366881,-0.163873814968881,
4.57960983324176));
#27170=CARTESIAN_POINT('Ctrl Pts',(21.742338376032,-0.259411224460086,4.54360647774573));
#27171=CARTESIAN_POINT('Ctrl Pts',(21.7502910153758,-0.340482865683332,
4.48691599054611));
#27172=CARTESIAN_POINT('Ctrl Pts',(21.7582436547196,-0.421554506906578,
4.4302255033465));
#27173=CARTESIAN_POINT('Ctrl Pts',(21.7661962940634,-0.488160379861865,
4.3528478844433));
#27174=CARTESIAN_POINT('Ctrl Pts',(21.7741489334072,-0.532157009426634,
4.26424360160945));
#27175=CARTESIAN_POINT('Ctrl Pts',(21.782101572751,-0.576153638991403,4.1756393187756));
#27176=CARTESIAN_POINT('Ctrl Pts',(21.7900542120948,-0.597541025165654,
4.0758083720111));
#27177=CARTESIAN_POINT('Ctrl Pts',(21.7980068514386,-0.593704268699233,
3.9769564542281));
#27178=CARTESIAN_POINT('Ctrl Pts',(21.8059594907824,-0.589867512232813,
3.87810453644509));
#27179=CARTESIAN_POINT('Ctrl Pts',(21.8139121301262,-0.560806613125721,
3.78023164764359));
#27180=CARTESIAN_POINT('Ctrl Pts',(21.82186476947,-0.510074662095298,3.69530408148155));
#27181=CARTESIAN_POINT('Ctrl Pts',(21.8298174088138,-0.459342711064876,
3.61037651531951));
#27182=CARTESIAN_POINT('Ctrl Pts',(21.8377700481576,-0.386939708111122,
3.53839427179695));
#27183=CARTESIAN_POINT('Ctrl Pts',(21.8457226875014,-0.301717906454235,
3.48815816056295));
#27184=CARTESIAN_POINT('Ctrl Pts',(21.8536753268452,-0.216496104797349,
3.43792204932895));
#27185=CARTESIAN_POINT('Ctrl Pts',(21.8616279661891,-0.118455504437329,
3.40943207038352));
#27186=CARTESIAN_POINT('Ctrl Pts',(21.8695806055329,-0.0195829040543552,
3.40617151167847));
#27187=CARTESIAN_POINT('Ctrl Pts',(21.8775332448767,0.0792896963286298,
3.40291095297342));
#27188=CARTESIAN_POINT('Ctrl Pts',(21.8854858842205,0.178994296734569,3.42487981450875));
#27189=CARTESIAN_POINT('Ctrl Pts',(21.8934385235643,0.267340651814441,3.46939210375187));
#27190=CARTESIAN_POINT('Ctrl Pts',(21.9013911629081,0.355687006894294,3.51390439299499));
#27191=CARTESIAN_POINT('Ctrl Pts',(21.9093438022519,0.432675116648084,3.58096010994589));
#27192=CARTESIAN_POINT('Ctrl Pts',(21.9172964415957,0.488892136101412,3.66236077992681));
#27193=CARTESIAN_POINT('Ctrl Pts',(21.9252490809395,0.545109155554752,3.74376144990775));
#27194=CARTESIAN_POINT('Ctrl Pts',(21.9332017202833,0.580555084707621,3.8395070729187));
#27195=CARTESIAN_POINT('Ctrl Pts',(21.9411543596271,0.590896175957217,3.93789144251738));
#27196=CARTESIAN_POINT('Ctrl Pts',(21.9491069989709,0.601237267206812,4.03627581211605));
#27197=CARTESIAN_POINT('Ctrl Pts',(21.9570596383147,0.58647352055314,4.13729892830245));
#27198=CARTESIAN_POINT('Ctrl Pts',(21.9650122776585,0.548410005102802,4.22860933921557));
#27199=CARTESIAN_POINT('Ctrl Pts',(21.9729649170023,0.510346489652465,4.31991975012869));
#27200=CARTESIAN_POINT('Ctrl Pts',(21.9809175563462,0.448983205405461,4.40151745576853));
#27201=CARTESIAN_POINT('Ctrl Pts',(21.98887019569,0.371822649612145,4.46342602528218));
#27202=CARTESIAN_POINT('Ctrl Pts',(21.9968228350338,0.29466209381883,4.52533459479583));
#27203=CARTESIAN_POINT('Ctrl Pts',(22.0047754743776,0.201704266479203,4.5675540281833));
#27204=CARTESIAN_POINT('Ctrl Pts',(22.0127281137214,0.104314528045707,4.58492242469582));
#27205=CARTESIAN_POINT('Ctrl Pts',(22.0155369387284,0.069917050565085,4.59105683924014));
#27206=CARTESIAN_POINT('Ctrl Pts',(22.0183457637354,0.0349667096964542,
4.59409118517947));
#27207=CARTESIAN_POINT('Ctrl Pts',(22.0211545887425,1.20066176157995E-5,
4.59406577061205));
#27208=CARTESIAN_POINT('Origin',(4.,0.,4.));
#27209=CARTESIAN_POINT('',(22.4288454112575,5.18920962550018E-6,4.59405135764298));
#27210=CARTESIAN_POINT('',(22.3211545887424,-7.30827440488969E-6,4.59414400810326));
#27211=CARTESIAN_POINT('',(4.,-7.27562663373442E-17,4.5941));
#27212=CARTESIAN_POINT('Ctrl Pts',(22.4288454112575,5.18920962550018E-6,
4.59405135764298));
#27213=CARTESIAN_POINT('Ctrl Pts',(22.4253213780041,0.0438634191921666,
4.5940647188338));
#27214=CARTESIAN_POINT('Ctrl Pts',(22.4217973447507,0.0877187745911938,
4.589273164082));
#27215=CARTESIAN_POINT('Ctrl Pts',(22.4182733114973,0.130485535360993,4.57964583089408));
#27216=CARTESIAN_POINT('Ctrl Pts',(22.4103206721535,0.226996720088313,4.55791995512033));
#27217=CARTESIAN_POINT('Ctrl Pts',(22.4023680328097,0.317964089339764,4.51156722320365));
#27218=CARTESIAN_POINT('Ctrl Pts',(22.3944153934659,0.392265646131591,4.44625488916104));
#27219=CARTESIAN_POINT('Ctrl Pts',(22.3864627541221,0.4665672029234,4.38094255511845));
#27220=CARTESIAN_POINT('Ctrl Pts',(22.3785101147783,0.524202947255594,4.29667061894994));
#27221=CARTESIAN_POINT('Ctrl Pts',(22.3705574754345,0.558126122886914,4.20374247196213));
#27222=CARTESIAN_POINT('Ctrl Pts',(22.3626048360906,0.592049298518242,4.11081432497429));
#27223=CARTESIAN_POINT('Ctrl Pts',(22.3546521967468,0.602259905448686,4.00922996716717));
#27224=CARTESIAN_POINT('Ctrl Pts',(22.346699557403,0.587509558716917,3.91140947017845));
#27225=CARTESIAN_POINT('Ctrl Pts',(22.3387469180592,0.572759211985149,3.81358897318973));
#27226=CARTESIAN_POINT('Ctrl Pts',(22.3307942787154,0.533047911591167,3.71953233701942));
#27227=CARTESIAN_POINT('Ctrl Pts',(22.3228416393716,0.473230904440663,3.6407392662825));
#27228=CARTESIAN_POINT('Ctrl Pts',(22.3148890000278,0.413413897290173,3.5619461955456));
#27229=CARTESIAN_POINT('Ctrl Pts',(22.306936360684,0.333491183383171,3.49841669024209));
#27230=CARTESIAN_POINT('Ctrl Pts',(22.2989837213402,0.243234403245124,3.45791809774646));
#27231=CARTESIAN_POINT('Ctrl Pts',(22.2910310819964,0.152977623107077,3.41741950525082));
#27232=CARTESIAN_POINT('Ctrl Pts',(22.2830784426526,0.0523867767379842,
3.39995182556307));
#27233=CARTESIAN_POINT('Ctrl Pts',(22.2751258033088,-0.0462395349927855,
3.40765072037886));
#27234=CARTESIAN_POINT('Ctrl Pts',(22.267173163965,-0.144865846723578,3.41534961519466));
#27235=CARTESIAN_POINT('Ctrl Pts',(22.2592205246212,-0.241527623816046,
3.448215084514));
#27236=CARTESIAN_POINT('Ctrl Pts',(22.2512678852774,-0.324406647450603,
3.50222887712101));
#27237=CARTESIAN_POINT('Ctrl Pts',(22.2433152459336,-0.40728567108515,3.55624266972802));
#27238=CARTESIAN_POINT('Ctrl Pts',(22.2353626065897,-0.476381941261788,
3.63140478562268));
#27239=CARTESIAN_POINT('Ctrl Pts',(22.2274099672459,-0.523247497912515,
3.71852563243507));
#27240=CARTESIAN_POINT('Ctrl Pts',(22.2194573279021,-0.570113054563243,
3.80564647924745));
#27241=CARTESIAN_POINT('Ctrl Pts',(22.2115046885583,-0.59474789768806,3.90472605697756));
#27242=CARTESIAN_POINT('Ctrl Pts',(22.2035520492145,-0.594140082177443,
4.00365053781872));
#27243=CARTESIAN_POINT('Ctrl Pts',(22.1955994098707,-0.593532266666827,
4.10257501865988));
#27244=CARTESIAN_POINT('Ctrl Pts',(22.1876467705269,-0.567681792520777,
4.2013444026121));
#27245=CARTESIAN_POINT('Ctrl Pts',(22.1796941311831,-0.519749232289404,
4.2878827872712));
#27246=CARTESIAN_POINT('Ctrl Pts',(22.1717414918393,-0.471816672058032,
4.37442117193029));
#27247=CARTESIAN_POINT('Ctrl Pts',(22.1637888524955,-0.401802025741336,
4.44872855729627));
#27248=CARTESIAN_POINT('Ctrl Pts',(22.1558362131517,-0.318265537426909,
4.50171985346399));
#27249=CARTESIAN_POINT('Ctrl Pts',(22.1478835738079,-0.234729049112483,
4.55471114963171));
#27250=CARTESIAN_POINT('Ctrl Pts',(22.1399309344641,-0.137670718800326,
4.58638635660118));
#27251=CARTESIAN_POINT('Ctrl Pts',(22.1319782951203,-0.0389572492816432,
4.5928727489116));
#27252=CARTESIAN_POINT('Ctrl Pts',(22.1309340004994,-0.0259947671705595,
4.5937245044491));
#27253=CARTESIAN_POINT('Ctrl Pts',(22.1298897058784,-0.0130037447923657,
4.5941419185755));
#27254=CARTESIAN_POINT('Ctrl Pts',(22.1288454112575,-1.19684274697274E-5,
4.59413016891312));
#27255=CARTESIAN_POINT('Ctrl Pts',(22.0211545887425,1.20066176157995E-5,
4.59406577061205));
#27256=CARTESIAN_POINT('Ctrl Pts',(22.0262984030792,-0.064000704172389,
4.59401922879619));
#27257=CARTESIAN_POINT('Ctrl Pts',(22.031442217416,-0.128028044405449,4.5837112392356));
#27258=CARTESIAN_POINT('Ctrl Pts',(22.0365860317528,-0.188701337098646,
4.56338935830438));
#27259=CARTESIAN_POINT('Ctrl Pts',(22.0445386710966,-0.282505814282095,
4.53197053576284));
#27260=CARTESIAN_POINT('Ctrl Pts',(22.0524913104404,-0.368293119121642,
4.4766155310422));
#27261=CARTESIAN_POINT('Ctrl Pts',(22.0604439497842,-0.435574585201076,
4.40409224738955));
#27262=CARTESIAN_POINT('Ctrl Pts',(22.068396589128,-0.502856051280518,4.33156896373689));
#27263=CARTESIAN_POINT('Ctrl Pts',(22.0763492284718,-0.551631678599843,
4.24187740115222));
#27264=CARTESIAN_POINT('Ctrl Pts',(22.0843018678156,-0.575937982408454,
4.14598357473613));
#27265=CARTESIAN_POINT('Ctrl Pts',(22.0922545071594,-0.600244286217068,
4.05008974832002));
#27266=CARTESIAN_POINT('Ctrl Pts',(22.1002071465032,-0.600081266514962,
3.94799365807249));
#27267=CARTESIAN_POINT('Ctrl Pts',(22.1081597858471,-0.575468854681199,
3.85217794154701));
#27268=CARTESIAN_POINT('Ctrl Pts',(22.1161124251909,-0.550856442847438,
3.75636222502155));
#27269=CARTESIAN_POINT('Ctrl Pts',(22.1240650645347,-0.501794638882025,
3.66682688221814));
#27270=CARTESIAN_POINT('Ctrl Pts',(22.1320177038785,-0.434281916527717,
3.5945188282416));
#27271=CARTESIAN_POINT('Ctrl Pts',(22.1399703432223,-0.366769194173409,
3.52221077426505));
#27272=CARTESIAN_POINT('Ctrl Pts',(22.1479229825661,-0.280805553430205,
3.46713000911538));
#27273=CARTESIAN_POINT('Ctrl Pts',(22.1558756219099,-0.186901220180937,
3.43601090651668));
#27274=CARTESIAN_POINT('Ctrl Pts',(22.1638282612537,-0.0929968869316588,
3.40489180391798));
#27275=CARTESIAN_POINT('Ctrl Pts',(22.1717809005975,0.00884813882368474,
3.39773436387026));
#27276=CARTESIAN_POINT('Ctrl Pts',(22.1797335399413,0.106181915586414,3.41541368090248));
#27277=CARTESIAN_POINT('Ctrl Pts',(22.1876861792851,0.203515692349121,3.4330929979347));
#27278=CARTESIAN_POINT('Ctrl Pts',(22.1956388186289,0.296338220119215,3.47560907204686));
#27279=CARTESIAN_POINT('Ctrl Pts',(22.2035914579727,0.373300680656879,3.53776373412001));
#27280=CARTESIAN_POINT('Ctrl Pts',(22.2115440973165,0.450263141194552,3.59991839619317));
#27281=CARTESIAN_POINT('Ctrl Pts',(22.2194967366603,0.511365534499791,3.68171164622733));
#27282=CARTESIAN_POINT('Ctrl Pts',(22.2274493760041,0.549137260797828,3.7731431454068));
#27283=CARTESIAN_POINT('Ctrl Pts',(22.2354020153479,0.586908987095865,3.86457464458628));
#27284=CARTESIAN_POINT('Ctrl Pts',(22.2433546546918,0.6013500463867,3.96564439291107));
#27285=CARTESIAN_POINT('Ctrl Pts',(22.2513072940356,0.590694822479903,4.06399523710107));
#27286=CARTESIAN_POINT('Ctrl Pts',(22.2592599333794,0.580039598573106,4.16234608129106));
#27287=CARTESIAN_POINT('Ctrl Pts',(22.2672125727232,0.544288091468676,4.25797802134625));
#27288=CARTESIAN_POINT('Ctrl Pts',(22.275165212067,0.487811409852587,4.33919875012361));
#27289=CARTESIAN_POINT('Ctrl Pts',(22.2831178514108,0.431334728236497,4.42041947890096));
#27290=CARTESIAN_POINT('Ctrl Pts',(22.2910704907546,0.354132872108749,4.48722899640046));
#27291=CARTESIAN_POINT('Ctrl Pts',(22.2990231300984,0.265644819817582,4.53145892916239));
#27292=CARTESIAN_POINT('Ctrl Pts',(22.3064002829798,0.183560135512932,4.57248819778762));
#27293=CARTESIAN_POINT('Ctrl Pts',(22.3137774358611,0.0917635873240076,
4.59408754951618));
#27294=CARTESIAN_POINT('Ctrl Pts',(22.3211545887424,-7.30827440488969E-6,
4.59414400810326));
#27295=CARTESIAN_POINT('Origin',(4.,0.,4.));
#27296=CARTESIAN_POINT('',(22.7288454112575,-7.11440487624268E-7,4.59414971000239));
#27297=CARTESIAN_POINT('',(22.6211545887425,-1.51245797256638E-7,4.59404869726453));
#27298=CARTESIAN_POINT('',(4.,-7.27562663373442E-17,4.5941));
#27299=CARTESIAN_POINT('Ctrl Pts',(22.7288454112575,-7.11440487624268E-7,
4.59414971000239));
#27300=CARTESIAN_POINT('Ctrl Pts',(22.7287056894736,0.0017373052546791,
4.59414999869406));
#27301=CARTESIAN_POINT('Ctrl Pts',(22.7285659676897,0.0034753215591825,
4.59414251282321));
#27302=CARTESIAN_POINT('Ctrl Pts',(22.7284262459057,0.00521327185949689,
4.59412723628209));
#27303=CARTESIAN_POINT('Ctrl Pts',(22.7204736065619,0.104133365400505,4.59325773105135));
#27304=CARTESIAN_POINT('Ctrl Pts',(22.7125209672181,0.202839630323109,4.56714939948764));
#27305=CARTESIAN_POINT('Ctrl Pts',(22.7045683278743,0.289252680684759,4.51898953373575));
#27306=CARTESIAN_POINT('Ctrl Pts',(22.6966156885305,0.375665731046408,4.47082966798385));
#27307=CARTESIAN_POINT('Ctrl Pts',(22.6886630491867,0.449785566847107,4.40061826804377));
#27308=CARTESIAN_POINT('Ctrl Pts',(22.6807104098429,0.502555912967013,4.31694216252228));
#27309=CARTESIAN_POINT('Ctrl Pts',(22.6727577704991,0.555326259086918,4.23326605700079));
#27310=CARTESIAN_POINT('Ctrl Pts',(22.6648051311553,0.586747115526033,4.13612524589788));
#27311=CARTESIAN_POINT('Ctrl Pts',(22.6568524918115,0.592973744123511,4.03739517928057));
#27312=CARTESIAN_POINT('Ctrl Pts',(22.6488998524677,0.59920037272099,3.93866511266326));
#27313=CARTESIAN_POINT('Ctrl Pts',(22.6409472131239,0.580232773476834,3.83834579053153));
#27314=CARTESIAN_POINT('Ctrl Pts',(22.6329945737801,0.538391640361539,3.74870332422701));
#27315=CARTESIAN_POINT('Ctrl Pts',(22.6250419344363,0.496550507246239,3.65906085792248));
#27316=CARTESIAN_POINT('Ctrl Pts',(22.6170892950925,0.431835840259791,3.58009524744515));
#27317=CARTESIAN_POINT('Ctrl Pts',(22.6091366557487,0.35215901686313,3.52146073929621));
#27318=CARTESIAN_POINT('Ctrl Pts',(22.6011840164048,0.272482193466486,3.46282623114728));
#27319=CARTESIAN_POINT('Ctrl Pts',(22.593231377061,0.17784321365963,3.42452282532672));
#27320=CARTESIAN_POINT('Ctrl Pts',(22.5852787377172,0.0798134434713266,
3.41123383340666));
#27321=CARTESIAN_POINT('Ctrl Pts',(22.5773260983734,-0.0182163267169884,
3.3979448414866));
#27322=CARTESIAN_POINT('Ctrl Pts',(22.5693734590296,-0.119636887286728,
3.40967026346704));
#27323=CARTESIAN_POINT('Ctrl Pts',(22.5614208196858,-0.212048437952692,
3.44497640167274));
#27324=CARTESIAN_POINT('Ctrl Pts',(22.553468180342,-0.304459988618666,3.48028253987845));
#27325=CARTESIAN_POINT('Ctrl Pts',(22.5455155409982,-0.387862529380837,
3.53916939430943));
#27326=CARTESIAN_POINT('Ctrl Pts',(22.5375629016544,-0.452058834188948,
3.61443730067171));
#27327=CARTESIAN_POINT('Ctrl Pts',(22.5296102623106,-0.516255138997059,
3.689705207034));
#27328=CARTESIAN_POINT('Ctrl Pts',(22.5216576229668,-0.561245207851117,
3.7813541653276));
#27329=CARTESIAN_POINT('Ctrl Pts',(22.513704983623,-0.581528460676763,3.87817881267738));
#27330=CARTESIAN_POINT('Ctrl Pts',(22.5057523442792,-0.601811713502406,
3.97500346002715));
#27331=CARTESIAN_POINT('Ctrl Pts',(22.4977997049354,-0.597388150299644,
4.07700379643311));
#27332=CARTESIAN_POINT('Ctrl Pts',(22.4898470655916,-0.568798575589296,
4.17170890717095));
#27333=CARTESIAN_POINT('Ctrl Pts',(22.4818944262477,-0.540209000878948,
4.26641401790879));
#27334=CARTESIAN_POINT('Ctrl Pts',(22.4739417869039,-0.487453414661012,
4.35382390297851));
#27335=CARTESIAN_POINT('Ctrl Pts',(22.4659891475601,-0.416981925106977,
4.42325150516024));
#27336=CARTESIAN_POINT('Ctrl Pts',(22.4580365082163,-0.346510435552941,
4.49267910734197));
#27337=CARTESIAN_POINT('Ctrl Pts',(22.4500838688725,-0.258323042662803,
4.54412442663572));
#27338=CARTESIAN_POINT('Ctrl Pts',(22.4421312295287,-0.163201846116148,
4.57129757646718));
#27339=CARTESIAN_POINT('Ctrl Pts',(22.4377026234383,-0.11023146834083,4.58642955613285));
#27340=CARTESIAN_POINT('Ctrl Pts',(22.4332740173479,-0.0551108697057404,
4.59403456681078));
#27341=CARTESIAN_POINT('Ctrl Pts',(22.4288454112575,5.18920962550018E-6,
4.59405135764298));
#27342=CARTESIAN_POINT('Ctrl Pts',(22.3211545887424,-7.30827440488969E-6,
4.59414400810326));
#27343=CARTESIAN_POINT('Ctrl Pts',(22.3217300752049,-0.00716629073194701,
4.59414841239758));
#27344=CARTESIAN_POINT('Ctrl Pts',(22.3223055616673,-0.0143251170819474,
4.59402171850555));
#27345=CARTESIAN_POINT('Ctrl Pts',(22.3228810481298,-0.0214791647150919,
4.59376292335171));
#27346=CARTESIAN_POINT('Ctrl Pts',(22.3308336874736,-0.120340848501978,
4.59018663675477));
#27347=CARTESIAN_POINT('Ctrl Pts',(22.3387863268174,-0.218289967621164,
4.56138371553656));
#27348=CARTESIAN_POINT('Ctrl Pts',(22.3467389661612,-0.303350908332583,
4.51087570903952));
#27349=CARTESIAN_POINT('Ctrl Pts',(22.3546916055051,-0.388411849044011,
4.46036770254246));
#27350=CARTESIAN_POINT('Ctrl Pts',(22.3626442448489,-0.460584611347669,
4.38815461076656));
#27351=CARTESIAN_POINT('Ctrl Pts',(22.3705968841927,-0.511045091866278,
4.3030654678256));
#27352=CARTESIAN_POINT('Ctrl Pts',(22.3785495235365,-0.561505572384874,
4.21797632488466));
#27353=CARTESIAN_POINT('Ctrl Pts',(22.3865021628803,-0.590253771118432,
4.12001113077866));
#27354=CARTESIAN_POINT('Ctrl Pts',(22.3944548022241,-0.593774829630164,
4.02114746451658));
#27355=CARTESIAN_POINT('Ctrl Pts',(22.4024074415679,-0.597295888141896,
3.92228379825449));
#27356=CARTESIAN_POINT('Ctrl Pts',(22.4103600809117,-0.575589806431797,
3.82252165983632));
#27357=CARTESIAN_POINT('Ctrl Pts',(22.4183127202555,-0.531310447862662,
3.73405832985033));
#27358=CARTESIAN_POINT('Ctrl Pts',(22.4262653595993,-0.487031089293526,
3.64559499986435));
#27359=CARTESIAN_POINT('Ctrl Pts',(22.4342179989431,-0.420178453865353,
3.56843047831055));
#27360=CARTESIAN_POINT('Ctrl Pts',(22.4421706382869,-0.338926188203527,
3.51199917808983));
#27361=CARTESIAN_POINT('Ctrl Pts',(22.4501232776307,-0.257673922541701,
3.45556787786912));
#27362=CARTESIAN_POINT('Ctrl Pts',(22.4580759169745,-0.162022026646223,
3.41986979898149));
#27363=CARTESIAN_POINT('Ctrl Pts',(22.4660285563183,-0.0636652448434586,
3.40926951931498));
#27364=CARTESIAN_POINT('Ctrl Pts',(22.4739811956621,0.0346915369593057,
3.39866923964846));
#27365=CARTESIAN_POINT('Ctrl Pts',(22.4819338350059,0.135753204669356,3.41316675920307));
#27366=CARTESIAN_POINT('Ctrl Pts',(22.4898864743497,0.227163587879617,3.45098955584192));
#27367=CARTESIAN_POINT('Ctrl Pts',(22.4978391136936,0.318573971089878,3.48881235248077));
#27368=CARTESIAN_POINT('Ctrl Pts',(22.5057917530374,0.40033306980035,3.54996042620388));
#27369=CARTESIAN_POINT('Ctrl Pts',(22.5137443923812,0.462444730281743,3.62695759769032));
#27370=CARTESIAN_POINT('Ctrl Pts',(22.521697031725,0.524556390763143,3.70395476917678));
#27371=CARTESIAN_POINT('Ctrl Pts',(22.5296496710688,0.567020613015458,3.79680103842659));
#27372=CARTESIAN_POINT('Ctrl Pts',(22.5376023104126,0.584645549343987,3.89414467407578));
#27373=CARTESIAN_POINT('Ctrl Pts',(22.5455549497564,0.602270485672515,3.99148830972497));
#27374=CARTESIAN_POINT('Ctrl Pts',(22.5535075891002,0.595056136077256,4.09332931177355));
#27375=CARTESIAN_POINT('Ctrl Pts',(22.561460228444,0.563884587368514,4.18721625032571));
#27376=CARTESIAN_POINT('Ctrl Pts',(22.5694128677878,0.532713038659782,4.28110318887784));
#27377=CARTESIAN_POINT('Ctrl Pts',(22.5773655071316,0.477584290837583,4.36703606393356));
#27378=CARTESIAN_POINT('Ctrl Pts',(22.5853181464754,0.405238519368296,4.43450837402952));
#27379=CARTESIAN_POINT('Ctrl Pts',(22.5932707858192,0.332892747898984,4.5019806841255));
#27380=CARTESIAN_POINT('Ctrl Pts',(22.601223425163,0.24332995278257,4.55099242926169));
#27381=CARTESIAN_POINT('Ctrl Pts',(22.6091760645068,0.14750052788588,4.57555132613148));
#27382=CARTESIAN_POINT('Ctrl Pts',(22.6131689059187,0.0993867282199646,
4.58788179608141));
#27383=CARTESIAN_POINT('Ctrl Pts',(22.6171617473306,0.0496932250345643,
4.5940481472271));
#27384=CARTESIAN_POINT('Ctrl Pts',(22.6211545887425,-1.51173456864708E-7,
4.59404872180247));
#27385=CARTESIAN_POINT('Origin',(3.42660065607856,0.,4.));
#27386=CARTESIAN_POINT('',(22.7766006560786,-4.98014040841517E-7,4.41590979742004));
#27387=CARTESIAN_POINT('',(22.8,4.87367679877478E-13,4.415875));
#27388=CARTESIAN_POINT('',(3.42660065607856,4.87367679877478E-13,4.415875));
#27389=CARTESIAN_POINT('',(22.8,-0.195748955928421,4.36692555359082));
#27390=CARTESIAN_POINT('Ctrl Pts',(22.7766006560786,-4.98014040834069E-7,
4.41590979742004));
#27391=CARTESIAN_POINT('Ctrl Pts',(22.7844004373857,-0.0679170312443507,
4.41589851620688));
#27392=CARTESIAN_POINT('Ctrl Pts',(22.7922002186928,-0.135834416676695,
4.39892762624317));
#27393=CARTESIAN_POINT('Ctrl Pts',(22.8,-0.195762566582618,4.36695865185838));
#27394=CARTESIAN_POINT('Origin',(22.8,0.,4.));
#27395=CARTESIAN_POINT('Origin',(3.42660065607856,0.,4.));
#27396=CARTESIAN_POINT('',(22.4766006560785,3.63249072247605E-6,4.41584094994071));
#27397=CARTESIAN_POINT('',(22.5733993439214,-1.05822049303872E-7,4.41583910483016));
#27398=CARTESIAN_POINT('',(3.42660065607856,4.87367679877478E-13,4.415875));
#27399=CARTESIAN_POINT('Ctrl Pts',(22.4766006560785,3.63249072248342E-6,
4.41584094994071));
#27400=CARTESIAN_POINT('Ctrl Pts',(22.4810292621689,-0.0385780726118879,
4.41582919621688));
#27401=CARTESIAN_POINT('Ctrl Pts',(22.4934105076031,-0.146451497349971,
4.40094585736882));
#27402=CARTESIAN_POINT('Ctrl Pts',(22.5137443923812,-0.304292138366774,
4.30886736509782));
#27403=CARTESIAN_POINT('Ctrl Pts',(22.5376023104126,-0.415080201412036,
4.12530439950267));
#27404=CARTESIAN_POINT('Ctrl Pts',(22.561460228444,-0.424369795825249,3.91110111771763));
#27405=CARTESIAN_POINT('Ctrl Pts',(22.5853181464754,-0.329889515310188,
3.71863599132299));
#27406=CARTESIAN_POINT('Ctrl Pts',(22.6091760645068,-0.154742073939436,
3.59497211022641));
#27407=CARTESIAN_POINT('Ctrl Pts',(22.6330339825383,0.0582436639512456,
3.57034842802071));
#27408=CARTESIAN_POINT('Ctrl Pts',(22.6568919005697,0.256987911016647,3.65078654733876));
#27409=CARTESIAN_POINT('Ctrl Pts',(22.6807498186011,0.39289034562191,3.81661632308649));
#27410=CARTESIAN_POINT('Ctrl Pts',(22.7046077366325,0.432722782933869,4.02728943245291));
#27411=CARTESIAN_POINT('Ctrl Pts',(22.7284656546639,0.366738191089385,4.2312875884069));
#27412=CARTESIAN_POINT('Ctrl Pts',(22.7523235726953,0.211084664509997,4.37873330099785));
#27413=CARTESIAN_POINT('Ctrl Pts',(22.7683685731669,0.0716802821347026,
4.41560650088387));
#27414=CARTESIAN_POINT('Ctrl Pts',(22.7764609342946,0.00121612829983627,
4.41590999950663));
#27415=CARTESIAN_POINT('Ctrl Pts',(22.7766006560786,-4.98014040834069E-7,
4.41590979742004));
#27416=CARTESIAN_POINT('',(22.8,0.415641328671541,4.01393920819689));
#27417=CARTESIAN_POINT('Origin',(22.8,0.,4.));
#27418=CARTESIAN_POINT('Ctrl Pts',(22.5733993439214,-1.0582204931428E-7,
4.41583910483016));
#27419=CARTESIAN_POINT('Ctrl Pts',(22.5773591418533,-0.034498011376554,
4.41583950370926));
#27420=CARTESIAN_POINT('Ctrl Pts',(22.5892715791291,-0.138279341065089,
4.40307041914735));
#27421=CARTESIAN_POINT('Ctrl Pts',(22.6091366557487,-0.295063722636797,
4.31769517074077));
#27422=CARTESIAN_POINT('Ctrl Pts',(22.6329945737801,-0.411209141905604,
4.13747522778479));
#27423=CARTESIAN_POINT('Ctrl Pts',(22.6568524918115,-0.426804986482714,
3.92363755172126));
#27424=CARTESIAN_POINT('Ctrl Pts',(22.6807104098429,-0.33803111495158,3.72847502015617));
#27425=CARTESIAN_POINT('Ctrl Pts',(22.7045683278743,-0.16660749730952,3.59970312177549));
#27426=CARTESIAN_POINT('Ctrl Pts',(22.7284262459057,0.0455714674079685,
3.56882345794434));
#27427=CARTESIAN_POINT('Ctrl Pts',(22.7522841639372,0.246577802732478,3.64336153500176));
#27428=CARTESIAN_POINT('Ctrl Pts',(22.7761420819686,0.387346815298129,3.80514019809748));
#27429=CARTESIAN_POINT('Ctrl Pts',(22.7920473606562,0.417963038852713,3.94471011778788));
#27430=CARTESIAN_POINT('Ctrl Pts',(22.8,0.415641328671541,4.01393920819689));
#27431=CARTESIAN_POINT('Origin',(3.42660065607856,0.,4.));
#27432=CARTESIAN_POINT('',(22.1766006560786,-8.37799962078257E-6,4.41589611849309));
#27433=CARTESIAN_POINT('',(22.2733993439214,-5.11585294796223E-6,4.41590580604266));
#27434=CARTESIAN_POINT('',(3.42660065607856,4.87367679877478E-13,4.415875));
#27435=CARTESIAN_POINT('Ctrl Pts',(22.1766006560786,-8.37799962077716E-6,
4.41589611849309));
#27436=CARTESIAN_POINT('Ctrl Pts',(22.1776449506995,-0.0091027307950905,
4.41590434335565));
#27437=CARTESIAN_POINT('Ctrl Pts',(22.1866418846642,-0.0874489573854402,
4.4133870032437));
#27438=CARTESIAN_POINT('Ctrl Pts',(22.2035914579727,-0.232253957950086,
4.36612956178204));
#27439=CARTESIAN_POINT('Ctrl Pts',(22.2274493760041,-0.379286482964224,
4.21008217638027));
#27440=CARTESIAN_POINT('Ctrl Pts',(22.2513072940356,-0.433573131350875,
4.00266397632408));
#27441=CARTESIAN_POINT('Ctrl Pts',(22.275165212067,-0.381839338801546,3.79459436150246));
#27442=CARTESIAN_POINT('Ctrl Pts',(22.2990231300984,-0.236735426869051,
3.63675202040985));
#27443=CARTESIAN_POINT('Ctrl Pts',(22.3228810481298,-0.0337432544318164,
3.56773370504276));
#27444=CARTESIAN_POINT('Ctrl Pts',(22.3467389661613,0.177500062688638,3.60441627341574));
#27445=CARTESIAN_POINT('Ctrl Pts',(22.3705968841926,0.345339779804043,3.73782983856348));
#27446=CARTESIAN_POINT('Ctrl Pts',(22.3944548022241,0.428734513273282,3.93535114928888));
#27447=CARTESIAN_POINT('Ctrl Pts',(22.4183127202555,0.407291980919218,4.1486808655136));
#27448=CARTESIAN_POINT('Ctrl Pts',(22.4421706382869,0.286255462618544,4.32565405918856));
#27449=CARTESIAN_POINT('Ctrl Pts',(22.4615999502279,0.130682174689606,4.40492695636159));
#27450=CARTESIAN_POINT('Ctrl Pts',(22.4730766228251,0.0307047625933256,
4.41585030288671));
#27451=CARTESIAN_POINT('Ctrl Pts',(22.4766006560785,3.63249072248342E-6,
4.41584094994071));
#27452=CARTESIAN_POINT('Ctrl Pts',(22.2733993439214,-5.11585294797612E-6,
4.41590580604266));
#27453=CARTESIAN_POINT('Ctrl Pts',(22.2739748303838,-0.0050164638240448,
4.41590888908576));
#27454=CARTESIAN_POINT('Ctrl Pts',(22.2825029561901,-0.0792779396689182,
4.41459464077989));
#27455=CARTESIAN_POINT('Ctrl Pts',(22.2989837213402,-0.221370022215225,
4.37281103827166));
#27456=CARTESIAN_POINT('Ctrl Pts',(22.3228416393716,-0.372934645290675,
4.22116172228637));
#27457=CARTESIAN_POINT('Ctrl Pts',(22.346699557403,-0.43330658847365,4.01543234121164));
#27458=CARTESIAN_POINT('Ctrl Pts',(22.3705574754345,-0.387723268841402,
3.80592933171158));
#27459=CARTESIAN_POINT('Ctrl Pts',(22.3944153934659,-0.247331046528593,
3.64388188817752));
#27460=CARTESIAN_POINT('Ctrl Pts',(22.4182733114973,-0.0464596501027702,
3.56891502119853));
#27461=CARTESIAN_POINT('Ctrl Pts',(22.4421312295287,0.165772403721094,3.59936017830047));
#27462=CARTESIAN_POINT('Ctrl Pts',(22.4659891475602,0.337468575289321,3.7277726770023));
#27463=CARTESIAN_POINT('Ctrl Pts',(22.4898470655915,0.426644514167594,3.92275218663495));
#27464=CARTESIAN_POINT('Ctrl Pts',(22.513704983623,0.411494197867752,4.13662086224655));
#27465=CARTESIAN_POINT('Ctrl Pts',(22.5375629016544,0.295722435535401,4.31708206952049));
#27466=CARTESIAN_POINT('Ctrl Pts',(22.5574610217539,0.138855410360913,4.40292493148274));
#27467=CARTESIAN_POINT('Ctrl Pts',(22.5694065025095,0.0347856757474044,
4.41583870262252));
#27468=CARTESIAN_POINT('Ctrl Pts',(22.5733993439214,-1.0582204931428E-7,
4.41583910483016));
#27469=CARTESIAN_POINT('Origin',(3.42660065607856,0.,4.));
#27470=CARTESIAN_POINT('',(21.8766006560786,1.03078286340212E-5,4.41586151989188));
#27471=CARTESIAN_POINT('',(21.9733993439214,8.40473402259622E-6,4.41585103914036));
#27472=CARTESIAN_POINT('',(3.42660065607856,4.87367679877478E-13,4.415875));
#27473=CARTESIAN_POINT('Ctrl Pts',(21.8766006560786,1.03078286340201E-5,
4.41586151989188));
#27474=CARTESIAN_POINT('Ctrl Pts',(21.8822132785738,-0.0488795353146484,
4.415816298089));
#27475=CARTESIAN_POINT('Ctrl Pts',(21.8957785404128,-0.167079919178725,
4.39498170153279));
#27476=CARTESIAN_POINT('Ctrl Pts',(21.9172964415957,-0.326407159500644,
4.28539643168872));
#27477=CARTESIAN_POINT('Ctrl Pts',(21.9411543596271,-0.423245389017799,
4.09410684177624));
#27478=CARTESIAN_POINT('Ctrl Pts',(21.9650122776585,-0.416588591947193,
3.87980556563057));
#27479=CARTESIAN_POINT('Ctrl Pts',(21.98887019569,-0.30806453650007,3.69489510271888));
#27480=CARTESIAN_POINT('Ctrl Pts',(22.0127281137213,-0.12421031036921,3.58459109808296));
#27481=CARTESIAN_POINT('Ctrl Pts',(22.0365860317528,0.0900167200678817,
3.57586588547707));
#27482=CARTESIAN_POINT('Ctrl Pts',(22.0604439497842,0.282232210442068,3.67085301705332));
#27483=CARTESIAN_POINT('Ctrl Pts',(22.0843018678157,0.405434237512275,3.8463255517439));
#27484=CARTESIAN_POINT('Ctrl Pts',(22.108159785847,0.429496549703537,4.05937567504088));
#27485=CARTESIAN_POINT('Ctrl Pts',(22.1320177038785,0.348535256241736,4.25790682842971));
#27486=CARTESIAN_POINT('Ctrl Pts',(22.1548313272889,0.18962186617866,4.38744320371645));
#27487=CARTESIAN_POINT('Ctrl Pts',(22.1696923113557,0.0601536901409818,
4.41584170838249));
#27488=CARTESIAN_POINT('Ctrl Pts',(22.1766006560786,-8.37799962077716E-6,
4.41589611849309));
#27489=CARTESIAN_POINT('Ctrl Pts',(21.9733993439214,8.40473402260317E-6,
4.41585103914036));
#27490=CARTESIAN_POINT('Ctrl Pts',(21.9785431582582,-0.044801031555974,
4.41581845947763));
#27491=CARTESIAN_POINT('Ctrl Pts',(21.9916396119388,-0.158914563981884,
4.39744691543598));
#27492=CARTESIAN_POINT('Ctrl Pts',(22.0126887049632,-0.317860118355158,
4.29488591379237));
#27493=CARTESIAN_POINT('Ctrl Pts',(22.0365466229946,-0.420290167226249,
4.10653136780738));
#27494=CARTESIAN_POINT('Ctrl Pts',(22.060404541026,-0.419947821735935,3.89212700053744));
#27495=CARTESIAN_POINT('Ctrl Pts',(22.0842624590574,-0.316916794682727,
3.70410052003731));
#27496=CARTESIAN_POINT('Ctrl Pts',(22.1081203770888,-0.136390978688423,
3.58842952252864));
#27497=CARTESIAN_POINT('Ctrl Pts',(22.1319782951203,0.0774861468089536,
3.57339871771534));
#27498=CARTESIAN_POINT('Ctrl Pts',(22.1558362131517,0.27241579873489,3.66268354680831));
#27499=CARTESIAN_POINT('Ctrl Pts',(22.1796941311831,0.400732367405962,3.83445143701846));
#27500=CARTESIAN_POINT('Ctrl Pts',(22.2035520492145,0.431058956528623,4.04670046033727));
#27501=CARTESIAN_POINT('Ctrl Pts',(22.227409967246,0.355979888945518,4.24752994899471));
#27502=CARTESIAN_POINT('Ctrl Pts',(22.2506923988149,0.197764744804664,4.38444734931837));
#27503=CARTESIAN_POINT('Ctrl Pts',(22.26602219104,0.064235283418036,4.41586628455644));
#27504=CARTESIAN_POINT('Ctrl Pts',(22.2733993439214,-5.11585294797612E-6,
4.41590580604266));
#27505=CARTESIAN_POINT('Origin',(3.42660065607856,0.,4.));
#27506=CARTESIAN_POINT('',(21.5766006560785,-1.05752387382048E-5,4.41586434469346));
#27507=CARTESIAN_POINT('',(21.6733993439214,-1.08222664516599E-5,4.41587700699864));
#27508=CARTESIAN_POINT('',(3.42660065607856,4.87367679877478E-13,4.415875));
#27509=CARTESIAN_POINT('Ctrl Pts',(21.5766006560785,-1.05752387381843E-5,
4.41586434469346));
#27510=CARTESIAN_POINT('Ctrl Pts',(21.5788289671043,-0.0194203346498642,
4.41588296395747));
#27511=CARTESIAN_POINT('Ctrl Pts',(21.5890099174739,-0.10809016089515,4.40978779866957));
#27512=CARTESIAN_POINT('Ctrl Pts',(21.6071435071872,-0.258824259222961,
4.34785450957493));
#27513=CARTESIAN_POINT('Ctrl Pts',(21.6310014252187,-0.39385182381868,4.18131050126406));
#27514=CARTESIAN_POINT('Ctrl Pts',(21.6548593432501,-0.432571889182456,
3.97043113659525));
#27515=CARTESIAN_POINT('Ctrl Pts',(21.6787172612815,-0.365516344619441,
3.76678216446856));
#27516=CARTESIAN_POINT('Ctrl Pts',(21.702575179313,-0.209082097331647,3.62016130585559));
#27517=CARTESIAN_POINT('Ctrl Pts',(21.7264330973443,-0.00152158196427748,
3.56642135455923));
#27518=CARTESIAN_POINT('Ctrl Pts',(21.7502910153758,0.206411001640417,3.61870319251831));
#27519=CARTESIAN_POINT('Ctrl Pts',(21.7741489334072,0.363870472821225,3.76422248622317));
#27520=CARTESIAN_POINT('Ctrl Pts',(21.7980068514386,0.432353701764573,3.96739580449697));
#27521=CARTESIAN_POINT('Ctrl Pts',(21.82186476947,0.395114673548107,4.17854173669174));
#27522=CARTESIAN_POINT('Ctrl Pts',(21.8457226875014,0.261259344941517,4.3460293508861));
#27523=CARTESIAN_POINT('Ctrl Pts',(21.8639679830376,0.110037800305057,4.4094070875278));
#27524=CARTESIAN_POINT('Ctrl Pts',(21.87426063923,0.0203934810735595,4.41588037378429));
#27525=CARTESIAN_POINT('Ctrl Pts',(21.8766006560786,1.03078286340201E-5,
4.41586151989188));
#27526=CARTESIAN_POINT('Ctrl Pts',(21.6733993439214,-1.0822266451653E-5,
4.41587700699864));
#27527=CARTESIAN_POINT('Ctrl Pts',(21.6751588467887,-0.0153356749568721,
4.41589290068126));
#27528=CARTESIAN_POINT('Ctrl Pts',(21.6848709889998,-0.0999166717736498,
4.41130778913604));
#27529=CARTESIAN_POINT('Ctrl Pts',(21.7025357705547,-0.248467031045983,
4.35532645760922));
#27530=CARTESIAN_POINT('Ctrl Pts',(21.7263936885861,-0.388341045935521,
4.1928315042612));
#27531=CARTESIAN_POINT('Ctrl Pts',(21.7502516066176,-0.433255096896122,
3.98318399549658));
#27532=CARTESIAN_POINT('Ctrl Pts',(21.774109524649,-0.372226475033738,3.77764845789182));
#27533=CARTESIAN_POINT('Ctrl Pts',(21.7979674426804,-0.220178340780001,
3.62648392906691));
#27534=CARTESIAN_POINT('Ctrl Pts',(21.8218253607118,-0.0142906046679706,
3.56665425395863));
#27535=CARTESIAN_POINT('Ctrl Pts',(21.8456832787432,0.195091573553633,3.61278941785858));
#27536=CARTESIAN_POINT('Ctrl Pts',(21.8695411967747,0.356768547853618,3.75360811649661));
#27537=CARTESIAN_POINT('Ctrl Pts',(21.8933991148061,0.431205894023261,3.95467634223136));
#27538=CARTESIAN_POINT('Ctrl Pts',(21.9172570328375,0.400201653291494,4.16682743688221));
#27539=CARTESIAN_POINT('Ctrl Pts',(21.941114950869,0.271337207055788,4.33818467892719));
#27540=CARTESIAN_POINT('Ctrl Pts',(21.9598290545635,0.118211900824938,4.40773087908456));
#27541=CARTESIAN_POINT('Ctrl Pts',(21.9705905189143,0.0244769910710258,
4.41586882955141));
#27542=CARTESIAN_POINT('Ctrl Pts',(21.9733993439214,8.40473402260317E-6,
4.41585103914036));
#27543=CARTESIAN_POINT('Origin',(3.42660065607856,0.,4.));
#27544=CARTESIAN_POINT('',(21.2766006560785,8.9771325895615E-6,4.41589335210553));
#27545=CARTESIAN_POINT('',(21.3733993439214,1.06214664634743E-5,4.41588075133303));
#27546=CARTESIAN_POINT('',(3.42660065607856,4.87367679877478E-13,4.415875));
#27547=CARTESIAN_POINT('Ctrl Pts',(21.2766006560785,8.97713258955941E-6,
4.41589335210553));
#27548=CARTESIAN_POINT('Ctrl Pts',(21.2833972949786,-0.0591814269577189,
4.41583723296416));
#27549=CARTESIAN_POINT('Ctrl Pts',(21.2981465732225,-0.187680420990878,
4.38813575385326));
#27550=CARTESIAN_POINT('Ctrl Pts',(21.3208484908102,-0.346716519889314,
4.26034671465164));
#27551=CARTESIAN_POINT('Ctrl Pts',(21.3447064088417,-0.429069235164158,
4.0623886883135));
#27552=CARTESIAN_POINT('Ctrl Pts',(21.368564326873,-0.406502834830527,3.8491749282489));
#27553=CARTESIAN_POINT('Ctrl Pts',(21.3924222449045,-0.284535418465691,
3.67284200661995));
#27554=CARTESIAN_POINT('Ctrl Pts',(21.4162801629359,-0.0929913416969399,
3.5765081259772));
#27555=CARTESIAN_POINT('Ctrl Pts',(21.4401380809674,0.121291651150069,3.58372954422009));
#27556=CARTESIAN_POINT('Ctrl Pts',(21.4639959989987,0.305915531372611,3.69274042788069));
#27557=CARTESIAN_POINT('Ctrl Pts',(21.4878539170302,0.415734731202803,3.87688464650718));
#27558=CARTESIAN_POINT('Ctrl Pts',(21.5117118350615,0.423895464867194,4.09113392265755));
#27559=CARTESIAN_POINT('Ctrl Pts',(21.535569753093,0.328402210690932,4.28309847227994));
#27560=CARTESIAN_POINT('Ctrl Pts',(21.5571993600986,0.169024930905334,4.39437398220882));
#27561=CARTESIAN_POINT('Ctrl Pts',(21.5708763277605,0.0498513310028489,
4.41581651349798));
#27562=CARTESIAN_POINT('Ctrl Pts',(21.5766006560785,-1.05752387381843E-5,
4.41586434469346));
#27563=CARTESIAN_POINT('Ctrl Pts',(21.3733993439214,1.06214664634605E-5,
4.41588075133303));
#27564=CARTESIAN_POINT('Ctrl Pts',(21.379727174663,-0.0551018547626871,
4.41582358345633));
#27565=CARTESIAN_POINT('Ctrl Pts',(21.3940076447484,-0.1795281855266,4.39095386216025));
#27566=CARTESIAN_POINT('Ctrl Pts',(21.4162407541777,-0.338898428465248,
4.27044521104599));
#27567=CARTESIAN_POINT('Ctrl Pts',(21.4400986722091,-0.427045644525908,
4.07499849655415));
#27568=CARTESIAN_POINT('Ctrl Pts',(21.4639565902406,-0.410768568010174,
3.86121260673678));
#27569=CARTESIAN_POINT('Ctrl Pts',(21.4878145082719,-0.294047387504818,
3.68136401506497));
#27570=CARTESIAN_POINT('Ctrl Pts',(21.5116724263034,-0.105423611064507,
3.57943060117972));
#27571=CARTESIAN_POINT('Ctrl Pts',(21.5355303443348,0.108979109962582,3.58033786138646));
#27572=CARTESIAN_POINT('Ctrl Pts',(21.5593882623662,0.296733470072461,3.68386394585134));
#27573=CARTESIAN_POINT('Ctrl Pts',(21.5832461803976,0.411928413892185,3.86469390692879));
#27574=CARTESIAN_POINT('Ctrl Pts',(21.6071040984291,0.426395639810567,4.07860989342611));
#27575=CARTESIAN_POINT('Ctrl Pts',(21.6309620164605,0.33659751701124,4.27330361969026));
#27576=CARTESIAN_POINT('Ctrl Pts',(21.6530604316246,0.177184770587036,4.39173732935402));
#27577=CARTESIAN_POINT('Ctrl Pts',(21.6672062074449,0.0539299276789421,
4.41582106406873));
#27578=CARTESIAN_POINT('Ctrl Pts',(21.6733993439214,-1.0822266451653E-5,
4.41587700699864));
#27579=CARTESIAN_POINT('Origin',(3.42660065607856,0.,4.));
#27580=CARTESIAN_POINT('',(20.9766006560786,-4.48287659654576E-6,4.41584197426197));
#27581=CARTESIAN_POINT('',(21.0733993439214,-7.65157297119567E-6,4.41584853425778));
#27582=CARTESIAN_POINT('',(3.42660065607856,4.87367679877478E-13,4.415875));
#27583=CARTESIAN_POINT('Ctrl Pts',(20.9766006560786,-4.48287659652116E-6,
4.41584197426197));
#27584=CARTESIAN_POINT('Ctrl Pts',(20.9800129835092,-0.0297322302090305,
4.41585318364051));
#27585=CARTESIAN_POINT('Ctrl Pts',(20.9913779502836,-0.128734546054536,
4.40538471300776));
#27586=CARTESIAN_POINT('Ctrl Pts',(21.0106955564018,-0.28396276796243,4.32765515869354));
#27587=CARTESIAN_POINT('Ctrl Pts',(21.0345534744332,-0.40623841344949,4.15153583326342));
#27588=CARTESIAN_POINT('Ctrl Pts',(21.0584113924646,-0.429177699343215,
3.93836186909709));
#27589=CARTESIAN_POINT('Ctrl Pts',(21.082269310496,-0.347171348131155,3.74026010679315));
#27590=CARTESIAN_POINT('Ctrl Pts',(21.1061272285274,-0.180272145040548,
3.605671823621));
#27591=CARTESIAN_POINT('Ctrl Pts',(21.1299851465589,0.0307085077608185,
3.56750752082027));
#27592=CARTESIAN_POINT('Ctrl Pts',(21.1538430645903,0.234180094072738,3.63509941005724));
#27593=CARTESIAN_POINT('Ctrl Pts',(21.1777009826217,0.380388268371489,3.79191943321731));
#27594=CARTESIAN_POINT('Ctrl Pts',(21.2015589006531,0.433581149524578,3.99962082296209));
#27595=CARTESIAN_POINT('Ctrl Pts',(21.2254168186846,0.380751629084578,4.2074149318183));
#27596=CARTESIAN_POINT('Ctrl Pts',(21.2492747367159,0.234817963878357,4.36449043997717));
#27597=CARTESIAN_POINT('Ctrl Pts',(21.2663360158473,0.0893960873046664,
4.41308118928586));
#27598=CARTESIAN_POINT('Ctrl Pts',(21.2754446556348,0.0100763257733538,
4.41590289708112));
#27599=CARTESIAN_POINT('Ctrl Pts',(21.2766006560785,8.97713258955941E-6,
4.41589335210553));
#27600=CARTESIAN_POINT('Ctrl Pts',(21.0733993439214,-7.65157297121996E-6,
4.41584853425778));
#27601=CARTESIAN_POINT('Ctrl Pts',(21.0763428631935,-0.0256500457845501,
4.41586537097631));
#27602=CARTESIAN_POINT('Ctrl Pts',(21.0872390218095,-0.120560449820324,
4.40722571769055));
#27603=CARTESIAN_POINT('Ctrl Pts',(21.1060878197692,-0.274189543318984,
4.33587624407661));
#27604=CARTESIAN_POINT('Ctrl Pts',(21.1299457378007,-0.401599180171465,
4.16343456021562));
#27605=CARTESIAN_POINT('Ctrl Pts',(21.1538036558321,-0.430806878168669,
3.95102867450389));
#27606=CARTESIAN_POINT('Ctrl Pts',(21.1776615738635,-0.354670559489406,
3.75059761183336));
#27607=CARTESIAN_POINT('Ctrl Pts',(21.2015194918949,-0.191807627993766,
3.61115222665144));
#27608=CARTESIAN_POINT('Ctrl Pts',(21.2253774099264,0.0179574932869785,
3.56679071405539));
#27609=CARTESIAN_POINT('Ctrl Pts',(21.2492353279577,0.223331518303719,3.62836067225603));
#27610=CARTESIAN_POINT('Ctrl Pts',(21.2730932459892,0.374094903668402,3.78080656934254));
#27611=CARTESIAN_POINT('Ctrl Pts',(21.2969511640206,0.433381894944723,3.98685123093373));
#27612=CARTESIAN_POINT('Ctrl Pts',(21.320809082052,0.386695207821707,4.19611112472705));
#27613=CARTESIAN_POINT('Ctrl Pts',(21.3446670000834,0.245451009020076,4.35741650656472));
#27614=CARTESIAN_POINT('Ctrl Pts',(21.3621970873732,0.0975684711839555,
4.41172139589413));
#27615=CARTESIAN_POINT('Ctrl Pts',(21.3717745353192,0.014161952170494,4.41589543043265));
#27616=CARTESIAN_POINT('Ctrl Pts',(21.3733993439214,1.06214664634605E-5,
4.41588075133303));
#27617=CARTESIAN_POINT('Origin',(3.42660065607856,0.,4.));
#27618=CARTESIAN_POINT('',(20.6766006560786,1.29204965968245E-6,4.41591114679826));
#27619=CARTESIAN_POINT('',(20.7733993439214,3.9567662055099E-6,4.41590779860895));
#27620=CARTESIAN_POINT('',(3.42660065607856,4.87367679877478E-13,4.415875));
#27621=CARTESIAN_POINT('Ctrl Pts',(20.6766006560786,1.29076178055295E-6,
4.41591111076812));
#27622=CARTESIAN_POINT('Ctrl Pts',(20.6766286720397,-0.000242659277546582,
4.41591112051333));
#27623=CARTESIAN_POINT('Ctrl Pts',(20.6846093273446,-0.0697345275278937,
4.41585145172406));
#27624=CARTESIAN_POINT('Ctrl Pts',(20.7005426219933,-0.208420567790133,
4.38020336888205));
#27625=CARTESIAN_POINT('Ctrl Pts',(20.7244005400248,-0.365106210756856,
4.23385701605743));
#27626=CARTESIAN_POINT('Ctrl Pts',(20.7482584580562,-0.432520392530856,
4.03032528343114));
#27627=CARTESIAN_POINT('Ctrl Pts',(20.7721163760876,-0.394167874571092,
3.81937870627435));
#27628=CARTESIAN_POINT('Ctrl Pts',(20.795974294119,-0.259432524437891,3.65259868360638));
#27629=CARTESIAN_POINT('Ctrl Pts',(20.8198322121504,-0.0612578225112809,
3.57076788979259));
#27630=CARTESIAN_POINT('Ctrl Pts',(20.8436901301819,0.151895538690754,3.5938959627232));
#27631=CARTESIAN_POINT('Ctrl Pts',(20.8675480482132,0.327906592802717,3.71632757520176));
#27632=CARTESIAN_POINT('Ctrl Pts',(20.8914059662447,0.423735399567132,3.90812480123879));
#27633=CARTESIAN_POINT('Ctrl Pts',(20.9152638842761,0.415949440063929,4.12238802732943));
#27634=CARTESIAN_POINT('Ctrl Pts',(20.9391218023075,0.30645246920106,4.30672404095661));
#27635=CARTESIAN_POINT('Ctrl Pts',(20.9595673929083,0.148398440326279,4.40042000858165));
#27636=CARTESIAN_POINT('Ctrl Pts',(20.9720603441653,0.0395501167658222,
4.4158270594931));
#27637=CARTESIAN_POINT('Ctrl Pts',(20.9766006560786,-4.48287659652116E-6,
4.41584197426197));
#27638=CARTESIAN_POINT('Ctrl Pts',(20.7733993439214,3.95676620551077E-6,
4.41590779860895));
#27639=CARTESIAN_POINT('Ctrl Pts',(20.7809111910678,-0.0654084660523611,
4.41587519962517));
#27640=CARTESIAN_POINT('Ctrl Pts',(20.7963756775582,-0.200102595337945,
4.3835597345012));
#27641=CARTESIAN_POINT('Ctrl Pts',(20.8197928033922,-0.358062019934396,
4.24450842127602));
#27642=CARTESIAN_POINT('Ctrl Pts',(20.8436507214237,-0.431438726014498,
4.04305074550709));
#27643=CARTESIAN_POINT('Ctrl Pts',(20.867508639455,-0.399316990859146,3.83106596928302));
#27644=CARTESIAN_POINT('Ctrl Pts',(20.8913665574865,-0.269551332195825,
3.66039017609669));
#27645=CARTESIAN_POINT('Ctrl Pts',(20.9152244755179,-0.0738730526583281,
3.57275822989076));
#27646=CARTESIAN_POINT('Ctrl Pts',(20.9390823935493,0.139869212314499,3.58959853735383));
#27647=CARTESIAN_POINT('Ctrl Pts',(20.9629403115807,0.319409638666883,3.70679317993256));
#27648=CARTESIAN_POINT('Ctrl Pts',(20.9867982296122,0.420845711130686,3.8956848776653));
#27649=CARTESIAN_POINT('Ctrl Pts',(21.0106561476436,0.419373541863394,4.11008446384341));
#27650=CARTESIAN_POINT('Ctrl Pts',(21.034514065675,0.315353119032788,4.29756540021079));
#27651=CARTESIAN_POINT('Ctrl Pts',(21.0554284644342,0.156567902793621,4.39812991232556));
#27652=CARTESIAN_POINT('Ctrl Pts',(21.0683902238497,0.0436291721249729,
4.41581988245125));
#27653=CARTESIAN_POINT('Ctrl Pts',(21.0733993439214,-7.65157297121996E-6,
4.41584853425778));
#27654=CARTESIAN_POINT('Origin',(3.42660065607856,0.,4.));
#27655=CARTESIAN_POINT('',(20.3766006560786,0.000383027521040961,4.41597069455794));
#27656=CARTESIAN_POINT('',(20.4733993439214,0.000101608071013781,4.41586489633469));
#27657=CARTESIAN_POINT('',(3.42660065607856,4.87367679877478E-13,4.415875));
#27658=CARTESIAN_POINT('Ctrl Pts',(20.3766006560786,0.000383027521040954,
4.41597069455794));
#27659=CARTESIAN_POINT('Ctrl Pts',(20.3891496392578,-0.108893832387875,
4.41487837761012));
#27660=CARTESIAN_POINT('Ctrl Pts',(20.4176039011246,-0.35839559572325,4.31454223548297));
#27661=CARTESIAN_POINT('Ctrl Pts',(20.4540108023354,-0.457800032585507,
3.97025345815189));
#27662=CARTESIAN_POINT('Ctrl Pts',(20.4858213597105,-0.325993724402262,
3.71529210935379));
#27663=CARTESIAN_POINT('Ctrl Pts',(20.509679277742,-0.15096738523986,3.59329490328468));
#27664=CARTESIAN_POINT('Ctrl Pts',(20.5335371957734,0.0630371972956549,
3.57102347342756));
#27665=CARTESIAN_POINT('Ctrl Pts',(20.5573951138048,0.260511246441404,3.65349437971329));
#27666=CARTESIAN_POINT('Ctrl Pts',(20.5812530318362,0.394877283734959,3.82077798440408));
#27667=CARTESIAN_POINT('Ctrl Pts',(20.6051109498677,0.432370081305563,4.03184236506754));
#27668=CARTESIAN_POINT('Ctrl Pts',(20.6289688678991,0.364303478986858,4.23514367899931));
#27669=CARTESIAN_POINT('Ctrl Pts',(20.6527987699694,0.207251017164088,4.38076243960928));
#27670=CARTESIAN_POINT('Ctrl Pts',(20.6686760326959,0.0690052481014253,
4.41590835422812));
#27671=CARTESIAN_POINT('Ctrl Pts',(20.6766006560786,1.29076178055295E-6,
4.41591111076812));
#27672=CARTESIAN_POINT('Ctrl Pts',(20.4733993439214,0.000101608071013788,
4.4158648963347));
#27673=CARTESIAN_POINT('Ctrl Pts',(20.4775268795984,-0.0359150725839473,
4.41584626969953));
#27674=CARTESIAN_POINT('Ctrl Pts',(20.4896070546192,-0.141401612166324,
4.40227446254147));
#27675=CARTESIAN_POINT('Ctrl Pts',(20.5096398689838,-0.298255971346869,
4.31460392554555));
#27676=CARTESIAN_POINT('Ctrl Pts',(20.5334977870152,-0.412709509332759,
4.13311446574462));
#27677=CARTESIAN_POINT('Ctrl Pts',(20.5573557050466,-0.425936384696969,
3.91915434697803));
#27678=CARTESIAN_POINT('Ctrl Pts',(20.581213623078,-0.335173342752607,3.72492109335083));
#27679=CARTESIAN_POINT('Ctrl Pts',(20.6050715411095,-0.162364888615448,
3.59797442377207));
#27680=CARTESIAN_POINT('Ctrl Pts',(20.6289294591408,0.0501004451364318,
3.56932214892951));
#27681=CARTESIAN_POINT('Ctrl Pts',(20.6527873771723,0.250339089241223,3.64598859455508));
#27682=CARTESIAN_POINT('Ctrl Pts',(20.6766452952037,0.389350172549011,3.80921715950176));
#27683=CARTESIAN_POINT('Ctrl Pts',(20.7005032132352,0.433161330121289,4.01909908002448));
#27684=CARTESIAN_POINT('Ctrl Pts',(20.7243611312665,0.371049143609512,4.22430982617278));
#27685=CARTESIAN_POINT('Ctrl Pts',(20.748219049298,0.218207240773441,4.37467120177868));
#27686=CARTESIAN_POINT('Ctrl Pts',(20.7645651201829,0.0769305199015265,
4.41491906931248));
#27687=CARTESIAN_POINT('Ctrl Pts',(20.772958551724,0.00384233167249433,
4.41590971150433));
#27688=CARTESIAN_POINT('Ctrl Pts',(20.7733993439214,3.95676620551077E-6,
4.41590779860895));
#27689=CARTESIAN_POINT('Origin',(3.42660065607856,0.,4.));
#27690=CARTESIAN_POINT('',(20.0766006560786,-0.000186622634748148,4.41645953600834));
#27691=CARTESIAN_POINT('',(20.1733993439214,-0.000111611226006447,4.41653056081536));
#27692=CARTESIAN_POINT('',(3.42660065607856,4.87367679877478E-13,4.415875));
#27693=CARTESIAN_POINT('Ctrl Pts',(20.0766006560786,-0.000186622634748109,
4.41645953600834));
#27694=CARTESIAN_POINT('Ctrl Pts',(20.0778126884445,-0.0107019642254321,
4.4165186149328));
#27695=CARTESIAN_POINT('Ctrl Pts',(20.0949299994981,-0.159149739060163,
4.41138240526969));
#27696=CARTESIAN_POINT('Ctrl Pts',(20.1279525892393,-0.432744382500041,
4.23375285658289));
#27697=CARTESIAN_POINT('Ctrl Pts',(20.1756684253021,-0.430649333670284,
3.76246031529274));
#27698=CARTESIAN_POINT('Ctrl Pts',(20.223384261365,-0.033136228617316,3.50924504180455));
#27699=CARTESIAN_POINT('Ctrl Pts',(20.2711000974278,0.394908089060633,3.70680919012016));
#27700=CARTESIAN_POINT('Ctrl Pts',(20.3188159334906,0.460110046434968,4.17340395051402));
#27701=CARTESIAN_POINT('Ctrl Pts',(20.3539827863742,0.197028357007358,4.40022211154544));
#27702=CARTESIAN_POINT('Ctrl Pts',(20.3732443605702,0.0296097328916507,
4.416262840815));
#27703=CARTESIAN_POINT('Ctrl Pts',(20.3766006560786,0.000383027521040954,
4.41597069455794));
#27704=CARTESIAN_POINT('Ctrl Pts',(20.1733993439214,-0.000111611226006447,
4.41653056081536));
#27705=CARTESIAN_POINT('Ctrl Pts',(20.1741425681289,-0.00655727229825777,
4.41655465488103));
#27706=CARTESIAN_POINT('Ctrl Pts',(20.190791071024,-0.150919726673813,4.41348743992374));
#27707=CARTESIAN_POINT('Ctrl Pts',(20.2233448526067,-0.425711472830213,
4.24633918020534));
#27708=CARTESIAN_POINT('Ctrl Pts',(20.2710606886696,-0.437384262562023,
3.77535541015343));
#27709=CARTESIAN_POINT('Ctrl Pts',(20.3187765247324,-0.0477164433392854,
3.51022640082505));
#27710=CARTESIAN_POINT('Ctrl Pts',(20.3664923607953,0.386374384143037,3.69571627142296));
#27711=CARTESIAN_POINT('Ctrl Pts',(20.4062555575143,0.45143962727185,4.08165775845481));
#27712=CARTESIAN_POINT('Ctrl Pts',(20.4380661148895,0.291471375703242,4.31996082336987));
#27713=CARTESIAN_POINT('Ctrl Pts',(20.4577964972439,0.136183087716603,4.40372206768731));
#27714=CARTESIAN_POINT('Ctrl Pts',(20.4695742402546,0.0334792813416625,
4.41588215816259));
#27715=CARTESIAN_POINT('Ctrl Pts',(20.4733993439214,0.000101608071013788,
4.4158648963347));
#27716=CARTESIAN_POINT('Origin',(3.42660065607856,0.,4.));
#27717=CARTESIAN_POINT('',(19.7766006560786,-0.000280998963924209,4.41539029291088));
#27718=CARTESIAN_POINT('',(19.8733993439214,-0.000322938566065189,4.41548189938477));
#27719=CARTESIAN_POINT('',(3.42660065607856,4.87367679877478E-13,4.415875));
#27720=CARTESIAN_POINT('Ctrl Pts',(19.7766006560786,-0.000280998963924181,
4.41539029291088));
#27721=CARTESIAN_POINT('Ctrl Pts',(19.7823810163188,-0.0507615353771658,
4.41570272077311));
#27722=CARTESIAN_POINT('Ctrl Pts',(19.8040666552467,-0.23976299482565,4.3837755623668));
#27723=CARTESIAN_POINT('Ctrl Pts',(19.8416575728622,-0.481212499922896,
4.10168523844358));
#27724=CARTESIAN_POINT('Ctrl Pts',(19.8893734089251,-0.345789702982467,
3.65023692191923));
#27725=CARTESIAN_POINT('Ctrl Pts',(19.9370892449879,0.107175910646637,3.51998011832295));
#27726=CARTESIAN_POINT('Ctrl Pts',(19.9848050810508,0.461722480014006,3.83053541934297));
#27727=CARTESIAN_POINT('Ctrl Pts',(20.0313088847476,0.394022427012164,4.28486673161383));
#27728=CARTESIAN_POINT('Ctrl Pts',(20.0619074097569,0.127288937001902,4.4157433330307));
#27729=CARTESIAN_POINT('Ctrl Pts',(20.0766006560786,-0.000186622634748109,
4.41645953600834));
#27730=CARTESIAN_POINT('Ctrl Pts',(19.8733993439214,-0.000322938566065196,
4.41548189938477));
#27731=CARTESIAN_POINT('Ctrl Pts',(19.8787108960032,-0.0466836533228258,
4.41581668875846));
#27732=CARTESIAN_POINT('Ctrl Pts',(19.8999277267727,-0.231469429366377,
4.38724295332581));
#27733=CARTESIAN_POINT('Ctrl Pts',(19.9370498362297,-0.47800980043334,4.11581244897344));
#27734=CARTESIAN_POINT('Ctrl Pts',(19.9847656722926,-0.355939225796451,
3.66057517601247));
#27735=CARTESIAN_POINT('Ctrl Pts',(20.0324815083554,0.0929888682922082,
3.51702731322357));
#27736=CARTESIAN_POINT('Ctrl Pts',(20.0801973444182,0.456536973876988,3.81701888067549));
#27737=CARTESIAN_POINT('Ctrl Pts',(20.1271699562736,0.401683300383188,4.27772103607547));
#27738=CARTESIAN_POINT('Ctrl Pts',(20.1582372894413,0.131382308576697,4.41603903277767));
#27739=CARTESIAN_POINT('Ctrl Pts',(20.1733993439214,-0.000111611226006447,
4.41653056081536));
#27740=CARTESIAN_POINT('Origin',(3.42660065607856,0.,4.));
#27741=CARTESIAN_POINT('',(19.4766006560786,0.000302289446139524,4.41543216566181));
#27742=CARTESIAN_POINT('',(19.5733993439214,0.000255464646300079,4.41534829948978));
#27743=CARTESIAN_POINT('',(3.42660065607856,4.87367679877478E-13,4.415875));
#27744=CARTESIAN_POINT('Ctrl Pts',(19.4766006560786,0.000302289446139546,
4.41543216566181));
#27745=CARTESIAN_POINT('Ctrl Pts',(19.4869493441932,-0.0900510892866153,
4.41482666801407));
#27746=CARTESIAN_POINT('Ctrl Pts',(19.5132033109954,-0.320168095705801,
4.3413809155508));
#27747=CARTESIAN_POINT('Ctrl Pts',(19.5553625564852,-0.490312813065352,
3.96128857502183));
#27748=CARTESIAN_POINT('Ctrl Pts',(19.603078392548,-0.232620797759261,3.56664935826393));
#27749=CARTESIAN_POINT('Ctrl Pts',(19.6507942286109,0.238690449241969,3.56996267500769));
#27750=CARTESIAN_POINT('Ctrl Pts',(19.6985100646737,0.490808633485035,3.96818593857384));
#27751=CARTESIAN_POINT('Ctrl Pts',(19.7404455404963,0.316268156276861,4.34384396940031));
#27752=CARTESIAN_POINT('Ctrl Pts',(19.7664757376312,0.0881410531427697,
4.41484304213512));
#27753=CARTESIAN_POINT('Ctrl Pts',(19.7766006560786,-0.000280998963924181,
4.41539029291088));
#27754=CARTESIAN_POINT('Ctrl Pts',(19.5733993439214,0.000255464646300094,
4.41534829948978));
#27755=CARTESIAN_POINT('Ctrl Pts',(19.5832792238775,-0.0860485087386658,
4.41486588036018));
#27756=CARTESIAN_POINT('Ctrl Pts',(19.6090643825213,-0.311990568344336,
4.34649332259355));
#27757=CARTESIAN_POINT('Ctrl Pts',(19.6507548198527,-0.491240257057309,
3.97574594767572));
#27758=CARTESIAN_POINT('Ctrl Pts',(19.6984706559155,-0.245282818621706,
3.57368850533185));
#27759=CARTESIAN_POINT('Ctrl Pts',(19.7461864919783,0.225921452997342,3.56311925573479));
#27760=CARTESIAN_POINT('Ctrl Pts',(19.7939023280412,0.489658867576397,3.95374471702426));
#27761=CARTESIAN_POINT('Ctrl Pts',(19.8363066120222,0.324430886710512,4.33863507066385));
#27762=CARTESIAN_POINT('Ctrl Pts',(19.8628056173156,0.0921420753912029,
4.4148141723173));
#27763=CARTESIAN_POINT('Ctrl Pts',(19.8733993439214,-0.000322938566065196,
4.41548189938477));
#27764=CARTESIAN_POINT('Origin',(3.42660065607856,0.,4.));
#27765=CARTESIAN_POINT('',(19.1766006560786,0.000155842099650094,4.41649089206047));
#27766=CARTESIAN_POINT('',(19.2733993439214,0.000220989830587742,4.4164164649367));
#27767=CARTESIAN_POINT('',(3.42660065607856,4.87367679877478E-13,4.415875));
#27768=CARTESIAN_POINT('Ctrl Pts',(19.1766006560786,0.000155842099650088,
4.41649089206047));
#27769=CARTESIAN_POINT('Ctrl Pts',(19.1915176720675,-0.129233580897558,
4.41587069825202));
#27770=CARTESIAN_POINT('Ctrl Pts',(19.2223399667441,-0.397695790553126,
4.28149179527637));
#27771=CARTESIAN_POINT('Ctrl Pts',(19.2690675401082,-0.459293044881286,
3.82405931712685));
#27772=CARTESIAN_POINT('Ctrl Pts',(19.316783376171,-0.100417177000157,3.51852142809106));
#27773=CARTESIAN_POINT('Ctrl Pts',(19.3644992122339,0.350673329058588,3.65513271950473));
#27774=CARTESIAN_POINT('Ctrl Pts',(19.4122150482967,0.479735122332443,4.10844094226069));
#27775=CARTESIAN_POINT('Ctrl Pts',(19.4495821962449,0.235804435834584,4.38544967282755));
#27776=CARTESIAN_POINT('Ctrl Pts',(19.4710440655056,0.0488163355692654,
4.4157572795781));
#27777=CARTESIAN_POINT('Ctrl Pts',(19.4766006560786,0.000302289446139546,
4.41543216566181));
#27778=CARTESIAN_POINT('Ctrl Pts',(19.2733993439214,0.000220989830587761,
4.4164164649367));
#27779=CARTESIAN_POINT('Ctrl Pts',(19.2878475517519,-0.125161313229646,
4.41561068768233));
#27780=CARTESIAN_POINT('Ctrl Pts',(19.31820103827,-0.389985711500173,4.28851341748863));
#27781=CARTESIAN_POINT('Ctrl Pts',(19.3644598034757,-0.464275578741542,
3.8376626582024));
#27782=CARTESIAN_POINT('Ctrl Pts',(19.4121756395385,-0.114554038379521,
3.52168776344319));
#27783=CARTESIAN_POINT('Ctrl Pts',(19.4598914756013,0.340364234683876,3.64495435060606));
#27784=CARTESIAN_POINT('Ctrl Pts',(19.5076073116642,0.482720800247919,4.09426482953845));
#27785=CARTESIAN_POINT('Ctrl Pts',(19.5454432677708,0.244097666198316,4.38190156491584));
#27786=CARTESIAN_POINT('Ctrl Pts',(19.5673739451899,0.0528892875329133,
4.41564251031262));
#27787=CARTESIAN_POINT('Ctrl Pts',(19.5733993439214,0.000255464646300094,
4.41534829948978));
#27788=CARTESIAN_POINT('Origin',(3.42660065607856,0.,4.));
#27789=CARTESIAN_POINT('',(18.8766006560785,-0.00038196507782994,4.41590683121974));
#27790=CARTESIAN_POINT('',(18.9733993439214,-0.000368287616214491,4.41603142687637));
#27791=CARTESIAN_POINT('',(3.42660065607856,4.87367679877478E-13,4.415875));
#27792=CARTESIAN_POINT('Ctrl Pts',(18.8766006560785,-0.000381965077829925,
4.41590683121974));
#27793=CARTESIAN_POINT('Ctrl Pts',(18.8801807212542,-0.0315488007868432,
4.41619587167324));
#27794=CARTESIAN_POINT('Ctrl Pts',(18.8996660651174,-0.200861076696893,
4.39874895857547));
#27795=CARTESIAN_POINT('Ctrl Pts',(18.9350566876684,-0.462607878309702,
4.16703046362027));
#27796=CARTESIAN_POINT('Ctrl Pts',(18.9827725237311,-0.39069124519864,3.70122654773242));
#27797=CARTESIAN_POINT('Ctrl Pts',(19.030488359794,0.0400031699426168,3.50979089028978));
#27798=CARTESIAN_POINT('Ctrl Pts',(19.0782041958568,0.433962058584907,3.76852180111673));
#27799=CARTESIAN_POINT('Ctrl Pts',(19.1259200319197,0.429406911488226,4.23982270375453));
#27800=CARTESIAN_POINT('Ctrl Pts',(19.1587188519936,0.155221332864305,4.41240136130926));
#27801=CARTESIAN_POINT('Ctrl Pts',(19.1756123933799,0.00872798149047904,
4.41653198033223));
#27802=CARTESIAN_POINT('Ctrl Pts',(19.1766006560786,0.000155842099650088,
4.41649089206047));
#27803=CARTESIAN_POINT('Ctrl Pts',(18.9733993439214,-0.000368287616214533,
4.41603142687637));
#27804=CARTESIAN_POINT('Ctrl Pts',(18.9765106009386,-0.0274330213022572,
4.4162811262788));
#27805=CARTESIAN_POINT('Ctrl Pts',(18.9955271366434,-0.192586232161443,
4.40152565608163));
#27806=CARTESIAN_POINT('Ctrl Pts',(19.0304489510358,-0.457487847288108,
4.18058265263639));
#27807=CARTESIAN_POINT('Ctrl Pts',(19.0781647870987,-0.399321187381313,
3.71286272589862));
#27808=CARTESIAN_POINT('Ctrl Pts',(19.1258806231614,0.0255482632835279,
3.50882537619781));
#27809=CARTESIAN_POINT('Ctrl Pts',(19.1735964592243,0.426956350589889,3.75584124112414));
#27810=CARTESIAN_POINT('Ctrl Pts',(19.2213122952871,0.436283851722622,4.22707185138688));
#27811=CARTESIAN_POINT('Ctrl Pts',(19.2545799235195,0.163455264474221,4.41023200720537));
#27812=CARTESIAN_POINT('Ctrl Pts',(19.2719422730642,0.0128655269200745,
4.41649772584937));
#27813=CARTESIAN_POINT('Ctrl Pts',(19.2733993439214,0.000220989830587761,
4.4164164649367));
#27814=CARTESIAN_POINT('Origin',(3.42660065607856,0.,4.));
#27815=CARTESIAN_POINT('',(18.5766006560786,2.82854505807383E-5,4.41518799822097));
#27816=CARTESIAN_POINT('',(18.6733993439214,-3.94222854199766E-5,4.41518963037823));
#27817=CARTESIAN_POINT('',(3.42660065607856,4.87367679877478E-13,4.415875));
#27818=CARTESIAN_POINT('Ctrl Pts',(18.5766006560786,2.82854505807215E-5,
4.41518799822097));
#27819=CARTESIAN_POINT('Ctrl Pts',(18.5847490491285,-0.0712192880865648,
4.41514491699706));
#27820=CARTESIAN_POINT('Ctrl Pts',(18.6088027208661,-0.281596950705947,
4.36382162423513));
#27821=CARTESIAN_POINT('Ctrl Pts',(18.6487616712913,-0.49096944006335,4.0292272779409));
#27822=CARTESIAN_POINT('Ctrl Pts',(18.6964775073541,-0.290120809601049,
3.60284116440841));
#27823=CARTESIAN_POINT('Ctrl Pts',(18.744193343417,0.177150224400508,3.54117212067402));
#27824=CARTESIAN_POINT('Ctrl Pts',(18.7919091794797,0.481741481528227,3.90085177849878));
#27825=CARTESIAN_POINT('Ctrl Pts',(18.836044950367,0.354281053487698,4.31776308733785));
#27826=CARTESIAN_POINT('Ctrl Pts',(18.8642754425666,0.106917172161326,4.4149117417093));
#27827=CARTESIAN_POINT('Ctrl Pts',(18.8766006560785,-0.000381965077829925,
4.41590683121974));
#27828=CARTESIAN_POINT('Ctrl Pts',(18.6733993439214,-3.94222854199489E-5,
4.41518963037823));
#27829=CARTESIAN_POINT('Ctrl Pts',(18.6810789288129,-0.0671871929144198,
4.41524623173262));
#27830=CARTESIAN_POINT('Ctrl Pts',(18.704663792392,-0.273330541024821,4.36810584919535));
#27831=CARTESIAN_POINT('Ctrl Pts',(18.7441539346588,-0.489895661254576,
4.0436745456279));
#27832=CARTESIAN_POINT('Ctrl Pts',(18.7918697707216,-0.301692008317894,
3.6115580391236));
#27833=CARTESIAN_POINT('Ctrl Pts',(18.8395856067845,0.163560057986223,3.53615376224111));
#27834=CARTESIAN_POINT('Ctrl Pts',(18.8873014428472,0.478612406344963,3.88670662268212));
#27835=CARTESIAN_POINT('Ctrl Pts',(18.9319060218929,0.362263203066427,4.31165738429376));
#27836=CARTESIAN_POINT('Ctrl Pts',(18.960605322251,0.110926532249199,4.41500462017153));
#27837=CARTESIAN_POINT('Ctrl Pts',(18.9733993439214,-0.000368287616214533,
4.41603142687637));
#27838=CARTESIAN_POINT('Origin',(3.42660065607856,0.,4.));
#27839=CARTESIAN_POINT('',(18.2766006560786,0.000371443240938316,4.41601098728712));
#27840=CARTESIAN_POINT('',(18.3733993439214,0.000382963303967143,4.41588626824893));
#27841=CARTESIAN_POINT('',(3.42660065607856,4.87367679877478E-13,4.415875));
#27842=CARTESIAN_POINT('Ctrl Pts',(18.2766006560785,0.000371443240938293,
4.41601098728712));
#27843=CARTESIAN_POINT('Ctrl Pts',(18.2893173770028,-0.110264925490287,
4.41498710445335));
#27844=CARTESIAN_POINT('Ctrl Pts',(18.3179393766147,-0.360950442388199,
4.31267773405576));
#27845=CARTESIAN_POINT('Ctrl Pts',(18.3624666549143,-0.479157019140895,
3.88903254594255));
#27846=CARTESIAN_POINT('Ctrl Pts',(18.4101824909771,-0.165810997523729,
3.5369536330429));
#27847=CARTESIAN_POINT('Ctrl Pts',(18.4578983270399,0.299801814449608,3.61009732380414));
#27848=CARTESIAN_POINT('Ctrl Pts',(18.5056141631028,0.49010200717001,4.04129464153984));
#27849=CARTESIAN_POINT('Ctrl Pts',(18.5451816061157,0.274694351318236,4.36741107590602));
#27850=CARTESIAN_POINT('Ctrl Pts',(18.5688437704409,0.0678526130816757,
4.41522900951301));
#27851=CARTESIAN_POINT('Ctrl Pts',(18.5766006560786,2.82854505807215E-5,
4.41518799822097));
#27852=CARTESIAN_POINT('Ctrl Pts',(18.3733993439214,0.000382963303967157,
4.41588626824893));
#27853=CARTESIAN_POINT('Ctrl Pts',(18.3856472566872,-0.106256708375174,
4.41489942083623));
#27854=CARTESIAN_POINT('Ctrl Pts',(18.4138004481407,-0.352960303644862,
4.31875095920395));
#27855=CARTESIAN_POINT('Ctrl Pts',(18.4578589182817,-0.482217355384067,
3.90319273261591));
#27856=CARTESIAN_POINT('Ctrl Pts',(18.5055747543446,-0.179376629827252,
3.54203793877243));
#27857=CARTESIAN_POINT('Ctrl Pts',(18.5532905904074,0.288188414964166,3.60143675240633));
#27858=CARTESIAN_POINT('Ctrl Pts',(18.6010064264702,0.491105603945206,4.02684232898929));
#27859=CARTESIAN_POINT('Ctrl Pts',(18.6410426776416,0.282958802096416,4.36309886994028));
#27860=CARTESIAN_POINT('Ctrl Pts',(18.6651736501253,0.0718833454275778,
4.41512900400112));
#27861=CARTESIAN_POINT('Ctrl Pts',(18.6733993439214,-3.94222854199489E-5,
4.41518963037823));
#27862=CARTESIAN_POINT('Origin',(3.42660065607856,0.,4.));
#27863=CARTESIAN_POINT('',(17.9766006560786,-0.000210814279110197,4.41643020456723));
#27864=CARTESIAN_POINT('',(18.0733993439214,-0.000144384975211464,4.41650095473263));
#27865=CARTESIAN_POINT('',(3.42660065607856,4.87367679877478E-13,4.415875));
#27866=CARTESIAN_POINT('Ctrl Pts',(17.9766006560786,-0.000210814279110157,
4.41643020456723));
#27867=CARTESIAN_POINT('Ctrl Pts',(17.9779804261896,-0.0121834889824064,
4.41650424974197));
#27868=CARTESIAN_POINT('Ctrl Pts',(17.9952654749882,-0.162096873242269,
4.41059855206721));
#27869=CARTESIAN_POINT('Ctrl Pts',(18.0284558024744,-0.435175833605105,
4.22918817311999));
#27870=CARTESIAN_POINT('Ctrl Pts',(18.0761716385373,-0.428137176707308,
3.75791781814212));
#27871=CARTESIAN_POINT('Ctrl Pts',(18.1238874746,-0.0279335627019553,3.5089552556775));
#27872=CARTESIAN_POINT('Ctrl Pts',(18.1716033106629,0.397921871745719,3.71092663761881));
#27873=CARTESIAN_POINT('Ctrl Pts',(18.2193191467257,0.458359528554279,4.17835853620019));
#27874=CARTESIAN_POINT('Ctrl Pts',(18.2543182618643,0.193950155243433,4.40107745006558));
#27875=CARTESIAN_POINT('Ctrl Pts',(18.2734120983152,0.0281121206155762,
4.41626771302466));
#27876=CARTESIAN_POINT('Ctrl Pts',(18.2766006560785,0.000371443240938293,
4.41601098728712));
#27877=CARTESIAN_POINT('Ctrl Pts',(18.0733993439214,-0.000144384975211439,
4.41650095473263));
#27878=CARTESIAN_POINT('Ctrl Pts',(18.0743103058739,-0.00804551399413891,
4.41653639380418));
#27879=CARTESIAN_POINT('Ctrl Pts',(18.0911265465141,-0.153864670001157,
4.41274680364665));
#27880=CARTESIAN_POINT('Ctrl Pts',(18.1238480658419,-0.428237044548737,
4.24190547436581));
#27881=CARTESIAN_POINT('Ctrl Pts',(18.1715639019047,-0.435081213444543,
3.7706322547532));
#27882=CARTESIAN_POINT('Ctrl Pts',(18.2192797379675,-0.0423836094492617,
3.50999096487715));
#27883=CARTESIAN_POINT('Ctrl Pts',(18.2669955740304,0.389235515258945,3.69933251171255));
#27884=CARTESIAN_POINT('Ctrl Pts',(18.3147114100932,0.463413677146622,4.16478163940629));
#27885=CARTESIAN_POINT('Ctrl Pts',(18.3501793333902,0.202226156869028,4.39827758107438));
#27886=CARTESIAN_POINT('Ctrl Pts',(18.3697419779996,0.0322267809866215,
4.41618095209965));
#27887=CARTESIAN_POINT('Ctrl Pts',(18.3733993439214,0.000382963303967157,
4.41588626824893));
#27888=CARTESIAN_POINT('Origin',(3.42660065607856,0.,4.));
#27889=CARTESIAN_POINT('',(17.6766006560786,-0.000263771022561219,4.41536107794487));
#27890=CARTESIAN_POINT('',(17.7733993439214,-0.000309142357869163,4.41544738986064));
#27891=CARTESIAN_POINT('',(3.42660065607856,4.87367679877478E-13,4.415875));
#27892=CARTESIAN_POINT('Ctrl Pts',(17.6766006560786,-0.000263771022561289,
4.41536107794487));
#27893=CARTESIAN_POINT('Ctrl Pts',(17.6825487540639,-0.0522183410383149,
4.41566152300153));
#27894=CARTESIAN_POINT('Ctrl Pts',(17.7044021307368,-0.24273028972288,4.38249735042552));
#27895=CARTESIAN_POINT('Ctrl Pts',(17.7421607860973,-0.48225726547346,4.09660825404716));
#27896=CARTESIAN_POINT('Ctrl Pts',(17.7898766221602,-0.342084653792828,
3.64661166616396));
#27897=CARTESIAN_POINT('Ctrl Pts',(17.837592458223,0.112229559114723,3.52113702282083));
#27898=CARTESIAN_POINT('Ctrl Pts',(17.8853082942859,0.463481641013499,3.83540961967535));
#27899=CARTESIAN_POINT('Ctrl Pts',(17.9316443602377,0.391261919872151,4.28736986940801));
#27900=CARTESIAN_POINT('Ctrl Pts',(17.962075147502,0.125831334120538,4.41565069513148));
#27901=CARTESIAN_POINT('Ctrl Pts',(17.9766006560786,-0.000210814279110157,
4.41643020456723));
#27902=CARTESIAN_POINT('Ctrl Pts',(17.7733993439214,-0.000309142357869142,
4.41544738986064));
#27903=CARTESIAN_POINT('Ctrl Pts',(17.7788786337482,-0.0481438769258273,
4.41577602216682));
#27904=CARTESIAN_POINT('Ctrl Pts',(17.8002632022627,-0.23443694547481,4.38601982759396));
#27905=CARTESIAN_POINT('Ctrl Pts',(17.8375530494648,-0.479202773223469,
4.11076970247734));
#27906=CARTESIAN_POINT('Ctrl Pts',(17.8852688855277,-0.352344189444135,
3.65683998336499));
#27907=CARTESIAN_POINT('Ctrl Pts',(17.9329847215905,0.0980774850139738,
3.51803938772416));
#27908=CARTESIAN_POINT('Ctrl Pts',(17.9807005576534,0.458433095867658,3.82183063825345));
#27909=CARTESIAN_POINT('Ctrl Pts',(18.0275054317636,0.3989600628602,4.28031410431705));
#27910=CARTESIAN_POINT('Ctrl Pts',(18.0584050271863,0.129907183855675,4.41591763216682));
#27911=CARTESIAN_POINT('Ctrl Pts',(18.0733993439214,-0.000144384975211439,
4.41650095473263));
#27912=CARTESIAN_POINT('Origin',(3.42660065607856,0.,4.));
#27913=CARTESIAN_POINT('',(17.3766006560786,0.000316824918469052,4.41546566829253));
#27914=CARTESIAN_POINT('',(17.4733993439214,0.000273208168652644,4.41537657040552));
#27915=CARTESIAN_POINT('',(3.42660065607856,4.87367679877478E-13,4.415875));
#27916=CARTESIAN_POINT('Ctrl Pts',(17.3766006560786,0.000316824918469058,
4.41546566829253));
#27917=CARTESIAN_POINT('Ctrl Pts',(17.3871170819382,-0.0914824399419538,
4.4148173972429));
#27918=CARTESIAN_POINT('Ctrl Pts',(17.4135387864855,-0.323087181591141,
4.33950699049548));
#27919=CARTESIAN_POINT('Ctrl Pts',(17.4558657697204,-0.489877595596684,
3.956123284257));
#27920=CARTESIAN_POINT('Ctrl Pts',(17.5035816057832,-0.228040769637767,
3.56422180844494));
#27921=CARTESIAN_POINT('Ctrl Pts',(17.551297441846,0.243209403937772,3.57250215124727));
#27922=CARTESIAN_POINT('Ctrl Pts',(17.5990132779089,0.491116639619549,3.97336034645914));
#27923=CARTESIAN_POINT('Ctrl Pts',(17.6407810159864,0.313340775136121,4.34566293955037));
#27924=CARTESIAN_POINT('Ctrl Pts',(17.6666434753763,0.0867087440962768,
4.41485812965324));
#27925=CARTESIAN_POINT('Ctrl Pts',(17.6766006560786,-0.000263771022561289,
4.41536107794487));
#27926=CARTESIAN_POINT('Ctrl Pts',(17.4733993439214,0.000273208168652693,
4.41537657040552));
#27927=CARTESIAN_POINT('Ctrl Pts',(17.4834469616226,-0.0874810350323011,
4.41484969107387));
#27928=CARTESIAN_POINT('Ctrl Pts',(17.5093998580114,-0.314919534962053,
4.34468516187688));
#27929=CARTESIAN_POINT('Ctrl Pts',(17.5512580330878,-0.490957336521241,
3.97057010757845));
#27930=CARTESIAN_POINT('Ctrl Pts',(17.5989738691507,-0.240776309167652,
3.57112706567612));
#27931=CARTESIAN_POINT('Ctrl Pts',(17.6466897052135,0.230513307714322,3.56552463842171));
#27932=CARTESIAN_POINT('Ctrl Pts',(17.6944055412763,0.490119007219086,3.95890762096741));
#27933=CARTESIAN_POINT('Ctrl Pts',(17.7366420875123,0.321513805022658,4.34052027563639));
#27934=CARTESIAN_POINT('Ctrl Pts',(17.7629733550606,0.090710757213051,4.41482206853766));
#27935=CARTESIAN_POINT('Ctrl Pts',(17.7733993439214,-0.000309142357869142,
4.41544738986064));
#27936=CARTESIAN_POINT('Origin',(3.42660065607856,0.,4.));
#27937=CARTESIAN_POINT('',(17.0766006560786,0.000130763213737631,4.41651185352269));
#27938=CARTESIAN_POINT('',(17.1733993439214,0.000198609043858391,4.41644558073401));
#27939=CARTESIAN_POINT('',(3.42660065607856,4.87367679877478E-13,4.415875));
#27940=CARTESIAN_POINT('Ctrl Pts',(17.0766006560786,0.000130763213737628,
4.41651185352269));
#27941=CARTESIAN_POINT('Ctrl Pts',(17.0916854098125,-0.130696083011285,
4.41597403242798));
#27942=CARTESIAN_POINT('Ctrl Pts',(17.1226754422341,-0.400436570105288,
4.2789290971087));
#27943=CARTESIAN_POINT('Ctrl Pts',(17.1695707533433,-0.457413284126125,
3.81922856321607));
#27944=CARTESIAN_POINT('Ctrl Pts',(17.2172865894061,-0.0953372598908034,
3.51748986360026));
#27945=CARTESIAN_POINT('Ctrl Pts',(17.265002425469,0.354288437054553,3.6588476466131));
#27946=CARTESIAN_POINT('Ctrl Pts',(17.3127182615318,0.478565610824392,4.11349088504481));
#27947=CARTESIAN_POINT('Ctrl Pts',(17.349917671735,0.232837083242772,4.38668157013213));
#27948=CARTESIAN_POINT('Ctrl Pts',(17.3712118032506,0.0473568302064652,
4.41579785693967));
#27949=CARTESIAN_POINT('Ctrl Pts',(17.3766006560786,0.000316824918469058,
4.41546566829253));
#27950=CARTESIAN_POINT('Ctrl Pts',(17.1733993439214,0.000198609043858397,
4.41644558073401));
#27951=CARTESIAN_POINT('Ctrl Pts',(17.1880152894969,-0.126615914365149,
4.41569892234974));
#27952=CARTESIAN_POINT('Ctrl Pts',(17.2185365137601,-0.392752582168809,
4.28602487069057));
#27953=CARTESIAN_POINT('Ctrl Pts',(17.2649630167107,-0.462538907526291,
3.83277863809798));
#27954=CARTESIAN_POINT('Ctrl Pts',(17.3126788527736,-0.109506707187599,
3.52050703244687));
#27955=CARTESIAN_POINT('Ctrl Pts',(17.3603946888365,0.344087187338735,3.64856119684745));
#27956=CARTESIAN_POINT('Ctrl Pts',(17.4081105248993,0.481700523269991,4.09934702176407));
#27957=CARTESIAN_POINT('Ctrl Pts',(17.4457787432609,0.241130489326423,4.3831889686244));
#27958=CARTESIAN_POINT('Ctrl Pts',(17.467541682935,0.0514330574063097,4.41568373580506));
#27959=CARTESIAN_POINT('Ctrl Pts',(17.4733993439214,0.000273208168652693,
4.41537657040552));
#27960=CARTESIAN_POINT('Origin',(3.42660065607856,0.,4.));
#27961=CARTESIAN_POINT('',(16.7766006560786,-0.000383680820852129,4.41586226484778));
#27962=CARTESIAN_POINT('',(16.8733993439214,-0.000374684679869397,4.41598699190495));
#27963=CARTESIAN_POINT('',(3.42660065607856,4.87367679877478E-13,4.415875));
#27964=CARTESIAN_POINT('Ctrl Pts',(16.7766006560786,-0.000383680820852189,
4.41586226484779));
#27965=CARTESIAN_POINT('Ctrl Pts',(16.7803484589992,-0.0330197262611539,
4.41616320579436));
#27966=CARTESIAN_POINT('Ctrl Pts',(16.8000015406075,-0.203823433586872,
4.39772119122577));
#27967=CARTESIAN_POINT('Ctrl Pts',(16.8355599009034,-0.464342533291602,
4.16214572651883));
#27968=CARTESIAN_POINT('Ctrl Pts',(16.8832757369663,-0.387520750342007,
3.69712561530174));
#27969=CARTESIAN_POINT('Ctrl Pts',(16.9309915730291,0.0451673004198413,
3.51023971187451));
#27970=CARTESIAN_POINT('Ctrl Pts',(16.978707409092,0.436377524217892,3.7731082169636));
#27971=CARTESIAN_POINT('Ctrl Pts',(17.0264232451548,0.426855552995382,4.24433493759383));
#27972=CARTESIAN_POINT('Ctrl Pts',(17.0590543274837,0.152277829190936,4.41314658311127));
#27973=CARTESIAN_POINT('Ctrl Pts',(17.0757801311249,0.00724700082869906,
4.41654110793655));
#27974=CARTESIAN_POINT('Ctrl Pts',(17.0766006560786,0.000130763213737628,
4.41651185352269));
#27975=CARTESIAN_POINT('Ctrl Pts',(16.8733993439214,-0.000374684679869387,
4.41598699190495));
#27976=CARTESIAN_POINT('Ctrl Pts',(16.8766783386836,-0.0289064002234668,
4.4162516892709));
#27977=CARTESIAN_POINT('Ctrl Pts',(16.8958626121335,-0.195546116663039,
4.40054826733105));
#27978=CARTESIAN_POINT('Ctrl Pts',(16.9309521642709,-0.459365614209645,
4.17575112327883));
#27979=CARTESIAN_POINT('Ctrl Pts',(16.9786680003337,-0.396272847821079,
3.70867019559999));
#27980=CARTESIAN_POINT('Ctrl Pts',(17.0263838363966,0.0307233721630972,
3.5091219099869));
#27981=CARTESIAN_POINT('Ctrl Pts',(17.0740996724594,0.429505846750062,3.76035452756312));
#27982=CARTESIAN_POINT('Ctrl Pts',(17.1218155085223,0.433866493469502,4.23165726989771));
#27983=CARTESIAN_POINT('Ctrl Pts',(17.1549153990096,0.160507997039396,4.41102293437065));
#27984=CARTESIAN_POINT('Ctrl Pts',(17.1721100108093,0.0113854435377776,
4.41651144656345));
#27985=CARTESIAN_POINT('Ctrl Pts',(17.1733993439214,0.000198609043858397,
4.41644558073401));
#27986=CARTESIAN_POINT('Origin',(3.42660065607856,0.,4.));
#27987=CARTESIAN_POINT('',(16.4766006560786,5.2409936866527E-5,4.41519222098806));
#27988=CARTESIAN_POINT('',(16.5733993439214,-1.52272386678698E-5,4.41518677123726));
#27989=CARTESIAN_POINT('',(3.42660065607856,4.87367679877478E-13,4.415875));
#27990=CARTESIAN_POINT('Ctrl Pts',(16.4766006560786,5.2409936866539E-5,
4.41519222098806));
#27991=CARTESIAN_POINT('Ctrl Pts',(16.4849167868736,-0.0726599781719204,
4.41511070701236));
#27992=CARTESIAN_POINT('Ctrl Pts',(16.5091381963562,-0.284551613766983,
4.36224737480062));
#27993=CARTESIAN_POINT('Ctrl Pts',(16.5492648845264,-0.4912502013546,4.02405128938415));
#27994=CARTESIAN_POINT('Ctrl Pts',(16.5969807205893,-0.285919008936969,
3.59980561575594));
#27995=CARTESIAN_POINT('Ctrl Pts',(16.6446965566521,0.181976008816936,3.54306460296116));
#27996=CARTESIAN_POINT('Ctrl Pts',(16.6924123927149,0.482759657613431,3.90593439612197));
#27997=CARTESIAN_POINT('Ctrl Pts',(16.7363804258571,0.351413532087107,4.31989995948535));
#27998=CARTESIAN_POINT('Ctrl Pts',(16.7644431803116,0.105484194296011,4.41488604428797));
#27999=CARTESIAN_POINT('Ctrl Pts',(16.7766006560786,-0.000383680820852189,
4.41586226484779));
#28000=CARTESIAN_POINT('Ctrl Pts',(16.5733993439214,-1.52272386678906E-5,
4.41518677123726));
#28001=CARTESIAN_POINT('Ctrl Pts',(16.5812466665579,-0.0686308195205231,
4.41520910309265));
#28002=CARTESIAN_POINT('Ctrl Pts',(16.6049992678821,-0.276289552895371,
4.36659242126669));
#28003=CARTESIAN_POINT('Ctrl Pts',(16.6446571478939,-0.490328743065594,
4.03850907134293));
#28004=CARTESIAN_POINT('Ctrl Pts',(16.6923729839567,-0.297581432841348,
3.60840005658827));
#28005=CARTESIAN_POINT('Ctrl Pts',(16.7400888200196,0.168439486040012,3.53790329540825));
#28006=CARTESIAN_POINT('Ctrl Pts',(16.7878046560824,0.479779833116189,3.89175704832657));
#28007=CARTESIAN_POINT('Ctrl Pts',(16.832241497383,0.359412856911567,4.31386464726761));
#28008=CARTESIAN_POINT('Ctrl Pts',(16.860773059996,0.109491163683573,4.41496773315674));
#28009=CARTESIAN_POINT('Ctrl Pts',(16.8733993439214,-0.000374684679869387,
4.41598699190495));
#28010=CARTESIAN_POINT('Origin',(3.42660065607856,0.,4.));
#28011=CARTESIAN_POINT('',(16.1766006560786,0.000364146841390381,4.41605523138122));
#28012=CARTESIAN_POINT('',(16.2733993439214,0.000380345806842055,4.41593091837313));
#28013=CARTESIAN_POINT('',(3.42660065607856,4.87367679877478E-13,4.415875));
#28014=CARTESIAN_POINT('Ctrl Pts',(16.1766006560786,0.000364146841390366,
4.41605523138122));
#28015=CARTESIAN_POINT('Ctrl Pts',(16.1894851147479,-0.111700864104492,
4.41502624848758));
#28016=CARTESIAN_POINT('Ctrl Pts',(16.2182748521048,-0.363797281821349,
4.31045679267864));
#28017=CARTESIAN_POINT('Ctrl Pts',(16.2629698681494,-0.477960913216358,
3.88398883549692));
#28018=CARTESIAN_POINT('Ctrl Pts',(16.3106857042122,-0.160921706883503,
3.53523185446324));
#28019=CARTESIAN_POINT('Ctrl Pts',(16.358401540275,0.303894378979202,3.6132786128531));
#28020=CARTESIAN_POINT('Ctrl Pts',(16.4061173763379,0.489639580609251,4.04645757153336));
#28021=CARTESIAN_POINT('Ctrl Pts',(16.4455170816057,0.271734615807756,4.36891289568356));
#28022=CARTESIAN_POINT('Ctrl Pts',(16.4690115081859,0.0664083969439258,
4.41526660914191));
#28023=CARTESIAN_POINT('Ctrl Pts',(16.4766006560786,5.2409936866539E-5,
4.41519222098806));
#28024=CARTESIAN_POINT('Ctrl Pts',(16.2733993439214,0.000380345806842052,
4.41593091837313));
#28025=CARTESIAN_POINT('Ctrl Pts',(16.2858149944323,-0.107690075887363,
4.41492720978183));
#28026=CARTESIAN_POINT('Ctrl Pts',(16.3141359236307,-0.35582464097624,4.31660057631701));
#28027=CARTESIAN_POINT('Ctrl Pts',(16.3583621315169,-0.481170314810987,
3.89811598262401));
#28028=CARTESIAN_POINT('Ctrl Pts',(16.4060779675797,-0.174540169679895,
3.54017290856226));
#28029=CARTESIAN_POINT('Ctrl Pts',(16.4537938036425,0.292372898913969,3.60449612791703));
#28030=CARTESIAN_POINT('Ctrl Pts',(16.5015096397054,0.490795435699827,4.0320166386149));
#28031=CARTESIAN_POINT('Ctrl Pts',(16.5413781531317,0.280003220364278,4.36466130212541));
#28032=CARTESIAN_POINT('Ctrl Pts',(16.5653413878703,0.0704421061260754,
4.4151638399628));
#28033=CARTESIAN_POINT('Ctrl Pts',(16.5733993439214,-1.52272386678906E-5,
4.41518677123726));
#28034=CARTESIAN_POINT('Origin',(3.42660065607856,0.,4.));
#28035=CARTESIAN_POINT('',(15.8766006560786,-0.00023258108979477,4.41639972388928));
#28036=CARTESIAN_POINT('',(15.9733993439214,-0.000169011902647176,4.4164782780785));
#28037=CARTESIAN_POINT('',(3.42660065607856,4.87367679877478E-13,4.415875));
#28038=CARTESIAN_POINT('Ctrl Pts',(15.8766006560786,-0.000232581089794846,
4.41639972388928));
#28039=CARTESIAN_POINT('Ctrl Pts',(15.8781481639346,-0.0136633580705269,
4.41648966084242));
#28040=CARTESIAN_POINT('Ctrl Pts',(15.8956009504782,-0.165044849757219,
4.40979870506104));
#28041=CARTESIAN_POINT('Ctrl Pts',(15.9289590157095,-0.437567097060412,
4.22458909239344));
#28042=CARTESIAN_POINT('Ctrl Pts',(15.9766748517724,-0.425562075928853,
3.75341909160864));
#28043=CARTESIAN_POINT('Ctrl Pts',(16.0243906878352,-0.0227568523576073,
3.50868813313462));
#28044=CARTESIAN_POINT('Ctrl Pts',(16.072106523898,0.400946338892803,3.71513642180785));
#28045=CARTESIAN_POINT('Ctrl Pts',(16.1198223599609,0.456454337785543,4.1831793175245));
#28046=CARTESIAN_POINT('Ctrl Pts',(16.1546537373544,0.190990792023167,4.40204523666471));
#28047=CARTESIAN_POINT('Ctrl Pts',(16.1735798360603,0.0266382990664043,
4.41629648110721));
#28048=CARTESIAN_POINT('Ctrl Pts',(16.1766006560786,0.000364146841390366,
4.41605523138122));
#28049=CARTESIAN_POINT('Ctrl Pts',(15.9733993439214,-0.000169011902647174,
4.4164782780785));
#28050=CARTESIAN_POINT('Ctrl Pts',(15.974478043619,-0.00952634975615679,
4.4165263696097));
#28051=CARTESIAN_POINT('Ctrl Pts',(15.9914620220042,-0.156808910032117,
4.4119928338179));
#28052=CARTESIAN_POINT('Ctrl Pts',(16.024351279077,-0.430762722000766,4.23737881579128));
#28053=CARTESIAN_POINT('Ctrl Pts',(16.0720671151398,-0.432639725453012,
3.76605963834362));
#28054=CARTESIAN_POINT('Ctrl Pts',(16.1197829512026,-0.0372170120039125,
3.50957149464017));
#28055=CARTESIAN_POINT('Ctrl Pts',(16.1674987872655,0.392382656225717,3.70345139362117));
#28056=CARTESIAN_POINT('Ctrl Pts',(16.2152146233283,0.461651293660056,4.16965644082667));
#28057=CARTESIAN_POINT('Ctrl Pts',(16.2505148088803,0.199264245432362,4.39929555075695));
#28058=CARTESIAN_POINT('Ctrl Pts',(16.2699097157447,0.0307553622657438,
4.41621302761729));
#28059=CARTESIAN_POINT('Ctrl Pts',(16.2733993439214,0.000380345806842052,
4.41593091837313));
#28060=CARTESIAN_POINT('Origin',(3.42660065607856,0.,4.));
#28061=CARTESIAN_POINT('',(15.5766006560786,-0.000245472137683418,4.41533389801214));
#28062=CARTESIAN_POINT('',(15.6733993439214,-0.00029394562308721,4.41541483535501));
#28063=CARTESIAN_POINT('',(3.42660065607856,4.87367679877478E-13,4.415875));
#28064=CARTESIAN_POINT('Ctrl Pts',(15.5766006560786,-0.000245472137683396,
4.41533389801214));
#28065=CARTESIAN_POINT('Ctrl Pts',(15.5827164918089,-0.0536739331835165,
4.41562024719655));
#28066=CARTESIAN_POINT('Ctrl Pts',(15.6047376062269,-0.245697356182912,
4.38119912149661));
#28067=CARTESIAN_POINT('Ctrl Pts',(15.6426639993325,-0.483248643997369,
4.09152034160055));
#28068=CARTESIAN_POINT('Ctrl Pts',(15.6903798353953,-0.338341267922855,
3.64302603558196));
#28069=CARTESIAN_POINT('Ctrl Pts',(15.7380956714582,0.117270100534806,3.52234641383892));
#28070=CARTESIAN_POINT('Ctrl Pts',(15.785811507521,0.465190531238913,3.84030342991275));
#28071=CARTESIAN_POINT('Ctrl Pts',(15.8319798357278,0.388490242362186,4.28984418805176));
#28072=CARTESIAN_POINT('Ctrl Pts',(15.862242885247,0.124378106492246,4.41556528924811));
#28073=CARTESIAN_POINT('Ctrl Pts',(15.8766006560786,-0.000232581089794846,
4.41639972388928));
#28074=CARTESIAN_POINT('Ctrl Pts',(15.6733993439214,-0.000293945623087231,
4.41541483535501));
#28075=CARTESIAN_POINT('Ctrl Pts',(15.6790463714933,-0.0496027558454661,
4.41573527017753));
#28076=CARTESIAN_POINT('Ctrl Pts',(15.7005986777528,-0.23740431922453,4.38477730872224));
#28077=CARTESIAN_POINT('Ctrl Pts',(15.7380562626999,-0.480343569999647,
4.1057131950703));
#28078=CARTESIAN_POINT('Ctrl Pts',(15.7857720987628,-0.348708030819167,
3.6531456586776));
#28079=CARTESIAN_POINT('Ctrl Pts',(15.8334879348256,0.103151458625294,3.5190998009613));
#28080=CARTESIAN_POINT('Ctrl Pts',(15.8812037708885,0.460285376424935,3.82667199562295));
#28081=CARTESIAN_POINT('Ctrl Pts',(15.9278409072537,0.396214095655672,4.28286244744368));
#28082=CARTESIAN_POINT('Ctrl Pts',(15.9585727649314,0.128446309981357,4.41581726659612));
#28083=CARTESIAN_POINT('Ctrl Pts',(15.9733993439214,-0.000169011902647174,
4.4164782780785));
#28084=CARTESIAN_POINT('Origin',(3.42660065607856,0.,4.));
#28085=CARTESIAN_POINT('',(15.2766006560786,0.000330084823988869,4.41550084660604));
#28086=CARTESIAN_POINT('',(15.3733993439214,0.000289868078815952,4.41540680128743));
#28087=CARTESIAN_POINT('',(3.42660065607856,4.87367679877478E-13,4.415875));
#28088=CARTESIAN_POINT('Ctrl Pts',(15.2766006560786,0.000330084823988861,
4.41550084660604));
#28089=CARTESIAN_POINT('Ctrl Pts',(15.2872848196833,-0.0929135079625664,
4.41481081573461));
#28090=CARTESIAN_POINT('Ctrl Pts',(15.3138742619755,-0.32600240339937,4.33760928826424));
#28091=CARTESIAN_POINT('Ctrl Pts',(15.3563689829555,-0.489387968817152,
3.95096286275689));
#28092=CARTESIAN_POINT('Ctrl Pts',(15.4040848190183,-0.223435404337718,
3.56184267101825));
#28093=CARTESIAN_POINT('Ctrl Pts',(15.4518006550811,0.24770132994065,3.57508909640066));
#28094=CARTESIAN_POINT('Ctrl Pts',(15.499516491144,0.491370121559653,3.97853774265298));
#28095=CARTESIAN_POINT('Ctrl Pts',(15.5411164914764,0.310410063586636,4.3474585185963));
#28096=CARTESIAN_POINT('Ctrl Pts',(15.5668112131213,0.0852759340546689,
4.41487554708019));
#28097=CARTESIAN_POINT('Ctrl Pts',(15.5766006560786,-0.000245472137683396,
4.41533389801214));
#28098=CARTESIAN_POINT('Ctrl Pts',(15.3733993439214,0.000289868078815973,
4.41540680128743));
#28099=CARTESIAN_POINT('Ctrl Pts',(15.3836146993676,-0.0889130762729256,
4.41483587894927));
#28100=CARTESIAN_POINT('Ctrl Pts',(15.4097353335015,-0.317845114095608,
4.34285359523591));
#28101=CARTESIAN_POINT('Ctrl Pts',(15.4517612463229,-0.490619905976795,
3.96539750426199));
#28102=CARTESIAN_POINT('Ctrl Pts',(15.4994770823858,-0.236243011612202,
3.56861332390027));
#28103=CARTESIAN_POINT('Ctrl Pts',(15.5471929184486,0.235079475381852,3.56797816593814));
#28104=CARTESIAN_POINT('Ctrl Pts',(15.5949087545115,0.490524862970081,3.9640753057054));
#28105=CARTESIAN_POINT('Ctrl Pts',(15.6369775630024,0.318592711010818,4.34238143198936));
#28106=CARTESIAN_POINT('Ctrl Pts',(15.6631410928057,0.0892792238074376,
4.41483274135358));
#28107=CARTESIAN_POINT('Ctrl Pts',(15.6733993439214,-0.000293945623087231,
4.41541483535501));
#28108=CARTESIAN_POINT('Origin',(3.42660065607856,0.,4.));
#28109=CARTESIAN_POINT('',(14.9766006560786,0.000104941934236194,4.41652945172571));
#28110=CARTESIAN_POINT('',(15.0733993439214,0.000175165248676303,4.41647198785975));
#28111=CARTESIAN_POINT('',(3.42660065607856,4.87367679877478E-13,4.415875));
#28112=CARTESIAN_POINT('Ctrl Pts',(14.9766006560786,0.000104941934236227,
4.41652945172572));
#28113=CARTESIAN_POINT('Ctrl Pts',(14.9918531475576,-0.132161740438444,
4.41608294134065));
#28114=CARTESIAN_POINT('Ctrl Pts',(15.0230109177242,-0.40316752945992,4.27633971254324));
#28115=CARTESIAN_POINT('Ctrl Pts',(15.0700739665785,-0.455482716161518,
3.8144178884426));
#28116=CARTESIAN_POINT('Ctrl Pts',(15.1177898026413,-0.0902467530057116,
3.51651189422706));
#28117=CARTESIAN_POINT('Ctrl Pts',(15.1655056387041,0.357864192060027,3.66260046696357));
#28118=CARTESIAN_POINT('Ctrl Pts',(15.2132214747669,0.47734294310866,4.11852822244656));
#28119=CARTESIAN_POINT('Ctrl Pts',(15.2502531472251,0.229869832763757,4.3878938710325));
#28120=CARTESIAN_POINT('Ctrl Pts',(15.2713795409956,0.0458961718568525,
4.41583804947224));
#28121=CARTESIAN_POINT('Ctrl Pts',(15.2766006560786,0.000330084823988861,
4.41550084660604));
#28122=CARTESIAN_POINT('Ctrl Pts',(15.0733993439214,0.000175165248676341,
4.41647198785975));
#28123=CARTESIAN_POINT('Ctrl Pts',(15.0881830272419,-0.128073190246274,
4.41579247653651));
#28124=CARTESIAN_POINT('Ctrl Pts',(15.1188719892501,-0.395510344386944,
4.28350986851547));
#28125=CARTESIAN_POINT('Ctrl Pts',(15.1654662299459,-0.46075086019608,3.82791319143947));
#28126=CARTESIAN_POINT('Ctrl Pts',(15.2131820660087,-0.104447211543591,
3.51937956259357));
#28127=CARTESIAN_POINT('Ctrl Pts',(15.2608979020716,0.347771918596306,3.652207076714));
#28128=CARTESIAN_POINT('Ctrl Pts',(15.3086137381344,0.480626744730421,4.10441818376995));
#28129=CARTESIAN_POINT('Ctrl Pts',(15.346114218751,0.238163166260598,4.38445638366753));
#28130=CARTESIAN_POINT('Ctrl Pts',(15.36770942068,0.0499756483669043,4.41572480336754));
#28131=CARTESIAN_POINT('Ctrl Pts',(15.3733993439214,0.000289868078815973,
4.41540680128743));
#28132=CARTESIAN_POINT('Origin',(3.42660065607856,0.,4.));
#28133=CARTESIAN_POINT('',(14.6766006560786,-0.000383732061438463,4.41581798673635));
#28134=CARTESIAN_POINT('',(14.7733993439214,-0.000379407362125217,4.41594234696178));
#28135=CARTESIAN_POINT('',(3.42660065607856,4.87367679877478E-13,4.415875));
#28136=CARTESIAN_POINT('Ctrl Pts',(14.6766006560786,-0.000383732061438387,
4.41581798673635));
#28137=CARTESIAN_POINT('Ctrl Pts',(14.6805161967443,-0.0344897130604965,
4.41612948839573));
#28138=CARTESIAN_POINT('Ctrl Pts',(14.7003370160976,-0.206786574235377,
4.39667515056147));
#28139=CARTESIAN_POINT('Ctrl Pts',(14.7360631141386,-0.466025611307368,
4.15724297904063));
#28140=CARTESIAN_POINT('Ctrl Pts',(14.7837789502014,-0.38430721152129,3.69305832471834));
#28141=CARTESIAN_POINT('Ctrl Pts',(14.8314947862642,0.0503264139313189,
3.51074293371195));
#28142=CARTESIAN_POINT('Ctrl Pts',(14.8792106223271,0.438744519099385,3.77771983486548));
#28143=CARTESIAN_POINT('Ctrl Pts',(14.9269264583899,0.42425678142631,4.24882003188202));
#28144=CARTESIAN_POINT('Ctrl Pts',(14.9593898029737,0.149335702075518,4.41387566524124));
#28145=CARTESIAN_POINT('Ctrl Pts',(14.97594786887,0.00576578747519492,4.41654856180149));
#28146=CARTESIAN_POINT('Ctrl Pts',(14.9766006560786,0.000104941934236227,
4.41652945172572));
#28147=CARTESIAN_POINT('Ctrl Pts',(14.7733993439214,-0.000379407362125234,
4.41594234696178));
#28148=CARTESIAN_POINT('Ctrl Pts',(14.7768460764287,-0.0303789312965351,
4.41622104989506));
#28149=CARTESIAN_POINT('Ctrl Pts',(14.7961980876235,-0.198506931257387,
4.39955296987463));
#28150=CARTESIAN_POINT('Ctrl Pts',(14.831455377506,-0.461192356972643,4.17090007232882));
#28151=CARTESIAN_POINT('Ctrl Pts',(14.8791712135689,-0.393180492164677,
3.7045100248179));
#28152=CARTESIAN_POINT('Ctrl Pts',(14.9268870496317,0.0358950684576197,
3.50947296821438));
#28153=CARTESIAN_POINT('Ctrl Pts',(14.9746028856945,0.432007635398663,3.76489443262817));
#28154=CARTESIAN_POINT('Ctrl Pts',(15.0223187217574,0.431400943461215,4.23621695712364));
#28155=CARTESIAN_POINT('Ctrl Pts',(15.0552508744997,0.157562060208247,4.41179740605063));
#28156=CARTESIAN_POINT('Ctrl Pts',(15.0722777485543,0.00990499767517082,
4.41652354042182));
#28157=CARTESIAN_POINT('Ctrl Pts',(15.0733993439214,0.000175165248676341,
4.41647198785975));
#28158=CARTESIAN_POINT('Origin',(3.42660065607856,0.,4.));
#28159=CARTESIAN_POINT('',(14.3766006560786,7.63317591858645E-5,4.41519896243726));
#28160=CARTESIAN_POINT('',(14.4733993439214,9.02664646690309E-6,4.41518644689786));
#28161=CARTESIAN_POINT('',(3.42660065607856,4.87367679877478E-13,4.415875));
#28162=CARTESIAN_POINT('Ctrl Pts',(14.3766006560786,7.63317591858798E-5,
4.41519896243726));
#28163=CARTESIAN_POINT('Ctrl Pts',(14.3850845246186,-0.0740996743586071,
4.41507773880187));
#28164=CARTESIAN_POINT('Ctrl Pts',(14.4094736718463,-0.287504468978829,
4.360651101065));
#28165=CARTESIAN_POINT('Ctrl Pts',(14.4497680977616,-0.491476396904638,
4.01887262932433));
#28166=CARTESIAN_POINT('Ctrl Pts',(14.4974839338244,-0.281685449746218,
3.59681451879656));
#28167=CARTESIAN_POINT('Ctrl Pts',(14.5451997698872,0.186781580201919,3.54500783946397));
#28168=CARTESIAN_POINT('Ctrl Pts',(14.59291560595,0.483724211046603,3.91102746210588));
#28169=CARTESIAN_POINT('Ctrl Pts',(14.6367159013472,0.348540265561382,4.32201186060262));
#28170=CARTESIAN_POINT('Ctrl Pts',(14.6646109180567,0.104051852208848,4.41486414061182));
#28171=CARTESIAN_POINT('Ctrl Pts',(14.6766006560786,-0.000383732061438387,
4.41581798673635));
#28172=CARTESIAN_POINT('Ctrl Pts',(14.4733993439214,9.0266464668684E-6,
4.41518644689786));
#28173=CARTESIAN_POINT('Ctrl Pts',(14.481414404303,-0.0700733710850898,
4.41517292627706));
#28174=CARTESIAN_POINT('Ctrl Pts',(14.5053347433722,-0.279247125311621,
4.3650573561381));
#28175=CARTESIAN_POINT('Ctrl Pts',(14.545160361129,-0.490707361486496,4.03333931965322));
#28176=CARTESIAN_POINT('Ctrl Pts',(14.5928761971918,-0.293437803431633,
3.60528557111603));
#28177=CARTESIAN_POINT('Ctrl Pts',(14.6405920332547,0.173300204635467,3.53970415608515));
#28178=CARTESIAN_POINT('Ctrl Pts',(14.6883078693175,0.480893968219416,3.89681949708321));
#28179=CARTESIAN_POINT('Ctrl Pts',(14.7325769728731,0.356556173733762,4.31604662460621));
#28180=CARTESIAN_POINT('Ctrl Pts',(14.760940797741,0.10805675748006,4.41493494840171));
#28181=CARTESIAN_POINT('Ctrl Pts',(14.7733993439214,-0.000379407362125234,
4.41594234696178));
#28182=CARTESIAN_POINT('Origin',(3.42660065607856,0.,4.));
#28183=CARTESIAN_POINT('',(14.0766006560786,0.000355193352615291,4.41609897421413));
#28184=CARTESIAN_POINT('',(14.1733993439214,0.000376051973931104,4.41597558743442));
#28185=CARTESIAN_POINT('',(3.42660065607856,4.87367679877478E-13,4.415875));
#28186=CARTESIAN_POINT('Ctrl Pts',(14.0766006560786,0.000355193352615277,
4.41609897421413));
#28187=CARTESIAN_POINT('Ctrl Pts',(14.0896528524929,-0.113137957382804,
4.41506966208575));
#28188=CARTESIAN_POINT('Ctrl Pts',(14.1186103275949,-0.366637448157006,
4.30821039815648));
#28189=CARTESIAN_POINT('Ctrl Pts',(14.1634730813845,-0.476711717661702,
3.87895801102093));
#28190=CARTESIAN_POINT('Ctrl Pts',(14.2111889174473,-0.156014541823709,
3.53356170012368));
#28191=CARTESIAN_POINT('Ctrl Pts',(14.2589047535102,0.307953188363286,3.61650285707861));
#28192=CARTESIAN_POINT('Ctrl Pts',(14.306620589573,0.4891227672074,4.05161534124029));
#28193=CARTESIAN_POINT('Ctrl Pts',(14.3458525570958,0.268773633406098,4.37039329245586));
#28194=CARTESIAN_POINT('Ctrl Pts',(14.369179245931,0.0649630708582953,4.4153050049005));
#28195=CARTESIAN_POINT('Ctrl Pts',(14.3766006560786,7.63317591858798E-5,
4.41519896243726));
#28196=CARTESIAN_POINT('Ctrl Pts',(14.1733993439214,0.000376051973931098,
4.41597558743442));
#28197=CARTESIAN_POINT('Ctrl Pts',(14.1859827321773,-0.109124255432428,
4.41495896305428));
#28198=CARTESIAN_POINT('Ctrl Pts',(14.2144713991208,-0.358682910161539,
4.31442504752535));
#28199=CARTESIAN_POINT('Ctrl Pts',(14.258865344752,-0.480069828122688,3.8930505494253));
#28200=CARTESIAN_POINT('Ctrl Pts',(14.3065811808148,-0.169684322438749,
3.53835895376334));
#28201=CARTESIAN_POINT('Ctrl Pts',(14.3542970168777,0.296524907469595,3.60759943412104));
#28202=CARTESIAN_POINT('Ctrl Pts',(14.4020128529405,0.49043075222644,4.0371873919842));
#28203=CARTESIAN_POINT('Ctrl Pts',(14.4417136286217,0.277046036654804,4.36620192284859));
#28204=CARTESIAN_POINT('Ctrl Pts',(14.4655091256154,0.0689998253659925,
4.41519975692232));
#28205=CARTESIAN_POINT('Ctrl Pts',(14.4733993439214,9.0266464668684E-6,
4.41518644689786));
#28206=CARTESIAN_POINT('Origin',(3.42660065607856,0.,4.));
#28207=CARTESIAN_POINT('',(13.7766006560786,-0.000253139125078747,4.41636688691614));
#28208=CARTESIAN_POINT('',(13.8733993439214,-0.000192710833643805,4.4164526008213));
#28209=CARTESIAN_POINT('',(3.42660065607856,4.87367679877478E-13,4.415875));
#28210=CARTESIAN_POINT('Ctrl Pts',(13.7766006560786,-0.000253139125078718,
4.41636688691614));
#28211=CARTESIAN_POINT('Ctrl Pts',(13.7783159016796,-0.0151427949580853,
4.41647347977994));
#28212=CARTESIAN_POINT('Ctrl Pts',(13.7959364259683,-0.167994124135391,
4.40898222403799));
#28213=CARTESIAN_POINT('Ctrl Pts',(13.8294622289446,-0.439909757638992,
4.21996506537626));
#28214=CARTESIAN_POINT('Ctrl Pts',(13.8771780650075,-0.422939705734467,
3.74894775411238));
#28215=CARTESIAN_POINT('Ctrl Pts',(13.9248939010703,-0.0175776142901187,
3.50847558318244));
#28216=CARTESIAN_POINT('Ctrl Pts',(13.9726097371332,0.403926270823208,3.71937784729135));
#28217=CARTESIAN_POINT('Ctrl Pts',(14.020325573196,0.454498446235019,4.18797975215946));
#28218=CARTESIAN_POINT('Ctrl Pts',(14.0549892128445,0.188032430710383,4.40299531219535));
#28219=CARTESIAN_POINT('Ctrl Pts',(14.0737475738053,0.0251636842930195,
4.41632397176197));
#28220=CARTESIAN_POINT('Ctrl Pts',(14.0766006560786,0.000355193352615277,
4.41609897421413));
#28221=CARTESIAN_POINT('Ctrl Pts',(13.8733993439214,-0.000192710833643682,
4.4164526008213));
#28222=CARTESIAN_POINT('Ctrl Pts',(13.874645781364,-0.0110068809386406,
4.41651469495978));
#28223=CARTESIAN_POINT('Ctrl Pts',(13.8917974974943,-0.15975450351916,4.41122255187585));
#28224=CARTESIAN_POINT('Ctrl Pts',(13.9248544923121,-0.433240552373761,
4.23282579030437));
#28225=CARTESIAN_POINT('Ctrl Pts',(13.9725703283749,-0.430150181893835,
3.76151300691929));
#28226=CARTESIAN_POINT('Ctrl Pts',(14.0202861644378,-0.032046280669499,
3.50920649887429));
#28227=CARTESIAN_POINT('Ctrl Pts',(14.0680020005006,0.39548621318905,3.70760321474174));
#28228=CARTESIAN_POINT('Ctrl Pts',(14.1157178365634,0.459837632138507,4.1745123976147));
#28229=CARTESIAN_POINT('Ctrl Pts',(14.1508502843704,0.196303200904851,4.40029544879449));
#28230=CARTESIAN_POINT('Ctrl Pts',(14.1700774534897,0.0292830534939708,
4.41624396624722));
#28231=CARTESIAN_POINT('Ctrl Pts',(14.1733993439214,0.000376051973931098,
4.41597558743442));
#28232=CARTESIAN_POINT('Origin',(3.42660065607856,0.,4.));
#28233=CARTESIAN_POINT('',(13.4766006560786,-0.000226204729293368,4.4153088088013));
#28234=CARTESIAN_POINT('',(13.5733993439214,-0.000277574767750837,4.41538411867388));
#28235=CARTESIAN_POINT('',(3.42660065607856,4.87367679877478E-13,4.415875));
#28236=CARTESIAN_POINT('Ctrl Pts',(13.4766006560786,-0.000226204729293314,
4.4153088088013));
#28237=CARTESIAN_POINT('Ctrl Pts',(13.482884229554,-0.0551283395969922,
4.41557894444213));
#28238=CARTESIAN_POINT('Ctrl Pts',(13.505073081717,-0.248664136397309,4.37988069596112));
#28239=CARTESIAN_POINT('Ctrl Pts',(13.5431672125676,-0.484186345555107,
4.08642226350871));
#28240=CARTESIAN_POINT('Ctrl Pts',(13.5908830486304,-0.334560300710407,
3.63948005597396));
#28241=CARTESIAN_POINT('Ctrl Pts',(13.6385988846933,0.122297616148583,3.52360886035071));
#28242=CARTESIAN_POINT('Ctrl Pts',(13.6863147207561,0.466847750307624,3.8452149784873));
#28243=CARTESIAN_POINT('Ctrl Pts',(13.7323153112179,0.38570983934117,4.29229218593957));
#28244=CARTESIAN_POINT('Ctrl Pts',(13.762410622992,0.122927301498021,4.41548505619568));
#28245=CARTESIAN_POINT('Ctrl Pts',(13.7766006560786,-0.000253139125078718,
4.41636688691614));
#28246=CARTESIAN_POINT('Ctrl Pts',(13.5733993439214,-0.000277574767750817,
4.41538411867388));
#28247=CARTESIAN_POINT('Ctrl Pts',(13.5792141092383,-0.0510604653080308,
4.41569425641003));
#28248=CARTESIAN_POINT('Ctrl Pts',(13.6009341532429,-0.240371663949131,
4.38351498152559));
#28249=CARTESIAN_POINT('Ctrl Pts',(13.6385594759351,-0.481431012491488,
4.10064494554323));
#28250=CARTESIAN_POINT('Ctrl Pts',(13.6862753119979,-0.345033139360895,
3.64948986092447));
#28251=CARTESIAN_POINT('Ctrl Pts',(13.7339911480608,0.108213974662067,3.52021363031051));
#28252=CARTESIAN_POINT('Ctrl Pts',(13.7817069841236,0.462086530666827,3.83153260544464));
#28253=CARTESIAN_POINT('Ctrl Pts',(13.8281763827438,0.393458703070077,4.28538422885222));
#28254=CARTESIAN_POINT('Ctrl Pts',(13.8587405026764,0.126988323162951,4.4157223370415));
#28255=CARTESIAN_POINT('Ctrl Pts',(13.8733993439214,-0.000192710833643682,
4.4164526008213));
#28256=CARTESIAN_POINT('Origin',(3.42660065607856,0.,4.));
#28257=CARTESIAN_POINT('',(13.1766006560786,0.000342007958933446,4.41553758638116));
#28258=CARTESIAN_POINT('',(13.2733993439214,0.000305371599794934,4.41543889539504));
#28259=CARTESIAN_POINT('',(3.42660065607856,4.87367679877478E-13,4.415875));
#28260=CARTESIAN_POINT('Ctrl Pts',(13.1766006560786,0.000342007958933428,
4.41553758638117));
#28261=CARTESIAN_POINT('Ctrl Pts',(13.1874525574283,-0.0943443719380771,
4.41480703635833));
#28262=CARTESIAN_POINT('Ctrl Pts',(13.2142097374657,-0.328913583769224,
4.33568767983454));
#28263=CARTESIAN_POINT('Ctrl Pts',(13.2568721961906,-0.488843983144383,
3.94580788806928));
#28264=CARTESIAN_POINT('Ctrl Pts',(13.3045880322534,-0.218805220893238,
3.55951220202843));
#28265=CARTESIAN_POINT('Ctrl Pts',(13.3523038683163,0.252165742455243,3.57772323864086));
#28266=CARTESIAN_POINT('Ctrl Pts',(13.4000197043791,0.491569024438394,3.98371752277252));
#28267=CARTESIAN_POINT('Ctrl Pts',(13.4414519669665,0.307476227900318,4.34923088347422));
#28268=CARTESIAN_POINT('Ctrl Pts',(13.4669789508664,0.0838425436168888,
4.41489516431802));
#28269=CARTESIAN_POINT('Ctrl Pts',(13.4766006560786,-0.000226204729293314,
4.4153088088013));
#28270=CARTESIAN_POINT('Ctrl Pts',(13.2733993439214,0.000305371599794949,
4.41543889539504));
#28271=CARTESIAN_POINT('Ctrl Pts',(13.2837824371127,-0.0903447040275099,
4.41482455235666));
#28272=CARTESIAN_POINT('Ctrl Pts',(13.3100708089916,-0.320767143545349,
4.3409984814332));
#28273=CARTESIAN_POINT('Ctrl Pts',(13.352264459558,-0.490227979701372,3.96022874442655));
#28274=CARTESIAN_POINT('Ctrl Pts',(13.3999802956209,-0.23168347330409,3.56614749850931));
#28275=CARTESIAN_POINT('Ctrl Pts',(13.4476961316837,0.239619531536799,3.57047968038978));
#28276=CARTESIAN_POINT('Ctrl Pts',(13.4954119677466,0.490876233547033,3.96924698078795));
#28277=CARTESIAN_POINT('Ctrl Pts',(13.5373130384925,0.315668023336251,4.34421900798688));
#28278=CARTESIAN_POINT('Ctrl Pts',(13.5633088305507,0.0878472949503496,
4.41484592860038));
#28279=CARTESIAN_POINT('Ctrl Pts',(13.5733993439214,-0.000277574767750817,
4.41538411867388));
#28280=CARTESIAN_POINT('Origin',(3.42660065607856,0.,4.));
#28281=CARTESIAN_POINT('',(12.8766006560786,7.85109994957766E-5,4.41654344863055));
#28282=CARTESIAN_POINT('',(12.9733993439214,0.000150764780949702,4.41649545414489));
#28283=CARTESIAN_POINT('',(3.42660065607856,4.87367679877478E-13,4.415875));
#28284=CARTESIAN_POINT('Ctrl Pts',(12.8766006560786,7.85109994958138E-5,
4.41654344863055));
#28285=CARTESIAN_POINT('Ctrl Pts',(12.8920208853026,-0.133630732206743,
4.41619751255639));
#28286=CARTESIAN_POINT('Ctrl Pts',(12.9233463932143,-0.405888408666218,
4.27372356364211));
#28287=CARTESIAN_POINT('Ctrl Pts',(12.9705771798136,-0.453501555338242,
3.80962782724943));
#28288=CARTESIAN_POINT('Ctrl Pts',(13.0182930158764,-0.0851462219395619,
3.51558762841831));
#28289=CARTESIAN_POINT('Ctrl Pts',(13.0660088519392,0.361400197209248,3.66639076405307));
#28290=CARTESIAN_POINT('Ctrl Pts',(13.1137246880021,0.476067254403989,4.1235523942958));
#28291=CARTESIAN_POINT('Ctrl Pts',(13.1505886227152,0.226902767145371,4.38908671404106));
#28292=CARTESIAN_POINT('Ctrl Pts',(13.1715472787407,0.0444343739838573,
4.41587777975472));
#28293=CARTESIAN_POINT('Ctrl Pts',(13.1766006560786,0.000342007958933428,
4.41553758638117));
#28294=CARTESIAN_POINT('Ctrl Pts',(12.9733993439214,0.000150764780949724,
4.4164954541449));
#28295=CARTESIAN_POINT('Ctrl Pts',(12.988350764987,-0.12953330947047,4.41589144324702));
#28296=CARTESIAN_POINT('Ctrl Pts',(13.0192074647402,-0.39825874617628,4.28096832590395));
#28297=CARTESIAN_POINT('Ctrl Pts',(13.065969443181,-0.458911634846768,3.82306685936703));
#28298=CARTESIAN_POINT('Ctrl Pts',(13.1136852792439,-0.0993761143989603,
3.51830547777773));
#28299=CARTESIAN_POINT('Ctrl Pts',(13.1614011153067,0.351418020999476,3.65589158776806));
#28300=CARTESIAN_POINT('Ctrl Pts',(13.2091169513695,0.479499580452807,4.10947774749948));
#28301=CARTESIAN_POINT('Ctrl Pts',(13.2464496942411,0.235195791588524,4.38570395495548));
#28302=CARTESIAN_POINT('Ctrl Pts',(13.2678771584251,0.0485170676377186,
4.41576563003508));
#28303=CARTESIAN_POINT('Ctrl Pts',(13.2733993439214,0.000305371599794949,
4.41543889539504));
#28304=CARTESIAN_POINT('Origin',(3.42660065607856,0.,4.));
#28305=CARTESIAN_POINT('',(12.5766006560786,-0.000382134531266273,4.41577416496379));
#28306=CARTESIAN_POINT('',(12.6733993439214,-0.000382453243898073,4.41589767499446));
#28307=CARTESIAN_POINT('',(3.42660065607856,4.87367679877478E-13,4.415875));
#28308=CARTESIAN_POINT('Ctrl Pts',(12.5766006560786,-0.000382134531266193,
4.41577416496379));
#28309=CARTESIAN_POINT('Ctrl Pts',(12.5806839344893,-0.0359587315295452,
4.41609477791077));
#28310=CARTESIAN_POINT('Ctrl Pts',(12.6006724915877,-0.209750441210566,
4.39561070447123));
#28311=CARTESIAN_POINT('Ctrl Pts',(12.6365663273737,-0.4676569254097,4.15232276575852));
#28312=CARTESIAN_POINT('Ctrl Pts',(12.6842821634365,-0.381050985679211,
3.68902512775968));
#28313=CARTESIAN_POINT('Ctrl Pts',(12.7319979994994,0.0554799374235607,
3.5113004999026));
#28314=CARTESIAN_POINT('Ctrl Pts',(12.7797138355622,0.441062780321708,3.78235614259331));
#28315=CARTESIAN_POINT('Ctrl Pts',(12.8274296716251,0.421610885427219,4.2532774884218));
#28316=CARTESIAN_POINT('Ctrl Pts',(12.8597252784638,0.146394963767536,4.4145887178469));
#28317=CARTESIAN_POINT('Ctrl Pts',(12.876115606615,0.00428438860018927,
4.4165543301878));
#28318=CARTESIAN_POINT('Ctrl Pts',(12.8766006560786,7.85109994958138E-5,
4.41654344863055));
#28319=CARTESIAN_POINT('Ctrl Pts',(12.6733993439214,-0.000382453243898042,
4.41589767499447));
#28320=CARTESIAN_POINT('Ctrl Pts',(12.6770138141737,-0.0318505807336982,
4.4161892599907));
#28321=CARTESIAN_POINT('Ctrl Pts',(12.6965335631136,-0.201468625965512,
4.39853963407534));
#28322=CARTESIAN_POINT('Ctrl Pts',(12.7319585907412,-0.462967872677167,
4.16603003860975));
#28323=CARTESIAN_POINT('Ctrl Pts',(12.779674426804,-0.390044463885,3.70038267566003));
#28324=CARTESIAN_POINT('Ctrl Pts',(12.8273902628668,0.0410627776982723,
3.50987851185683));
#28325=CARTESIAN_POINT('Ctrl Pts',(12.8751060989297,0.434461438689172,3.76946045210395));
#28326=CARTESIAN_POINT('Ctrl Pts',(12.9228219349925,0.42888747548329,4.24075040649094));
#28327=CARTESIAN_POINT('Ctrl Pts',(12.9555863499897,0.154617472482897,4.41255553662561));
#28328=CARTESIAN_POINT('Ctrl Pts',(12.9724454862994,0.00842423538524961,
4.41653398830136));
#28329=CARTESIAN_POINT('Ctrl Pts',(12.9733993439214,0.000150764780949724,
4.4164954541449));
#28330=CARTESIAN_POINT('Origin',(3.42660065607856,0.,4.));
#28331=CARTESIAN_POINT('',(12.2766006560786,9.99581421417901E-5,4.41520820259509));
#28332=CARTESIAN_POINT('',(12.3733993439214,3.32456539758885E-5,4.41518865831861));
#28333=CARTESIAN_POINT('',(3.42660065607856,4.87367679877478E-13,4.415875));
#28334=CARTESIAN_POINT('Ctrl Pts',(12.2766006560786,9.99581421418094E-5,
4.41520820259509));
#28335=CARTESIAN_POINT('Ctrl Pts',(12.2852522623637,-0.0755384113923865,
4.41504611816934));
#28336=CARTESIAN_POINT('Ctrl Pts',(12.3098091473364,-0.290455378639464,
4.35903266527152));
#28337=CARTESIAN_POINT('Ctrl Pts',(12.3502713109967,-0.49164800158875,4.0136918729824));
#28338=CARTESIAN_POINT('Ctrl Pts',(12.3979871470595,-0.277420602272412,
3.59386820576715));
#28339=CARTESIAN_POINT('Ctrl Pts',(12.4457029831224,0.191566404775332,3.54700161433684));
#28340=CARTESIAN_POINT('Ctrl Pts',(12.4934188191852,0.484635034689867,3.91613041073711));
#28341=CARTESIAN_POINT('Ctrl Pts',(12.5370513768373,0.345661459897227,4.32409890635003));
#28342=CARTESIAN_POINT('Ctrl Pts',(12.5647786558017,0.102620036091023,4.41484591908716));
#28343=CARTESIAN_POINT('Ctrl Pts',(12.5766006560786,-0.000382134531266193,
4.41577416496379));
#28344=CARTESIAN_POINT('Ctrl Pts',(12.3733993439214,3.32456539758746E-5,
4.41518865831861));
#28345=CARTESIAN_POINT('Ctrl Pts',(12.381582142048,-0.071514873974996,4.41513780400291));
#28346=CARTESIAN_POINT('Ctrl Pts',(12.4056702188623,-0.282203129244181,
4.36350051499509));
#28347=CARTESIAN_POINT('Ctrl Pts',(12.4456635743641,-0.491031474462283,
4.0281658647901));
#28348=CARTESIAN_POINT('Ctrl Pts',(12.493379410427,-0.289261580343189,3.60221492864948));
#28349=CARTESIAN_POINT('Ctrl Pts',(12.5410952464898,0.178141673866572,3.54155614424011));
#28350=CARTESIAN_POINT('Ctrl Pts',(12.5888110825527,0.481954687902679,3.90189340664049));
#28351=CARTESIAN_POINT('Ctrl Pts',(12.6329124483632,0.353693368040787,4.31820342736526));
#28352=CARTESIAN_POINT('Ctrl Pts',(12.6611085354861,0.106623193447456,4.41490615616012));
#28353=CARTESIAN_POINT('Ctrl Pts',(12.6733993439214,-0.000382453243898042,
4.41589767499447));
#28354=CARTESIAN_POINT('Origin',(3.42660065607856,0.,4.));
#28355=CARTESIAN_POINT('',(11.9766006560786,0.000344603143201134,4.41614202049347));
#28356=CARTESIAN_POINT('',(12.0733993439214,0.00037008249145147,4.41602009379307));
#28357=CARTESIAN_POINT('',(3.42660065607856,4.87367679877478E-13,4.415875));
#28358=CARTESIAN_POINT('Ctrl Pts',(11.9766006560786,0.000344603143201134,
4.41614202049347));
#28359=CARTESIAN_POINT('Ctrl Pts',(11.989820590238,-0.114576335025177,4.41511745277426));
#28360=CARTESIAN_POINT('Ctrl Pts',(12.018945803085,-0.369470719226983,4.30593844396252));
#28361=CARTESIAN_POINT('Ctrl Pts',(12.0639762946196,-0.475409571231627,
3.87394063131468));
#28362=CARTESIAN_POINT('Ctrl Pts',(12.1116921306825,-0.151090047408964,
3.53194335553704));
#28363=CARTESIAN_POINT('Ctrl Pts',(12.1594079667453,0.311977791768556,3.61976969834691));
#28364=CARTESIAN_POINT('Ctrl Pts',(12.2071238028081,0.488551624369653,4.05676737776005));
#28365=CARTESIAN_POINT('Ctrl Pts',(12.2461880325859,0.265811525316043,4.37185240566124));
#28366=CARTESIAN_POINT('Ctrl Pts',(12.269346983676,0.0635166157645696,4.41534409728183));
#28367=CARTESIAN_POINT('Ctrl Pts',(12.2766006560786,9.99581421418094E-5,
4.41520820259509));
#28368=CARTESIAN_POINT('Ctrl Pts',(12.0733993439214,0.000370082491451453,
4.41602009379308));
#28369=CARTESIAN_POINT('Ctrl Pts',(12.0861504699224,-0.110559366248508,
4.41499479059613));
#28370=CARTESIAN_POINT('Ctrl Pts',(12.1148068746109,-0.361534897467509,
4.3122242613332));
#28371=CARTESIAN_POINT('Ctrl Pts',(12.1593685579871,-0.478916017555994,
3.88799699566402));
#28372=CARTESIAN_POINT('Ctrl Pts',(12.2070843940499,-0.164809627468288,
3.53659627586117));
#28373=CARTESIAN_POINT('Ctrl Pts',(12.2548002301128,0.300643979445627,3.61074632631782));
#28374=CARTESIAN_POINT('Ctrl Pts',(12.3025160661756,0.490011594032383,4.04235401475446));
#28375=CARTESIAN_POINT('Ctrl Pts',(12.3420491041118,0.274087380788525,4.36772087084377));
#28376=CARTESIAN_POINT('Ctrl Pts',(12.3656768633604,0.0675564760281007,
4.41523665186048));
#28377=CARTESIAN_POINT('Ctrl Pts',(12.3733993439214,3.32456539758746E-5,
4.41518865831861));
#28378=CARTESIAN_POINT('Origin',(3.42660065607856,0.,4.));
#28379=CARTESIAN_POINT('',(11.6766006560786,-0.000272404999166542,4.41633191892761));
#28380=CARTESIAN_POINT('',(11.7733993439214,-0.000215373091504267,4.41642415578018));
#28381=CARTESIAN_POINT('',(3.42660065607856,4.87367679877478E-13,4.415875));
#28382=CARTESIAN_POINT('Ctrl Pts',(11.6766006560786,-0.000272404999166455,
4.41633191892761));
#28383=CARTESIAN_POINT('Ctrl Pts',(11.6784836394247,-0.0166217551361539,
4.41645573239506));
#28384=CARTESIAN_POINT('Ctrl Pts',(11.6962719014584,-0.170944672110958,
4.40814899119985));
#28385=CARTESIAN_POINT('Ctrl Pts',(11.7299654421798,-0.44220355512924,4.21531660568344));
#28386=CARTESIAN_POINT('Ctrl Pts',(11.7776812782426,-0.420270357404582,
3.74450430230823));
#28387=CARTESIAN_POINT('Ctrl Pts',(11.8253971143054,-0.0123964237846327,
3.50831762943));
#28388=CARTESIAN_POINT('Ctrl Pts',(11.8731129503683,0.406861336540243,3.72365044295193));
#28389=CARTESIAN_POINT('Ctrl Pts',(11.9208287864311,0.452492071153857,4.1927593068956));
#28390=CARTESIAN_POINT('Ctrl Pts',(11.9553246883346,0.185075114683736,4.40392780377));
#28391=CARTESIAN_POINT('Ctrl Pts',(11.9739153115504,0.0236883133891,4.41635013933017));
#28392=CARTESIAN_POINT('Ctrl Pts',(11.9766006560786,0.000344603143201134,
4.41614202049347));
#28393=CARTESIAN_POINT('Ctrl Pts',(11.7733993439214,-0.000215373091504231,
4.41642415578018));
#28394=CARTESIAN_POINT('Ctrl Pts',(11.7748135191091,-0.0124870613922979,
4.41650138834433));
#28395=CARTESIAN_POINT('Ctrl Pts',(11.7921329729843,-0.162701432614141,
4.41043584391465));
#28396=CARTESIAN_POINT('Ctrl Pts',(11.8253577055472,-0.435670260442099,
4.22824690363353));
#28397=CARTESIAN_POINT('Ctrl Pts',(11.8730735416101,-0.427612859293677,
3.75699286549843));
#28398=CARTESIAN_POINT('Ctrl Pts',(11.9207893776729,-0.0268719897862959,
3.50889601812151));
#28399=CARTESIAN_POINT('Ctrl Pts',(11.9685052137357,0.398545841420554,3.71178751390968));
#28400=CARTESIAN_POINT('Ctrl Pts',(12.0162210497986,0.457972894034889,4.17934897039372));
#28401=CARTESIAN_POINT('Ctrl Pts',(12.0511857598605,0.193343073938706,4.40127740506484));
#28402=CARTESIAN_POINT('Ctrl Pts',(12.0702451912347,0.0278098881012828,
4.41627371553856));
#28403=CARTESIAN_POINT('Ctrl Pts',(12.0733993439214,0.000370082491451453,
4.41602009379308));
#28404=CARTESIAN_POINT('Origin',(3.42660065607856,0.,4.));
#28405=CARTESIAN_POINT('',(11.3766006560786,-0.000206048103233091,4.41528588740701));
#28406=CARTESIAN_POINT('',(11.4733993439214,-0.000260100423148973,4.41535533657191));
#28407=CARTESIAN_POINT('',(3.42660065607856,4.87367679877478E-13,4.415875));
#28408=CARTESIAN_POINT('Ctrl Pts',(11.3766006560786,-0.000206048103232999,
4.41528588740701));
#28409=CARTESIAN_POINT('Ctrl Pts',(11.383051967299,-0.0565815589273492,
4.41553770218085));
#28410=CARTESIAN_POINT('Ctrl Pts',(11.4054085572071,-0.251630532720247,
4.37854193442951));
#28411=CARTESIAN_POINT('Ctrl Pts',(11.4436704258028,-0.485070265991237,
4.08131458604192));
#28412=CARTESIAN_POINT('Ctrl Pts',(11.4913862618656,-0.330742172127369,
3.63597412121053));
#28413=CARTESIAN_POINT('Ctrl Pts',(11.5391020979284,0.127311547523522,3.52492422212962));
#28414=CARTESIAN_POINT('Ctrl Pts',(11.5868179339912,0.468453114143607,3.85014371984754));
#28415=CARTESIAN_POINT('Ctrl Pts',(11.632650786708,0.382920955827079,4.29471395365306));
#28416=CARTESIAN_POINT('Ctrl Pts',(11.6625783607371,0.121478760105588,4.41540989855421));
#28417=CARTESIAN_POINT('Ctrl Pts',(11.6766006560786,-0.000272404999166455,
4.41633191892761));
#28418=CARTESIAN_POINT('Ctrl Pts',(11.4733993439214,-0.000260100423148869,
4.41535533657191));
#28419=CARTESIAN_POINT('Ctrl Pts',(11.4793818469834,-0.0525169974224216,
4.41565306322741));
#28420=CARTESIAN_POINT('Ctrl Pts',(11.501269628733,-0.243338890257842,4.3822327073369));
#28421=CARTESIAN_POINT('Ctrl Pts',(11.5390626891702,-0.482464979911041,
4.09556551685319));
#28422=CARTESIAN_POINT('Ctrl Pts',(11.586778525233,-0.341319923258817,3.64587299617429));
#28423=CARTESIAN_POINT('Ctrl Pts',(11.6344943612959,0.113264470804062,3.5213807520529));
#28424=CARTESIAN_POINT('Ctrl Pts',(11.6822101973587,0.463836358529674,3.83641192782507));
#28425=CARTESIAN_POINT('Ctrl Pts',(11.7285118582339,0.390694138047139,4.28787953265104));
#28426=CARTESIAN_POINT('Ctrl Pts',(11.7589082404215,0.125533053862222,4.41563275094549));
#28427=CARTESIAN_POINT('Ctrl Pts',(11.7733993439214,-0.000215373091504231,
4.41642415578018));
#28428=CARTESIAN_POINT('Origin',(3.42660065607856,0.,4.));
#28429=CARTESIAN_POINT('',(11.0766006560786,0.000352537510456688,4.41557576695298));
#28430=CARTESIAN_POINT('',(11.1733993439214,0.000319650745578964,4.41547275084625));
#28431=CARTESIAN_POINT('',(3.42660065607856,4.87367679877478E-13,4.415875));
#28432=CARTESIAN_POINT('Ctrl Pts',(11.0766006560786,0.000352537510456667,
4.41557576695298));
#28433=CARTESIAN_POINT('Ctrl Pts',(11.0876202951733,-0.0957751134661499,
4.41480617263661));
#28434=CARTESIAN_POINT('Ctrl Pts',(11.1145452129557,-0.331820540820521,
4.33374203885914));
#28435=CARTESIAN_POINT('Ctrl Pts',(11.1573754094257,-0.488245699001722,
3.94065893278431));
#28436=CARTESIAN_POINT('Ctrl Pts',(11.2050912454886,-0.214150733603143,
3.55723066033293));
#28437=CARTESIAN_POINT('Ctrl Pts',(11.2528070815514,0.256602145595791,3.58040428537983));
#28438=CARTESIAN_POINT('Ctrl Pts',(11.3005229176142,0.491713326162588,3.98889911147238));
#28439=CARTESIAN_POINT('Ctrl Pts',(11.3417874424566,0.304539430122629,4.35098016691413));
#28440=CARTESIAN_POINT('Ctrl Pts',(11.3671466886114,0.0824085130402235,
4.41491686960609));
#28441=CARTESIAN_POINT('Ctrl Pts',(11.3766006560786,-0.000206048103232999,
4.41528588740701));
#28442=CARTESIAN_POINT('Ctrl Pts',(11.1733993439214,0.000319650745578978,
4.41547275084625));
#28443=CARTESIAN_POINT('Ctrl Pts',(11.1839501748577,-0.0917759901056567,
4.4148158243975));
#28444=CARTESIAN_POINT('Ctrl Pts',(11.2104062844816,-0.32368545017211,4.33911969104981));
#28445=CARTESIAN_POINT('Ctrl Pts',(11.2527676727932,-0.489781601228288,
3.95506440219344));
#28446=CARTESIAN_POINT('Ctrl Pts',(11.300483508856,-0.227098200695192,3.56372986339542));
#28447=CARTESIAN_POINT('Ctrl Pts',(11.3481993449188,0.244132971891272,3.57302890392028));
#28448=CARTESIAN_POINT('Ctrl Pts',(11.3959151809817,0.491173079921361,3.97442207176994));
#28449=CARTESIAN_POINT('Ctrl Pts',(11.4376485139825,0.312739912806573,4.34603313379779));
#28450=CARTESIAN_POINT('Ctrl Pts',(11.4634765682958,0.0864149014017155,
4.41486151738456));
#28451=CARTESIAN_POINT('Ctrl Pts',(11.4733993439214,-0.000260100423148869,
4.41535533657191));
#28452=CARTESIAN_POINT('Origin',(3.42660065607856,0.,4.));
#28453=CARTESIAN_POINT('',(10.7766006560786,5.16128798610187E-5,4.41655360457584));
#28454=CARTESIAN_POINT('',(10.8733993439214,0.000125523266313186,4.41651574507477));
#28455=CARTESIAN_POINT('',(3.42660065607856,4.87367679877478E-13,4.415875));
#28456=CARTESIAN_POINT('Ctrl Pts',(10.7766006560786,5.16128798610299E-5,
4.41655360457584));
#28457=CARTESIAN_POINT('Ctrl Pts',(10.7921886230477,-0.135103241057852,
4.41631783152902));
#28458=CARTESIAN_POINT('Ctrl Pts',(10.8236818687044,-0.408598944994929,
4.27108057505162));
#28459=CARTESIAN_POINT('Ctrl Pts',(10.8710803930487,-0.451470021714238,
3.80485891169382));
#28460=CARTESIAN_POINT('Ctrl Pts',(10.9187962291115,-0.080036233235122,
3.51471716883706));
#28461=CARTESIAN_POINT('Ctrl Pts',(10.9665120651743,0.364896059739551,3.6702181168734));
#28462=CARTESIAN_POINT('Ctrl Pts',(11.0142279012372,0.47473868640782,4.1285628425314));
#28463=CARTESIAN_POINT('Ctrl Pts',(11.0509240982053,0.223935965514619,4.3902602363912));
#28464=CARTESIAN_POINT('Ctrl Pts',(11.0717150164857,0.0429714521173939,
4.4159169723618));
#28465=CARTESIAN_POINT('Ctrl Pts',(11.0766006560786,0.000352537510456667,
4.41557576695298));
#28466=CARTESIAN_POINT('Ctrl Pts',(10.8733993439214,0.000125523266313226,
4.41651574507477));
#28467=CARTESIAN_POINT('Ctrl Pts',(10.888518502732,-0.130996444363694,4.41599591363288));
#28468=CARTESIAN_POINT('Ctrl Pts',(10.9195429402303,-0.400997532511054,
4.27840016053723));
#28469=CARTESIAN_POINT('Ctrl Pts',(10.9664726564161,-0.45702143577077,3.81824018018824));
#28470=CARTESIAN_POINT('Ctrl Pts',(11.014188492479,-0.0942939790271268,
3.51728489730359));
#28471=CARTESIAN_POINT('Ctrl Pts',(11.0619043285418,0.355025089556487,3.65961432075161));
#28472=CARTESIAN_POINT('Ctrl Pts',(11.1096201646047,0.478319155637209,4.11452515096033));
#28473=CARTESIAN_POINT('Ctrl Pts',(11.1467851697312,0.23222845252417,4.38693182090163));
#28474=CARTESIAN_POINT('Ctrl Pts',(11.1680448961701,0.0470573247768451,
4.41580613485813));
#28475=CARTESIAN_POINT('Ctrl Pts',(11.1733993439214,0.000319650745578978,
4.41547275084625));
#28476=CARTESIAN_POINT('Origin',(3.42660065607856,0.,4.));
#28477=CARTESIAN_POINT('',(10.4766006560786,-0.000378910032885682,4.4157309619862));
#28478=CARTESIAN_POINT('',(10.5733993439214,-0.000383826598418624,4.41585315377736));
#28479=CARTESIAN_POINT('',(3.42660065607856,4.87367679877478E-13,4.415875));
#28480=CARTESIAN_POINT('Ctrl Pts',(10.4766006560786,-0.000378910032885704,
4.4157309619862));
#28481=CARTESIAN_POINT('Ctrl Pts',(10.4808516722344,-0.0374267536145521,
4.41605913507464));
#28482=CARTESIAN_POINT('Ctrl Pts',(10.5010079670778,-0.212714974368116,
4.3945277200383));
#28483=CARTESIAN_POINT('Ctrl Pts',(10.5370695406088,-0.469236294399976,
4.14738563318641));
#28484=CARTESIAN_POINT('Ctrl Pts',(10.5847853766716,-0.377752434501872,
3.68502647241413));
#28485=CARTESIAN_POINT('Ctrl Pts',(10.6325012127345,0.0606272984676223,
3.51191234851464));
#28486=CARTESIAN_POINT('Ctrl Pts',(10.6802170487973,0.443332050383407,3.78701662516801));
#28487=CARTESIAN_POINT('Ctrl Pts',(10.7279328848602,0.418918158891686,4.25770681210006));
#28488=CARTESIAN_POINT('Ctrl Pts',(10.7600607539539,0.143455624352724,4.41528584951654));
#28489=CARTESIAN_POINT('Ctrl Pts',(10.7762833443601,0.00280285164340033,
4.41655840401831));
#28490=CARTESIAN_POINT('Ctrl Pts',(10.7766006560786,5.16128798610299E-5,
4.41655360457584));
#28491=CARTESIAN_POINT('Ctrl Pts',(10.5733993439214,-0.000383826598418617,
4.41585315377736));
#28492=CARTESIAN_POINT('Ctrl Pts',(10.5771815519187,-0.0333213161677604,
4.41615637378185));
#28493=CARTESIAN_POINT('Ctrl Pts',(10.5968690386037,-0.20443114816448,4.39750812937281));
#28494=CARTESIAN_POINT('Ctrl Pts',(10.6324618039763,-0.464691964107356,
4.16114156306187));
#28495=CARTESIAN_POINT('Ctrl Pts',(10.6801776400391,-0.386865111317189,
3.69628860657276));
#28496=CARTESIAN_POINT('Ctrl Pts',(10.7278934761019,0.0462259258804368,
3.51033849586834));
#28497=CARTESIAN_POINT('Ctrl Pts',(10.7756093121648,0.436866984064762,3.77405207881873));
#28498=CARTESIAN_POINT('Ctrl Pts',(10.8233251482276,0.426326368719826,4.24525711444552));
#28499=CARTESIAN_POINT('Ctrl Pts',(10.8559218254798,0.151674250044741,4.4132974389186));
#28500=CARTESIAN_POINT('Ctrl Pts',(10.8726132240444,0.00694320316194716,
4.41654277368359));
#28501=CARTESIAN_POINT('Ctrl Pts',(10.8733993439214,0.000125523266313226,
4.41651574507477));
#28502=CARTESIAN_POINT('Origin',(3.42660065607856,0.,4.));
#28503=CARTESIAN_POINT('',(10.1766006560786,0.000123197149224082,4.41521991402453));
#28504=CARTESIAN_POINT('',(10.2733993439214,5.7336166378985E-5,4.41519339896199));
#28505=CARTESIAN_POINT('',(3.42660065607856,4.87367679877478E-13,4.415875));
#28506=CARTESIAN_POINT('Ctrl Pts',(10.1766006560786,0.000123197149224097,
4.41521991402453));
#28507=CARTESIAN_POINT('Ctrl Pts',(10.1854200001087,-0.0769762270984491,
4.41501595190525));
#28508=CARTESIAN_POINT('Ctrl Pts',(10.2101446228264,-0.293404201931947,
4.35739193013711));
#28509=CARTESIAN_POINT('Ctrl Pts',(10.2507745242318,-0.491764996345908,
4.00850959581219));
#28510=CARTESIAN_POINT('Ctrl Pts',(10.2984903602946,-0.273124940234581,
3.59096700393021));
#28511=CARTESIAN_POINT('Ctrl Pts',(10.3462061963575,0.196329951061554,3.54904570612073));
#28512=CARTESIAN_POINT('Ctrl Pts',(10.3939220324203,0.485492027373267,3.92124267520431));
#28513=CARTESIAN_POINT('Ctrl Pts',(10.4373868523273,0.34277731801193,4.32616121393696));
#28514=CARTESIAN_POINT('Ctrl Pts',(10.4649463935468,0.101188639822117,4.41483126760997));
#28515=CARTESIAN_POINT('Ctrl Pts',(10.4766006560786,-0.000378910032885704,
4.4157309619862));
#28516=CARTESIAN_POINT('Ctrl Pts',(10.2733993439214,5.73361663789851E-5,
4.41519339896199));
#28517=CARTESIAN_POINT('Ctrl Pts',(10.2817498797931,-0.0729553575157724,
4.41510384014646));
#28518=CARTESIAN_POINT('Ctrl Pts',(10.3060056943524,-0.285157432566911,
4.36192175935665));
#28519=CARTESIAN_POINT('Ctrl Pts',(10.3461667875993,-0.491301045992024,
4.02298928139638));
#28520=CARTESIAN_POINT('Ctrl Pts',(10.3938826236621,-0.285053227451061,
3.599188470261));
#28521=CARTESIAN_POINT('Ctrl Pts',(10.4415984597249,0.182963355965895,3.54345905416307));
#28522=CARTESIAN_POINT('Ctrl Pts',(10.4893142957878,0.482961874346273,3.9069782134126));
#28523=CARTESIAN_POINT('Ctrl Pts',(10.5332479238533,0.35082465130295,4.32033516829581));
#28524=CARTESIAN_POINT('Ctrl Pts',(10.5612762732311,0.105190355120073,4.41488124595214));
#28525=CARTESIAN_POINT('Ctrl Pts',(10.5733993439214,-0.000383826598418617,
4.41585315377736));
#28526=CARTESIAN_POINT('Origin',(3.42660065607856,0.,4.));
#28527=CARTESIAN_POINT('',(9.87660065607859,0.000332404019580576,4.41618417038907));
#28528=CARTESIAN_POINT('',(9.9733993439214,0.000362444897862246,4.41606425076498));
#28529=CARTESIAN_POINT('',(3.42660065607856,4.87367679877478E-13,4.415875));
#28530=CARTESIAN_POINT('Ctrl Pts',(9.87660065607859,0.000332404019580564,
4.41618417038907));
#28531=CARTESIAN_POINT('Ctrl Pts',(9.88998832798303,-0.116016130490024,
4.41516972706101));
#28532=CARTESIAN_POINT('Ctrl Pts',(9.91928127857509,-0.372296869871387,
4.30364082544554));
#28533=CARTESIAN_POINT('Ctrl Pts',(9.96447950785476,-0.474054618562381,
3.8689372536849));
#28534=CARTESIAN_POINT('Ctrl Pts',(10.0121953439176,-0.146148770628728,
3.53037700046135));
#28535=CARTESIAN_POINT('Ctrl Pts',(10.0599111799804,0.315967742161179,3.62307877379278));
#28536=CARTESIAN_POINT('Ctrl Pts',(10.1076270160433,0.487926215535836,4.06191310882887));
#28537=CARTESIAN_POINT('Ctrl Pts',(10.146523508076,0.262848409674369,4.37329037489646));
#28538=CARTESIAN_POINT('Ctrl Pts',(10.1695147214211,0.062069015396409,4.41538378814543));
#28539=CARTESIAN_POINT('Ctrl Pts',(10.1766006560786,0.000123197149224097,
4.41521991402453));
#28540=CARTESIAN_POINT('Ctrl Pts',(9.9733993439214,0.000362444897862267,
4.41606425076498));
#28541=CARTESIAN_POINT('Ctrl Pts',(9.9863182076674,-0.111995531308361,4.41503480155798));
#28542=CARTESIAN_POINT('Ctrl Pts',(10.015142350101,-0.364380386131072,4.30999810797653));
#28543=CARTESIAN_POINT('Ctrl Pts',(10.0598717712222,-0.477709011270712,
3.88295588266498));
#28544=CARTESIAN_POINT('Ctrl Pts',(10.1075876072851,-0.159916626226494,
3.53488507064564));
#28545=CARTESIAN_POINT('Ctrl Pts',(10.1553034433479,0.304729657315094,3.61393645496551));
#28546=CARTESIAN_POINT('Ctrl Pts',(10.2030192794107,0.489538007675758,4.04751593304174));
#28547=CARTESIAN_POINT('Ctrl Pts',(10.2423845796019,0.271127379494919,4.3692182851415));
#28548=CARTESIAN_POINT('Ctrl Pts',(10.2658446011055,0.0661120339180705,
4.41527442296197));
#28549=CARTESIAN_POINT('Ctrl Pts',(10.2733993439214,5.73361663789851E-5,
4.41519339896199));
#28550=CARTESIAN_POINT('Origin',(3.42660065607856,0.,4.));
#28551=CARTESIAN_POINT('',(9.57660065607859,-0.000290304052950346,4.41629504206998));
#28552=CARTESIAN_POINT('',(9.6733993439214,-0.000236899196693507,4.41639317328699));
#28553=CARTESIAN_POINT('',(3.42660065607856,4.87367679877478E-13,4.415875));
#28554=CARTESIAN_POINT('Ctrl Pts',(9.57660065607859,-0.000290304052950335,
4.41629504206998));
#28555=CARTESIAN_POINT('Ctrl Pts',(9.57865137716975,-0.0181001948149981,
4.41643644713422));
#28556=CARTESIAN_POINT('Ctrl Pts',(9.59660737694851,-0.173896467062472,
4.40729888742394));
#28557=CARTESIAN_POINT('Ctrl Pts',(9.63046865541489,-0.444448234747017,
4.21064422964382));
#28558=CARTESIAN_POINT('Ctrl Pts',(9.67818449147773,-0.41755432743774,3.74008922975375));
#28559=CARTESIAN_POINT('Ctrl Pts',(9.72590032754057,-0.00721385634321597,
3.50821428942208));
#28560=CARTESIAN_POINT('Ctrl Pts',(9.77361616360341,0.40975121003073,3.72795373420991));
#28561=CARTESIAN_POINT('Ctrl Pts',(9.82133199966624,0.450435435400681,4.19751745084266));
#28562=CARTESIAN_POINT('Ctrl Pts',(9.85566016382464,0.182118884769847,4.40484283743537));
#28563=CARTESIAN_POINT('Ctrl Pts',(9.87408304929542,0.0222122246324328,
4.41637494063069));
#28564=CARTESIAN_POINT('Ctrl Pts',(9.87660065607859,0.000332404019580564,
4.41618417038907));
#28565=CARTESIAN_POINT('Ctrl Pts',(9.6733993439214,-0.00023689919669354,
4.41639317328699));
#28566=CARTESIAN_POINT('Ctrl Pts',(9.67498125685411,-0.0139668454918635,
4.4164864708936));
#28567=CARTESIAN_POINT('Ctrl Pts',(9.69246844847443,-0.165649677201134,
4.40963259460397));
#28568=CARTESIAN_POINT('Ctrl Pts',(9.72586091878235,-0.438051576325333,
4.22364266437974));
#28569=CARTESIAN_POINT('Ctrl Pts',(9.77357675484519,-0.425028039486299,
3.75249971615691));
#28570=CARTESIAN_POINT('Ctrl Pts',(9.82129259090803,-0.0216947140899849,
3.50864008686857));
#28571=CARTESIAN_POINT('Ctrl Pts',(9.86900842697087,0.401561201071248,3.7160038263529));
#28572=CARTESIAN_POINT('Ctrl Pts',(9.91672426303371,0.456057286475463,4.18416562194019));
#28573=CARTESIAN_POINT('Ctrl Pts',(9.95152123535055,0.190383912560376,4.40224154849284));
#28574=CARTESIAN_POINT('Ctrl Pts',(9.97041292897978,0.0263359008882403,
4.4163022254471));
#28575=CARTESIAN_POINT('Ctrl Pts',(9.9733993439214,0.000362444897862267,
4.41606425076498));
#28576=CARTESIAN_POINT('Origin',(3.42660065607856,0.,4.));
#28577=CARTESIAN_POINT('',(9.27660065607858,-0.000185084181660103,4.41526520375254));
#28578=CARTESIAN_POINT('',(9.37339934392141,-0.000241596553487405,4.41532857883968));
#28579=CARTESIAN_POINT('',(3.42660065607856,4.87367679877478E-13,4.415875));
#28580=CARTESIAN_POINT('Ctrl Pts',(9.27660065607858,-0.000185084181660189,
4.41526520375254));
#28581=CARTESIAN_POINT('Ctrl Pts',(9.28321970504406,-0.0580335922681754,
4.4154966095816));
#28582=CARTESIAN_POINT('Ctrl Pts',(9.30574403269715,-0.254596444523232,
4.37718269734299));
#28583=CARTESIAN_POINT('Ctrl Pts',(9.34417363903789,-0.485900307124067,
4.07619787653679));
#28584=CARTESIAN_POINT('Ctrl Pts',(9.39188947510068,-0.326887306273347,
3.63250862071426));
#28585=CARTESIAN_POINT('Ctrl Pts',(9.43960531116356,0.13231133773591,3.52629235307153));
#28586=CARTESIAN_POINT('Ctrl Pts',(9.48732114722637,0.470006444430667,3.85508910653225));
#28587=CARTESIAN_POINT('Ctrl Pts',(9.53298626219807,0.380123833963086,4.29710958399465));
#28588=CARTESIAN_POINT('Ctrl Pts',(9.56274609848214,0.120032327051623,4.41533971732329));
#28589=CARTESIAN_POINT('Ctrl Pts',(9.57660065607859,-0.000290304052950335,
4.41629504206998));
#28590=CARTESIAN_POINT('Ctrl Pts',(9.3733993439214,-0.000241596553487357,
4.41532857883968));
#28591=CARTESIAN_POINT('Ctrl Pts',(9.37954958472843,-0.0539723465869793,
4.41561177485228));
#28592=CARTESIAN_POINT('Ctrl Pts',(9.40160510422307,-0.246305905820531,
4.3809303471886));
#28593=CARTESIAN_POINT('Ctrl Pts',(9.43956590240532,-0.483445357410111,
4.09047547319903));
#28594=CARTESIAN_POINT('Ctrl Pts',(9.48728173846818,-0.337568794959357,
3.64229546617122));
#28595=CARTESIAN_POINT('Ctrl Pts',(9.53499757453099,0.118302386066128,3.5226010365501));
#28596=CARTESIAN_POINT('Ctrl Pts',(9.58271341059386,0.465534665650901,3.84130942079228));
#28597=CARTESIAN_POINT('Ctrl Pts',(9.62884733372396,0.387920650713885,4.29034844530944));
#28598=CARTESIAN_POINT('Ctrl Pts',(9.65907597816649,0.124080336294106,4.41554841393524));
#28599=CARTESIAN_POINT('Ctrl Pts',(9.6733993439214,-0.00023689919669354,
4.41639317328699));
#28600=CARTESIAN_POINT('Origin',(3.42660065607856,0.,4.));
#28601=CARTESIAN_POINT('',(8.97660065607858,0.000361621133123973,4.41561526113518));
#28602=CARTESIAN_POINT('',(9.0733993439214,0.00033264130393823,4.41550825894961));
#28603=CARTESIAN_POINT('',(3.42660065607856,4.87367679877478E-13,4.415875));
#28604=CARTESIAN_POINT('Ctrl Pts',(8.97660065607858,0.000361621133123963,
4.41561526113518));
#28605=CARTESIAN_POINT('Ctrl Pts',(8.98778803291839,-0.097205817696177,
4.41480833810253));
#28606=CARTESIAN_POINT('Ctrl Pts',(9.01488068844582,-0.334723089553266,
4.33177224018802));
#28607=CARTESIAN_POINT('Ctrl Pts',(9.05787862266083,-0.487593182843731,
3.93551656882348));
#28608=CARTESIAN_POINT('Ctrl Pts',(9.10559445872368,-0.209472459465777,
3.55499829935456));
#28609=CARTESIAN_POINT('Ctrl Pts',(9.15331029478651,0.261010046587687,3.58313193881964));
#28610=CARTESIAN_POINT('Ctrl Pts',(9.20102613084934,0.491803010703882,3.99408193320625));
#28611=CARTESIAN_POINT('Ctrl Pts',(9.24212291794672,0.301599829163518,4.35270650246492));
#28612=CARTESIAN_POINT('Ctrl Pts',(9.26731442635645,0.0809737859182142,
4.41494055172187));
#28613=CARTESIAN_POINT('Ctrl Pts',(9.27660065607858,-0.000185084181660189,
4.41526520375254));
#28614=CARTESIAN_POINT('Ctrl Pts',(9.0733993439214,0.000332641303938268,
4.41550825894961));
#28615=CARTESIAN_POINT('Ctrl Pts',(9.08411791260276,-0.093207009794584,
4.4148098083896));
#28616=CARTESIAN_POINT('Ctrl Pts',(9.11074175997173,-0.326599857706223,
4.33721709571948));
#28617=CARTESIAN_POINT('Ctrl Pts',(9.1532708860283,-0.489280820139143,3.94990505119329));
#28618=CARTESIAN_POINT('Ctrl Pts',(9.20098672209113,-0.222487703095825,
3.56136068709803));
#28619=CARTESIAN_POINT('Ctrl Pts',(9.24870255815399,0.248619295113741,3.57562555337399));
#28620=CARTESIAN_POINT('Ctrl Pts',(9.29641839421681,0.49141536912078,3.97960000382683));
#28621=CARTESIAN_POINT('Ctrl Pts',(9.33798398947263,0.309808547095179,4.34782394055348));
#28622=CARTESIAN_POINT('Ctrl Pts',(9.36364430604082,0.0849819773478622,
4.41487939515448));
#28623=CARTESIAN_POINT('Ctrl Pts',(9.3733993439214,-0.000241596553487357,
4.41532857883968));
#28624=CARTESIAN_POINT('Origin',(3.42660065607856,0.,4.));
#28625=CARTESIAN_POINT('',(8.67660065607859,2.43999233753954E-5,4.41655967853978));
#28626=CARTESIAN_POINT('',(8.77339934392141,9.9565801791445E-5,4.41653262406943));
#28627=CARTESIAN_POINT('',(3.42660065607856,4.87367679877478E-13,4.415875));
#28628=CARTESIAN_POINT('Ctrl Pts',(8.67660065607859,2.43999233753836E-5,
4.41655967853978));
#28629=CARTESIAN_POINT('Ctrl Pts',(8.69235636079272,-0.136579453435425,
4.41644398151286));
#28630=CARTESIAN_POINT('Ctrl Pts',(8.72401734419445,-0.411298873006737,
4.26841067400337));
#28631=CARTESIAN_POINT('Ctrl Pts',(8.7715836062838,-0.449388340942622,3.80011167148426));
#28632=CARTESIAN_POINT('Ctrl Pts',(8.81929944234665,-0.0749173544856965,
3.51390061216986));
#28633=CARTESIAN_POINT('Ctrl Pts',(8.86701527840948,0.368351391347115,3.67408210030036));
#28634=CARTESIAN_POINT('Ctrl Pts',(8.91473111447233,0.473357386691186,4.13355901061654));
#28635=CARTESIAN_POINT('Ctrl Pts',(8.95125957369535,0.220969504140389,4.39141457480799));
#28636=CARTESIAN_POINT('Ctrl Pts',(8.97188275423077,0.0415074238114615,
4.41595555392421));
#28637=CARTESIAN_POINT('Ctrl Pts',(8.97660065607858,0.000361621133123963,
4.41561526113518));
#28638=CARTESIAN_POINT('Ctrl Pts',(8.77339934392141,9.95658017914599E-5,
4.41653262406943));
#28639=CARTESIAN_POINT('Ctrl Pts',(8.78868624047708,-0.132462770989084,
4.416105976883));
#28640=CARTESIAN_POINT('Ctrl Pts',(8.81987841572037,-0.403726445587972,
4.27580529254432));
#28641=CARTESIAN_POINT('Ctrl Pts',(8.86697586965126,-0.455080472922433,
3.81343369002772));
#28642=CARTESIAN_POINT('Ctrl Pts',(8.91469170571412,-0.0892013699275644,
3.51631793453238));
#28643=CARTESIAN_POINT('Ctrl Pts',(8.96240754177693,0.358592723611288,3.66337486216116));
#28644=CARTESIAN_POINT('Ctrl Pts',(9.0101233778398,0.477085601399612,4.11955983351088));
#28645=CARTESIAN_POINT('Ctrl Pts',(9.04712064522126,0.229261233371815,4.38814011953822));
#28646=CARTESIAN_POINT('Ctrl Pts',(9.06821263391514,0.0455964315317218,
4.41584623882512));
#28647=CARTESIAN_POINT('Ctrl Pts',(9.0733993439214,0.000332641303938268,
4.41550825894961));
#28648=CARTESIAN_POINT('Origin',(3.42660065607856,0.,4.));
#28649=CARTESIAN_POINT('',(8.37660065607859,-0.000374086211409503,4.41568853448753));
#28650=CARTESIAN_POINT('',(8.47339934392141,-0.000383538171196851,4.41580895574666));
#28651=CARTESIAN_POINT('',(3.42660065607856,4.87367679877478E-13,4.415875));
#28652=CARTESIAN_POINT('Ctrl Pts',(8.37660065607859,-0.000374086211409545,
4.41568853448753));
#28653=CARTESIAN_POINT('Ctrl Pts',(8.38101940997943,-0.0388937529272332,
4.41602262289185));
#28654=CARTESIAN_POINT('Ctrl Pts',(8.40134344256788,-0.215680110827853,
4.3934260635833));
#28655=CARTESIAN_POINT('Ctrl Pts',(8.43757275384394,-0.470763542849379,
4.14243212971755));
#28656=CARTESIAN_POINT('Ctrl Pts',(8.48528858990678,-0.37441192437669,3.68106280283335));
#28657=CARTESIAN_POINT('Ctrl Pts',(8.53300442596962,0.0657679253190804,
3.51257841158684));
#28658=CARTESIAN_POINT('Ctrl Pts',(8.58072026203246,0.445552077224736,3.79170076492532));
#28659=CARTESIAN_POINT('Ctrl Pts',(8.62843609809529,0.41617890091499,4.26210751092856));
#28660=CARTESIAN_POINT('Ctrl Pts',(8.66039622944401,0.140517691799823,4.41596716726027));
#28661=CARTESIAN_POINT('Ctrl Pts',(8.6764510821051,0.00132122424898086,
4.41656077688887));
#28662=CARTESIAN_POINT('Ctrl Pts',(8.67660065607859,2.43999233753836E-5,
4.41655967853978));
#28663=CARTESIAN_POINT('Ctrl Pts',(8.47339934392141,-0.000383538171196768,
4.41580895574666));
#28664=CARTESIAN_POINT('Ctrl Pts',(8.47734928966379,-0.0347911067166248,
4.41612244784963));
#28665=CARTESIAN_POINT('Ctrl Pts',(8.4972045140938,-0.207394442561863,4.39645832432586));
#28666=CARTESIAN_POINT('Ctrl Pts',(8.5329650172114,-0.466364439759318,4.15623518867385));
#28667=CARTESIAN_POINT('Ctrl Pts',(8.58068085327425,-0.383642787608637,
3.69222827230584));
#28668=CARTESIAN_POINT('Ctrl Pts',(8.62839668933707,0.0513839395061145,
3.51085286915611));
#28669=CARTESIAN_POINT('Ctrl Pts',(8.67611252539993,0.439224004328866,3.77866880275638));
#28670=CARTESIAN_POINT('Ctrl Pts',(8.72382836146275,0.42371790764641,4.24973658040369));
#28671=CARTESIAN_POINT('Ctrl Pts',(8.75625730096992,0.148732406864234,4.41402322426773));
#28672=CARTESIAN_POINT('Ctrl Pts',(8.77278096178947,0.00546194790078228,
4.41654988270631));
#28673=CARTESIAN_POINT('Ctrl Pts',(8.77339934392141,9.95658017914599E-5,
4.41653262406943));
#28674=CARTESIAN_POINT('Origin',(3.42660065607856,0.,4.));
#28675=CARTESIAN_POINT('',(8.07660065607859,0.000145957947245773,4.41523406184916));
#28676=CARTESIAN_POINT('',(8.1733993439214,8.12049300508987E-5,4.41520065480005));
#28677=CARTESIAN_POINT('',(3.42660065607856,4.87367679877478E-13,4.415875));
#28678=CARTESIAN_POINT('Ctrl Pts',(8.07660065607858,0.00014595794724577,
4.41523406184916));
#28679=CARTESIAN_POINT('Ctrl Pts',(8.08558773785375,-0.0784131624224431,
4.41498734772332));
#28680=CARTESIAN_POINT('Ctrl Pts',(8.11048009831652,-0.296350794919178,
4.35572875890285));
#28681=CARTESIAN_POINT('Ctrl Pts',(8.15127773746691,-0.491827368180951,
4.00332637343646));
#28682=CARTESIAN_POINT('Ctrl Pts',(8.19899357352975,-0.268798940774433,
3.58811123553743));
#28683=CARTESIAN_POINT('Ctrl Pts',(8.24670940959259,0.201071689948468,3.55113988776764));
#28684=CARTESIAN_POINT('Ctrl Pts',(8.29442524565542,0.486295093906121,3.92636368766143));
#28685=CARTESIAN_POINT('Ctrl Pts',(8.33772232781743,0.339888039743562,4.32819890206972));
#28686=CARTESIAN_POINT('Ctrl Pts',(8.36511413129181,0.0997575609540166,
4.41482007364463));
#28687=CARTESIAN_POINT('Ctrl Pts',(8.37660065607859,-0.000374086211409545,
4.41568853448753));
#28688=CARTESIAN_POINT('Ctrl Pts',(8.1733993439214,8.12049300509751E-5,
4.41520065480005));
#28689=CARTESIAN_POINT('Ctrl Pts',(8.18191761753811,-0.0743948540356096,
4.41507113968239));
#28690=CARTESIAN_POINT('Ctrl Pts',(8.20634116984244,-0.288109900049694,
4.36032095112539));
#28691=CARTESIAN_POINT('Ctrl Pts',(8.24667000083438,-0.491516046133,4.01781014446235));
#28692=CARTESIAN_POINT('Ctrl Pts',(8.29438583689722,-0.280813212199106,
3.59620653211525));
#28693=CARTESIAN_POINT('Ctrl Pts',(8.34210167296004,0.187764715363875,3.54541267448783));
#28694=CARTESIAN_POINT('Ctrl Pts',(8.38981750902289,0.483915415676709,3.91207335260334));
#28695=CARTESIAN_POINT('Ctrl Pts',(8.43358339934334,0.347950231939931,4.32244196179047));
#28696=CARTESIAN_POINT('Ctrl Pts',(8.46144401097618,0.1037581297464,4.41486010664565));
#28697=CARTESIAN_POINT('Ctrl Pts',(8.47339934392141,-0.000383538171196768,
4.41580895574666));
#28698=CARTESIAN_POINT('Origin',(3.42660065607856,0.,4.));
#28699=CARTESIAN_POINT('',(7.77660065607858,0.000318631424802313,4.41622521972442));
#28700=CARTESIAN_POINT('',(7.8733993439214,0.000353153796088606,4.4161078667978));
#28701=CARTESIAN_POINT('',(3.42660065607856,4.87367679877478E-13,4.415875));
#28702=CARTESIAN_POINT('Ctrl Pts',(7.77660065607859,0.000318631424802297,
4.41622521972442));
#28703=CARTESIAN_POINT('Ctrl Pts',(7.79015606572807,-0.117457481003694,
4.41522659035305));
#28704=CARTESIAN_POINT('Ctrl Pts',(7.81961675406517,-0.375115671948731,
4.30131743988157));
#28705=CARTESIAN_POINT('Ctrl Pts',(7.86498272108989,-0.472647010158531,
3.86394843388276));
#28706=CARTESIAN_POINT('Ctrl Pts',(7.91269855715272,-0.141191260335066,
3.52886280888004));
#28707=CARTESIAN_POINT('Ctrl Pts',(7.96041439321556,0.31992259635559,3.62642971585976));
#28708=CARTESIAN_POINT('Ctrl Pts',(8.0081302292784,0.48724661017382,4.0670519628834));
#28709=CARTESIAN_POINT('Ctrl Pts',(8.04685898356608,0.259884401562094,4.37470733986759));
#28710=CARTESIAN_POINT('Ctrl Pts',(8.06968245916614,0.0606202562326388,
4.41542398077349));
#28711=CARTESIAN_POINT('Ctrl Pts',(8.07660065607858,0.00014595794724577,
4.41523406184916));
#28712=CARTESIAN_POINT('Ctrl Pts',(7.8733993439214,0.000353153796088627,
4.4161078667978));
#28713=CARTESIAN_POINT('Ctrl Pts',(7.88648594541244,-0.113432877329791,
4.41507910421771));
#28714=CARTESIAN_POINT('Ctrl Pts',(7.9154778255911,-0.367219156371593,4.30774647947464));
#28715=CARTESIAN_POINT('Ctrl Pts',(7.96037498445733,-0.476448943335793,
3.87792777037096));
#28716=CARTESIAN_POINT('Ctrl Pts',(8.0080908205202,-0.1550058622045,3.53322552818936));
#28717=CARTESIAN_POINT('Ctrl Pts',(8.05580665658301,0.308781487260178,3.61716946571973));
#28718=CARTESIAN_POINT('Ctrl Pts',(8.10352249264587,0.489010045760349,4.0526725734847));
#28719=CARTESIAN_POINT('Ctrl Pts',(8.14272005509199,0.26816615642074,4.37069430501912));
#28720=CARTESIAN_POINT('Ctrl Pts',(8.1660123388505,0.064666477720629,4.4153129696744));
#28721=CARTESIAN_POINT('Ctrl Pts',(8.1733993439214,8.12049300509751E-5,
4.41520065480005));
#28722=CARTESIAN_POINT('Origin',(3.42660065607856,0.,4.));
#28723=CARTESIAN_POINT('',(7.47660065607859,-0.000306770237538029,4.41625647512786));
#28724=CARTESIAN_POINT('',(7.5733993439214,-0.000257198714157858,4.41635988094829));
#28725=CARTESIAN_POINT('',(3.42660065607856,4.87367679877478E-13,4.415875));
#28726=CARTESIAN_POINT('Ctrl Pts',(7.47660065607859,-0.00030677023753798,
4.41625647512786));
#28727=CARTESIAN_POINT('Ctrl Pts',(7.47881911491479,-0.0195780710793754,
4.41641565502598));
#28728=CARTESIAN_POINT('Ctrl Pts',(7.4969428524386,-0.176849480241104,4.4064317922735));
#28729=CARTESIAN_POINT('Ctrl Pts',(7.53097186865002,-0.44664354691983,4.20594845626764));
#28730=CARTESIAN_POINT('Ctrl Pts',(7.57868770471286,-0.414791917646955,
3.73570302684109));
#28731=CARTESIAN_POINT('Ctrl Pts',(7.62640354077569,-0.00203048755240202,
3.50816557464413));
#28732=CARTESIAN_POINT('Ctrl Pts',(7.67411937683853,0.412595570264971,3.73228724307244));
#28733=CARTESIAN_POINT('Ctrl Pts',(7.72183521290137,0.448328767436039,4.20225365549051));
#28734=CARTESIAN_POINT('Ctrl Pts',(7.75599563931472,0.179163779268806,4.40574053813273));
#28735=CARTESIAN_POINT('Ctrl Pts',(7.77425078704046,0.0207354574140521,
4.41639833498254));
#28736=CARTESIAN_POINT('Ctrl Pts',(7.77660065607859,0.000318631424802297,
4.41622521972442));
#28737=CARTESIAN_POINT('Ctrl Pts',(7.5733993439214,-0.000257198714157839,
4.41635988094829));
#28738=CARTESIAN_POINT('Ctrl Pts',(7.57514899459915,-0.0154461882200338,
4.41646996636401));
#28739=CARTESIAN_POINT('Ctrl Pts',(7.59280392396451,-0.168599214901356,
4.40881268721627));
#28740=CARTESIAN_POINT('Ctrl Pts',(7.62636413201748,-0.440384235482588,
4.21901358396786));
#28741=CARTESIAN_POINT('Ctrl Pts',(7.67407996808031,-0.422396009600076,
3.7480340579683));
#28742=CARTESIAN_POINT('Ctrl Pts',(7.72179580414317,-0.0165150286377962,
3.50843873354525));
#28743=CARTESIAN_POINT('Ctrl Pts',(7.76951164020598,0.404531957204003,3.72025168374225));
#28744=CARTESIAN_POINT('Ctrl Pts',(7.81722747626884,0.454091022239626,4.18896181724392));
#28745=CARTESIAN_POINT('Ctrl Pts',(7.85185671084063,0.187425762196077,4.40318800700955));
#28746=CARTESIAN_POINT('Ctrl Pts',(7.87058066672482,0.02486112795907,4.41632944836175));
#28747=CARTESIAN_POINT('Ctrl Pts',(7.8733993439214,0.000353153796088627,
4.4161078667978));
#28748=CARTESIAN_POINT('Origin',(3.42660065607856,0.,4.));
#28749=CARTESIAN_POINT('',(7.17660065607858,-0.000163391746992416,4.4152468210878));
#28750=CARTESIAN_POINT('',(7.2733993439214,-0.000222139526412562,4.4153039283715));
#28751=CARTESIAN_POINT('',(3.42660065607856,4.87367679877478E-13,4.415875));
#28752=CARTESIAN_POINT('Ctrl Pts',(7.17660065607859,-0.000163391746992363,
4.4152468210878));
#28753=CARTESIAN_POINT('Ctrl Pts',(7.18338744278911,-0.0594844418834033,
4.41545575762517));
#28754=CARTESIAN_POINT('Ctrl Pts',(7.20607950818724,-0.257561782965025,
4.37580284351512));
#28755=CARTESIAN_POINT('Ctrl Pts',(7.24467685227299,-0.486676365692783,
4.07107270446015));
#28756=CARTESIAN_POINT('Ctrl Pts',(7.29239268833582,-0.322996137187983,
3.62908393881966));
#28757=CARTESIAN_POINT('Ctrl Pts',(7.34010852439867,0.137296434535941,3.52771310152703));
#28758=CARTESIAN_POINT('Ctrl Pts',(7.3878243604615,0.471507566988788,3.86005058906394));
#28759=CARTESIAN_POINT('Ctrl Pts',(7.43332173768814,0.377318713751663,4.29947917201381));
#28760=CARTESIAN_POINT('Ctrl Pts',(7.46291383622717,0.118587850938607,4.41527441201542));
#28761=CARTESIAN_POINT('Ctrl Pts',(7.47660065607859,-0.00030677023753798,
4.41625647512786));
#28762=CARTESIAN_POINT('Ctrl Pts',(7.2733993439214,-0.000222139526412493,
4.4153039283715));
#28763=CARTESIAN_POINT('Ctrl Pts',(7.27971732247348,-0.0554265094472961,
4.41557047734173));
#28764=CARTESIAN_POINT('Ctrl Pts',(7.30194057971316,-0.249272617462211,
4.37960776139715));
#28765=CARTESIAN_POINT('Ctrl Pts',(7.34006911564044,-0.484372034479295,
4.08537538031203));
#28766=CARTESIAN_POINT('Ctrl Pts',(7.3877849517033,-0.333780171974684,3.63875766810317));
#28767=CARTESIAN_POINT('Ctrl Pts',(7.43550078776612,0.123327161313159,3.52387434835784));
#28768=CARTESIAN_POINT('Ctrl Pts',(7.48321662382897,0.467181263150904,3.84622454030349));
#28769=CARTESIAN_POINT('Ctrl Pts',(7.52918280921405,0.385138488472668,4.29279105563264));
#28770=CARTESIAN_POINT('Ctrl Pts',(7.55924371591154,0.122630008444172,4.41546922990911));
#28771=CARTESIAN_POINT('Ctrl Pts',(7.5733993439214,-0.000257198714157839,
4.41635988094829));
#28772=CARTESIAN_POINT('Origin',(3.42660065607856,0.,4.));
#28773=CARTESIAN_POINT('',(6.87660065607859,0.000369753976522709,4.4156559906262));
#28774=CARTESIAN_POINT('',(6.9733993439214,0.000344359613660638,4.41554532105972));
#28775=CARTESIAN_POINT('',(3.42660065607856,4.87367679877478E-13,4.415875));
#28776=CARTESIAN_POINT('Ctrl Pts',(6.87660065607859,0.000369753976522759,
4.4156559906262));
#28777=CARTESIAN_POINT('Ctrl Pts',(6.88795577066343,-0.0986361616094132,
4.41481368816743));
#28778=CARTESIAN_POINT('Ctrl Pts',(6.91521616393589,-0.337621850525623,
4.32977807754403));
#28779=CARTESIAN_POINT('Ctrl Pts',(6.95838183589596,-0.486886005735063,
3.93038141845316));
#28780=CARTESIAN_POINT('Ctrl Pts',(7.0060976719588,-0.204771183672361,3.55281534000283));
#28781=CARTESIAN_POINT('Ctrl Pts',(7.05381350802163,0.265389096458903,3.58590591031157));
#28782=CARTESIAN_POINT('Ctrl Pts',(7.10152934408448,0.491837993618785,3.99926540470374));
#28783=CARTESIAN_POINT('Ctrl Pts',(7.14245839343679,0.298657604039877,4.35441002681052));
#28784=CARTESIAN_POINT('Ctrl Pts',(7.16748216410149,0.0795383202432945,
4.41496610118));
#28785=CARTESIAN_POINT('Ctrl Pts',(7.17660065607859,-0.000163391746992363,
4.4152468210878));
#28786=CARTESIAN_POINT('Ctrl Pts',(6.9733993439214,0.00034435961366068,
4.41554532105972));
#28787=CARTESIAN_POINT('Ctrl Pts',(6.9842856503478,-0.0946377878655052,
4.41480662962373));
#28788=CARTESIAN_POINT('Ctrl Pts',(7.0110772354618,-0.329510302625179,4.33529054280597));
#28789=CARTESIAN_POINT('Ctrl Pts',(7.05377409926342,-0.488725618924084,
3.94475128051735));
#28790=CARTESIAN_POINT('Ctrl Pts',(7.10148993532626,-0.21785253135038,3.55904022429238));
#28791=CARTESIAN_POINT('Ctrl Pts',(7.14920577138909,0.253078023397415,3.57826934481931));
#28792=CARTESIAN_POINT('Ctrl Pts',(7.19692160745195,0.491603063369337,3.98478019943955));
#28793=CARTESIAN_POINT('Ctrl Pts',(7.2383194649627,0.306874094293292,4.34959156107453));
#28794=CARTESIAN_POINT('Ctrl Pts',(7.26381204378586,0.0835484619188193,
4.41489945011039));
#28795=CARTESIAN_POINT('Ctrl Pts',(7.2733993439214,-0.000222139526412493,
4.4153039283715));
#28796=CARTESIAN_POINT('Origin',(3.42660065607856,0.,4.));
#28797=CARTESIAN_POINT('',(6.57660065607858,1.8302248101926E-5,4.41656360501758));
#28798=CARTESIAN_POINT('',(6.6733993439214,7.63499956435865E-5,4.4165465803965));
#28799=CARTESIAN_POINT('',(3.42660065607856,4.87367679877478E-13,4.415875));
#28800=CARTESIAN_POINT('Ctrl Pts',(6.57660065607858,1.83022481018748E-5,
4.41656360501758));
#28801=CARTESIAN_POINT('Ctrl Pts',(6.57661881985014,-0.000139156870309867,
4.41656362372179));
#28802=CARTESIAN_POINT('Ctrl Pts',(6.59254226230931,-0.138177237712184,
4.41649399470799));
#28803=CARTESIAN_POINT('Ctrl Pts',(6.62437098345609,-0.41404349770976,4.26553045144514));
#28804=CARTESIAN_POINT('Ctrl Pts',(6.67208681951894,-0.447234019333667,
3.79538894860702));
#28805=CARTESIAN_POINT('Ctrl Pts',(6.71980265558177,-0.0698021891909718,
3.51313682319347));
#28806=CARTESIAN_POINT('Ctrl Pts',(6.76751849164461,0.371772181936036,3.67798293440124));
#28807=CARTESIAN_POINT('Ctrl Pts',(6.81523432770745,0.471920133146607,4.13853999974893));
#28808=CARTESIAN_POINT('Ctrl Pts',(6.85159504918544,0.21800401543618,4.39254992240466));
#28809=CARTESIAN_POINT('Ctrl Pts',(6.87205049197582,0.0400429038769189,
4.41599351380864));
#28810=CARTESIAN_POINT('Ctrl Pts',(6.87660065607859,0.000369753976522759,
4.4156559906262));
#28811=CARTESIAN_POINT('Ctrl Pts',(6.6733993439214,7.63499956435956E-5,
4.4165465803965));
#28812=CARTESIAN_POINT('Ctrl Pts',(6.68885397822212,-0.133927014866661,
4.41622291450327));
#28813=CARTESIAN_POINT('Ctrl Pts',(6.72021389121046,-0.406451392834186,
4.27318229388465));
#28814=CARTESIAN_POINT('Ctrl Pts',(6.76747908288639,-0.453085647428837,
3.80864864857145));
#28815=CARTESIAN_POINT('Ctrl Pts',(6.81519491894923,-0.0841006081168706,
3.51540431248109));
#28816=CARTESIAN_POINT('Ctrl Pts',(6.86291075501207,0.362121456530253,3.66717299786736));
#28817=CARTESIAN_POINT('Ctrl Pts',(6.91062659107491,0.475798562415156,4.124581128109));
#28818=CARTESIAN_POINT('Ctrl Pts',(6.94745612071136,0.226294304474162,4.38932900794447));
#28819=CARTESIAN_POINT('Ctrl Pts',(6.96838037166019,0.0441344886838037,
4.41588588393584));
#28820=CARTESIAN_POINT('Ctrl Pts',(6.9733993439214,0.00034435961366068,
4.41554532105972));
#28821=CARTESIAN_POINT('Origin',(3.42660065607856,0.,4.));
#28822=CARTESIAN_POINT('',(6.27660065607859,-8.94903747701068E-6,4.41582842213685));
#28823=CARTESIAN_POINT('',(6.3733993439214,-0.000441664590319634,4.4157663968931));
#28824=CARTESIAN_POINT('',(3.42660065607856,4.87367679877478E-13,4.415875));
#28825=CARTESIAN_POINT('Ctrl Pts',(6.27660065607859,-8.94903747701223E-6,
4.41582842213685));
#28826=CARTESIAN_POINT('Ctrl Pts',(6.28118714772447,-0.0399801639742102,
4.41579747358059));
#28827=CARTESIAN_POINT('Ctrl Pts',(6.29372627871415,-0.149263049162913,
4.40013952362907));
#28828=CARTESIAN_POINT('Ctrl Pts',(6.31421804904765,-0.307151379675736,
4.3060270879454));
#28829=CARTESIAN_POINT('Ctrl Pts',(6.33807596707907,-0.416657206472865,
4.12081787696614));
#28830=CARTESIAN_POINT('Ctrl Pts',(6.36193388511048,-0.422829889105799,
3.9075587958503));
#28831=CARTESIAN_POINT('Ctrl Pts',(6.39374444248571,-0.296437506874183,
3.64987069373525));
#28832=CARTESIAN_POINT('Ctrl Pts',(6.43350763920474,0.0703302468340302,
3.51324810367198));
#28833=CARTESIAN_POINT('Ctrl Pts',(6.48122347526758,0.448014600657906,3.7964368525222));
#28834=CARTESIAN_POINT('Ctrl Pts',(6.52892114755886,0.413253290380966,4.26628466471864));
#28835=CARTESIAN_POINT('Ctrl Pts',(6.56071354116253,0.137741412285014,4.41654724519979));
#28836=CARTESIAN_POINT('Ctrl Pts',(6.57660065607858,1.83022481018748E-5,
4.41656360501758));
#28837=CARTESIAN_POINT('Ctrl Pts',(6.3733993439214,-0.000441664590319611,
4.4157663968931));
#28838=CARTESIAN_POINT('Ctrl Pts',(6.37751702740883,-0.0362476131304844,
4.41610293027605));
#28839=CARTESIAN_POINT('Ctrl Pts',(6.39753998958387,-0.210006484715375,
4.39546152579387));
#28840=CARTESIAN_POINT('Ctrl Pts',(6.43346823044653,-0.468271923807345,
4.15124960425567));
#28841=CARTESIAN_POINT('Ctrl Pts',(6.48118406650937,-0.380227249479543,
3.6882349865083));
#28842=CARTESIAN_POINT('Ctrl Pts',(6.52889990257221,0.0564566449812287,
3.51140415777354));
#28843=CARTESIAN_POINT('Ctrl Pts',(6.57661573863504,0.441574375138847,3.78331933667001));
#28844=CARTESIAN_POINT('Ctrl Pts',(6.62433157469789,0.421040068198854,4.25418342072721));
#28845=CARTESIAN_POINT('Ctrl Pts',(6.65659277646,0.145792717270209,4.41473316952435));
#28846=CARTESIAN_POINT('Ctrl Pts',(6.6729486995345,0.00398377756883227,
4.41655601822694));
#28847=CARTESIAN_POINT('Ctrl Pts',(6.6733993439214,7.63499956435956E-5,
4.4165465803965));
#28848=CARTESIAN_POINT('Origin',(3.42660065607856,0.,4.));
#28849=CARTESIAN_POINT('',(5.97660065607859,-9.19412645702589E-6,4.41589218083175));
#28850=CARTESIAN_POINT('',(6.0733993439214,-6.65563173402051E-6,4.41590255337155));
#28851=CARTESIAN_POINT('',(3.42660065607856,4.87367679877478E-13,4.415875));
#28852=CARTESIAN_POINT('Ctrl Pts',(5.97660065607858,-9.19412645705893E-6,
4.41589218083175));
#28853=CARTESIAN_POINT('Ctrl Pts',(5.97780283625498,-0.0104787976275591,
4.4159022685469));
#28854=CARTESIAN_POINT('Ctrl Pts',(5.98695765577519,-0.0902010538040918,
4.41295272969856));
#28855=CARTESIAN_POINT('Ctrl Pts',(6.0040651146392,-0.23587461323539,4.36380751861078));
#28856=CARTESIAN_POINT('Ctrl Pts',(6.02792303267061,-0.381351759249696,
4.20630938167977));
#28857=CARTESIAN_POINT('Ctrl Pts',(6.05178095070204,-0.433578399193506,
3.9983625870902));
#28858=CARTESIAN_POINT('Ctrl Pts',(6.07563886873346,-0.379782579589031,
3.79081692866841));
#28859=CARTESIAN_POINT('Ctrl Pts',(6.09949678676487,-0.233120953551068,
3.63442082419035));
#28860=CARTESIAN_POINT('Ctrl Pts',(6.12335470479629,-0.0294522997972467,
3.5674214393556));
#28861=CARTESIAN_POINT('Ctrl Pts',(6.14721262282771,0.181413325723775,3.60619428643423));
#28862=CARTESIAN_POINT('Ctrl Pts',(6.17107054085913,0.347927737305898,3.74127281623538));
#28863=CARTESIAN_POINT('Ctrl Pts',(6.19492845889055,0.429346806292137,3.93959933010928));
#28864=CARTESIAN_POINT('Ctrl Pts',(6.21878637692197,0.405811992579865,4.15272917617017));
#28865=CARTESIAN_POINT('Ctrl Pts',(6.24264429495339,0.282982581651336,4.32844890303245));
#28866=CARTESIAN_POINT('Ctrl Pts',(6.26191572133893,0.127967070080381,4.40561019629887));
#28867=CARTESIAN_POINT('Ctrl Pts',(6.27323450838066,0.029326984292613,4.415851136102));
#28868=CARTESIAN_POINT('Ctrl Pts',(6.27660065607859,-8.94903747701223E-6,
4.41582842213685));
#28869=CARTESIAN_POINT('Ctrl Pts',(6.0733993439214,-6.65563173397714E-6,
4.41590255337156));
#28870=CARTESIAN_POINT('Ctrl Pts',(6.07413271593935,-0.00639299139291402,
4.41590724351385));
#28871=CARTESIAN_POINT('Ctrl Pts',(6.0828187273011,-0.0820297780542147,
4.41420140028919));
#28872=CARTESIAN_POINT('Ctrl Pts',(6.09945737800665,-0.2250554921608,4.3705991908187));
#28873=CARTESIAN_POINT('Ctrl Pts',(6.12331529603809,-0.375113923638194,
4.21744656883549));
#28874=CARTESIAN_POINT('Ctrl Pts',(6.1471732140695,-0.433431396087355,4.01114207710762));
#28875=CARTESIAN_POINT('Ctrl Pts',(6.17103113210093,-0.385792139046387,
3.80207577201042));
#28876=CARTESIAN_POINT('Ctrl Pts',(6.19488905013233,-0.243761337718234,
3.64147770828707));
#28877=CARTESIAN_POINT('Ctrl Pts',(6.21874696816376,-0.042227823444436,
3.56841523311022));
#28878=CARTESIAN_POINT('Ctrl Pts',(6.24260488619517,0.16982704650124,3.60113783246665));
#28879=CARTESIAN_POINT('Ctrl Pts',(6.2664628042266,0.339985970990829,3.73091992247201));
#28880=CARTESIAN_POINT('Ctrl Pts',(6.29032072225801,0.427700638223926,3.92738904240251));
#28881=CARTESIAN_POINT('Ctrl Pts',(6.31417864028943,0.409561128158778,4.13996490148311));
#28882=CARTESIAN_POINT('Ctrl Pts',(6.34187151417723,0.27471212230801,4.35031587281991));
#28883=CARTESIAN_POINT('Ctrl Pts',(6.36161174872122,0.102059178040878,4.41480301073152));
#28884=CARTESIAN_POINT('Ctrl Pts',(6.3733993439214,-0.000441664590319611,
4.4157663968931));
#28885=CARTESIAN_POINT('Origin',(3.42660065607856,0.,4.));
#28886=CARTESIAN_POINT('',(5.67660065607858,1.06631253201556E-5,4.41586554077139));
#28887=CARTESIAN_POINT('',(5.7733993439214,9.17748676071416E-6,4.4158542849441));
#28888=CARTESIAN_POINT('',(3.42660065607856,4.87367679877478E-13,4.415875));
#28889=CARTESIAN_POINT('Ctrl Pts',(5.67660065607858,1.06631253201268E-5,
4.41586554077139));
#28890=CARTESIAN_POINT('Ctrl Pts',(5.68237116412931,-0.050253077703417,
4.41581669384736));
#28891=CARTESIAN_POINT('Ctrl Pts',(5.69609431152383,-0.169828933264711,
4.3941204493343));
#28892=CARTESIAN_POINT('Ctrl Pts',(5.71777009826218,-0.329222253834466,
4.28214440376531));
#28893=CARTESIAN_POINT('Ctrl Pts',(5.74162801629359,-0.424158110434281,
4.08990358344764));
#28894=CARTESIAN_POINT('Ctrl Pts',(5.76548593432501,-0.415375755386326,
3.8756788878607));
#28895=CARTESIAN_POINT('Ctrl Pts',(5.78934385235642,-0.305022713182347,
3.69185409099321));
#28896=CARTESIAN_POINT('Ctrl Pts',(5.81320177038785,-0.120083309624962,
3.58337936191985));
#28897=CARTESIAN_POINT('Ctrl Pts',(5.83705968841926,0.0942197354074567,
3.57677972866706));
#28898=CARTESIAN_POINT('Ctrl Pts',(5.86091760645069,0.285483486244351,3.673668977605));
#28899=CARTESIAN_POINT('Ctrl Pts',(5.8847755244821,0.406938752801468,3.85035505520226));
#28900=CARTESIAN_POINT('Ctrl Pts',(5.90863344251353,0.428886400972996,4.06363338935351));
#28901=CARTESIAN_POINT('Ctrl Pts',(5.93249136054494,0.345959657594393,4.261351642888));
#28902=CARTESIAN_POINT('Ctrl Pts',(5.95514709839996,0.186877681905787,4.38841966610496));
#28903=CARTESIAN_POINT('Ctrl Pts',(5.96985019691118,0.0587795235055939,
4.41583553648629));
#28904=CARTESIAN_POINT('Ctrl Pts',(5.97660065607858,-9.19412645705893E-6,
4.41589218083175));
#28905=CARTESIAN_POINT('Ctrl Pts',(5.7733993439214,9.17748676073846E-6,
4.4158542849441));
#28906=CARTESIAN_POINT('Ctrl Pts',(5.77870104381367,-0.0461746181927863,
4.41581721944429));
#28907=CARTESIAN_POINT('Ctrl Pts',(5.79195538304975,-0.161664917198308,
4.3966319946429));
#28908=CARTESIAN_POINT('Ctrl Pts',(5.81316236162963,-0.320769768688322,
4.29171820750724));
#28909=CARTESIAN_POINT('Ctrl Pts',(5.83702027966105,-0.421326288178809,
4.10235681181338));
#28910=CARTESIAN_POINT('Ctrl Pts',(5.86087819769247,-0.418857046020503,
3.88796639709818));
#28911=CARTESIAN_POINT('Ctrl Pts',(5.88473611572389,-0.313965860818636,
3.70097123187977));
#28912=CARTESIAN_POINT('Ctrl Pts',(5.90859403375531,-0.132301443679057,
3.58709678011166));
#28913=CARTESIAN_POINT('Ctrl Pts',(5.93245195178673,0.0817142298265842,
3.57418834816524));
#28914=CARTESIAN_POINT('Ctrl Pts',(5.95630986981814,0.275748643515392,3.66540258613358));
#28915=CARTESIAN_POINT('Ctrl Pts',(5.98016778784957,0.402354822815078,3.83843477537114));
#28916=CARTESIAN_POINT('Ctrl Pts',(6.00402570588098,0.430574627524036,4.05097449853386));
#28917=CARTESIAN_POINT('Ctrl Pts',(6.02788362391241,0.353506566116634,4.25104874587108));
#28918=CARTESIAN_POINT('Ctrl Pts',(6.05100816992587,0.195023852357142,4.38547315270063));
#28919=CARTESIAN_POINT('Ctrl Pts',(6.06618007659554,0.06286002589468,4.4158563839102));
#28920=CARTESIAN_POINT('Ctrl Pts',(6.0733993439214,-6.65563173397714E-6,
4.41590255337156));
#28921=CARTESIAN_POINT('Origin',(3.42660065607856,0.,4.));
#28922=CARTESIAN_POINT('',(5.37660065607858,-1.01751121954902E-5,4.41586038335289));
#28923=CARTESIAN_POINT('',(5.4733993439214,-1.09014992595302E-5,4.41587264340464));
#28924=CARTESIAN_POINT('',(3.42660065607856,4.87367679877478E-13,4.415875));
#28925=CARTESIAN_POINT('Ctrl Pts',(5.37660065607859,-1.01751121954468E-5,
4.41586038335289));
#28926=CARTESIAN_POINT('Ctrl Pts',(5.37898685265982,-0.0207957689391596,
4.41587928195339));
#28927=CARTESIAN_POINT('Ctrl Pts',(5.38932568858487,-0.110842971866809,
4.40924760552439));
#28928=CARTESIAN_POINT('Ctrl Pts',(5.40761716385372,-0.26226226804932,4.34526983614494));
#28929=CARTESIAN_POINT('Ctrl Pts',(5.43147508188515,-0.395631058815178,
4.17739453851434));
#28930=CARTESIAN_POINT('Ctrl Pts',(5.45533299991656,-0.432257278927009,
3.96614144408682));
#28931=CARTESIAN_POINT('Ctrl Pts',(5.47919091794798,-0.363184819889405,
3.76316768886851));
#28932=CARTESIAN_POINT('Ctrl Pts',(5.5030488359794,-0.205303779432806,3.61810588490468));
#28933=CARTESIAN_POINT('Ctrl Pts',(5.52690675401082,0.00277962745745752,
3.56642759466814));
#28934=CARTESIAN_POINT('Ctrl Pts',(5.55076467204224,0.210183339719457,3.62076956781107));
#28935=CARTESIAN_POINT('Ctrl Pts',(5.57462259007365,0.36619150013966,3.76784371165257));
#28936=CARTESIAN_POINT('Ctrl Pts',(5.59848050810508,0.432655863921731,3.97168639180759));
#28937=CARTESIAN_POINT('Ctrl Pts',(5.62233842613649,0.393324083661671,4.18245252040861));
#28938=CARTESIAN_POINT('Ctrl Pts',(5.64619634416792,0.257813851021257,4.34860403787086));
#28939=CARTESIAN_POINT('Ctrl Pts',(5.66428375414861,0.107285005985459,4.40994309575933));
#28940=CARTESIAN_POINT('Ctrl Pts',(5.6744185247855,0.0190180158238588,4.41588401235146));
#28941=CARTESIAN_POINT('Ctrl Pts',(5.67660065607858,1.06631253201268E-5,
4.41586554077139));
#28942=CARTESIAN_POINT('Ctrl Pts',(5.4733993439214,-1.0901499259525E-5,
4.41587264340464));
#28943=CARTESIAN_POINT('Ctrl Pts',(5.47531673234419,-0.0167114040746605,
4.41588973972128));
#28944=CARTESIAN_POINT('Ctrl Pts',(5.48518676011079,-0.102669266038577,
4.41080986982701));
#28945=CARTESIAN_POINT('Ctrl Pts',(5.50300942722118,-0.251979671819092,
4.35284416104532));
#28946=CARTESIAN_POINT('Ctrl Pts',(5.52686734525261,-0.390234841353927,
4.18896964197264));
#28947=CARTESIAN_POINT('Ctrl Pts',(5.55072526328402,-0.433066962396004,
3.97888689800548));
#28948=CARTESIAN_POINT('Ctrl Pts',(5.57458318131544,-0.370002414621403,
3.77396688259));
#28949=CARTESIAN_POINT('Ctrl Pts',(5.59844109934686,-0.21646219781534,3.62431812139094));
#28950=CARTESIAN_POINT('Ctrl Pts',(5.62229901737828,-0.00999107731853999,
3.56653381289738));
#28951=CARTESIAN_POINT('Ctrl Pts',(5.64615693540971,0.198923133709572,3.61474379450078));
#28952=CARTESIAN_POINT('Ctrl Pts',(5.67001485344111,0.359195220034686,3.75715941257656));
#28953=CARTESIAN_POINT('Ctrl Pts',(5.69387277147254,0.431634290692432,3.95895616900985));
#28954=CARTESIAN_POINT('Ctrl Pts',(5.71773068950395,0.398527019959163,4.1707892603438));
#28955=CARTESIAN_POINT('Ctrl Pts',(5.74158860753538,0.267969036875697,4.34085972491723));
#28956=CARTESIAN_POINT('Ctrl Pts',(5.76014482567452,0.115458993192439,4.40830959117706));
#28957=CARTESIAN_POINT('Ctrl Pts',(5.77074840446986,0.0231018550196917,
4.41587281831976));
#28958=CARTESIAN_POINT('Ctrl Pts',(5.7733993439214,9.17748676073846E-6,
4.4158542849441));
#28959=CARTESIAN_POINT('Origin',(3.42660065607856,0.,4.));
#28960=CARTESIAN_POINT('',(5.07660065607859,8.10857529294212E-6,4.41589722116852));
#28961=CARTESIAN_POINT('',(5.1733993439214,1.02299162792543E-5,4.4158851107878));
#28962=CARTESIAN_POINT('',(3.42660065607856,4.87367679877478E-13,4.415875));
#28963=CARTESIAN_POINT('Ctrl Pts',(5.07660065607858,8.10857529294148E-6,
4.41589722116852));
#28964=CARTESIAN_POINT('Ctrl Pts',(5.08355518053415,-0.060555656273516,
4.41584370653314));
#28965=CARTESIAN_POINT('Ctrl Pts',(5.09846234433351,-0.190424342306974,
4.38715451669839));
#28966=CARTESIAN_POINT('Ctrl Pts',(5.1213221474767,-0.349282119693095,4.256894448863));
#28967=CARTESIAN_POINT('Ctrl Pts',(5.1451800655081,-0.4296670234643,4.05812921762123));
#28968=CARTESIAN_POINT('Ctrl Pts',(5.16903798353954,-0.404986636103755,
3.84514980926298));
#28969=CARTESIAN_POINT('Ctrl Pts',(5.19289590157095,-0.281275984601366,
3.67003549057442));
#28970=CARTESIAN_POINT('Ctrl Pts',(5.21675381960238,-0.0887856930599551,
3.5756064824932));
#28971=CARTESIAN_POINT('Ctrl Pts',(5.24061173763379,0.125415118908336,3.58495324968971));
#28972=CARTESIAN_POINT('Ctrl Pts',(5.26446965566521,0.308948518064291,3.69579025298356));
#28973=CARTESIAN_POINT('Ctrl Pts',(5.28832757369662,0.416935588964862,3.88101482593007));
#28974=CARTESIAN_POINT('Ctrl Pts',(5.31218549172805,0.422970551266107,4.09533451502773));
#28975=CARTESIAN_POINT('Ctrl Pts',(5.33604340975946,0.325577692296299,4.28634231834109));
#28976=CARTESIAN_POINT('Ctrl Pts',(5.35751513120965,0.166275769440666,4.39523064161658));
#28977=CARTESIAN_POINT('Ctrl Pts',(5.37103421331602,0.0484777907299229,
4.41581629730449));
#28978=CARTESIAN_POINT('Ctrl Pts',(5.37660065607859,-1.01751121954468E-5,
4.41586038335289));
#28979=CARTESIAN_POINT('Ctrl Pts',(5.1733993439214,1.02299162792474E-5,
4.4158851107878));
#28980=CARTESIAN_POINT('Ctrl Pts',(5.17988506021851,-0.0564756498766958,
4.41582730150705));
#28981=CARTESIAN_POINT('Ctrl Pts',(5.19432341585943,-0.182274442988225,
4.39002065289559));
#28982=CARTESIAN_POINT('Ctrl Pts',(5.21671441084416,-0.341564590845109,
4.26707000444592));
#28983=CARTESIAN_POINT('Ctrl Pts',(5.24057232887557,-0.427768622694993,
4.07075847957352));
#28984=CARTESIAN_POINT('Ctrl Pts',(5.264430246907,-0.409371574112622,3.85714457902312));
#28985=CARTESIAN_POINT('Ctrl Pts',(5.2882881649384,-0.290872024601924,3.6784627202051));
#28986=CARTESIAN_POINT('Ctrl Pts',(5.31214608296984,-0.101246341881189,
3.57840548479658));
#28987=CARTESIAN_POINT('Ctrl Pts',(5.33600400100125,0.113136829324483,3.58143959235932));
#28988=CARTESIAN_POINT('Ctrl Pts',(5.35986191903268,0.299854963974951,3.68682312094679));
#28989=CARTESIAN_POINT('Ctrl Pts',(5.38371983706408,0.413250392048343,3.8687869272297));
#28990=CARTESIAN_POINT('Ctrl Pts',(5.40757775509551,0.425594842551202,4.08283590397723));
#28991=CARTESIAN_POINT('Ctrl Pts',(5.43143567312693,0.333869761079625,4.27662924579771));
#28992=CARTESIAN_POINT('Ctrl Pts',(5.45337620273556,0.174437273907163,4.39264091290779));
#28993=CARTESIAN_POINT('Ctrl Pts',(5.46736409300038,0.0525562895569378,
4.41581883033293));
#28994=CARTESIAN_POINT('Ctrl Pts',(5.4733993439214,-1.0901499259525E-5,
4.41587264340464));
#28995=CARTESIAN_POINT('Origin',(3.42660065607856,0.,4.));
#28996=CARTESIAN_POINT('',(4.77660065607858,-3.27394476109793E-6,4.41584059078716));
#28997=CARTESIAN_POINT('',(4.8733993439214,-6.67049670156904E-6,4.4158459349409));
#28998=CARTESIAN_POINT('',(3.42660065607856,4.87367679877478E-13,4.415875));
#28999=CARTESIAN_POINT('Ctrl Pts',(4.77660065607858,-3.27394476113199E-6,
4.41584059078717));
#29000=CARTESIAN_POINT('Ctrl Pts',(4.78017086906467,-0.0311067951354469,
4.4158491206715));
#29001=CARTESIAN_POINT('Ctrl Pts',(4.79169372139456,-0.131487321212171,
4.40473555835468));
#29002=CARTESIAN_POINT('Ctrl Pts',(4.81116921306824,-0.287199161490599,
4.32482210305491));
#29003=CARTESIAN_POINT('Ctrl Pts',(4.83502713109967,-0.407721671464292,
4.14749845969467));
#29004=CARTESIAN_POINT('Ctrl Pts',(4.85888504913109,-0.42854512664958,3.93410742516172));
#29005=CARTESIAN_POINT('Ctrl Pts',(4.8827429671625,-0.344577625034195,3.73682892005441));
#29006=CARTESIAN_POINT('Ctrl Pts',(4.90660088519393,-0.176351507991885,
3.60390291263011));
#29007=CARTESIAN_POINT('Ctrl Pts',(4.93045880322534,0.0349973564730633,
3.56783343253575));
#29008=CARTESIAN_POINT('Ctrl Pts',(4.95431672125677,0.237788413971502,3.63744045016736));
#29009=CARTESIAN_POINT('Ctrl Pts',(4.97817463928818,0.382433727027559,3.79570315365689));
#29010=CARTESIAN_POINT('Ctrl Pts',(5.0020325573196,0.433563576539811,4.00392200101168));
#29011=CARTESIAN_POINT('Ctrl Pts',(5.02589047535102,0.378675321553375,4.21118181228595));
#29012=CARTESIAN_POINT('Ctrl Pts',(5.04974839338244,0.231190635538481,4.36680191797922));
#29013=CARTESIAN_POINT('Ctrl Pts',(5.0666517869583,0.086644022961884,4.4135113916189));
#29014=CARTESIAN_POINT('Ctrl Pts',(5.07560254119034,0.00870023350343714,
4.41590490160082));
#29015=CARTESIAN_POINT('Ctrl Pts',(5.07660065607858,8.10857529294148E-6,
4.41589722116852));
#29016=CARTESIAN_POINT('Ctrl Pts',(4.8733993439214,-6.67049670157252E-6,
4.41584593494091));
#29017=CARTESIAN_POINT('Ctrl Pts',(4.87650074874903,-0.0270249643080214,
4.41586127519519));
#29018=CARTESIAN_POINT('Ctrl Pts',(4.88755479292047,-0.123313358466266,
4.40662010077424));
#29019=CARTESIAN_POINT('Ctrl Pts',(4.90656147643571,-0.277507970732168,
4.33313973520738));
#29020=CARTESIAN_POINT('Ctrl Pts',(4.93041939446713,-0.403200703213916,
4.15944262266324));
#29021=CARTESIAN_POINT('Ctrl Pts',(4.95427731249855,-0.430299880793222,
3.94675744574809));
#29022=CARTESIAN_POINT('Ctrl Pts',(4.97813523052996,-0.352179016385168,
3.7470915236456));
#29023=CARTESIAN_POINT('Ctrl Pts',(5.00199314856139,-0.187940789307144,
3.60926861310034));
#29024=CARTESIAN_POINT('Ctrl Pts',(5.0258510665928,0.0222540801607904,3.56699016996131));
#29025=CARTESIAN_POINT('Ctrl Pts',(5.04970898462423,0.227007220840439,3.63059442521772));
#29026=CARTESIAN_POINT('Ctrl Pts',(5.07356690265564,0.376250912472057,3.7845284059142));
#29027=CARTESIAN_POINT('Ctrl Pts',(5.09742482068706,0.433491007135177,3.99115106069306));
#29028=CARTESIAN_POINT('Ctrl Pts',(5.12128273871848,0.384730742495793,4.19993752217271));
#29029=CARTESIAN_POINT('Ctrl Pts',(5.1451406567499,0.241893331461176,4.35983381329239));
#29030=CARTESIAN_POINT('Ctrl Pts',(5.16251285848421,0.0948160588051851,
4.41219316122439));
#29031=CARTESIAN_POINT('Ctrl Pts',(5.17193242087471,0.0127860645481494,
4.41589818594594));
#29032=CARTESIAN_POINT('Ctrl Pts',(5.1733993439214,1.02299162792474E-5,
4.4158851107878));
#29033=CARTESIAN_POINT('Origin',(3.42660065607856,0.,4.));
#29034=CARTESIAN_POINT('',(4.47660065607858,-1.72413508574122E-6,4.41591032029986));
#29035=CARTESIAN_POINT('',(4.5733993439214,2.6062779713001E-6,4.4159095790646));
#29036=CARTESIAN_POINT('',(3.42660065607856,4.87367679877478E-13,4.415875));
#29037=CARTESIAN_POINT('Ctrl Pts',(4.47660065607858,-1.72413508575881E-6,
4.41591032029986));
#29038=CARTESIAN_POINT('Ctrl Pts',(4.47678655759518,-0.00162050728124812,
4.41591069657345));
#29039=CARTESIAN_POINT('Ctrl Pts',(4.48492509845559,-0.0724886630755744,
4.4155056303295));
#29040=CARTESIAN_POINT('Ctrl Pts',(4.5010162786598,-0.212178818846594,4.37811758201071));
#29041=CARTESIAN_POINT('Ctrl Pts',(4.52487419669122,-0.367409789343613,
4.23022337776645));
#29042=CARTESIAN_POINT('Ctrl Pts',(4.54873211472264,-0.432799058467291,
4.02603328640456));
#29043=CARTESIAN_POINT('Ctrl Pts',(4.57259003275406,-0.392357168499796,
3.8154773474345));
#29044=CARTESIAN_POINT('Ctrl Pts',(4.59644795078547,-0.255973263285106,
3.65004222328625));
#29045=CARTESIAN_POINT('Ctrl Pts',(4.6203058688169,-0.0569969226013119,
3.57018130821703));
#29046=CARTESIAN_POINT('Ctrl Pts',(4.64416378684831,0.155916718210686,3.59542277130738));
#29047=CARTESIAN_POINT('Ctrl Pts',(4.66802170487973,0.330704474340828,3.71959438727947));
#29048=CARTESIAN_POINT('Ctrl Pts',(4.69187962291115,0.424625978282027,3.91233281365517));
#29049=CARTESIAN_POINT('Ctrl Pts',(4.71573754094257,0.41471486395576,4.1265082550995));
#29050=CARTESIAN_POINT('Ctrl Pts',(4.73959545897399,0.303394668785218,4.30974898215573));
#29051=CARTESIAN_POINT('Ctrl Pts',(4.75988316401932,0.145646585585232,4.40116103141851));
#29052=CARTESIAN_POINT('Ctrl Pts',(4.77221822972086,0.0381762104768988,
4.41583012037823));
#29053=CARTESIAN_POINT('Ctrl Pts',(4.77660065607858,-3.27394476113199E-6,
4.41584059078717));
#29054=CARTESIAN_POINT('Ctrl Pts',(4.5733993439214,2.60627797130011E-6,
4.4159095790646));
#29055=CARTESIAN_POINT('Ctrl Pts',(4.58106907662335,-0.0667838229435618,
4.4158868274511));
#29056=CARTESIAN_POINT('Ctrl Pts',(4.59669144866912,-0.202842099803805,
4.38250385602613));
#29057=CARTESIAN_POINT('Ctrl Pts',(4.62026646005868,-0.360469908510665,
4.24094439618412));
#29058=CARTESIAN_POINT('Ctrl Pts',(4.6441243780901,-0.431844582779732,4.03876871570463));
#29059=CARTESIAN_POINT('Ctrl Pts',(4.66798229612152,-0.397621493350665,
3.82711302819544));
#29060=CARTESIAN_POINT('Ctrl Pts',(4.69184021415294,-0.266169117804412,
3.65773291463971));
#29061=CARTESIAN_POINT('Ctrl Pts',(4.71569813218436,-0.0696311426542753,
3.57204642662242));
#29062=CARTESIAN_POINT('Ctrl Pts',(4.73955605021577,0.143933543589337,3.59100624451743));
#29063=CARTESIAN_POINT('Ctrl Pts',(4.76341396824719,0.322302557754209,3.70997617639404));
#29064=CARTESIAN_POINT('Ctrl Pts',(4.78727188627862,0.421859817202848,3.8998648332327));
#29065=CARTESIAN_POINT('Ctrl Pts',(4.81112980431003,0.41826086011465,4.11423926597311));
#29066=CARTESIAN_POINT('Ctrl Pts',(4.83498772234146,0.312385729531365,4.30067908636799));
#29067=CARTESIAN_POINT('Ctrl Pts',(4.85574423554524,0.15381688120809,4.39891624198015));
#29068=CARTESIAN_POINT('Ctrl Pts',(4.86854810940522,0.04225549351942,4.41582193963064));
#29069=CARTESIAN_POINT('Ctrl Pts',(4.8733993439214,-6.67049670157252E-6,
4.41584593494091));
#29070=CARTESIAN_POINT('Origin',(3.42660065607856,0.,4.));
#29071=CARTESIAN_POINT('',(4.17660065607858,5.88453344125852E-6,4.41584444980552));
#29072=CARTESIAN_POINT('',(4.2733993439214,2.51014653358805E-6,4.41583996132385));
#29073=CARTESIAN_POINT('',(3.42660065607856,4.87367679877478E-13,4.415875));
#29074=CARTESIAN_POINT('Ctrl Pts',(4.17660065607858,5.88453344126799E-6,
4.41584444980552));
#29075=CARTESIAN_POINT('Ctrl Pts',(4.18135488546951,-0.0414115481342504,
4.41582334930757));
#29076=CARTESIAN_POINT('Ctrl Pts',(4.19406175420423,-0.152126265423154,
4.3993918905015));
#29077=CARTESIAN_POINT('Ctrl Pts',(4.21472126228278,-0.310547447266788,
4.30257739619942));
#29078=CARTESIAN_POINT('Ctrl Pts',(4.23857918031418,-0.417556725585918,
4.11678647978038));
#29079=CARTESIAN_POINT('Ctrl Pts',(4.26243709834561,-0.422462345057068,
3.90243789311793));
#29080=CARTESIAN_POINT('Ctrl Pts',(4.28629501637703,-0.324064236326554,
3.71194600226016));
#29081=CARTESIAN_POINT('Ctrl Pts',(4.31015293440845,-0.146423688323203,
3.59189110566319));
#29082=CARTESIAN_POINT('Ctrl Pts',(4.33401085243986,0.0670214896752265,
3.5716299793216));
#29083=CARTESIAN_POINT('Ctrl Pts',(4.35786877047129,0.264078061498623,3.65611697628114));
#29084=CARTESIAN_POINT('Ctrl Pts',(4.38172668850271,0.396560367883193,3.82469274783887));
#29085=CARTESIAN_POINT('Ctrl Pts',(4.40558460653412,0.432072854850341,4.03613591352675));
#29086=CARTESIAN_POINT('Ctrl Pts',(4.42944252456555,0.361931763288092,4.23874286631049));
#29087=CARTESIAN_POINT('Ctrl Pts',(4.45311454108036,0.204524647174786,4.38184685695289));
#29088=CARTESIAN_POINT('Ctrl Pts',(4.46883391825138,0.0676290543833733,
4.4158946000499));
#29089=CARTESIAN_POINT('Ctrl Pts',(4.47660065607858,-1.72413508575881E-6,
4.41591032029986));
#29090=CARTESIAN_POINT('Ctrl Pts',(4.2733993439214,2.51014653359152E-6,
4.41583996132385));
#29091=CARTESIAN_POINT('Ctrl Pts',(4.27768476515387,-0.0373320337329404,
4.41583213221101));
#29092=CARTESIAN_POINT('Ctrl Pts',(4.28992282573015,-0.143955736965383,
4.40160880992953));
#29093=CARTESIAN_POINT('Ctrl Pts',(4.31011352565024,-0.301501118270308,
4.3115924136571));
#29094=CARTESIAN_POINT('Ctrl Pts',(4.33397144368164,-0.413936097932681,
4.12903358037428));
#29095=CARTESIAN_POINT('Ctrl Pts',(4.35782936171308,-0.425152419412173,
3.91492252699502));
#29096=CARTESIAN_POINT('Ctrl Pts',(4.38168727974448,-0.332407397051365,
3.72161523052345));
#29097=CARTESIAN_POINT('Ctrl Pts',(4.40554519777592,-0.158379709595794,
3.5963805946708));
#29098=CARTESIAN_POINT('Ctrl Pts',(4.42940311580732,0.0543761300157755,
3.56984189703405));
#29099=CARTESIAN_POINT('Ctrl Pts',(4.45326103383876,0.25383552520097,3.64848857324589));
#29100=CARTESIAN_POINT('Ctrl Pts',(4.47711895187016,0.39122521984844,3.81308936806525));
#29101=CARTESIAN_POINT('Ctrl Pts',(4.50097686990159,0.432949691632991,4.02339490384879));
#29102=CARTESIAN_POINT('Ctrl Pts',(4.524834787933,0.368806170420464,4.22797974831721));
#29103=CARTESIAN_POINT('Ctrl Pts',(4.54869270596443,0.214479494504121,4.37681733431002));
#29104=CARTESIAN_POINT('Ctrl Pts',(4.56488089129389,0.0741790848482271,
4.4152866170047));
#29105=CARTESIAN_POINT('Ctrl Pts',(4.57311643727954,0.0024660981813593,
4.41591041828323));
#29106=CARTESIAN_POINT('Ctrl Pts',(4.5733993439214,2.60627797130011E-6,
4.4159095790646));
#29107=CARTESIAN_POINT('Origin',(4.,0.,4.));
#29108=CARTESIAN_POINT('',(4.,-7.34788079488412E-17,4.6));
#29109=CARTESIAN_POINT('Origin',(4.,0.,4.));
#29110=CARTESIAN_POINT('',(4.,-0.219892372742957,4.3529863453938));
#29111=CARTESIAN_POINT('Ctrl Pts',(4.,-0.219914231356238,4.35301468169996));
#29112=CARTESIAN_POINT('Ctrl Pts',(4.,-0.219843051329574,4.3531167999744));
#29113=CARTESIAN_POINT('Ctrl Pts',(4.,-0.219771822781512,4.35321888245988));
#29114=CARTESIAN_POINT('Ctrl Pts',(4.,-0.21970054575756,4.3533209291203));
#29115=CARTESIAN_POINT('Ctrl Pts',(4.,-0.207925336055227,4.3701793886806));
#29116=CARTESIAN_POINT('Ctrl Pts',(4.,-0.194831304039315,4.38605734350833));
#29117=CARTESIAN_POINT('Ctrl Pts',(4.,-0.18064579384139,4.40088380688851));
#29118=CARTESIAN_POINT('Ctrl Pts',(4.,-0.168975273508986,4.41308164397169));
#29119=CARTESIAN_POINT('Ctrl Pts',(4.,-0.156565051628872,4.42456888924957));
#29120=CARTESIAN_POINT('Ctrl Pts',(4.,-0.143515931303371,4.43531683418355));
#29121=CARTESIAN_POINT('Ctrl Pts',(4.,-0.133182439541062,4.44382804395605));
#29122=CARTESIAN_POINT('Ctrl Pts',(4.,-0.122447811630206,4.45187590303098));
#29123=CARTESIAN_POINT('Ctrl Pts',(4.,-0.111352162047151,4.45944712768208));
#29124=CARTESIAN_POINT('Ctrl Pts',(4.,-0.105068105051177,4.46373511522897));
#29125=CARTESIAN_POINT('Ctrl Pts',(4.,-0.0986661212125077,4.46787107983396));
#29126=CARTESIAN_POINT('Ctrl Pts',(4.,-0.0921733602714696,4.47184061613108));
#29127=CARTESIAN_POINT('Ctrl Pts',(4.,-0.0718171345235072,4.48428598070136));
#29128=CARTESIAN_POINT('Ctrl Pts',(4.,-0.0505350523745213,4.49512244469223));
#29129=CARTESIAN_POINT('Ctrl Pts',(4.,-0.0285775088988711,4.50429938857761));
#29130=CARTESIAN_POINT('Ctrl Pts',(4.,-0.00645956782426854,4.51354336909515));
#29131=CARTESIAN_POINT('Ctrl Pts',(4.,0.0163444141029789,4.52110543571878));
#29132=CARTESIAN_POINT('Ctrl Pts',(4.,0.0396343143342583,4.52702898180467));
#29133=CARTESIAN_POINT('Ctrl Pts',(4.,0.0479455316904685,4.52914285427945));
#29134=CARTESIAN_POINT('Ctrl Pts',(4.,0.0563191235587283,4.53104786585874));
#29135=CARTESIAN_POINT('Ctrl Pts',(4.,0.0647475081636451,4.53274519105122));
#29136=CARTESIAN_POINT('Ctrl Pts',(4.,0.0709442475001029,4.53399310299165));
#29137=CARTESIAN_POINT('Ctrl Pts',(4.,0.0771669940275102,4.53512789739638));
#29138=CARTESIAN_POINT('Ctrl Pts',(4.,0.0834037601527001,4.53614909266968));
#29139=CARTESIAN_POINT('Ctrl Pts',(4.,0.108500755516298,4.54025842313435));
#29140=CARTESIAN_POINT('Ctrl Pts',(4.,0.133859781029961,4.54253781872753));
#29141=CARTESIAN_POINT('Ctrl Pts',(3.99999999999999,0.159256593756596,4.54305292380224));
#29142=CARTESIAN_POINT('Ctrl Pts',(3.99999999999999,0.185497795908202,4.5435851550133));
#29143=CARTESIAN_POINT('Ctrl Pts',(3.99999999999998,0.211780221987087,4.54223483664603));
#29144=CARTESIAN_POINT('Ctrl Pts',(3.99999999999998,0.237902321580844,4.5390442708621));
#29145=CARTESIAN_POINT('Ctrl Pts',(3.99999999999998,0.243507595489062,4.53835964001621));
#29146=CARTESIAN_POINT('Ctrl Pts',(3.99999999999998,0.249105619801251,4.53759013757336));
#29147=CARTESIAN_POINT('Ctrl Pts',(3.99999999999998,0.254694598474614,4.53673594206822));
#29148=CARTESIAN_POINT('',(4.,-0.219892372743086,3.64701365460628));
#29149=CARTESIAN_POINT('Ctrl Pts',(4.,0.254721014554616,3.46322028700966));
#29150=CARTESIAN_POINT('Ctrl Pts',(4.,0.254552373521139,3.46319452321125));
#29151=CARTESIAN_POINT('Ctrl Pts',(4.,0.254383724765285,3.46316883668624));
#29152=CARTESIAN_POINT('Ctrl Pts',(4.,0.254215068323085,3.46314322746093));
#29153=CARTESIAN_POINT('Ctrl Pts',(4.,0.228435861761457,3.4592288468388));
#29154=CARTESIAN_POINT('Ctrl Pts',(4.,0.202474691352968,3.45711700011808));
#29155=CARTESIAN_POINT('Ctrl Pts',(4.,0.176517231963435,3.45683380906617));
#29156=CARTESIAN_POINT('Ctrl Pts',(4.,0.151199179447316,3.45655759382427));
#29157=CARTESIAN_POINT('Ctrl Pts',(4.,0.125883695414598,3.45802192769867));
#29158=CARTESIAN_POINT('Ctrl Pts',(4.,0.1007794950383,3.46128259448669));
#29159=CARTESIAN_POINT('Ctrl Pts',(4.,0.0854593772715275,3.46327245269535));
#29160=CARTESIAN_POINT('Ctrl Pts',(4.,0.0702187270328167,3.46593187194604));
#29161=CARTESIAN_POINT('Ctrl Pts',(4.,0.0551140352340102,3.4692772918897));
#29162=CARTESIAN_POINT('Ctrl Pts',(4.,0.0468842919617017,3.47110003330284));
#29163=CARTESIAN_POINT('Ctrl Pts',(4.,0.0386923719445779,3.47312744960567));
#29164=CARTESIAN_POINT('Ctrl Pts',(4.,0.0305707631998946,3.47535548770785));
#29165=CARTESIAN_POINT('Ctrl Pts',(4.,0.0102648423897012,3.48092610391051));
#29166=CARTESIAN_POINT('Ctrl Pts',(4.,-0.00963556638195036,3.48775588581666));
#29167=CARTESIAN_POINT('Ctrl Pts',(4.,-0.0289965775380143,3.49587186612014));
#29168=CARTESIAN_POINT('Ctrl Pts',(4.,-0.047965755796229,3.50382359322137));
#29169=CARTESIAN_POINT('Ctrl Pts',(4.,-0.0664174073931304,3.51301096346156));
#29170=CARTESIAN_POINT('Ctrl Pts',(4.,-0.0841982143338667,3.52340033683134));
#29171=CARTESIAN_POINT('Ctrl Pts',(4.,-0.0930898199841631,3.5285957259532));
#29172=CARTESIAN_POINT('Ctrl Pts',(4.,-0.101813128894432,3.53409169793663));
#29173=CARTESIAN_POINT('Ctrl Pts',(4.,-0.110345561972859,3.53988353361915));
#29174=CARTESIAN_POINT('Ctrl Pts',(4.,-0.11586100642067,3.5436274303089));
#29175=CARTESIAN_POINT('Ctrl Pts',(4.,-0.121288652521606,3.54748953413154));
#29176=CARTESIAN_POINT('Ctrl Pts',(4.,-0.126621987542688,3.55146681430013));
#29177=CARTESIAN_POINT('Ctrl Pts',(4.,-0.143297831161627,3.56390265451229));
#29178=CARTESIAN_POINT('Ctrl Pts',(4.,-0.159061930875806,3.57746928852925));
#29179=CARTESIAN_POINT('Ctrl Pts',(4.,-0.173743808224101,3.59211536896244));
#29180=CARTESIAN_POINT('Ctrl Pts',(4.,-0.187864697165731,3.60620182877415));
#29181=CARTESIAN_POINT('Ctrl Pts',(4.,-0.200984288190684,3.62128798311348));
#29182=CARTESIAN_POINT('Ctrl Pts',(4.,-0.212904831975564,3.63731335989365));
#29183=CARTESIAN_POINT('Ctrl Pts',(4.,-0.21528245268753,3.64050971304978));
#29184=CARTESIAN_POINT('Ctrl Pts',(4.,-0.217612227418936,3.64374335030505));
#29185=CARTESIAN_POINT('Ctrl Pts',(4.,-0.219892372743211,3.64701365460636));
#29186=CARTESIAN_POINT('Origin',(4.,0.,4.));
#29187=CARTESIAN_POINT('Origin',(2.,0.,4.));
#29188=CARTESIAN_POINT('',(2.,-7.34788079488412E-17,4.6));
#29189=CARTESIAN_POINT('',(2.,-7.34788079488412E-17,4.6));
#29190=CARTESIAN_POINT('Origin',(2.,0.,4.));
#29191=CARTESIAN_POINT('Origin',(2.,0.,4.));
#29192=CARTESIAN_POINT('Ctrl Pts',(3.95224475517895,0.178288362465424,4.37571967666652));
#29193=CARTESIAN_POINT('Ctrl Pts',(3.96019739452275,0.115708609995841,4.40541533085819));
#29194=CARTESIAN_POINT('Ctrl Pts',(3.97610267321037,-0.0245105356436035,
4.43290545314371));
#29195=CARTESIAN_POINT('Ctrl Pts',(3.99996059124178,-0.228962993402626,
4.36819499612132));
#29196=CARTESIAN_POINT('Ctrl Pts',(4.0238185092732,-0.377374743411151,4.21349068386271));
#29197=CARTESIAN_POINT('Ctrl Pts',(4.04767642730463,-0.433534992178268,
4.00656196868444));
#29198=CARTESIAN_POINT('Ctrl Pts',(4.07153434533603,-0.383670022685343,
3.79803920418254));
#29199=CARTESIAN_POINT('Ctrl Pts',(4.09539226336747,-0.239994733226421,
3.63889579340969));
#29200=CARTESIAN_POINT('Ctrl Pts',(4.11925018139887,-0.0376302499649443,
3.56805514133307));
#29201=CARTESIAN_POINT('Ctrl Pts',(4.1431080994303,0.173933765839147,3.60283521426327));
#29202=CARTESIAN_POINT('Ctrl Pts',(4.16696601746172,0.342967344134064,3.73473372141871));
#29203=CARTESIAN_POINT('Ctrl Pts',(4.19082393549313,0.428135478754777,3.93149662217858));
#29204=CARTESIAN_POINT('Ctrl Pts',(4.21468185352456,0.40861313688017,4.1450106963618));
#29205=CARTESIAN_POINT('Ctrl Pts',(4.23853977155597,0.289173588337559,4.32306558264197));
#29206=CARTESIAN_POINT('Ctrl Pts',(4.2623976895874,0.0990233075312312,4.42212219878201));
#29207=CARTESIAN_POINT('Ctrl Pts',(4.28625560761881,-0.115340915390822,
4.41795840454656));
#29208=CARTESIAN_POINT('Ctrl Pts',(4.31011352565024,-0.301501118270308,
4.3115924136571));
#29209=CARTESIAN_POINT('Ctrl Pts',(4.33397144368164,-0.413936097932681,
4.12903358037428));
#29210=CARTESIAN_POINT('Ctrl Pts',(4.35782936171308,-0.425152419412173,
3.91492252699502));
#29211=CARTESIAN_POINT('Ctrl Pts',(4.38168727974448,-0.332407397051365,
3.72161523052345));
#29212=CARTESIAN_POINT('Ctrl Pts',(4.40554519777592,-0.158379709595794,
3.5963805946708));
#29213=CARTESIAN_POINT('Ctrl Pts',(4.42940311580732,0.0543761300157755,
3.56984189703405));
#29214=CARTESIAN_POINT('Ctrl Pts',(4.45326103383876,0.25383552520097,3.64848857324589));
#29215=CARTESIAN_POINT('Ctrl Pts',(4.47711895187016,0.39122521984844,3.81308936806525));
#29216=CARTESIAN_POINT('Ctrl Pts',(4.50097686990159,0.432949691632991,4.02339490384879));
#29217=CARTESIAN_POINT('Ctrl Pts',(4.524834787933,0.368806170420464,4.22797974831721));
#29218=CARTESIAN_POINT('Ctrl Pts',(4.54869270596443,0.214479494504121,4.37681733431002));
#29219=CARTESIAN_POINT('Ctrl Pts',(4.57255062399584,0.00770673985495463,
4.4335128177492));
#29220=CARTESIAN_POINT('Ctrl Pts',(4.59640854202726,-0.200950522604244,
4.38420260860549));
#29221=CARTESIAN_POINT('Ctrl Pts',(4.62026646005868,-0.360469908510665,
4.24094439618412));
#29222=CARTESIAN_POINT('Ctrl Pts',(4.6441243780901,-0.431844582779732,4.03876871570463));
#29223=CARTESIAN_POINT('Ctrl Pts',(4.66798229612152,-0.397621493350665,
3.82711302819544));
#29224=CARTESIAN_POINT('Ctrl Pts',(4.69184021415294,-0.266169117804412,
3.65773291463971));
#29225=CARTESIAN_POINT('Ctrl Pts',(4.71569813218436,-0.0696311426542753,
3.57204642662242));
#29226=CARTESIAN_POINT('Ctrl Pts',(4.73955605021577,0.143933543589337,3.59100624451743));
#29227=CARTESIAN_POINT('Ctrl Pts',(4.76341396824719,0.322302557754209,3.70997617639404));
#29228=CARTESIAN_POINT('Ctrl Pts',(4.78727188627862,0.421859817202848,3.8998648332327));
#29229=CARTESIAN_POINT('Ctrl Pts',(4.81112980431003,0.41826086011465,4.11423926597311));
#29230=CARTESIAN_POINT('Ctrl Pts',(4.83498772234146,0.312385729531365,4.30067908636799));
#29231=CARTESIAN_POINT('Ctrl Pts',(4.85884564037287,0.130123778861223,4.41359467981201));
#29232=CARTESIAN_POINT('Ctrl Pts',(4.88270355840429,-0.0839569802410516,
4.42537510794913));
#29233=CARTESIAN_POINT('Ctrl Pts',(4.90656147643571,-0.277507970732168,
4.33313973520738));
#29234=CARTESIAN_POINT('Ctrl Pts',(4.93041939446713,-0.403200703213916,
4.15944262266324));
#29235=CARTESIAN_POINT('Ctrl Pts',(4.95427731249855,-0.430299880793222,
3.94675744574809));
#29236=CARTESIAN_POINT('Ctrl Pts',(4.97813523052996,-0.352179016385168,
3.7470915236456));
#29237=CARTESIAN_POINT('Ctrl Pts',(5.00199314856139,-0.187940789307144,
3.60926861310034));
#29238=CARTESIAN_POINT('Ctrl Pts',(5.0258510665928,0.0222540801607904,3.56699016996131));
#29239=CARTESIAN_POINT('Ctrl Pts',(5.04970898462423,0.227007220840439,3.63059442521772));
#29240=CARTESIAN_POINT('Ctrl Pts',(5.07356690265564,0.376250912472057,3.7845284059142));
#29241=CARTESIAN_POINT('Ctrl Pts',(5.09742482068706,0.433491007135177,3.99115106069306));
#29242=CARTESIAN_POINT('Ctrl Pts',(5.12128273871848,0.384730742495793,4.19993752217271));
#29243=CARTESIAN_POINT('Ctrl Pts',(5.1451406567499,0.241893331461176,4.35983381329239));
#29244=CARTESIAN_POINT('Ctrl Pts',(5.16899857478132,0.0399064118422473,
4.43174093538579));
#29245=CARTESIAN_POINT('Ctrl Pts',(5.19285649281273,-0.171838712500945,
4.39807563839043));
#29246=CARTESIAN_POINT('Ctrl Pts',(5.21671441084416,-0.341564590845109,
4.26707000444592));
#29247=CARTESIAN_POINT('Ctrl Pts',(5.24057232887557,-0.427768622694993,
4.07075847957352));
#29248=CARTESIAN_POINT('Ctrl Pts',(5.264430246907,-0.409371574112622,3.85714457902312));
#29249=CARTESIAN_POINT('Ctrl Pts',(5.2882881649384,-0.290872024601924,3.6784627202051));
#29250=CARTESIAN_POINT('Ctrl Pts',(5.31214608296984,-0.101246341881189,
3.57840548479658));
#29251=CARTESIAN_POINT('Ctrl Pts',(5.33600400100125,0.113136829324483,3.58143959235932));
#29252=CARTESIAN_POINT('Ctrl Pts',(5.35986191903268,0.299854963974951,3.68682312094679));
#29253=CARTESIAN_POINT('Ctrl Pts',(5.38371983706408,0.413250392048343,3.8687869272297));
#29254=CARTESIAN_POINT('Ctrl Pts',(5.40757775509551,0.425594842551202,4.08283590397723));
#29255=CARTESIAN_POINT('Ctrl Pts',(5.43143567312693,0.333869761079625,4.27662924579771));
#29256=CARTESIAN_POINT('Ctrl Pts',(5.45529359115834,0.160504428594232,4.4027792017911));
#29257=CARTESIAN_POINT('Ctrl Pts',(5.47915150918977,-0.0521086087350157,
4.43043867146175));
#29258=CARTESIAN_POINT('Ctrl Pts',(5.50300942722118,-0.251979671819092,
4.35284416104532));
#29259=CARTESIAN_POINT('Ctrl Pts',(5.52686734525261,-0.390234841353927,
4.18896964197264));
#29260=CARTESIAN_POINT('Ctrl Pts',(5.55072526328402,-0.433066962396004,
3.97888689800548));
#29261=CARTESIAN_POINT('Ctrl Pts',(5.57458318131544,-0.370002414621403,
3.77396688259));
#29262=CARTESIAN_POINT('Ctrl Pts',(5.59844109934686,-0.21646219781534,3.62431812139094));
#29263=CARTESIAN_POINT('Ctrl Pts',(5.62229901737828,-0.00999107731853999,
3.56653381289738));
#29264=CARTESIAN_POINT('Ctrl Pts',(5.64615693540971,0.198923133709572,3.61474379450078));
#29265=CARTESIAN_POINT('Ctrl Pts',(5.67001485344111,0.359195220034686,3.75715941257656));
#29266=CARTESIAN_POINT('Ctrl Pts',(5.69387277147254,0.431634290692432,3.95895616900985));
#29267=CARTESIAN_POINT('Ctrl Pts',(5.71773068950395,0.398527019959163,4.1707892603438));
#29268=CARTESIAN_POINT('Ctrl Pts',(5.74158860753538,0.267969036875697,4.34085972491723));
#29269=CARTESIAN_POINT('Ctrl Pts',(5.76544652556679,0.0718853255354575,
4.42758070267197));
#29270=CARTESIAN_POINT('Ctrl Pts',(5.78930444359821,-0.141776307127955,
4.40974655013133));
#29271=CARTESIAN_POINT('Ctrl Pts',(5.81316236162963,-0.320769768688322,
4.29171820750724));
#29272=CARTESIAN_POINT('Ctrl Pts',(5.83702027966105,-0.421326288178809,
4.10235681181338));
#29273=CARTESIAN_POINT('Ctrl Pts',(5.86087819769247,-0.418857046020503,
3.88796639709818));
#29274=CARTESIAN_POINT('Ctrl Pts',(5.88473611572389,-0.313965860818636,
3.70097123187977));
#29275=CARTESIAN_POINT('Ctrl Pts',(5.90859403375531,-0.132301443679057,
3.58709678011166));
#29276=CARTESIAN_POINT('Ctrl Pts',(5.93245195178673,0.0817142298265842,
3.57418834816524));
#29277=CARTESIAN_POINT('Ctrl Pts',(5.95630986981814,0.275748643515392,3.66540258613358));
#29278=CARTESIAN_POINT('Ctrl Pts',(5.98016778784957,0.402354822815078,3.83843477537114));
#29279=CARTESIAN_POINT('Ctrl Pts',(6.00402570588098,0.430574627524036,4.05097449853386));
#29280=CARTESIAN_POINT('Ctrl Pts',(6.02788362391241,0.353506566116634,4.25104874587108));
#29281=CARTESIAN_POINT('Ctrl Pts',(6.05174154194382,0.189997730437525,4.38973628930191));
#29282=CARTESIAN_POINT('Ctrl Pts',(6.07559945997525,-0.0199730113800777,
4.43311976162365));
#29283=CARTESIAN_POINT('Ctrl Pts',(6.09945737800665,-0.2250554921608,4.3705991908187));
#29284=CARTESIAN_POINT('Ctrl Pts',(6.12331529603809,-0.375113923638194,
4.21744656883549));
#29285=CARTESIAN_POINT('Ctrl Pts',(6.1471732140695,-0.433431396087355,4.01114207710762));
#29286=CARTESIAN_POINT('Ctrl Pts',(6.17103113210093,-0.385792139046387,
3.80207577201042));
#29287=CARTESIAN_POINT('Ctrl Pts',(6.19488905013233,-0.243761337718234,
3.64147770828707));
#29288=CARTESIAN_POINT('Ctrl Pts',(6.21874696816376,-0.042227823444436,
3.56841523311022));
#29289=CARTESIAN_POINT('Ctrl Pts',(6.24260488619517,0.16982704650124,3.60113783246665));
#29290=CARTESIAN_POINT('Ctrl Pts',(6.2664628042266,0.339985970990829,3.73091992247201));
#29291=CARTESIAN_POINT('Ctrl Pts',(6.29032072225801,0.427700638223926,3.92738904240251));
#29292=CARTESIAN_POINT('Ctrl Pts',(6.31417864028943,0.409561128158778,4.13996490148311));
#29293=CARTESIAN_POINT('Ctrl Pts',(6.34598919766466,0.254661277208374,4.38159318714805));
#29294=CARTESIAN_POINT('Ctrl Pts',(6.38575239438369,-0.125272905304917,
4.47558432627151));
#29295=CARTESIAN_POINT('Ctrl Pts',(6.43346823044653,-0.468271923807345,
4.15124960425567));
#29296=CARTESIAN_POINT('Ctrl Pts',(6.48118406650937,-0.380227249479543,
3.6882349865083));
#29297=CARTESIAN_POINT('Ctrl Pts',(6.52889990257221,0.0564566449812287,
3.51140415777354));
#29298=CARTESIAN_POINT('Ctrl Pts',(6.57661573863504,0.441574375138847,3.78331933667001));
#29299=CARTESIAN_POINT('Ctrl Pts',(6.62433157469789,0.421040068198854,4.25418342072721));
#29300=CARTESIAN_POINT('Ctrl Pts',(6.67204741076071,0.0139362792425842,
4.49164405688148));
#29301=CARTESIAN_POINT('Ctrl Pts',(6.71976324682356,-0.406006764042365,
4.27761133505345));
#29302=CARTESIAN_POINT('Ctrl Pts',(6.76747908288639,-0.453085647428837,
3.80864864857145));
#29303=CARTESIAN_POINT('Ctrl Pts',(6.81519491894923,-0.0841006081168706,
3.51540431248109));
#29304=CARTESIAN_POINT('Ctrl Pts',(6.86291075501207,0.362121456530253,3.66717299786736));
#29305=CARTESIAN_POINT('Ctrl Pts',(6.91062659107491,0.475798562415156,4.124581128109));
#29306=CARTESIAN_POINT('Ctrl Pts',(6.95834242713775,0.152544250279933,4.46758486877347));
#29307=CARTESIAN_POINT('Ctrl Pts',(7.00605826320058,-0.310794706562241,
4.38119802990972));
#29308=CARTESIAN_POINT('Ctrl Pts',(7.05377409926342,-0.488725618924084,
3.94475128051735));
#29309=CARTESIAN_POINT('Ctrl Pts',(7.10148993532626,-0.21785253135038,3.55904022429238));
#29310=CARTESIAN_POINT('Ctrl Pts',(7.14920577138909,0.253078023397415,3.57826934481931));
#29311=CARTESIAN_POINT('Ctrl Pts',(7.19692160745195,0.491603063369337,3.98478019943955));
#29312=CARTESIAN_POINT('Ctrl Pts',(7.24463744351477,0.278681483980911,4.40526763942622));
#29313=CARTESIAN_POINT('Ctrl Pts',(7.29235327957762,-0.190157610347023,
4.45359156587464));
#29314=CARTESIAN_POINT('Ctrl Pts',(7.34006911564044,-0.484372034479295,
4.08537538031203));
#29315=CARTESIAN_POINT('Ctrl Pts',(7.3877849517033,-0.333780171974684,3.63875766810317));
#29316=CARTESIAN_POINT('Ctrl Pts',(7.43550078776612,0.123327161313159,3.52387434835784));
#29317=CARTESIAN_POINT('Ctrl Pts',(7.48321662382897,0.467181263150904,3.84622454030349));
#29318=CARTESIAN_POINT('Ctrl Pts',(7.5309324598918,0.382015623368301,4.30978910321172));
#29319=CARTESIAN_POINT('Ctrl Pts',(7.57864829595465,-0.0539608418635878,
4.4888695658253));
#29320=CARTESIAN_POINT('Ctrl Pts',(7.62636413201748,-0.440384235482588,
4.21901358396786));
#29321=CARTESIAN_POINT('Ctrl Pts',(7.67407996808031,-0.422396009600076,
3.7480340579683));
#29322=CARTESIAN_POINT('Ctrl Pts',(7.72179580414317,-0.0165150286377962,
3.50843873354525));
#29323=CARTESIAN_POINT('Ctrl Pts',(7.76951164020598,0.404531957204003,3.72025168374225));
#29324=CARTESIAN_POINT('Ctrl Pts',(7.81722747626884,0.454091022239626,4.18896181724392));
#29325=CARTESIAN_POINT('Ctrl Pts',(7.86494331233166,0.0866513144543145,
4.48414540641706));
#29326=CARTESIAN_POINT('Ctrl Pts',(7.91265914839452,-0.360361628691054,
4.33473081934393));
#29327=CARTESIAN_POINT('Ctrl Pts',(7.96037498445733,-0.476448943335793,
3.87792777037096));
#29328=CARTESIAN_POINT('Ctrl Pts',(8.0080908205202,-0.1550058622045,3.53322552818936));
#29329=CARTESIAN_POINT('Ctrl Pts',(8.05580665658301,0.308781487260178,3.61716946571973));
#29330=CARTESIAN_POINT('Ctrl Pts',(8.10352249264587,0.489010045760349,4.0526725734847));
#29331=CARTESIAN_POINT('Ctrl Pts',(8.1512383287087,0.220173154851853,4.43980564654689));
#29332=CARTESIAN_POINT('Ctrl Pts',(8.19895416477154,-0.250852131956433,
4.4230584271054));
#29333=CARTESIAN_POINT('Ctrl Pts',(8.24667000083438,-0.491516046133,4.01781014446235));
#29334=CARTESIAN_POINT('Ctrl Pts',(8.29438583689722,-0.280813212199106,
3.59620653211525));
#29335=CARTESIAN_POINT('Ctrl Pts',(8.34210167296004,0.187764715363875,3.54541267448783));
#29336=CARTESIAN_POINT('Ctrl Pts',(8.38981750902289,0.483915415676709,3.91207335260334));
#29337=CARTESIAN_POINT('Ctrl Pts',(8.43753334508573,0.335679143777854,4.35947842394856));
#29338=CARTESIAN_POINT('Ctrl Pts',(8.48524918114857,-0.120816450939738,
4.4767689272953));
#29339=CARTESIAN_POINT('Ctrl Pts',(8.5329650172114,-0.466364439759318,4.15623518867385));
#29340=CARTESIAN_POINT('Ctrl Pts',(8.58068085327425,-0.383642787608637,
3.69222827230584));
#29341=CARTESIAN_POINT('Ctrl Pts',(8.62839668933707,0.0513839395061145,
3.51085286915611));
#29342=CARTESIAN_POINT('Ctrl Pts',(8.67611252539993,0.439224004328866,3.77866880275638));
#29343=CARTESIAN_POINT('Ctrl Pts',(8.72382836146275,0.42371790764641,4.24973658040369));
#29344=CARTESIAN_POINT('Ctrl Pts',(8.7715441975256,0.0191051366342138,4.49146741357506));
#29345=CARTESIAN_POINT('Ctrl Pts',(8.81926003358843,-0.403052175319494,
4.28187615866228));
#29346=CARTESIAN_POINT('Ctrl Pts',(8.86697586965126,-0.455080472922433,
3.81343369002772));
#29347=CARTESIAN_POINT('Ctrl Pts',(8.91469170571412,-0.0892013699275644,
3.51631793453238));
#29348=CARTESIAN_POINT('Ctrl Pts',(8.96240754177693,0.358592723611288,3.66337486216116));
#29349=CARTESIAN_POINT('Ctrl Pts',(9.0101233778398,0.477085601399612,4.11955983351088));
#29350=CARTESIAN_POINT('Ctrl Pts',(9.05783921390261,0.157463430517111,4.46595117008304));
#29351=CARTESIAN_POINT('Ctrl Pts',(9.10555504996547,-0.306759831495564,
4.38445237758765));
#29352=CARTESIAN_POINT('Ctrl Pts',(9.1532708860283,-0.489280820139143,3.94990505119329));
#29353=CARTESIAN_POINT('Ctrl Pts',(9.20098672209113,-0.222487703095825,
3.56136068709803));
#29354=CARTESIAN_POINT('Ctrl Pts',(9.24870255815399,0.248619295113741,3.57562555337399));
#29355=CARTESIAN_POINT('Ctrl Pts',(9.29641839421681,0.49141536912078,3.97960000382683));
#29356=CARTESIAN_POINT('Ctrl Pts',(9.34413423027966,0.282937148266828,4.40230808465976));
#29357=CARTESIAN_POINT('Ctrl Pts',(9.39185006634249,-0.185366609388173,
4.45557046104408));
#29358=CARTESIAN_POINT('Ctrl Pts',(9.43956590240532,-0.483445357410111,
4.09047547319903));
#29359=CARTESIAN_POINT('Ctrl Pts',(9.48728173846818,-0.337568794959357,
3.64229546617122));
#29360=CARTESIAN_POINT('Ctrl Pts',(9.53499757453099,0.118302386066128,3.5226010365501));
#29361=CARTESIAN_POINT('Ctrl Pts',(9.58271341059386,0.465534665650901,3.84130942079228));
#29362=CARTESIAN_POINT('Ctrl Pts',(9.63042924665667,0.385259298596883,4.30574580568933));
#29363=CARTESIAN_POINT('Ctrl Pts',(9.67814508271952,-0.0488056103349303,
4.48941111271794));
#29364=CARTESIAN_POINT('Ctrl Pts',(9.72586091878235,-0.438051576325333,
4.22364266437974));
#29365=CARTESIAN_POINT('Ctrl Pts',(9.77357675484519,-0.425028039486299,
3.75249971615691));
#29366=CARTESIAN_POINT('Ctrl Pts',(9.82129259090803,-0.0216947140899849,
3.50864008686857));
#29367=CARTESIAN_POINT('Ctrl Pts',(9.86900842697087,0.401561201071248,3.7160038263529));
#29368=CARTESIAN_POINT('Ctrl Pts',(9.91672426303371,0.456057286475463,4.18416562194019));
#29369=CARTESIAN_POINT('Ctrl Pts',(9.96444009909655,0.0917489483659128,
4.48320529314746));
#29370=CARTESIAN_POINT('Ctrl Pts',(10.0121559351594,-0.356813860767086,
4.3385101085883));
#29371=CARTESIAN_POINT('Ctrl Pts',(10.0598717712222,-0.477709011270712,
3.88295588266498));
#29372=CARTESIAN_POINT('Ctrl Pts',(10.1075876072851,-0.159916626226494,
3.53488507064564));
#29373=CARTESIAN_POINT('Ctrl Pts',(10.1553034433479,0.304729657315094,3.61393645496551));
#29374=CARTESIAN_POINT('Ctrl Pts',(10.2030192794107,0.489538007675758,4.04751593304174));
#29375=CARTESIAN_POINT('Ctrl Pts',(10.2507351154736,0.224796073077312,4.43746079867915));
#29376=CARTESIAN_POINT('Ctrl Pts',(10.2984509515364,-0.246379554360218,
4.42567868168988));
#29377=CARTESIAN_POINT('Ctrl Pts',(10.3461667875993,-0.491301045992024,
4.02298928139638));
#29378=CARTESIAN_POINT('Ctrl Pts',(10.3938826236621,-0.285053227451061,
3.599188470261));
#29379=CARTESIAN_POINT('Ctrl Pts',(10.4415984597249,0.182963355965895,3.54345905416307));
#29380=CARTESIAN_POINT('Ctrl Pts',(10.4893142957878,0.482961874346273,3.9069782134126));
#29381=CARTESIAN_POINT('Ctrl Pts',(10.5370301318506,0.339449072190825,4.35592071060949));
#29382=CARTESIAN_POINT('Ctrl Pts',(10.5847459679134,-0.115785036052801,
4.47801574270962));
#29383=CARTESIAN_POINT('Ctrl Pts',(10.6324618039763,-0.464691964107356,
4.16114156306187));
#29384=CARTESIAN_POINT('Ctrl Pts',(10.6801776400391,-0.386865111317189,
3.69628860657276));
#29385=CARTESIAN_POINT('Ctrl Pts',(10.7278934761019,0.0462259258804368,
3.51033849586834));
#29386=CARTESIAN_POINT('Ctrl Pts',(10.7756093121648,0.436866984064762,3.77405207881873));
#29387=CARTESIAN_POINT('Ctrl Pts',(10.8233251482276,0.426326368719826,4.24525711444552));
#29388=CARTESIAN_POINT('Ctrl Pts',(10.8710409842905,0.0242836891050981,
4.49123876811122));
#29389=CARTESIAN_POINT('Ctrl Pts',(10.9187568203533,-0.400059075867425,
4.28610830234036));
#29390=CARTESIAN_POINT('Ctrl Pts',(10.9664726564161,-0.45702143577077,3.81824018018824));
#29391=CARTESIAN_POINT('Ctrl Pts',(11.014188492479,-0.0942939790271268,
3.51728489730359));
#29392=CARTESIAN_POINT('Ctrl Pts',(11.0619043285418,0.355025089556487,3.65961432075161));
#29393=CARTESIAN_POINT('Ctrl Pts',(11.1096201646047,0.478319155637209,4.11452515096033));
#29394=CARTESIAN_POINT('Ctrl Pts',(11.1573360006675,0.16236538121005,4.46426577284621));
#29395=CARTESIAN_POINT('Ctrl Pts',(11.2050518367304,-0.302691021094817,
4.38766399188028));
#29396=CARTESIAN_POINT('Ctrl Pts',(11.2527676727932,-0.489781601228288,
3.95506440219344));
#29397=CARTESIAN_POINT('Ctrl Pts',(11.300483508856,-0.227098200695192,3.56372986339542));
#29398=CARTESIAN_POINT('Ctrl Pts',(11.3481993449188,0.244132971891272,3.57302890392028));
#29399=CARTESIAN_POINT('Ctrl Pts',(11.3959151809817,0.491173079921361,3.97442207176994));
#29400=CARTESIAN_POINT('Ctrl Pts',(11.4436310170445,0.287161390990383,4.39930384468027));
#29401=CARTESIAN_POINT('Ctrl Pts',(11.4913468531074,-0.180555021833016,
4.45749875294131));
#29402=CARTESIAN_POINT('Ctrl Pts',(11.5390626891702,-0.482464979911041,
4.09556551685319));
#29403=CARTESIAN_POINT('Ctrl Pts',(11.586778525233,-0.341319923258817,3.64587299617429));
#29404=CARTESIAN_POINT('Ctrl Pts',(11.6344943612959,0.113264470804062,3.5213807520529));
#29405=CARTESIAN_POINT('Ctrl Pts',(11.6822101973587,0.463836358529674,3.83641192782507));
#29406=CARTESIAN_POINT('Ctrl Pts',(11.7299260334216,0.38846018117773,4.30166854740152));
#29407=CARTESIAN_POINT('Ctrl Pts',(11.7776418694844,-0.0436449577779122,
4.48989829813191));
#29408=CARTESIAN_POINT('Ctrl Pts',(11.8253577055472,-0.435670260442099,
4.22824690363353));
#29409=CARTESIAN_POINT('Ctrl Pts',(11.8730735416101,-0.427612859293677,
3.75699286549843));
#29410=CARTESIAN_POINT('Ctrl Pts',(11.9207893776729,-0.0268719897862959,
3.50889601812151));
#29411=CARTESIAN_POINT('Ctrl Pts',(11.9685052137357,0.398545841420554,3.71178751390968));
#29412=CARTESIAN_POINT('Ctrl Pts',(12.0162210497986,0.457972894034889,4.17934897039372));
#29413=CARTESIAN_POINT('Ctrl Pts',(12.0639368858614,0.0968363912382316,
4.48221150772657));
#29414=CARTESIAN_POINT('Ctrl Pts',(12.1116527219243,-0.353226459651896,
4.34225179773635));
#29415=CARTESIAN_POINT('Ctrl Pts',(12.1593685579871,-0.478916017555994,
3.88799699566402));
#29416=CARTESIAN_POINT('Ctrl Pts',(12.2070843940499,-0.164809627468288,
3.53659627586117));
#29417=CARTESIAN_POINT('Ctrl Pts',(12.2548002301128,0.300643979445627,3.61074632631782));
#29418=CARTESIAN_POINT('Ctrl Pts',(12.3025160661756,0.490011594032383,4.04235401475446));
#29419=CARTESIAN_POINT('Ctrl Pts',(12.3502319022385,0.229394022021679,4.43506735974179));
#29420=CARTESIAN_POINT('Ctrl Pts',(12.3979477383013,-0.241879610092261,
4.42825165390643));
#29421=CARTESIAN_POINT('Ctrl Pts',(12.4456635743641,-0.491031474462283,
4.0281658647901));
#29422=CARTESIAN_POINT('Ctrl Pts',(12.493379410427,-0.289261580343189,3.60221492864948));
#29423=CARTESIAN_POINT('Ctrl Pts',(12.5410952464898,0.178141673866572,3.54155614424011));
#29424=CARTESIAN_POINT('Ctrl Pts',(12.5888110825527,0.481954687902679,3.90189340664049));
#29425=CARTESIAN_POINT('Ctrl Pts',(12.6365269186155,0.343181296211668,4.35232346328687));
#29426=CARTESIAN_POINT('Ctrl Pts',(12.6842427546783,-0.110740760313508,
4.47920946240362));
#29427=CARTESIAN_POINT('Ctrl Pts',(12.7319585907412,-0.462967872677167,
4.16603003860975));
#29428=CARTESIAN_POINT('Ctrl Pts',(12.779674426804,-0.390044463885,3.70038267566003));
#29429=CARTESIAN_POINT('Ctrl Pts',(12.8273902628668,0.0410627776982723,
3.50987851185683));
#29430=CARTESIAN_POINT('Ctrl Pts',(12.8751060989297,0.434461438689172,3.76946045210395));
#29431=CARTESIAN_POINT('Ctrl Pts',(12.9228219349925,0.42888747548329,4.24075040649094));
#29432=CARTESIAN_POINT('Ctrl Pts',(12.9705377710553,0.0294595442590321,
4.49095555817611));
#29433=CARTESIAN_POINT('Ctrl Pts',(13.0182536071182,-0.397021539751646,
4.29030866646591));
#29434=CARTESIAN_POINT('Ctrl Pts',(13.065969443181,-0.458911634846768,3.82306685936703));
#29435=CARTESIAN_POINT('Ctrl Pts',(13.1136852792439,-0.0993761143989603,
3.51830547777773));
#29436=CARTESIAN_POINT('Ctrl Pts',(13.1614011153067,0.351418020999476,3.65589158776806));
#29437=CARTESIAN_POINT('Ctrl Pts',(13.2091169513695,0.479499580452807,4.10947774749948));
#29438=CARTESIAN_POINT('Ctrl Pts',(13.2568327874324,0.167249297126924,4.46252880717046));
#29439=CARTESIAN_POINT('Ctrl Pts',(13.3045486234952,-0.298588589211839,
4.39083254629632));
#29440=CARTESIAN_POINT('Ctrl Pts',(13.352264459558,-0.490227979701372,3.96022874442655));
#29441=CARTESIAN_POINT('Ctrl Pts',(13.3999802956209,-0.23168347330409,3.56614749850931));
#29442=CARTESIAN_POINT('Ctrl Pts',(13.4476961316837,0.239619531536799,3.57047968038978));
#29443=CARTESIAN_POINT('Ctrl Pts',(13.4954119677466,0.490876233547033,3.96924698078795));
#29444=CARTESIAN_POINT('Ctrl Pts',(13.5431278038094,0.291353737189313,4.39625525192456));
#29445=CARTESIAN_POINT('Ctrl Pts',(13.5908436398722,-0.175723379082843,
4.45937622804808));
#29446=CARTESIAN_POINT('Ctrl Pts',(13.6385594759351,-0.481431012491488,
4.10064494554323));
#29447=CARTESIAN_POINT('Ctrl Pts',(13.6862753119979,-0.345033139360895,
3.64948986092447));
#29448=CARTESIAN_POINT('Ctrl Pts',(13.7339911480608,0.108213974662067,3.52021363031051));
#29449=CARTESIAN_POINT('Ctrl Pts',(13.7817069841236,0.462086530666827,3.83153260544464));
#29450=CARTESIAN_POINT('Ctrl Pts',(13.8294228201864,0.391617915445045,4.297557781203));
#29451=CARTESIAN_POINT('Ctrl Pts',(13.8771386562493,-0.0384794573460961,
4.49033106796769));
#29452=CARTESIAN_POINT('Ctrl Pts',(13.9248544923121,-0.433240552373761,
4.23282579030437));
#29453=CARTESIAN_POINT('Ctrl Pts',(13.9725703283749,-0.430150181893835,
3.76151300691929));
#29454=CARTESIAN_POINT('Ctrl Pts',(14.0202861644378,-0.032046280669499,
3.50920649887429));
#29455=CARTESIAN_POINT('Ctrl Pts',(14.0680020005006,0.39548621318905,3.70760321474174));
#29456=CARTESIAN_POINT('Ctrl Pts',(14.1157178365634,0.459837632138507,4.1745123976147));
#29457=CARTESIAN_POINT('Ctrl Pts',(14.1634336726263,0.101913077983734,4.48116416053968));
#29458=CARTESIAN_POINT('Ctrl Pts',(14.2111495086891,-0.349599823817769,
4.34595547117883));
#29459=CARTESIAN_POINT('Ctrl Pts',(14.258865344752,-0.480069828122688,3.8930505494253));
#29460=CARTESIAN_POINT('Ctrl Pts',(14.3065811808148,-0.169684322438749,
3.53835895376334));
#29461=CARTESIAN_POINT('Ctrl Pts',(14.3542970168777,0.296524907469595,3.60759943412104));
#29462=CARTESIAN_POINT('Ctrl Pts',(14.4020128529405,0.49043075222644,4.0371873919842));
#29463=CARTESIAN_POINT('Ctrl Pts',(14.4497286890033,0.233966490966644,4.43262559558668));
#29464=CARTESIAN_POINT('Ctrl Pts',(14.4974445250662,-0.237352798985028,
4.43077705796148));
#29465=CARTESIAN_POINT('Ctrl Pts',(14.545160361129,-0.490707361486496,4.03333931965322));
#29466=CARTESIAN_POINT('Ctrl Pts',(14.5928761971918,-0.293437803431633,
3.60528557111603));
#29467=CARTESIAN_POINT('Ctrl Pts',(14.6405920332547,0.173300204635467,3.53970415608515));
#29468=CARTESIAN_POINT('Ctrl Pts',(14.6883078693175,0.480893968219416,3.89681949708321));
#29469=CARTESIAN_POINT('Ctrl Pts',(14.7360237053804,0.346875401282657,4.34868708154587));
#29470=CARTESIAN_POINT('Ctrl Pts',(14.7837395414432,-0.10568418401607,4.48034995378457));
#29471=CARTESIAN_POINT('Ctrl Pts',(14.831455377506,-0.461192356972643,4.17090007232882));
#29472=CARTESIAN_POINT('Ctrl Pts',(14.8791712135689,-0.393180492164677,
3.7045100248179));
#29473=CARTESIAN_POINT('Ctrl Pts',(14.9268870496317,0.0358950684576197,
3.50947296821438));
#29474=CARTESIAN_POINT('Ctrl Pts',(14.9746028856945,0.432007635398663,3.76489443262817));
#29475=CARTESIAN_POINT('Ctrl Pts',(15.0223187217574,0.431400943461215,4.23621695712364));
#29476=CARTESIAN_POINT('Ctrl Pts',(15.0700345578202,0.0346321271865876,
4.4906178152274));
#29477=CARTESIAN_POINT('Ctrl Pts',(15.1177503938831,-0.393939904367254,
4.2944767844824));
#29478=CARTESIAN_POINT('Ctrl Pts',(15.1654662299459,-0.46075086019608,3.82791319143947));
#29479=CARTESIAN_POINT('Ctrl Pts',(15.2131820660087,-0.104447211543591,
3.51937956259357));
#29480=CARTESIAN_POINT('Ctrl Pts',(15.2608979020716,0.347771918596306,3.652207076714));
#29481=CARTESIAN_POINT('Ctrl Pts',(15.3086137381344,0.480626744730421,4.10441818376995));
#29482=CARTESIAN_POINT('Ctrl Pts',(15.3563295741973,0.172114635785536,4.46074046598969));
#29483=CARTESIAN_POINT('Ctrl Pts',(15.4040454102601,-0.294452991525291,
4.39395768888776));
#29484=CARTESIAN_POINT('Ctrl Pts',(15.4517612463229,-0.490619905976795,
3.96539750426199));
#29485=CARTESIAN_POINT('Ctrl Pts',(15.4994770823858,-0.236243011612202,
3.56861332390027));
#29486=CARTESIAN_POINT('Ctrl Pts',(15.5471929184486,0.235079475381852,3.56797816593814));
#29487=CARTESIAN_POINT('Ctrl Pts',(15.5949087545115,0.490524862970081,3.9640753057054));
#29488=CARTESIAN_POINT('Ctrl Pts',(15.6426245905743,0.295513721197704,4.39316264501585));
#29489=CARTESIAN_POINT('Ctrl Pts',(15.6903404266371,-0.170872217813597,
4.46120267782338));
#29490=CARTESIAN_POINT('Ctrl Pts',(15.7380562626999,-0.480343569999647,
4.1057131950703));
#29491=CARTESIAN_POINT('Ctrl Pts',(15.7857720987628,-0.348708030819167,
3.6531456586776));
#29492=CARTESIAN_POINT('Ctrl Pts',(15.8334879348256,0.103151458625294,3.5190998009613));
#29493=CARTESIAN_POINT('Ctrl Pts',(15.8812037708885,0.460285376424935,3.82667199562295));
#29494=CARTESIAN_POINT('Ctrl Pts',(15.9289196069513,0.39473215065269,4.29341396369818));
#29495=CARTESIAN_POINT('Ctrl Pts',(15.9766354430142,-0.033309682798763,
4.49070937415524));
#29496=CARTESIAN_POINT('Ctrl Pts',(16.024351279077,-0.430762722000766,4.23737881579128));
#29497=CARTESIAN_POINT('Ctrl Pts',(16.0720671151398,-0.432639725453012,
3.76605963834362));
#29498=CARTESIAN_POINT('Ctrl Pts',(16.1197829512026,-0.0372170120039125,
3.50957149464017));
#29499=CARTESIAN_POINT('Ctrl Pts',(16.1674987872655,0.392382656225717,3.70345139362117));
#29500=CARTESIAN_POINT('Ctrl Pts',(16.2152146233283,0.461651293660056,4.16965644082667));
#29501=CARTESIAN_POINT('Ctrl Pts',(16.2629304593912,0.106978444708158,4.48006336792116));
#29502=CARTESIAN_POINT('Ctrl Pts',(16.310646295454,-0.345934356094203,4.34962071752925));
#29503=CARTESIAN_POINT('Ctrl Pts',(16.3583621315169,-0.481170314810987,
3.89811598262401));
#29504=CARTESIAN_POINT('Ctrl Pts',(16.4060779675797,-0.174540169679895,
3.54017290856226));
#29505=CARTESIAN_POINT('Ctrl Pts',(16.4537938036425,0.292372898913969,3.60449612791703));
#29506=CARTESIAN_POINT('Ctrl Pts',(16.5015096397054,0.490795435699827,4.0320166386149));
#29507=CARTESIAN_POINT('Ctrl Pts',(16.5492254757682,0.238512972024049,4.4301357774334));
#29508=CARTESIAN_POINT('Ctrl Pts',(16.596941311831,-0.23279962385521,4.43325461334514));
#29509=CARTESIAN_POINT('Ctrl Pts',(16.6446571478939,-0.490328743065594,
4.03850907134293));
#29510=CARTESIAN_POINT('Ctrl Pts',(16.6923729839567,-0.297581432841348,
3.60840005658827));
#29511=CARTESIAN_POINT('Ctrl Pts',(16.7400888200196,0.168439486040012,3.53790329540825));
#29512=CARTESIAN_POINT('Ctrl Pts',(16.7878046560824,0.479779833116189,3.89175704832657));
#29513=CARTESIAN_POINT('Ctrl Pts',(16.8355204921452,0.350530977080134,4.3450119692985));
#29514=CARTESIAN_POINT('Ctrl Pts',(16.8832363282081,-0.100615868820984,
4.4814370901721));
#29515=CARTESIAN_POINT('Ctrl Pts',(16.9309521642709,-0.459365614209645,
4.17575112327883));
#29516=CARTESIAN_POINT('Ctrl Pts',(16.9786680003337,-0.396272847821079,
3.70867019559999));
#29517=CARTESIAN_POINT('Ctrl Pts',(17.0263838363966,0.0307233721630972,
3.5091219099869));
#29518=CARTESIAN_POINT('Ctrl Pts',(17.0740996724594,0.429505846750062,3.76035452756312));
#29519=CARTESIAN_POINT('Ctrl Pts',(17.1218155085223,0.433866493469502,4.23165726989771));
#29520=CARTESIAN_POINT('Ctrl Pts',(17.1695313445851,0.039800863341802,4.49022557677993));
#29521=CARTESIAN_POINT('Ctrl Pts',(17.217247180648,-0.390814512007675,4.29861219341511));
#29522=CARTESIAN_POINT('Ctrl Pts',(17.2649630167107,-0.462538907526291,
3.83277863809798));
#29523=CARTESIAN_POINT('Ctrl Pts',(17.3126788527736,-0.109506707187599,
3.52050703244687));
#29524=CARTESIAN_POINT('Ctrl Pts',(17.3603946888365,0.344087187338735,3.64856119684745));
#29525=CARTESIAN_POINT('Ctrl Pts',(17.4081105248993,0.481700523269991,4.09934702176407));
#29526=CARTESIAN_POINT('Ctrl Pts',(17.4558263609621,0.176960856767158,4.45890094794434));
#29527=CARTESIAN_POINT('Ctrl Pts',(17.503542197025,-0.290284687397741,4.39703907252861));
#29528=CARTESIAN_POINT('Ctrl Pts',(17.5512580330878,-0.490957336521241,
3.97057010757845));
#29529=CARTESIAN_POINT('Ctrl Pts',(17.5989738691507,-0.240776309167652,
3.57112706567612));
#29530=CARTESIAN_POINT('Ctrl Pts',(17.6466897052135,0.230513307714322,3.56552463842171));
#29531=CARTESIAN_POINT('Ctrl Pts',(17.6944055412763,0.490119007219086,3.95890762096741));
#29532=CARTESIAN_POINT('Ctrl Pts',(17.7421213773392,0.299640880944266,4.39002636746625));
#29533=CARTESIAN_POINT('Ctrl Pts',(17.789837213402,-0.166002076869247,4.46297789939377));
#29534=CARTESIAN_POINT('Ctrl Pts',(17.8375530494648,-0.479202773223469,
4.11076970247734));
#29535=CARTESIAN_POINT('Ctrl Pts',(17.8852688855277,-0.352344189444135,
3.65683998336499));
#29536=CARTESIAN_POINT('Ctrl Pts',(17.9329847215905,0.0980774850139738,
3.51803938772416));
#29537=CARTESIAN_POINT('Ctrl Pts',(17.9807005576534,0.458433095867658,3.82183063825345));
#29538=CARTESIAN_POINT('Ctrl Pts',(18.0284163937162,0.397802540886209,4.28923755516265));
#29539=CARTESIAN_POINT('Ctrl Pts',(18.076132229779,-0.0281362083699241,
4.49103317467411));
#29540=CARTESIAN_POINT('Ctrl Pts',(18.1238480658419,-0.428237044548737,
4.24190547436581));
#29541=CARTESIAN_POINT('Ctrl Pts',(18.1715639019047,-0.435081213444543,
3.7706322547532));
#29542=CARTESIAN_POINT('Ctrl Pts',(18.2192797379675,-0.0423836094492617,
3.50999096487715));
#29543=CARTESIAN_POINT('Ctrl Pts',(18.2669955740304,0.389235515258945,3.69933251171255));
#29544=CARTESIAN_POINT('Ctrl Pts',(18.3147114100932,0.463413677146622,4.16478163940629));
#29545=CARTESIAN_POINT('Ctrl Pts',(18.3624272461561,0.112031928774586,4.4789092521418));
#29546=CARTESIAN_POINT('Ctrl Pts',(18.4101430822189,-0.342230463623947,
4.35324712966946));
#29547=CARTESIAN_POINT('Ctrl Pts',(18.4578589182817,-0.482217355384067,
3.90319273261591));
#29548=CARTESIAN_POINT('Ctrl Pts',(18.5055747543446,-0.179376629827252,
3.54203793877243));
#29549=CARTESIAN_POINT('Ctrl Pts',(18.5532905904074,0.288188414964166,3.60143675240633));
#29550=CARTESIAN_POINT('Ctrl Pts',(18.6010064264702,0.491105603945206,4.02684232898929));
#29551=CARTESIAN_POINT('Ctrl Pts',(18.6487222625331,0.243032960192409,4.42759818183915));
#29552=CARTESIAN_POINT('Ctrl Pts',(18.6964380985959,-0.228220590447982,
4.43568404486223));
#29553=CARTESIAN_POINT('Ctrl Pts',(18.7441539346588,-0.489895661254576,
4.0436745456279));
#29554=CARTESIAN_POINT('Ctrl Pts',(18.7918697707216,-0.301692008317894,
3.6115580391236));
#29555=CARTESIAN_POINT('Ctrl Pts',(18.8395856067845,0.163560057986223,3.53615376224111));
#29556=CARTESIAN_POINT('Ctrl Pts',(18.8873014428472,0.478612406344963,3.88670662268212));
#29557=CARTESIAN_POINT('Ctrl Pts',(18.9350172789101,0.35414761756175,4.34129853476112));
#29558=CARTESIAN_POINT('Ctrl Pts',(18.982733114973,-0.0955363776958117,
4.48247075080787));
#29559=CARTESIAN_POINT('Ctrl Pts',(19.0304489510358,-0.457487847288108,
4.18058265263639));
#29560=CARTESIAN_POINT('Ctrl Pts',(19.0781647870987,-0.399321187381313,
3.71286272589862));
#29561=CARTESIAN_POINT('Ctrl Pts',(19.1258806231614,0.0255482632835279,
3.50882537619781));
#29562=CARTESIAN_POINT('Ctrl Pts',(19.1735964592243,0.426956350589889,3.75584124112414));
#29563=CARTESIAN_POINT('Ctrl Pts',(19.2213122952871,0.436283851722622,4.22707185138688));
#29564=CARTESIAN_POINT('Ctrl Pts',(19.26902813135,0.0449651784623906,4.48977888620274));
#29565=CARTESIAN_POINT('Ctrl Pts',(19.3167439674128,-0.387645709555542,
4.3027144342981));
#29566=CARTESIAN_POINT('Ctrl Pts',(19.3644598034757,-0.464275578741542,
3.8376626582024));
#29567=CARTESIAN_POINT('Ctrl Pts',(19.4121756395385,-0.114554038379521,
3.52168776344319));
#29568=CARTESIAN_POINT('Ctrl Pts',(19.4598914756013,0.340364234683876,3.64495435060606));
#29569=CARTESIAN_POINT('Ctrl Pts',(19.5076073116642,0.482720800247919,4.09426482953845));
#29570=CARTESIAN_POINT('Ctrl Pts',(19.555323147727,0.181787415268628,4.45701044834135));
#29571=CARTESIAN_POINT('Ctrl Pts',(19.6030389837899,-0.28608412753634,4.40007637198121));
#29572=CARTESIAN_POINT('Ctrl Pts',(19.6507548198527,-0.491240257057309,
3.97574594767572));
#29573=CARTESIAN_POINT('Ctrl Pts',(19.6984706559155,-0.245282818621706,
3.57368850533185));
#29574=CARTESIAN_POINT('Ctrl Pts',(19.7461864919783,0.225921452997342,3.56311925573479));
#29575=CARTESIAN_POINT('Ctrl Pts',(19.7939023280412,0.489658867576397,3.95374471702426));
#29576=CARTESIAN_POINT('Ctrl Pts',(19.841618164104,0.303734463062876,4.38684635894002));
#29577=CARTESIAN_POINT('Ctrl Pts',(19.8893340001669,-0.161112940293692,
4.46470246728215));
#29578=CARTESIAN_POINT('Ctrl Pts',(19.9370498362297,-0.47800980043334,4.11581244897344));
#29579=CARTESIAN_POINT('Ctrl Pts',(19.9847656722926,-0.355939225796451,
3.66057517601247));
#29580=CARTESIAN_POINT('Ctrl Pts',(20.0324815083554,0.0929888682922082,
3.51702731322357));
#29581=CARTESIAN_POINT('Ctrl Pts',(20.0801973444182,0.456536973876988,3.81701888067549));
#29582=CARTESIAN_POINT('Ctrl Pts',(20.1279131804811,0.400815378068436,4.28501049648274));
#29583=CARTESIAN_POINT('Ctrl Pts',(20.1756290165439,-0.022934367574535,
4.49133741301101));
#29584=CARTESIAN_POINT('Ctrl Pts',(20.2233448526067,-0.425711472830213,
4.24633918020534));
#29585=CARTESIAN_POINT('Ctrl Pts',(20.2710606886696,-0.437384262562023,
3.77535541015343));
#29586=CARTESIAN_POINT('Ctrl Pts',(20.3187765247324,-0.0477164433392854,
3.51022640082505));
#29587=CARTESIAN_POINT('Ctrl Pts',(20.3664923607953,0.386374384143037,3.69571627142296));
#29588=CARTESIAN_POINT('Ctrl Pts',(20.4062555575143,0.45143962727185,4.08165775845481));
#29589=CARTESIAN_POINT('Ctrl Pts',(20.4380661148895,0.291471375703242,4.31996082336987));
#29590=CARTESIAN_POINT('Ctrl Pts',(20.461924032921,0.103697252552815,4.42124466395835));
#29591=CARTESIAN_POINT('Ctrl Pts',(20.4857819509523,-0.111451542568667,
4.41901444157942));
#29592=CARTESIAN_POINT('Ctrl Pts',(20.5096398689838,-0.298255971346869,
4.31460392554555));
#29593=CARTESIAN_POINT('Ctrl Pts',(20.5334977870152,-0.412709509332759,
4.13311446574462));
#29594=CARTESIAN_POINT('Ctrl Pts',(20.5573557050466,-0.425936384696969,
3.91915434697803));
#29595=CARTESIAN_POINT('Ctrl Pts',(20.581213623078,-0.335173342752607,3.72492109335083));
#29596=CARTESIAN_POINT('Ctrl Pts',(20.6050715411095,-0.162364888615448,
3.59797442377207));
#29597=CARTESIAN_POINT('Ctrl Pts',(20.6289294591408,0.0501004451364318,
3.56932214892951));
#29598=CARTESIAN_POINT('Ctrl Pts',(20.6527873771723,0.250339089241223,3.64598859455508));
#29599=CARTESIAN_POINT('Ctrl Pts',(20.6766452952037,0.389350172549011,3.80921715950176));
#29600=CARTESIAN_POINT('Ctrl Pts',(20.7005032132352,0.433161330121289,4.01909908002448));
#29601=CARTESIAN_POINT('Ctrl Pts',(20.7243611312665,0.371049143609512,4.22430982617278));
#29602=CARTESIAN_POINT('Ctrl Pts',(20.748219049298,0.218207240773441,4.37467120177868));
#29603=CARTESIAN_POINT('Ctrl Pts',(20.7720769673293,0.01200671405148,4.43341500212799));
#29604=CARTESIAN_POINT('Ctrl Pts',(20.7959348853608,-0.197129246586683,
4.38617716647524));
#29605=CARTESIAN_POINT('Ctrl Pts',(20.8197928033922,-0.358062019934396,
4.24450842127602));
#29606=CARTESIAN_POINT('Ctrl Pts',(20.8436507214237,-0.431438726014498,
4.04305074550709));
#29607=CARTESIAN_POINT('Ctrl Pts',(20.867508639455,-0.399316990859146,3.83106596928302));
#29608=CARTESIAN_POINT('Ctrl Pts',(20.8913665574865,-0.269551332195825,
3.66039017609669));
#29609=CARTESIAN_POINT('Ctrl Pts',(20.9152244755179,-0.0738730526583281,
3.57275822989076));
#29610=CARTESIAN_POINT('Ctrl Pts',(20.9390823935493,0.139869212314499,3.58959853735383));
#29611=CARTESIAN_POINT('Ctrl Pts',(20.9629403115807,0.319409638666883,3.70679317993256));
#29612=CARTESIAN_POINT('Ctrl Pts',(20.9867982296122,0.420845711130686,3.8956848776653));
#29613=CARTESIAN_POINT('Ctrl Pts',(21.0106561476436,0.419373541863394,4.11008446384341));
#29614=CARTESIAN_POINT('Ctrl Pts',(21.034514065675,0.315353119032788,4.29756540021079));
#29615=CARTESIAN_POINT('Ctrl Pts',(21.0583719837064,0.134220268060588,4.41228349058099));
#29616=CARTESIAN_POINT('Ctrl Pts',(21.0822299017379,-0.079733094278782,
4.42618703719455));
#29617=CARTESIAN_POINT('Ctrl Pts',(21.1060878197692,-0.274189543318984,
4.33587624407661));
#29618=CARTESIAN_POINT('Ctrl Pts',(21.1299457378007,-0.401599180171465,
4.16343456021562));
#29619=CARTESIAN_POINT('Ctrl Pts',(21.1538036558321,-0.430806878168669,
3.95102867450389));
#29620=CARTESIAN_POINT('Ctrl Pts',(21.1776615738635,-0.354670559489406,
3.75059761183336));
#29621=CARTESIAN_POINT('Ctrl Pts',(21.2015194918949,-0.191807627993766,
3.61115222665144));
#29622=CARTESIAN_POINT('Ctrl Pts',(21.2253774099264,0.0179574932869785,
3.56679071405539));
#29623=CARTESIAN_POINT('Ctrl Pts',(21.2492353279577,0.223331518303719,3.62836067225603));
#29624=CARTESIAN_POINT('Ctrl Pts',(21.2730932459892,0.374094903668402,3.78080656934254));
#29625=CARTESIAN_POINT('Ctrl Pts',(21.2969511640206,0.433381894944723,3.98685123093373));
#29626=CARTESIAN_POINT('Ctrl Pts',(21.320809082052,0.386695207821707,4.19611112472705));
#29627=CARTESIAN_POINT('Ctrl Pts',(21.3446670000834,0.245451009020076,4.35741650656472));
#29628=CARTESIAN_POINT('Ctrl Pts',(21.3685249181149,0.0441873525619181,
4.43132381671722));
#29629=CARTESIAN_POINT('Ctrl Pts',(21.3923828361462,-0.167881315237013,
4.39976070465745));
#29630=CARTESIAN_POINT('Ctrl Pts',(21.4162407541777,-0.338898428465248,
4.27044521104599));
#29631=CARTESIAN_POINT('Ctrl Pts',(21.4400986722091,-0.427045644525908,
4.07499849655415));
#29632=CARTESIAN_POINT('Ctrl Pts',(21.4639565902406,-0.410768568010174,
3.86121260673678));
#29633=CARTESIAN_POINT('Ctrl Pts',(21.4878145082719,-0.294047387504818,
3.68136401506497));
#29634=CARTESIAN_POINT('Ctrl Pts',(21.5116724263034,-0.105423611064507,
3.57943060117972));
#29635=CARTESIAN_POINT('Ctrl Pts',(21.5355303443348,0.108979109962582,3.58033786138646));
#29636=CARTESIAN_POINT('Ctrl Pts',(21.5593882623662,0.296733470072461,3.68386394585134));
#29637=CARTESIAN_POINT('Ctrl Pts',(21.5832461803976,0.411928413892185,3.86469390692879));
#29638=CARTESIAN_POINT('Ctrl Pts',(21.6071040984291,0.426395639810567,4.07860989342611));
#29639=CARTESIAN_POINT('Ctrl Pts',(21.6309620164605,0.33659751701124,4.27330361969026));
#29640=CARTESIAN_POINT('Ctrl Pts',(21.6548199344919,0.164492132570386,4.401167166299));
#29641=CARTESIAN_POINT('Ctrl Pts',(21.6786778525233,-0.0478360589596606,
4.43093441317345));
#29642=CARTESIAN_POINT('Ctrl Pts',(21.7025357705547,-0.248467031045983,
4.35532645760922));
#29643=CARTESIAN_POINT('Ctrl Pts',(21.7263936885861,-0.388341045935521,
4.1928315042612));
#29644=CARTESIAN_POINT('Ctrl Pts',(21.7502516066176,-0.433255096896122,
3.98318399549658));
#29645=CARTESIAN_POINT('Ctrl Pts',(21.774109524649,-0.372226475033738,3.77764845789182));
#29646=CARTESIAN_POINT('Ctrl Pts',(21.7979674426804,-0.220178340780001,
3.62648392906691));
#29647=CARTESIAN_POINT('Ctrl Pts',(21.8218253607118,-0.0142906046679706,
3.56665425395863));
#29648=CARTESIAN_POINT('Ctrl Pts',(21.8456832787432,0.195091573553633,3.61278941785858));
#29649=CARTESIAN_POINT('Ctrl Pts',(21.8695411967747,0.356768547853618,3.75360811649661));
#29650=CARTESIAN_POINT('Ctrl Pts',(21.8933991148061,0.431205894023261,3.95467634223136));
#29651=CARTESIAN_POINT('Ctrl Pts',(21.9172570328375,0.400201653291494,4.16682743688221));
#29652=CARTESIAN_POINT('Ctrl Pts',(21.941114950869,0.271337207055788,4.33818467892719));
#29653=CARTESIAN_POINT('Ctrl Pts',(21.9649728689003,0.0761234226178432,
4.4268465550088));
#29654=CARTESIAN_POINT('Ctrl Pts',(21.9888307869318,-0.137704612210607,
4.41113282132402));
#29655=CARTESIAN_POINT('Ctrl Pts',(22.0126887049632,-0.317860118355158,
4.29488591379237));
#29656=CARTESIAN_POINT('Ctrl Pts',(22.0365466229946,-0.420290167226249,
4.10653136780738));
#29657=CARTESIAN_POINT('Ctrl Pts',(22.060404541026,-0.419947821735935,3.89212700053744));
#29658=CARTESIAN_POINT('Ctrl Pts',(22.0842624590574,-0.316916794682727,
3.70410052003731));
#29659=CARTESIAN_POINT('Ctrl Pts',(22.1081203770888,-0.136390978688423,
3.58842952252864));
#29660=CARTESIAN_POINT('Ctrl Pts',(22.1319782951203,0.0774861468089536,
3.57339871771534));
#29661=CARTESIAN_POINT('Ctrl Pts',(22.1558362131517,0.27241579873489,3.66268354680831));
#29662=CARTESIAN_POINT('Ctrl Pts',(22.1796941311831,0.400732367405962,3.83445143701846));
#29663=CARTESIAN_POINT('Ctrl Pts',(22.2035520492145,0.431058956528623,4.04670046033727));
#29664=CARTESIAN_POINT('Ctrl Pts',(22.227409967246,0.355979888945518,4.24752994899471));
#29665=CARTESIAN_POINT('Ctrl Pts',(22.2512678852773,0.193854041863619,4.38783162256878));
#29666=CARTESIAN_POINT('Ctrl Pts',(22.2751258033088,-0.0156743990186396,
4.43329790005389));
#29667=CARTESIAN_POINT('Ctrl Pts',(22.2989837213402,-0.221370022215225,
4.37281103827166));
#29668=CARTESIAN_POINT('Ctrl Pts',(22.3228416393716,-0.372934645290675,
4.22116172228637));
#29669=CARTESIAN_POINT('Ctrl Pts',(22.346699557403,-0.43330658847365,4.01543234121164));
#29670=CARTESIAN_POINT('Ctrl Pts',(22.3705574754345,-0.387723268841402,
3.80592933171158));
#29671=CARTESIAN_POINT('Ctrl Pts',(22.3944153934659,-0.247331046528593,
3.64388188817752));
#29672=CARTESIAN_POINT('Ctrl Pts',(22.4182733114973,-0.0464596501027702,
3.56891502119853));
#29673=CARTESIAN_POINT('Ctrl Pts',(22.4421312295287,0.165772403721094,3.59936017830047));
#29674=CARTESIAN_POINT('Ctrl Pts',(22.4659891475602,0.337468575289321,3.7277726770023));
#29675=CARTESIAN_POINT('Ctrl Pts',(22.4898470655915,0.426644514167594,3.92275218663495));
#29676=CARTESIAN_POINT('Ctrl Pts',(22.513704983623,0.411494197867752,4.13662086224655));
#29677=CARTESIAN_POINT('Ctrl Pts',(22.5375629016544,0.295722435535401,4.31708206952049));
#29678=CARTESIAN_POINT('Ctrl Pts',(22.5614208196858,0.107638304484935,4.42000797176855));
#29679=CARTESIAN_POINT('Ctrl Pts',(22.5852787377172,-0.106765988085903,
4.42023067651324));
#29680=CARTESIAN_POINT('Ctrl Pts',(22.6091366557487,-0.295063722636797,
4.31769517074077));
#29681=CARTESIAN_POINT('Ctrl Pts',(22.6329945737801,-0.411209141905604,
4.13747522778479));
#29682=CARTESIAN_POINT('Ctrl Pts',(22.6568524918115,-0.426804986482714,
3.92363755172126));
#29683=CARTESIAN_POINT('Ctrl Pts',(22.6807104098429,-0.33803111495158,3.72847502015617));
#29684=CARTESIAN_POINT('Ctrl Pts',(22.7045683278743,-0.16660749730952,3.59970312177549));
#29685=CARTESIAN_POINT('Ctrl Pts',(22.7284262459057,0.0455714674079685,
3.56882345794434));
#29686=CARTESIAN_POINT('Ctrl Pts',(22.7522841639372,0.246577802732478,3.64336153500176));
#29687=CARTESIAN_POINT('Ctrl Pts',(22.7761420819686,0.387346815298129,3.80514019809748));
#29688=CARTESIAN_POINT('Ctrl Pts',(22.7920473606562,0.417963038852713,3.94471011778788));
#29689=CARTESIAN_POINT('Ctrl Pts',(22.8,0.415641328671541,4.01393920819689));
#29690=CARTESIAN_POINT('Ctrl Pts',(3.96816317011929,0.203757107801821,4.42939176513376));
#29691=CARTESIAN_POINT('Ctrl Pts',(3.9761158094631,0.132237748973037,4.46332948562603));
#29692=CARTESIAN_POINT('Ctrl Pts',(3.99202108815071,-0.0280119004087947,
4.49474661085258));
#29693=CARTESIAN_POINT('Ctrl Pts',(4.01587900618213,-0.261670681609628,
4.42079217330492));
#29694=CARTESIAN_POINT('Ctrl Pts',(4.03973692421355,-0.431283260509235,
4.24398813071681));
#29695=CARTESIAN_POINT('Ctrl Pts',(4.06359484224497,-0.495466080430727,
4.00749935521381));
#29696=CARTESIAN_POINT('Ctrl Pts',(4.08745276027639,-0.438477829352452,
3.76918881818141));
#29697=CARTESIAN_POINT('Ctrl Pts',(4.11131067830781,-0.274278321106756,
3.5873115455631));
#29698=CARTESIAN_POINT('Ctrl Pts',(4.13516859633923,-0.0430057845205295,
3.50635120590702));
#29699=CARTESIAN_POINT('Ctrl Pts',(4.15902651437064,0.198780450874126,3.54609966156282));
#29700=CARTESIAN_POINT('Ctrl Pts',(4.18288443240206,0.391960715466274,3.69684005745713));
#29701=CARTESIAN_POINT('Ctrl Pts',(4.20674235043348,0.489295238859844,3.92171081754005));
#29702=CARTESIAN_POINT('Ctrl Pts',(4.2306002684649,0.466984102771714,4.16572567991789));
#29703=CARTESIAN_POINT('Ctrl Pts',(4.25445818649632,0.330482445391075,4.36921595913043));
#29704=CARTESIAN_POINT('Ctrl Pts',(4.27831610452774,0.113168927396708,4.48242295331799));
#29705=CARTESIAN_POINT('Ctrl Pts',(4.30217402255916,-0.131817528672551,
4.47766435517297));
#29706=CARTESIAN_POINT('Ctrl Pts',(4.32603194059057,-0.344570980451485,
4.35610383169054));
#29707=CARTESIAN_POINT('Ctrl Pts',(4.349889858622,-0.473067456356951,4.14746621026076));
#29708=CARTESIAN_POINT('Ctrl Pts',(4.37374777665341,-0.485886045261059,
3.9027690893624));
#29709=CARTESIAN_POINT('Ctrl Pts',(4.39760569468484,-0.379892264971952,
3.68184757153936));
#29710=CARTESIAN_POINT('Ctrl Pts',(4.42146361271625,-0.181004475645389,
3.53872299041084));
#29711=CARTESIAN_POINT('Ctrl Pts',(4.44532153074767,0.0621438372772935,
3.50839320219298));
#29712=CARTESIAN_POINT('Ctrl Pts',(4.46917944877909,0.290096289836991,3.5982746675986));
#29713=CARTESIAN_POINT('Ctrl Pts',(4.49303736681051,0.447112297141319,3.78638891931142));
#29714=CARTESIAN_POINT('Ctrl Pts',(4.51689528484194,0.494797168872773,4.02673689903048));
#29715=CARTESIAN_POINT('Ctrl Pts',(4.54075320287334,0.421490654719143,4.26054697856981));
#29716=CARTESIAN_POINT('Ctrl Pts',(4.56461112090478,0.245118194360182,4.43064622472778));
#29717=CARTESIAN_POINT('Ctrl Pts',(4.58846903893618,0.00880765856895839,
4.49544073835303));
#29718=CARTESIAN_POINT('Ctrl Pts',(4.61232695696761,-0.229656589644598,
4.43908649592634));
#29719=CARTESIAN_POINT('Ctrl Pts',(4.63618487499902,-0.411963545977342,
4.2753636447643));
#29720=CARTESIAN_POINT('Ctrl Pts',(4.66004279303045,-0.493534193653132,
4.04430688170513));
#29721=CARTESIAN_POINT('Ctrl Pts',(4.68390071106186,-0.454422287381232,
3.80241587917234));
#29722=CARTESIAN_POINT('Ctrl Pts',(4.70775862909328,-0.304191753628974,
3.60883957626609));
#29723=CARTESIAN_POINT('Ctrl Pts',(4.7316165471247,-0.0795780500979935,
3.51091265195837));
#29724=CARTESIAN_POINT('Ctrl Pts',(4.75547446515612,0.164494654344808,3.53258090671894));
#29725=CARTESIAN_POINT('Ctrl Pts',(4.77933238318754,0.368343935055725,3.66854586202706));
#29726=CARTESIAN_POINT('Ctrl Pts',(4.80319030121895,0.482123090158262,3.88556038269908));
#29727=CARTESIAN_POINT('Ctrl Pts',(4.82704821925038,0.478010016947761,4.13055850707372));
#29728=CARTESIAN_POINT('Ctrl Pts',(4.85090613728179,0.357010473862124,4.34363152012653));
#29729=CARTESIAN_POINT('Ctrl Pts',(4.87476405531322,0.14871214514713,4.47267726617372));
#29730=CARTESIAN_POINT('Ctrl Pts',(4.89862197334463,-0.0959503538938319,
4.48614054517122));
#29731=CARTESIAN_POINT('Ctrl Pts',(4.92247989137606,-0.317150377772593,
4.38072921867179));
#29732=CARTESIAN_POINT('Ctrl Pts',(4.94633780940747,-0.460798495283114,
4.1822192273514));
#29733=CARTESIAN_POINT('Ctrl Pts',(4.97019572743889,-0.49176882879792,3.93915167139151));
#29734=CARTESIAN_POINT('Ctrl Pts',(4.99405364547031,-0.40248828815769,3.71096318925158));
#29735=CARTESIAN_POINT('Ctrl Pts',(5.01791156350173,-0.214788397502062,
3.55345208054429));
#29736=CARTESIAN_POINT('Ctrl Pts',(5.04176948153314,0.0254331070612992,
3.50513410186502));
#29737=CARTESIAN_POINT('Ctrl Pts',(5.06562739956457,0.259435524164246,3.57782431515618));
#29738=CARTESIAN_POINT('Ctrl Pts',(5.08948531759598,0.429998888727244,3.75374798322641));
#29739=CARTESIAN_POINT('Ctrl Pts',(5.11334323562741,0.495415812061873,3.98988697716804));
#29740=CARTESIAN_POINT('Ctrl Pts',(5.13720115365882,0.439690074491602,4.2284988806653));
#29741=CARTESIAN_POINT('Ctrl Pts',(5.16105907169025,0.276448136790977,4.41123658365534));
#29742=CARTESIAN_POINT('Ctrl Pts',(5.18491698972166,0.0456070993489057,
4.49341574008204));
#29743=CARTESIAN_POINT('Ctrl Pts',(5.20877490775308,-0.196386116196418,
4.45494130768376));
#29744=CARTESIAN_POINT('Ctrl Pts',(5.2326328257845,-0.390357576881318,4.3052213332044));
#29745=CARTESIAN_POINT('Ctrl Pts',(5.25649074381592,-0.488875976891831,
4.08086642869437));
#29746=CARTESIAN_POINT('Ctrl Pts',(5.28034866184734,-0.467850883838054,
3.83673747961128));
#29747=CARTESIAN_POINT('Ctrl Pts',(5.30420657987876,-0.332423505683668,
3.632530663945));
#29748=CARTESIAN_POINT('Ctrl Pts',(5.32806449791017,-0.115709525355139,
3.5181801106079));
#29749=CARTESIAN_POINT('Ctrl Pts',(5.3519224159416,0.129298585786916,3.52164764473745));
#29750=CARTESIAN_POINT('Ctrl Pts',(5.37578033397301,0.342689670681295,3.64208535978523));
#29751=CARTESIAN_POINT('Ctrl Pts',(5.39963825200445,0.472283796414913,3.85004295376459));
#29752=CARTESIAN_POINT('Ctrl Pts',(5.42349617003584,0.48639166917272,4.09466913029638));
#29753=CARTESIAN_POINT('Ctrl Pts',(5.44735408806728,0.381563529774833,4.31614612573549));
#29754=CARTESIAN_POINT('Ctrl Pts',(5.47121200609869,0.183432713764955,4.46031678178449));
#29755=CARTESIAN_POINT('Ctrl Pts',(5.49506992413012,-0.059552397366927,
4.49192744591021));
#29756=CARTESIAN_POINT('Ctrl Pts',(5.51892784216153,-0.287975325168481,
4.40324844967551));
#29757=CARTESIAN_POINT('Ctrl Pts',(5.54278576019295,-0.445980441674811,
4.21596422322942));
#29758=CARTESIAN_POINT('Ctrl Pts',(5.56664367822437,-0.494931191930538,
3.97587086145358));
#29759=CARTESIAN_POINT('Ctrl Pts',(5.59050159625579,-0.422857784100094,
3.74167773132221));
#29760=CARTESIAN_POINT('Ctrl Pts',(5.61435951428721,-0.247384129650275,
3.57065143242979));
#29761=CARTESIAN_POINT('Ctrl Pts',(5.63821743231862,-0.0114183168777074,
3.50461255354752));
#29762=CARTESIAN_POINT('Ctrl Pts',(5.66207535035005,0.227339585372105,3.55970939936999));
#29763=CARTESIAN_POINT('Ctrl Pts',(5.68593326838146,0.410506766445453,3.72246929038963));
#29764=CARTESIAN_POINT('Ctrl Pts',(5.70979118641288,0.493293861043031,3.9530929995654));
#29765=CARTESIAN_POINT('Ctrl Pts',(5.73364910444431,0.455457169749513,4.19518674831082));
#29766=CARTESIAN_POINT('Ctrl Pts',(5.75750702247572,0.306248793691327,4.38955201985635));
#29767=CARTESIAN_POINT('Ctrl Pts',(5.78136494050715,0.0821542461994931,
4.48866121222712));
#29768=CARTESIAN_POINT('Ctrl Pts',(5.80522285853855,-0.162029253596618,
4.46827942571263));
#29769=CARTESIAN_POINT('Ctrl Pts',(5.82908077656998,-0.366592184898752,
4.33339056701663));
#29770=CARTESIAN_POINT('Ctrl Pts',(5.85293869460139,-0.481513345756758,
4.11697862749145));
#29771=CARTESIAN_POINT('Ctrl Pts',(5.87679661263282,-0.478691368855474,
3.87196223809426));
#29772=CARTESIAN_POINT('Ctrl Pts',(5.90065453066423,-0.358816329143926,
3.65825454842257));
#29773=CARTESIAN_POINT('Ctrl Pts',(5.92451244869565,-0.151200892471453,
3.52811296978032));
#29774=CARTESIAN_POINT('Ctrl Pts',(5.94837036672708,0.093387223403125,3.5133605500302));
#29775=CARTESIAN_POINT('Ctrl Pts',(5.97222828475848,0.315139728168714,3.61760487120619));
#29776=CARTESIAN_POINT('Ctrl Pts',(5.99608620278992,0.459831779670103,3.81535495398299));
#29777=CARTESIAN_POINT('Ctrl Pts',(6.01994412082132,0.492082823488737,4.05825627791571));
#29778=CARTESIAN_POINT('Ctrl Pts',(6.04380203885276,0.404005480250355,4.28691141512903));
#29779=CARTESIAN_POINT('Ctrl Pts',(6.06765995688416,0.21713917558903,4.44541067075535));
#29780=CARTESIAN_POINT('Ctrl Pts',(6.09151787491559,-0.0228261843714051,
4.49499153360272));
#29781=CARTESIAN_POINT('Ctrl Pts',(6.11537579294701,-0.257204988275768,
4.42353981062321));
#29782=CARTESIAN_POINT('Ctrl Pts',(6.13923371097843,-0.428699479426561,
4.24850911946619));
#29783=CARTESIAN_POINT('Ctrl Pts',(6.16309162900984,-0.49534768549136,4.01273373861842));
#29784=CARTESIAN_POINT('Ctrl Pts',(6.18694954704127,-0.440903093044182,
3.77380201544612));
#29785=CARTESIAN_POINT('Ctrl Pts',(6.21080746507268,-0.278582990390117,
3.59026229064107));
#29786=CARTESIAN_POINT('Ctrl Pts',(6.23466538310411,-0.048260127889517,
3.50676273730504));
#29787=CARTESIAN_POINT('Ctrl Pts',(6.25852330113552,0.194087080856728,3.5441598063702));
#29788=CARTESIAN_POINT('Ctrl Pts',(6.28238121916694,0.388553448942855,3.69248145192407));
#29789=CARTESIAN_POINT('Ctrl Pts',(6.30623913719837,0.488798280742691,3.9170164641697));
#29790=CARTESIAN_POINT('Ctrl Pts',(6.33009705522977,0.468067515948433,4.15995908608738));
#29791=CARTESIAN_POINT('Ctrl Pts',(6.36190761260502,0.291040001689194,4.43610431491443));
#29792=CARTESIAN_POINT('Ctrl Pts',(6.40167080932402,-0.143168317426403,
4.54352222151223));
#29793=CARTESIAN_POINT('Ctrl Pts',(6.44938664538688,-0.535165231989368,
4.17285582464912));
#29794=CARTESIAN_POINT('Ctrl Pts',(6.49710248144971,-0.434543251113388,
3.64369891234367));
#29795=CARTESIAN_POINT('Ctrl Pts',(6.54481831751255,0.0645215567551043,
3.4416075490323));
#29796=CARTESIAN_POINT('Ctrl Pts',(6.59253415357539,0.504653900644641,3.75236619672659));
#29797=CARTESIAN_POINT('Ctrl Pts',(6.64024998963822,0.481186238846835,4.29049388273239));
#29798=CARTESIAN_POINT('Ctrl Pts',(6.68796582570107,0.01592709648968,4.56187610740764));
#29799=CARTESIAN_POINT('Ctrl Pts',(6.7356816617639,-0.464005405879062,4.31726850783359));
#29800=CARTESIAN_POINT('Ctrl Pts',(6.78339749782674,-0.517809574500644,
3.78131383674221));
#29801=CARTESIAN_POINT('Ctrl Pts',(6.83111333388957,-0.0961144992151805,
3.44617913151078));
#29802=CARTESIAN_POINT('Ctrl Pts',(6.87882916995242,0.413851019972934,3.61962818876606));
#29803=CARTESIAN_POINT('Ctrl Pts',(6.92654500601525,0.543767061592725,4.14237771887731));
#29804=CARTESIAN_POINT('Ctrl Pts',(6.97426084207809,0.174335412693353,4.53438003016987));
#29805=CARTESIAN_POINT('Ctrl Pts',(7.02197667814094,-0.355192171006393,
4.43565270890428));
#29806=CARTESIAN_POINT('Ctrl Pts',(7.06969251420376,-0.558540766450571,
3.93685892261342));
#29807=CARTESIAN_POINT('Ctrl Pts',(7.11740835026661,-0.248973074301851,
3.49604849518665));
#29808=CARTESIAN_POINT('Ctrl Pts',(7.16512418632944,0.289230577826905,3.51802452284194));
#29809=CARTESIAN_POINT('Ctrl Pts',(7.21284002239229,0.561829257914175,3.98260602935256));
#29810=CARTESIAN_POINT('Ctrl Pts',(7.26055585845511,0.318491529052478,4.46316069626365));
#29811=CARTESIAN_POINT('Ctrl Pts',(7.30827169451797,-0.217321894570402,
4.51838776411367));
#29812=CARTESIAN_POINT('Ctrl Pts',(7.35598753058078,-0.553565266295818,
4.09757137442565));
#29813=CARTESIAN_POINT('Ctrl Pts',(7.40370336664365,-0.381461142739227,
3.58715368886071));
#29814=CARTESIAN_POINT('Ctrl Pts',(7.45141920270646,0.140944621146953,3.45585912402047));
#29815=CARTESIAN_POINT('Ctrl Pts',(7.49913503876933,0.533918768911932,3.82425749787944));
#29816=CARTESIAN_POINT('Ctrl Pts',(7.54685087483214,0.436587096747522,4.3540429157916));
#29817=CARTESIAN_POINT('Ctrl Pts',(7.594566710895,-0.0616692246238245,4.5587052763707));
#29818=CARTESIAN_POINT('Ctrl Pts',(7.64228254695782,-0.503293747851232,
4.25029998493175));
#29819=CARTESIAN_POINT('Ctrl Pts',(7.68999838302067,-0.482735878399531,
3.7120403659385));
#29820=CARTESIAN_POINT('Ctrl Pts',(7.7377142190835,-0.0188742238918736,
3.43821850974892));
#29821=CARTESIAN_POINT('Ctrl Pts',(7.78543005514633,0.462319920793015,3.6802892401675));
#29822=CARTESIAN_POINT('Ctrl Pts',(7.83314589120918,0.518958568528469,4.21595528072725));
#29823=CARTESIAN_POINT('Ctrl Pts',(7.88086172727202,0.099029577569048,4.55330626409362));
#29824=CARTESIAN_POINT('Ctrl Pts',(7.92857756333485,-0.411839798232008,
4.38254759143289));
#29825=CARTESIAN_POINT('Ctrl Pts',(7.9762933993977,-0.544510350349916,3.86048957930736));
#29826=CARTESIAN_POINT('Ctrl Pts',(8.02400923546053,-0.177148669371157,
3.466546133148));
#29827=CARTESIAN_POINT('Ctrl Pts',(8.07172507152338,0.352891360472903,3.56248158116143));
#29828=CARTESIAN_POINT('Ctrl Pts',(8.1194409075862,0.558865824063627,4.06019692528064));
#29829=CARTESIAN_POINT('Ctrl Pts',(8.16715674364906,0.251625202160443,4.50263250666582));
#29830=CARTESIAN_POINT('Ctrl Pts',(8.21487257971187,-0.286686714637947,
4.48349292318459));
#29831=CARTESIAN_POINT('Ctrl Pts',(8.26258841577472,-0.561729810142263,
4.02035434884804));
#29832=CARTESIAN_POINT('Ctrl Pts',(8.31030425183756,-0.32092777766878,3.53852406277244));
#29833=CARTESIAN_POINT('Ctrl Pts',(8.3580200879004,0.21458717114652,3.4804742305729));
#29834=CARTESIAN_POINT('Ctrl Pts',(8.40573592396324,0.553043418849938,3.89951290636976));
#29835=CARTESIAN_POINT('Ctrl Pts',(8.45345176002607,0.383631385356639,4.41083042643994));
#29836=CARTESIAN_POINT('Ctrl Pts',(8.50116759608892,-0.13807525223727,4.54487604447167));
#29837=CARTESIAN_POINT('Ctrl Pts',(8.54888343215175,-0.532985261140852,
4.17855360686946));
#29838=CARTESIAN_POINT('Ctrl Pts',(8.59659926821459,-0.43844670370641,3.64826264467864));
#29839=CARTESIAN_POINT('Ctrl Pts',(8.64431510427743,0.0587242081113278,
3.4409775080543));
#29840=CARTESIAN_POINT('Ctrl Pts',(8.69203094034026,0.501967776032349,3.74705132745037));
#29841=CARTESIAN_POINT('Ctrl Pts',(8.73974677640311,0.484246611455832,4.28541180496438));
#29842=CARTESIAN_POINT('Ctrl Pts',(8.78746261246592,0.021834332487559,4.56167423035448));
#29843=CARTESIAN_POINT('Ctrl Pts',(8.83517844852879,-0.460628749968427,
4.32214256754115));
#29844=CARTESIAN_POINT('Ctrl Pts',(8.88289428459161,-0.520089363644054,
3.78678242815423));
#29845=CARTESIAN_POINT('Ctrl Pts',(8.93061012065447,-0.101943912081849,
3.44722326576734));
#29846=CARTESIAN_POINT('Ctrl Pts',(8.97832595671729,0.409818202553832,3.61528748398963));
#29847=CARTESIAN_POINT('Ctrl Pts',(9.02604179278014,0.545237955920739,4.1366391252272));
#29848=CARTESIAN_POINT('Ctrl Pts',(9.07375762884296,0.179957304801303,4.53251295530543));
#29849=CARTESIAN_POINT('Ctrl Pts',(9.12147346490582,-0.350580908316224,
4.43937194476168));
#29850=CARTESIAN_POINT('Ctrl Pts',(9.16918930096864,-0.559175278946307,
3.94274891673689));
#29851=CARTESIAN_POINT('Ctrl Pts',(9.21690513703149,-0.254270386902387,
3.49870043939378));
#29852=CARTESIAN_POINT('Ctrl Pts',(9.26462097309432,0.284134913886797,3.51500306204057));
#29853=CARTESIAN_POINT('Ctrl Pts',(9.31233680915716,0.56161475127612,3.97668583545263));
#29854=CARTESIAN_POINT('Ctrl Pts',(9.36005264522,0.323355121014866,4.45977836490307));
#29855=CARTESIAN_POINT('Ctrl Pts',(9.40776848128284,-0.211846492332409,
4.52064934726353));
#29856=CARTESIAN_POINT('Ctrl Pts',(9.45548431734568,-0.552506212093558,
4.10340002281193));
#29857=CARTESIAN_POINT('Ctrl Pts',(9.50320015340851,-0.385790975888367,
3.59119686639829));
#29858=CARTESIAN_POINT('Ctrl Pts',(9.55091598947136,0.135202049632292,3.45440391781584));
#29859=CARTESIAN_POINT('Ctrl Pts',(9.59863182553417,0.532036952624682,3.81864024657791));
#29860=CARTESIAN_POINT('Ctrl Pts',(9.64634766159704,0.440294135581046,4.34942202748599));
#29861=CARTESIAN_POINT('Ctrl Pts',(9.69406349765985,-0.0557775609627595,
4.55932418400469));
#29862=CARTESIAN_POINT('Ctrl Pts',(9.74177933372271,-0.500627865026369,
4.25559033604309));
#29863=CARTESIAN_POINT('Ctrl Pts',(9.78949516978553,-0.485743897486414,
3.71714394973028));
#29864=CARTESIAN_POINT('Ctrl Pts',(9.83721100584839,-0.0247938347541151,
3.43844862667992));
#29865=CARTESIAN_POINT('Ctrl Pts',(9.88492684191122,0.458924787935076,3.67543457032792));
#29866=CARTESIAN_POINT('Ctrl Pts',(9.93264267797406,0.521205716397956,4.21047394212484));
#29867=CARTESIAN_POINT('Ctrl Pts',(9.98035851403688,0.104855415711801,4.55223185431066));
#29868=CARTESIAN_POINT('Ctrl Pts',(10.0280743500997,-0.407785226630454,
4.3868667575037));
#29869=CARTESIAN_POINT('Ctrl Pts',(10.0757901861625,-0.54595042077573,3.86623596457089));
#29870=CARTESIAN_POINT('Ctrl Pts',(10.1235060222254,-0.182760942995651,
3.46844274359687));
#29871=CARTESIAN_POINT('Ctrl Pts',(10.1712218582882,0.34826072087591,3.55878673023755));
#29872=CARTESIAN_POINT('Ctrl Pts',(10.2189376943511,0.559469206087141,4.05430365143988));
#29873=CARTESIAN_POINT('Ctrl Pts',(10.2666535304139,0.256908510808291,4.49995269395588));
#29874=CARTESIAN_POINT('Ctrl Pts',(10.3143693664768,-0.281575222991369,
4.4864874848512));
#29875=CARTESIAN_POINT('Ctrl Pts',(10.3620852025396,-0.561484096926345,
4.02627333283551));
#29876=CARTESIAN_POINT('Ctrl Pts',(10.4098010386024,-0.325773485110519,
3.5419319750098));
#29877=CARTESIAN_POINT('Ctrl Pts',(10.4575168746653,0.209099930751681,3.47824153281512));
#29878=CARTESIAN_POINT('Ctrl Pts',(10.5052327107281,0.55195366278862,3.89368991932227));
#29879=CARTESIAN_POINT('Ctrl Pts',(10.552948546791,0.387939853388008,4.40676448870664));
#29880=CARTESIAN_POINT('Ctrl Pts',(10.6006643828538,-0.13232509260073,4.54630096923553));
#29881=CARTESIAN_POINT('Ctrl Pts',(10.6483802189166,-0.531073869970951,
4.18416086379456));
#29882=CARTESIAN_POINT('Ctrl Pts',(10.6960960549795,-0.442129340924997,
3.6529030034519));
#29883=CARTESIAN_POINT('Ctrl Pts',(10.7438118910423,0.0528293649267388,
3.44038965581316));
#29884=CARTESIAN_POINT('Ctrl Pts',(10.7915277271051,0.499274052081986,3.74177509795313));
#29885=CARTESIAN_POINT('Ctrl Pts',(10.839243563168,0.487227694891584,4.28029244094358));
#29886=CARTESIAN_POINT('Ctrl Pts',(10.8869593992308,0.0277526485205102,
4.56141292256198));
#29887=CARTESIAN_POINT('Ctrl Pts',(10.9346752352937,-0.457208082016334,
4.32697927894352));
#29888=CARTESIAN_POINT('Ctrl Pts',(10.9823910713565,-0.522307595786967,
3.79227553224832));
#29889=CARTESIAN_POINT('Ctrl Pts',(11.0301069074193,-0.107764007611043,
3.44832836054127));
#29890=CARTESIAN_POINT('Ctrl Pts',(11.0778227434822,0.405740926916492,3.61098974390844));
#29891=CARTESIAN_POINT('Ctrl Pts',(11.125538579545,0.54664772512998,4.13088523113667));
#29892=CARTESIAN_POINT('Ctrl Pts',(11.1732544156078,0.185559506100192,4.53058679668394));
#29893=CARTESIAN_POINT('Ctrl Pts',(11.2209702516707,-0.345930862581405,
4.4430423427091));
#29894=CARTESIAN_POINT('Ctrl Pts',(11.2686860877335,-0.559747597323992,
3.94864528834179));
#29895=CARTESIAN_POINT('Ctrl Pts',(11.3164019237964,-0.259539500620097,
3.50140805588402));
#29896=CARTESIAN_POINT('Ctrl Pts',(11.3641177598592,0.279007713031768,3.51203547753114));
#29897=CARTESIAN_POINT('Ctrl Pts',(11.411833595922,0.561337850721073,3.97076822846069));
#29898=CARTESIAN_POINT('Ctrl Pts',(11.4595494319849,0.328182802800164,4.45634496498341));
#29899=CARTESIAN_POINT('Ctrl Pts',(11.5072652680477,-0.206347562673641,
4.52285309839201));
#29900=CARTESIAN_POINT('Ctrl Pts',(11.5549811041106,-0.551385786278872,
4.10921718641821));
#29901=CARTESIAN_POINT('Ctrl Pts',(11.6026969401734,-0.390077958183356,
3.59528545163414));
#29902=CARTESIAN_POINT('Ctrl Pts',(11.6504127762362,0.129444461032819,3.45300931394821));
#29903=CARTESIAN_POINT('Ctrl Pts',(11.6981286122991,0.530096039923511,3.8130431397972));
#29904=CARTESIAN_POINT('Ctrl Pts',(11.7458444483619,0.443952268776438,4.34476232707146));
#29905=CARTESIAN_POINT('Ctrl Pts',(11.7935602844247,-0.0498797018717475,
4.55988096454574));
#29906=CARTESIAN_POINT('Ctrl Pts',(11.8412761204876,-0.497906374793238,
4.26085229740167));
#29907=CARTESIAN_POINT('Ctrl Pts',(11.8889919565504,-0.48869796246776,3.72227895182515));
#29908=CARTESIAN_POINT('Ctrl Pts',(11.9367077926133,-0.0307106916234339,
3.43874111807518));
#29909=CARTESIAN_POINT('Ctrl Pts',(11.9844236286761,0.455478679883424,3.67061595167475));
#29910=CARTESIAN_POINT('Ctrl Pts',(12.0321394647389,0.523394971212992,4.20496922507643));
#29911=CARTESIAN_POINT('Ctrl Pts',(12.0798553008018,0.110669607010866,4.5510961052335));
#29912=CARTESIAN_POINT('Ctrl Pts',(12.1275711368646,-0.403685360180124,
4.39114295225112));
#29913=CARTESIAN_POINT('Ctrl Pts',(12.1752869729274,-0.547329849620031,
3.8719972077086));
#29914=CARTESIAN_POINT('Ctrl Pts',(12.2230028089903,-0.188352916401613,
3.4703983969034));
#29915=CARTESIAN_POINT('Ctrl Pts',(12.2707186450531,0.34359139813055,3.55514088718992));
#29916=CARTESIAN_POINT('Ctrl Pts',(12.318434481116,0.560010444926212,4.04840434580723));
#29917=CARTESIAN_POINT('Ctrl Pts',(12.3661503171788,0.262163283277844,4.49721734887317));
#29918=CARTESIAN_POINT('Ctrl Pts',(12.4138661532417,-0.276432455305192,
4.48942800979656));
#29919=CARTESIAN_POINT('Ctrl Pts',(12.4615819893045,-0.561176016721412,
4.03218939850585));
#29920=CARTESIAN_POINT('Ctrl Pts',(12.5092978253673,-0.330583007179444,
3.54539076726965));
#29921=CARTESIAN_POINT('Ctrl Pts',(12.5570136614301,0.203589464528802,3.47606678951191));
#29922=CARTESIAN_POINT('Ctrl Pts',(12.604729497493,0.550802598333678,3.88787874069406));
#29923=CARTESIAN_POINT('Ctrl Pts',(12.6524453335558,0.392205230901379,4.40265336950419));
#29924=CARTESIAN_POINT('Ctrl Pts',(12.7001611696187,-0.126560234920843,
4.54766521348015));
#29925=CARTESIAN_POINT('Ctrl Pts',(12.7478770056815,-0.529103489635726,
4.18974766500481));
#29926=CARTESIAN_POINT('Ctrl Pts',(12.7955928417443,-0.44576286851447,3.65758191611243));
#29927=CARTESIAN_POINT('Ctrl Pts',(12.8433086778072,0.0469286537069902,
3.43986396243348));
#29928=CARTESIAN_POINT('Ctrl Pts',(12.89102451387,0.496524871139168,3.73652755085263));
#29929=CARTESIAN_POINT('Ctrl Pts',(12.9387403499328,0.490154659387074,4.27514194336855));
#29930=CARTESIAN_POINT('Ctrl Pts',(12.9864561859957,0.0336678819209607,
4.56108925568614));
#29931=CARTESIAN_POINT('Ctrl Pts',(13.0341720220585,-0.45373662956012,4.33177967103923));
#29932=CARTESIAN_POINT('Ctrl Pts',(13.0818878581214,-0.524467812480695,
3.79779170939055));
#29933=CARTESIAN_POINT('Ctrl Pts',(13.1296036941842,-0.113572133225654,
3.44949473238301));
#29934=CARTESIAN_POINT('Ctrl Pts',(13.177319530247,0.401618583502394,3.60673521324049));
#29935=CARTESIAN_POINT('Ctrl Pts',(13.2250353663099,0.547996775303968,4.12511679893576));
#29936=CARTESIAN_POINT('Ctrl Pts',(13.2727512023727,0.191141096329688,4.52860170299893));
#29937=CARTESIAN_POINT('Ctrl Pts',(13.3204670384356,-0.341242392487953,
4.4466635296155));
#29938=CARTESIAN_POINT('Ctrl Pts',(13.3681828744984,-0.560257741594785,
3.95454736418435));
#29939=CARTESIAN_POINT('Ctrl Pts',(13.4158987105612,-0.264779785921688,
3.5041710536014));
#29940=CARTESIAN_POINT('Ctrl Pts',(13.4636145466241,0.273849521323983,3.50912209380529));
#29941=CARTESIAN_POINT('Ctrl Pts',(13.5113303826869,0.560998599421335,3.96485386839523));
#29942=CARTESIAN_POINT('Ctrl Pts',(13.5590462187498,0.332974031597074,4.45286087643057));
#29943=CARTESIAN_POINT('Ctrl Pts',(13.6067620548126,-0.200825712906817,
4.52499877347948));
#29944=CARTESIAN_POINT('Ctrl Pts',(13.6544778908754,-0.550204115147588,
4.11502221869768));
#29945=CARTESIAN_POINT('Ctrl Pts',(13.7021937269383,-0.394321612469819,
3.5994189906415));
#29946=CARTESIAN_POINT('Ctrl Pts',(13.7499095630011,0.123672494356884,3.45167546721031));
#29947=CARTESIAN_POINT('Ctrl Pts',(13.7976253990639,0.528096246669736,3.80746679929733));
#29948=CARTESIAN_POINT('Ctrl Pts',(13.8453412351268,0.44756108986054,4.34006433209368));
#29949=CARTESIAN_POINT('Ctrl Pts',(13.8930570711896,-0.0439763023801491,
4.56037555616609));
#29950=CARTESIAN_POINT('Ctrl Pts',(13.9407729072525,-0.495129579482757,
4.26608528452492));
#29951=CARTESIAN_POINT('Ctrl Pts',(13.9884887433153,-0.491597745198497,
3.72744480185615));
#29952=CARTESIAN_POINT('Ctrl Pts',(14.0362045793781,-0.0366241372948624,
3.43909595144367));
#29953=CARTESIAN_POINT('Ctrl Pts',(14.083920415441,0.451981979421435,3.66583391943861));
#29954=CARTESIAN_POINT('Ctrl Pts',(14.1316362515038,0.525526089798339,4.19944174101915));
#29955=CARTESIAN_POINT('Ctrl Pts',(14.1793520875667,0.11647150565515,4.54989914301615));
#29956=CARTESIAN_POINT('Ctrl Pts',(14.2270679236295,-0.399540654275635,
4.39537570069553));
#29957=CARTESIAN_POINT('Ctrl Pts',(14.2747837596924,-0.548648483661927,
3.87777266878906));
#29958=CARTESIAN_POINT('Ctrl Pts',(14.3224995957551,-0.193923968459428,
3.47241287584284));
#29959=CARTESIAN_POINT('Ctrl Pts',(14.370215431818,0.338883910883161,3.5515444569815));
#29960=CARTESIAN_POINT('Ctrl Pts',(14.4179312678808,0.560489480462528,4.04249966364955));
#29961=CARTESIAN_POINT('Ctrl Pts',(14.4656471039437,0.267388935893957,4.49442677524682));
#29962=CARTESIAN_POINT('Ctrl Pts',(14.5133629400065,-0.271258982813659,
4.49231417140114));
#29963=CARTESIAN_POINT('Ctrl Pts',(14.5610787760694,-0.560805603747543,
4.03810188873054));
#29964=CARTESIAN_POINT('Ctrl Pts',(14.6087946121322,-0.335355809656676,
3.54890005536578));
#29965=CARTESIAN_POINT('Ctrl Pts',(14.656510448195,0.198056384554314,3.47395024222346));
#29966=CARTESIAN_POINT('Ctrl Pts',(14.7042262842579,0.549590353339887,3.88208001596329));
#29967=CARTESIAN_POINT('Ctrl Pts',(14.7519421203207,0.396427044118869,4.3984975254762));
#29968=CARTESIAN_POINT('Ctrl Pts',(14.7996579563836,-0.120781319530639,
4.54896862567174));
#29969=CARTESIAN_POINT('Ctrl Pts',(14.8473737924464,-0.527074338995675,
4.19531338994486));
#29970=CARTESIAN_POINT('Ctrl Pts',(14.8950896285092,-0.449346882879826,
3.66229886294881));
#29971=CARTESIAN_POINT('Ctrl Pts',(14.9428054645721,0.041022729875082,3.43940048630678));
#29972=CARTESIAN_POINT('Ctrl Pts',(14.9905213006349,0.493720538569869,3.73130926902151));
#29973=CARTESIAN_POINT('Ctrl Pts',(15.0382371366977,0.493027179828974,4.2699608843321));
#29974=CARTESIAN_POINT('Ctrl Pts',(15.0859529727606,0.0395793756528551,
4.56070326567839));
#29975=CARTESIAN_POINT('Ctrl Pts',(15.1336688088234,-0.450214778192253,
4.33654321062351));
#29976=CARTESIAN_POINT('Ctrl Pts',(15.1813846448863,-0.526569773778615,
3.80333034687015));
#29977=CARTESIAN_POINT('Ctrl Pts',(15.2291004809491,-0.119367643786657,
3.45072225173751));
#29978=CARTESIAN_POINT('Ctrl Pts',(15.2768163170119,0.397451630201876,3.60252436455885));
#29979=CARTESIAN_POINT('Ctrl Pts',(15.3245321530748,0.549284956596614,4.11933446935456));
#29980=CARTESIAN_POINT('Ctrl Pts',(15.3722479891376,0.196701455513243,4.52655789474516));
#29981=CARTESIAN_POINT('Ctrl Pts',(15.4199638252005,-0.336516018808871,
4.45023510325662));
#29982=CARTESIAN_POINT('Ctrl Pts',(15.4676796612633,-0.560705655094284,
3.96045448869));
#29983=CARTESIAN_POINT('Ctrl Pts',(15.5153954973261,-0.269990660741143,
3.50698912564524));
#29984=CARTESIAN_POINT('Ctrl Pts',(15.5631113333889,0.268660911710894,3.50626323446785));
#29985=CARTESIAN_POINT('Ctrl Pts',(15.6108271694518,0.560597035059331,3.95894341219528));
#29986=CARTESIAN_POINT('Ctrl Pts',(15.6585430055146,0.337728275218647,4.44932648624059));
#29987=CARTESIAN_POINT('Ctrl Pts',(15.7062588415775,-0.1952815563728,4.52708613419449));
#29988=CARTESIAN_POINT('Ctrl Pts',(15.7539746776403,-0.548961329954127,
4.12081447485494));
#29989=CARTESIAN_POINT('Ctrl Pts',(15.8016905137031,-0.398521467382777,
3.60359702428645));
#29990=CARTESIAN_POINT('Ctrl Pts',(15.849406349766,0.117886790727162,3.4504025257595));
#29991=CARTESIAN_POINT('Ctrl Pts',(15.8971221858288,0.526037794990907,3.80191184447176));
#29992=CARTESIAN_POINT('Ctrl Pts',(15.9448380218916,0.451120197982628,4.33532856438364));
#29993=CARTESIAN_POINT('Ctrl Pts',(15.9925538579545,-0.0380680182095728,
4.56080790392885));
#29994=CARTESIAN_POINT('Ctrl Pts',(16.0402696940173,-0.492297787528177,
4.27128871615743));
#29995=CARTESIAN_POINT('Ctrl Pts',(16.0879855300802,-0.494442923584513,
3.73264092602517));
#29996=CARTESIAN_POINT('Ctrl Pts',(16.135701366143,-0.0425335149309099,
3.43951308737216));
#29997=CARTESIAN_POINT('Ctrl Pts',(16.1834172022058,0.448435074945997,3.66108900478495));
#29998=CARTESIAN_POINT('Ctrl Pts',(16.2311330382687,0.52759883543946,4.19389210391969));
#29999=CARTESIAN_POINT('Ctrl Pts',(16.2788488743315,0.122260467197297,4.54864110061148));
#30000=CARTESIAN_POINT('Ctrl Pts',(16.3265647103944,-0.395351569291248,
4.39956453268331));
#30001=CARTESIAN_POINT('Ctrl Pts',(16.3742805464572,-0.549906176433804,
3.88356170630145));
#30002=CARTESIAN_POINT('Ctrl Pts',(16.42199638252,-0.199473480363076,3.47448595665642));
#30003=CARTESIAN_POINT('Ctrl Pts',(16.4697122185829,0.334138782019088,3.54799783908671));
#30004=CARTESIAN_POINT('Ctrl Pts',(16.5174280546457,0.560906259487099,4.0365902608309));
#30005=CARTESIAN_POINT('Ctrl Pts',(16.5651438907085,0.272584888215931,4.49158128304055));
#30006=CARTESIAN_POINT('Ctrl Pts',(16.6128597267714,-0.26605538016154,4.49514564908375));
#30007=CARTESIAN_POINT('Ctrl Pts',(16.6605755628342,-0.560372899148451,
4.04401014677825));
#30008=CARTESIAN_POINT('Ctrl Pts',(16.7082913988971,-0.340091362401967,
3.55245944950311));
#30009=CARTESIAN_POINT('Ctrl Pts',(16.7560072349599,0.19250130541649,3.4718921260458));
#30010=CARTESIAN_POINT('Ctrl Pts',(16.8037230710227,0.548317062457662,3.87629438922476));
#30011=CARTESIAN_POINT('Ctrl Pts',(16.8514389070856,0.400604824101502,4.39429741823411));
#30012=CARTESIAN_POINT('Ctrl Pts',(16.8991547431484,-0.114988988324618,
4.55021106103346));
#30013=CARTESIAN_POINT('Ctrl Pts',(16.9468705792113,-0.524986643439221,
4.20085742040038));
#30014=CARTESIAN_POINT('Ctrl Pts',(16.9945864152741,-0.45288098592576,3.66705332002498));
#30015=CARTESIAN_POINT('Ctrl Pts',(17.0423022513369,0.0351122494330066,
3.4389992789138));
#30016=CARTESIAN_POINT('Ctrl Pts',(17.0900180873998,0.490861365866046,3.72612083208173));
#30017=CARTESIAN_POINT('Ctrl Pts',(17.1377339234626,0.49584493715134,4.26474983932169));
#30018=CARTESIAN_POINT('Ctrl Pts',(17.1854497595254,0.0454864730955262,
4.56025499541263));
#30019=CARTESIAN_POINT('Ctrl Pts',(17.2331655955883,-0.446642919103261,
4.34126936858499));
#30020=CARTESIAN_POINT('Ctrl Pts',(17.2808814316511,-0.528613246204851,
3.80889082948154));
#30021=CARTESIAN_POINT('Ctrl Pts',(17.328597267714,-0.125149895556227,3.45201078225777));
#30022=CARTESIAN_POINT('Ctrl Pts',(17.3763131037768,0.393240529860342,3.59835766558462));
#30023=CARTESIAN_POINT('Ctrl Pts',(17.4240289398397,0.55051212592285,4.1135388846668));
#30024=CARTESIAN_POINT('Ctrl Pts',(17.4717447759024,0.202239966032548,4.52445559893916));
#30025=CARTESIAN_POINT('Ctrl Pts',(17.5194606119653,-0.331752266527324,
4.45375666691904));
#30026=CARTESIAN_POINT('Ctrl Pts',(17.5671764480281,-0.561091288070378,
3.96636600572338));
#30027=CARTESIAN_POINT('Ctrl Pts',(17.614892284091,-0.275171546279217,3.50986195899749));
#30028=CARTESIAN_POINT('Ctrl Pts',(17.6626081201538,0.263442460518632,3.50345921706735));
#30029=CARTESIAN_POINT('Ctrl Pts',(17.7103239562167,0.560133202238927,3.95303751636628));
#30030=CARTESIAN_POINT('Ctrl Pts',(17.7580397922795,0.342445005586054,4.44574218699675));
#30031=CARTESIAN_POINT('Ctrl Pts',(17.8057556283423,-0.189715708890181,
4.52911494868296));
#30032=CARTESIAN_POINT('Ctrl Pts',(17.8534714644052,-0.547657568741173,
4.12659331151364));
#30033=CARTESIAN_POINT('Ctrl Pts',(17.901187300468,-0.402677056422281,3.60781908849286));
#30034=CARTESIAN_POINT('Ctrl Pts',(17.9489031365308,0.112087992792125,3.44919063098808));
#30035=CARTESIAN_POINT('Ctrl Pts',(17.9966189725937,0.523920913530056,3.79637889233847));
#30036=CARTESIAN_POINT('Ctrl Pts',(18.0443348086565,0.454629197813879,4.33055554996792));
#30037=CARTESIAN_POINT('Ctrl Pts',(18.0920506447194,-0.0321555056241734,
4.56117795981091));
#30038=CARTESIAN_POINT('Ctrl Pts',(18.1397664807822,-0.489411313471489,
4.27646201432672));
#30039=CARTESIAN_POINT('Ctrl Pts',(18.1874823168451,-0.497233181596917,
3.73786674717144));
#30040=CARTESIAN_POINT('Ctrl Pts',(18.2351981529079,-0.0484381681459794,
3.43999247952716));
#30041=CARTESIAN_POINT('Ctrl Pts',(18.2829139889707,0.444838360430441,3.65638173475637));
#30042=CARTESIAN_POINT('Ctrl Pts',(18.3306298250336,0.529612977905601,4.18832093020544));
#30043=CARTESIAN_POINT('Ctrl Pts',(18.3783456610964,0.128035848626906,4.54732211775687));
#30044=CARTESIAN_POINT('Ctrl Pts',(18.4260614971592,-0.391118570530631,
4.40370898293889));
#30045=CARTESIAN_POINT('Ctrl Pts',(18.4737773332221,-0.551102788237131,
3.88936367722697));
#30046=CARTESIAN_POINT('Ctrl Pts',(18.5214931692849,-0.205000835699102,
3.47661740907615));
#30047=CARTESIAN_POINT('Ctrl Pts',(18.5692090053478,0.329356538604741,3.54450142744705));
#30048=CARTESIAN_POINT('Ctrl Pts',(18.6169248414106,0.561260735706054,4.03067679373969));
#30049=CARTESIAN_POINT('Ctrl Pts',(18.6646406774734,0.2777505631021,4.48868118831814));
#30050=CARTESIAN_POINT('Ctrl Pts',(18.7123565135363,-0.260822225340423,
4.49792212833724));
#30051=CARTESIAN_POINT('Ctrl Pts',(18.7600723495991,-0.559877950986752,
4.04991351638789));
#30052=CARTESIAN_POINT('Ctrl Pts',(18.8077881856619,-0.344789139412875,
3.55606855432066));
#30053=CARTESIAN_POINT('Ctrl Pts',(18.8555040217248,0.186924844147682,3.46989266958543));
#30054=CARTESIAN_POINT('Ctrl Pts',(18.9032198577876,0.546982867117114,3.87052250311704));
#30055=CARTESIAN_POINT('Ctrl Pts',(18.9509356938504,0.404738106803207,4.39005351430856));
#30056=CARTESIAN_POINT('Ctrl Pts',(18.9986515299133,-0.109183884691052,
4.55139238155646));
#30057=CARTESIAN_POINT('Ctrl Pts',(19.0463673659761,-0.522840634850846,
4.20637914057629));
#30058=CARTESIAN_POINT('Ctrl Pts',(19.094083202039,-0.456364785113784,3.67184475922049));
#30059=CARTESIAN_POINT('Ctrl Pts',(19.1417990381018,0.029197868913272,3.43866038485254));
#30060=CARTESIAN_POINT('Ctrl Pts',(19.1895148741647,0.487947670564988,3.72096281627648));
#30061=CARTESIAN_POINT('Ctrl Pts',(19.2372307102275,0.498607618457993,4.25950938727589));
#30062=CARTESIAN_POINT('Ctrl Pts',(19.2849465462903,0.0513885179525073,
4.55974449445321));
#30063=CARTESIAN_POINT('Ctrl Pts',(19.3326623823531,-0.44302144872845,4.34595762039384));
#30064=CARTESIAN_POINT('Ctrl Pts',(19.380378218416,-0.530598003365269,3.81447253878192));
#30065=CARTESIAN_POINT('Ctrl Pts',(19.4280940544788,-0.130918245164485,
3.45336018235082));
#30066=CARTESIAN_POINT('Ctrl Pts',(19.4758098905417,0.38898574814073,3.59423557624425));
#30067=CARTESIAN_POINT('Ctrl Pts',(19.5235257266045,0.551678150913516,4.10773069407674));
#30068=CARTESIAN_POINT('Ctrl Pts',(19.5712415626673,0.207756005258534,4.52229503878775));
#30069=CARTESIAN_POINT('Ctrl Pts',(19.6189573987302,-0.326951650734615,
4.4572278489044));
#30070=CARTESIAN_POINT('Ctrl Pts',(19.666673234793,-0.561414624206118,3.9722812219163));
#30071=CARTESIAN_POINT('Ctrl Pts',(19.7143890708559,-0.280321816997631,
3.51278930393937));
#30072=CARTESIAN_POINT('Ctrl Pts',(19.7621049069187,0.258194652845487,3.5007102220535));
#30073=CARTESIAN_POINT('Ctrl Pts',(19.8098207429815,0.559607330995945,3.94713708427543));
#30074=CARTESIAN_POINT('Ctrl Pts',(19.8575365790444,0.347123361713752,4.44210790974427));
#30075=CARTESIAN_POINT('Ctrl Pts',(19.9052524151072,-0.184128152223511,
4.53108587353909));
#30076=CARTESIAN_POINT('Ctrl Pts',(19.9529682511701,-0.546294178096705,
4.13235642149579));
#30077=CARTESIAN_POINT('Ctrl Pts',(20.0006840872329,-0.406785648814185,
3.61208785870539));
#30078=CARTESIAN_POINT('Ctrl Pts',(20.0483999232957,0.106272459957556,3.44803398021027));
#30079=CARTESIAN_POINT('Ctrl Pts',(20.0961157593586,0.5217539278249,3.7908797683689));
#30080=CARTESIAN_POINT('Ctrl Pts',(20.1438315954214,0.458072423058868,4.32572464996293));
#30081=CARTESIAN_POINT('Ctrl Pts',(20.1915474314842,-0.0262105744965466,
4.56152565902554));
#30082=CARTESIAN_POINT('Ctrl Pts',(20.2392632675471,-0.486524960252488,
4.28152908133109));
#30083=CARTESIAN_POINT('Ctrl Pts',(20.2869791036099,-0.499865224545849,
3.74326461201656));
#30084=CARTESIAN_POINT('Ctrl Pts',(20.3346949396728,-0.0545328049175168,
3.440261547834));
#30085=CARTESIAN_POINT('Ctrl Pts',(20.3824107757356,0.441568512678419,3.6522489094147));
#30086=CARTESIAN_POINT('Ctrl Pts',(20.4221739724547,0.515928418030698,4.09332268501583));
#30087=CARTESIAN_POINT('Ctrl Pts',(20.4539845298298,0.333108474939506,4.36566768059473));
#30088=CARTESIAN_POINT('Ctrl Pts',(20.4778424478613,0.118510552090848,4.48142006140068));
#30089=CARTESIAN_POINT('Ctrl Pts',(20.5017003658927,-0.127372553428812,
4.47887124859312));
#30090=CARTESIAN_POINT('Ctrl Pts',(20.5255582839241,-0.340862259689409,
4.35954554232165));
#30091=CARTESIAN_POINT('Ctrl Pts',(20.5494162019555,-0.471665647836603,
4.15213005589169));
#30092=CARTESIAN_POINT('Ctrl Pts',(20.5732741199869,-0.486782001098211,
3.90760543082941));
#30093=CARTESIAN_POINT('Ctrl Pts',(20.5971320380184,-0.38305332993788,3.68562568155832));
#30094=CARTESIAN_POINT('Ctrl Pts',(20.6209899560498,-0.185558943137764,
3.54054450025879));
#30095=CARTESIAN_POINT('Ctrl Pts',(20.6448478740812,0.0572573647513246,
3.50779920733485));
#30096=CARTESIAN_POINT('Ctrl Pts',(20.6687057921126,0.28610038304352,3.59541756340761));
#30097=CARTESIAN_POINT('Ctrl Pts',(20.6925637101441,0.444969396676924,3.78196356026503));
#30098=CARTESIAN_POINT('Ctrl Pts',(20.7164216281754,0.495039040219165,4.02182741068269));
#30099=CARTESIAN_POINT('Ctrl Pts',(20.7402795462069,0.424054039808096,4.25635280284423));
#30100=CARTESIAN_POINT('Ctrl Pts',(20.7641374642383,0.249378454468877,4.42819351412177));
#30101=CARTESIAN_POINT('Ctrl Pts',(20.7879953822697,0.0137218901755031,
4.49532894963167));
#30102=CARTESIAN_POINT('Ctrl Pts',(20.8118533003011,-0.22528943893053,4.44134312218709));
#30103=CARTESIAN_POINT('Ctrl Pts',(20.8357112183326,-0.409211687104306,
4.27943679589328));
#30104=CARTESIAN_POINT('Ctrl Pts',(20.859569136364,-0.493070359673604,4.04920060553547));
#30105=CARTESIAN_POINT('Ctrl Pts',(20.8834270543954,-0.456359989112496,
3.80693350349834));
#30106=CARTESIAN_POINT('Ctrl Pts',(20.9072849724268,-0.308057122141145,
3.61187643128937));
#30107=CARTESIAN_POINT('Ctrl Pts',(20.9311428904583,-0.0844259229598539,
3.51172613733272));
#30108=CARTESIAN_POINT('Ctrl Pts',(20.9550008084896,0.159849727585384,3.53097210659131));
#30109=CARTESIAN_POINT('Ctrl Pts',(20.9788587265211,0.365037758375503,3.66490817000854));
#30110=CARTESIAN_POINT('Ctrl Pts',(21.0027166445525,0.480964117596,3.88078331455297));
#30111=CARTESIAN_POINT('Ctrl Pts',(21.026574562584,0.479281646861755,4.12581018556955));
#30112=CARTESIAN_POINT('Ctrl Pts',(21.0504324806153,0.360401759160676,4.34007303948752));
#30113=CARTESIAN_POINT('Ctrl Pts',(21.0742903986468,0.153393823636192,4.47117877170218));
#30114=CARTESIAN_POINT('Ctrl Pts',(21.0981483166782,-0.0911230798336762,
4.48706845966041));
#30115=CARTESIAN_POINT('Ctrl Pts',(21.1220062347096,-0.313357908298923,
4.38385664171252));
#30116=CARTESIAN_POINT('Ctrl Pts',(21.145864152741,-0.458968192403581,4.18678141884249));
#30117=CARTESIAN_POINT('Ctrl Pts',(21.1697220707724,-0.492348251467217,
3.94403305123036));
#30118=CARTESIAN_POINT('Ctrl Pts',(21.1935799888039,-0.405335751726616,
3.71497012710753));
#30119=CARTESIAN_POINT('Ctrl Pts',(21.2174379068353,-0.21920761957706,3.55560477096155));
#30120=CARTESIAN_POINT('Ctrl Pts',(21.2412958248667,0.0205227466613194,
3.50490615340017));
#30121=CARTESIAN_POINT('Ctrl Pts',(21.2651537428981,0.255234742309135,3.57527146741714));
#30122=CARTESIAN_POINT('Ctrl Pts',(21.2890116609295,0.427534891009427,3.74949447702405));
#30123=CARTESIAN_POINT('Ctrl Pts',(21.312869578961,0.495291113040325,3.98497291063177));
#30124=CARTESIAN_POINT('Ctrl Pts',(21.3367274969923,0.441935166474334,4.22412587691986));
#30125=CARTESIAN_POINT('Ctrl Pts',(21.3605854150238,0.280514033632862,4.40847396123464));
#30126=CARTESIAN_POINT('Ctrl Pts',(21.3844433330552,0.0504995785194436,
4.49293903542029));
#30127=CARTESIAN_POINT('Ctrl Pts',(21.4083012510867,-0.191863399122956,
4.45686708805594));
#30128=CARTESIAN_POINT('Ctrl Pts',(21.432159169118,-0.387310549425693,4.3090786928523));
#30129=CARTESIAN_POINT('Ctrl Pts',(21.4560170871495,-0.488049720266331,
4.08571213811173));
#30130=CARTESIAN_POINT('Ctrl Pts',(21.4798750051809,-0.469447440294381,
3.84138663085107));
#30131=CARTESIAN_POINT('Ctrl Pts',(21.5037329232123,-0.336052473678932,
3.63584641288874));
#30132=CARTESIAN_POINT('Ctrl Pts',(21.5275908412437,-0.120483523363382,
3.51935166631968));
#30133=CARTESIAN_POINT('Ctrl Pts',(21.5514487592752,0.124546930319796,3.5203885299332));
#30134=CARTESIAN_POINT('Ctrl Pts',(21.5753066773065,0.339122266949511,3.63870346233219));
#30135=CARTESIAN_POINT('Ctrl Pts',(21.599164595338,0.470772971804989,3.84536523971104));
#30136=CARTESIAN_POINT('Ctrl Pts',(21.6230225133694,0.487306861455871,4.08983942814686));
#30137=CARTESIAN_POINT('Ctrl Pts',(21.6468804314008,0.384680949508402,4.31234542922385));
#30138=CARTESIAN_POINT('Ctrl Pts',(21.6707383494323,0.187990066907445,4.45847446473699));
#30139=CARTESIAN_POINT('Ctrl Pts',(21.6945962674636,-0.0546695077989956,
4.49249400502822));
#30140=CARTESIAN_POINT('Ctrl Pts',(21.7184541854951,-0.283960898681086,
4.40608534582272));
#30141=CARTESIAN_POINT('Ctrl Pts',(21.7423121035264,-0.443816114896065,
4.22037775802082));
#30142=CARTESIAN_POINT('Ctrl Pts',(21.766170021558,-0.495146201710716,3.98078180541326));
#30143=CARTESIAN_POINT('Ctrl Pts',(21.7900279395893,-0.425399554695369,
3.74588522487523));
#30144=CARTESIAN_POINT('Ctrl Pts',(21.8138858576208,-0.25163112890579,3.57312662880273));
#30145=CARTESIAN_POINT('Ctrl Pts',(21.8377437756521,-0.0163320378044167,
3.50475019978512));
#30146=CARTESIAN_POINT('Ctrl Pts',(21.8616016936836,0.222960681415914,3.55747583725374));
#30147=CARTESIAN_POINT('Ctrl Pts',(21.885459611715,0.407733440703041,3.71841068663001));
#30148=CARTESIAN_POINT('Ctrl Pts',(21.9093175297464,0.492804267302335,3.94820179346412));
#30149=CARTESIAN_POINT('Ctrl Pts',(21.9331754477779,0.457371026827486,4.19065897275109));
#30150=CARTESIAN_POINT('Ctrl Pts',(21.9570333658092,0.310098111756678,4.38649483975425));
#30151=CARTESIAN_POINT('Ctrl Pts',(21.9808912838407,0.0869977614584207,
4.48782219052945));
#30152=CARTESIAN_POINT('Ctrl Pts',(22.0047492018721,-0.15737591128791,4.46986372771052));
#30153=CARTESIAN_POINT('Ctrl Pts',(22.0286071199035,-0.363266886890503,
4.33701078463543));
#30154=CARTESIAN_POINT('Ctrl Pts',(22.0524650379349,-0.480329213457224,
4.12174952472744));
#30155=CARTESIAN_POINT('Ctrl Pts',(22.0763229559664,-0.479937963428243,
3.87671718963328));
#30156=CARTESIAN_POINT('Ctrl Pts',(22.1001808739978,-0.362188808094022,
3.66183085982978));
#30157=CARTESIAN_POINT('Ctrl Pts',(22.1240387920292,-0.155874623354616,
3.529636096341));
#30158=CARTESIAN_POINT('Ctrl Pts',(22.1478967100606,0.0885551527323001,
3.51245811975107));
#30159=CARTESIAN_POINT('Ctrl Pts',(22.1717546280921,0.311330781786364,3.61449741325855));
#30160=CARTESIAN_POINT('Ctrl Pts',(22.1956125461234,0.457977554205651,3.81080259009947));
#30161=CARTESIAN_POINT('Ctrl Pts',(22.2194704641549,0.492636339578261,4.05337168730347));
#30162=CARTESIAN_POINT('Ctrl Pts',(22.2433283821863,0.406832120751761,4.28288995313029));
#30163=CARTESIAN_POINT('Ctrl Pts',(22.2671863002177,0.22154636656941,4.44323391967918));
#30164=CARTESIAN_POINT('Ctrl Pts',(22.2910442182491,-0.0179135091400202,
4.49519511936025));
#30165=CARTESIAN_POINT('Ctrl Pts',(22.3149021362805,-0.2529930437236,4.42606762362056));
#30166=CARTESIAN_POINT('Ctrl Pts',(22.338760054312,-0.426208888077552,4.25275498785448));
#30167=CARTESIAN_POINT('Ctrl Pts',(22.3626179723434,-0.495205048933098,
4.01763687303198));
#30168=CARTESIAN_POINT('Ctrl Pts',(22.3864758903748,-0.443110087468167,
3.77820606161377));
#30169=CARTESIAN_POINT('Ctrl Pts',(22.4103338084062,-0.282662637164788,
3.59300991103726));
#30170=CARTESIAN_POINT('Ctrl Pts',(22.4341917264377,-0.0530964769854286,
3.50733392083031));
#30171=CARTESIAN_POINT('Ctrl Pts',(22.458049644469,0.189453226607198,3.5421282117862));
#30172=CARTESIAN_POINT('Ctrl Pts',(22.4819075625005,0.385676439696491,3.6888846179772));
#30173=CARTESIAN_POINT('Ctrl Pts',(22.5057654805319,0.487591287867653,3.9117172269821));
#30174=CARTESIAN_POINT('Ctrl Pts',(22.5296233985634,0.470276727405835,4.15613734610506));
#30175=CARTESIAN_POINT('Ctrl Pts',(22.5534813165947,0.337966804695391,4.36237769267677));
#30176=CARTESIAN_POINT('Ctrl Pts',(22.5773392346262,0.123014588878675,4.48000670597833));
#30177=CARTESIAN_POINT('Ctrl Pts',(22.6011971526576,-0.122017660845505,
4.48026122441149));
#30178=CARTESIAN_POINT('Ctrl Pts',(22.625055070689,-0.337213993725473,4.36307837627545));
#30179=CARTESIAN_POINT('Ctrl Pts',(22.6489129887204,-0.469950950795418,
4.15711375897153));
#30180=CARTESIAN_POINT('Ctrl Pts',(22.6727709067518,-0.487774683880463,
3.912729067726));
#30181=CARTESIAN_POINT('Ctrl Pts',(22.6966288247832,-0.386319338946922,
3.6896872918462));
#30182=CARTESIAN_POINT('Ctrl Pts',(22.7204867428147,-0.190407614498503,
3.54252014522276));
#30183=CARTESIAN_POINT('Ctrl Pts',(22.7443446608461,0.0520814161336476,
3.50722927763546));
#30184=CARTESIAN_POINT('Ctrl Pts',(22.7682025788775,0.281801791424649,3.59241522467272));
#30185=CARTESIAN_POINT('Ctrl Pts',(22.7920604969089,0.442679857002608,3.77730419914427));
#30186=CARTESIAN_POINT('Ctrl Pts',(22.8079657755965,0.477669651496365,3.93681187972983));
#30187=CARTESIAN_POINT('Ctrl Pts',(22.8159184149403,0.475016281724327,4.01593044384941));
#30188=CARTESIAN_POINT('Ctrl Pts',(3.98408158505964,0.229225853138217,4.48306385360099));
#30189=CARTESIAN_POINT('Ctrl Pts',(3.99203422440344,0.148766887950233,4.52124364039387));
#30190=CARTESIAN_POINT('Ctrl Pts',(4.00793950309106,-0.0315132651739855,
4.55658776856145));
#30191=CARTESIAN_POINT('Ctrl Pts',(4.03179742112247,-0.29437836981663,4.47338935048851));
#30192=CARTESIAN_POINT('Ctrl Pts',(4.0556553391539,-0.485191777607318,4.27448557757091));
#30193=CARTESIAN_POINT('Ctrl Pts',(4.07951325718531,-0.557397168683185,
4.00843674174317));
#30194=CARTESIAN_POINT('Ctrl Pts',(4.10337117521674,-0.493285636019562,
3.74033843218029));
#30195=CARTESIAN_POINT('Ctrl Pts',(4.12722909324815,-0.308561908987092,
3.53572729771651));
#30196=CARTESIAN_POINT('Ctrl Pts',(4.15108701127957,-0.0483813190761145,
3.44464727048097));
#30197=CARTESIAN_POINT('Ctrl Pts',(4.17494492931099,0.223627135909104,3.48936410886239));
#30198=CARTESIAN_POINT('Ctrl Pts',(4.19880284734241,0.440954086798485,3.65894639349553));
#30199=CARTESIAN_POINT('Ctrl Pts',(4.22266076537383,0.55045499896491,3.91192501290154));
#30200=CARTESIAN_POINT('Ctrl Pts',(4.24651868340524,0.525355068663259,4.18644066347397));
#30201=CARTESIAN_POINT('Ctrl Pts',(4.27037660143667,0.371791302444591,4.41536633561891));
#30202=CARTESIAN_POINT('Ctrl Pts',(4.29423451946808,0.127314547262185,4.54272370785395));
#30203=CARTESIAN_POINT('Ctrl Pts',(4.31809243749951,-0.14829414195428,4.5373703057994));
#30204=CARTESIAN_POINT('Ctrl Pts',(4.34195035553092,-0.387640842632661,
4.40061524972397));
#30205=CARTESIAN_POINT('Ctrl Pts',(4.36580827356235,-0.53219881478122,4.16589884014724));
#30206=CARTESIAN_POINT('Ctrl Pts',(4.38966619159376,-0.546619671109945,
3.89061565172978));
#30207=CARTESIAN_POINT('Ctrl Pts',(4.41352410962518,-0.427377132892538,
3.64207991255526));
#30208=CARTESIAN_POINT('Ctrl Pts',(4.4373820276566,-0.203629241694984,3.48106538615089));
#30209=CARTESIAN_POINT('Ctrl Pts',(4.46123994568802,0.0699115445388116,
3.44694450735191));
#30210=CARTESIAN_POINT('Ctrl Pts',(4.48509786371944,0.326357054473012,3.54806076195131));
#30211=CARTESIAN_POINT('Ctrl Pts',(4.50895578175085,0.502999374434197,3.7596884705576));
#30212=CARTESIAN_POINT('Ctrl Pts',(4.53281369978229,0.556644646112557,4.03007889421215));
#30213=CARTESIAN_POINT('Ctrl Pts',(4.55667161781369,0.474175139017821,4.29311420882242));
#30214=CARTESIAN_POINT('Ctrl Pts',(4.58052953584512,0.275756894216243,4.48447511514554));
#30215=CARTESIAN_POINT('Ctrl Pts',(4.60438745387653,0.00990857728296194,
4.55736865895685));
#30216=CARTESIAN_POINT('Ctrl Pts',(4.62824537190795,-0.258362656684952,
4.49397038324719));
#30217=CARTESIAN_POINT('Ctrl Pts',(4.65210328993938,-0.463457183444019,
4.30978289334447));
#30218=CARTESIAN_POINT('Ctrl Pts',(4.67596120797079,-0.555223804526532,
4.04984504770563));
#30219=CARTESIAN_POINT('Ctrl Pts',(4.69981912600221,-0.511223081411799,
3.77771873014923));
#30220=CARTESIAN_POINT('Ctrl Pts',(4.72367704403363,-0.342214389453536,
3.55994623789246));
#30221=CARTESIAN_POINT('Ctrl Pts',(4.74753496206505,-0.0895249575417115,
3.44977887729433));
#30222=CARTESIAN_POINT('Ctrl Pts',(4.77139288009647,0.185055765100279,3.47415556892044));
#30223=CARTESIAN_POINT('Ctrl Pts',(4.79525079812788,0.414385312357242,3.62711554766008));
#30224=CARTESIAN_POINT('Ctrl Pts',(4.81910871615931,0.542386363113676,3.87125593216545));
#30225=CARTESIAN_POINT('Ctrl Pts',(4.84296663419071,0.537759173780872,4.14687774817434));
#30226=CARTESIAN_POINT('Ctrl Pts',(4.86682455222215,0.401635218192884,4.38658395388507));
#30227=CARTESIAN_POINT('Ctrl Pts',(4.89068247025356,0.167300511433038,4.53175985253543));
#30228=CARTESIAN_POINT('Ctrl Pts',(4.91454038828499,-0.107943727546613,
4.54690598239331));
#30229=CARTESIAN_POINT('Ctrl Pts',(4.9383983063164,-0.356792784813018,4.42831870213619));
#30230=CARTESIAN_POINT('Ctrl Pts',(4.96225622434782,-0.518396287352312,
4.20499583203957));
#30231=CARTESIAN_POINT('Ctrl Pts',(4.98611414237924,-0.553237776802617,
3.93154589703492));
#30232=CARTESIAN_POINT('Ctrl Pts',(5.00997206041066,-0.452797559930213,
3.67483485485756));
#30233=CARTESIAN_POINT('Ctrl Pts',(5.03382997844208,-0.241636005696979,
3.49763554798826));
#30234=CARTESIAN_POINT('Ctrl Pts',(5.05768789647349,0.0286121339618079,
3.44327803376872));
#30235=CARTESIAN_POINT('Ctrl Pts',(5.08154581450492,0.291863827488053,3.52505420509465));
#30236=CARTESIAN_POINT('Ctrl Pts',(5.10540373253633,0.48374686498243,3.72296756053861));
#30237=CARTESIAN_POINT('Ctrl Pts',(5.12926165056775,0.557340616988569,3.98862289364304));
#30238=CARTESIAN_POINT('Ctrl Pts',(5.15311956859917,0.49464940648741,4.25706023915787));
#30239=CARTESIAN_POINT('Ctrl Pts',(5.17697748663059,0.311002942120779,4.46263935401832));
#30240=CARTESIAN_POINT('Ctrl Pts',(5.20083540466201,0.0513077868555636,
4.55509054477827));
#30241=CARTESIAN_POINT('Ctrl Pts',(5.22469332269342,-0.22093351989189,4.5118069769771));
#30242=CARTESIAN_POINT('Ctrl Pts',(5.24855124072485,-0.439150562917527,
4.34337266196288));
#30243=CARTESIAN_POINT('Ctrl Pts',(5.27240915875626,-0.549983331088669,
4.09097437781523));
#30244=CARTESIAN_POINT('Ctrl Pts',(5.29626707678769,-0.526330193563486,
3.81633038019944));
#30245=CARTESIAN_POINT('Ctrl Pts',(5.32012499481911,-0.373974986765411,
3.5865986076849));
#30246=CARTESIAN_POINT('Ctrl Pts',(5.34398291285052,-0.130172708829089,
3.45795473641922));
#30247=CARTESIAN_POINT('Ctrl Pts',(5.36784083088195,0.145460342249349,3.46185569711558));
#30248=CARTESIAN_POINT('Ctrl Pts',(5.39169874891335,0.385524377387638,3.59734759862366));
#30249=CARTESIAN_POINT('Ctrl Pts',(5.41555666694479,0.531317200781484,3.83129898029949));
#30250=CARTESIAN_POINT('Ctrl Pts',(5.4394145849762,0.547188495794237,4.10650235661553));
#30251=CARTESIAN_POINT('Ctrl Pts',(5.46327250300762,0.42925729847004,4.35566300567327));
#30252=CARTESIAN_POINT('Ctrl Pts',(5.48713042103904,0.206360998935678,4.51785436177788));
#30253=CARTESIAN_POINT('Ctrl Pts',(5.51098833907045,-0.0669961859988386,
4.55341622035867));
#30254=CARTESIAN_POINT('Ctrl Pts',(5.53484625710188,-0.323970978517869,
4.45365273830571));
#30255=CARTESIAN_POINT('Ctrl Pts',(5.55870417513329,-0.501726041995696,
4.2429588044862));
#30256=CARTESIAN_POINT('Ctrl Pts',(5.58256209316472,-0.556795421465071,
3.97285482490167));
#30257=CARTESIAN_POINT('Ctrl Pts',(5.60642001119613,-0.475713153578786,
3.70938858005442));
#30258=CARTESIAN_POINT('Ctrl Pts',(5.63027792922756,-0.27830606148521,3.51698474346866));
#30259=CARTESIAN_POINT('Ctrl Pts',(5.65413584725897,-0.0128455564368745,
3.44269129419766));
#30260=CARTESIAN_POINT('Ctrl Pts',(5.67799376529039,0.255756037034639,3.5046750042392));
#30261=CARTESIAN_POINT('Ctrl Pts',(5.70185168332181,0.46181831285622,3.68777916820271));
#30262=CARTESIAN_POINT('Ctrl Pts',(5.72570960135323,0.554953431393631,3.94722983012095));
#30263=CARTESIAN_POINT('Ctrl Pts',(5.74956751938465,0.512387319539865,4.21958423627784));
#30264=CARTESIAN_POINT('Ctrl Pts',(5.77342543741606,0.344528550506956,4.43824431479549));
#30265=CARTESIAN_POINT('Ctrl Pts',(5.79728335544749,0.0924231668635294,
4.54974172178225));
#30266=CARTESIAN_POINT('Ctrl Pts',(5.82114127347891,-0.182282200065281,
4.52681230129395));
#30267=CARTESIAN_POINT('Ctrl Pts',(5.84499919151032,-0.412414601109181,
4.37506292652603));
#30268=CARTESIAN_POINT('Ctrl Pts',(5.86885710954175,-0.541700403334708,
4.13160044316952));
#30269=CARTESIAN_POINT('Ctrl Pts',(5.89271502757316,-0.538525691690445,
3.85595807909033));
#30270=CARTESIAN_POINT('Ctrl Pts',(5.91657294560459,-0.403666797469215,
3.61553786496538));
#30271=CARTESIAN_POINT('Ctrl Pts',(5.94043086363599,-0.170100341263849,
3.46912915944898));
#30272=CARTESIAN_POINT('Ctrl Pts',(5.96428878166742,0.105060216979666,3.45253275189516));
#30273=CARTESIAN_POINT('Ctrl Pts',(5.98814669969884,0.354530812822036,3.5698071562788));
#30274=CARTESIAN_POINT('Ctrl Pts',(6.01200461773026,0.517308736525128,3.79227513259484));
#30275=CARTESIAN_POINT('Ctrl Pts',(6.03586253576167,0.553591019453439,4.06553805729756));
#30276=CARTESIAN_POINT('Ctrl Pts',(6.0597204537931,0.454504394384077,4.32277408438697));
#30277=CARTESIAN_POINT('Ctrl Pts',(6.08357837182452,0.244280620740535,4.50108505220882));
#30278=CARTESIAN_POINT('Ctrl Pts',(6.10743628985593,-0.0256793573627324,
4.55686330558177));
#30279=CARTESIAN_POINT('Ctrl Pts',(6.13129420788736,-0.289354484390735,
4.47648043042773));
#30280=CARTESIAN_POINT('Ctrl Pts',(6.15515212591877,-0.482285035214929,
4.27957167009689));
#30281=CARTESIAN_POINT('Ctrl Pts',(6.17901004395019,-0.557263974895364,
4.01432540012922));
#30282=CARTESIAN_POINT('Ctrl Pts',(6.20286796198161,-0.496014047041978,
3.74552825888183));
#30283=CARTESIAN_POINT('Ctrl Pts',(6.22672588001303,-0.313404643062,3.53904687299508));
#30284=CARTESIAN_POINT('Ctrl Pts',(6.25058379804445,-0.0542924323345977,
3.44511024149985));
#30285=CARTESIAN_POINT('Ctrl Pts',(6.27444171607587,0.218347115212216,3.48718178027374));
#30286=CARTESIAN_POINT('Ctrl Pts',(6.29829963410728,0.437120926894882,3.65404298137615));
#30287=CARTESIAN_POINT('Ctrl Pts',(6.32215755213871,0.549895923261456,3.90664388593688));
#30288=CARTESIAN_POINT('Ctrl Pts',(6.34601547017011,0.526573903738089,4.17995327069166));
#30289=CARTESIAN_POINT('Ctrl Pts',(6.37782602754536,0.327418726170013,4.4906154426808));
#30290=CARTESIAN_POINT('Ctrl Pts',(6.41758922426438,-0.161063729547888,
4.61146011675295));
#30291=CARTESIAN_POINT('Ctrl Pts',(6.46530506032721,-0.60205854017139,4.19446204504257));
#30292=CARTESIAN_POINT('Ctrl Pts',(6.51302089639007,-0.488859252747234,
3.59916283817905));
#30293=CARTESIAN_POINT('Ctrl Pts',(6.56073673245289,0.0725864685289804,
3.37181094029106));
#30294=CARTESIAN_POINT('Ctrl Pts',(6.60845256851574,0.567733426150434,3.72141305678318));
#30295=CARTESIAN_POINT('Ctrl Pts',(6.65616840457857,0.541332409494817,4.32680434473755));
#30296=CARTESIAN_POINT('Ctrl Pts',(6.70388424064141,0.0179179137367747,
4.6321081579338));
#30297=CARTESIAN_POINT('Ctrl Pts',(6.75160007670425,-0.522004047715759,
4.35692568061372));
#30298=CARTESIAN_POINT('Ctrl Pts',(6.79931591276708,-0.582533501572452,
3.75397902491298));
#30299=CARTESIAN_POINT('Ctrl Pts',(6.84703174882993,-0.10812839031349,3.37695395054049));
#30300=CARTESIAN_POINT('Ctrl Pts',(6.89474758489276,0.465580583415614,3.57208337966475));
#30301=CARTESIAN_POINT('Ctrl Pts',(6.9424634209556,0.611735560770294,4.16017430964564));
#30302=CARTESIAN_POINT('Ctrl Pts',(6.99017925701844,0.196126575106773,4.60117519156627));
#30303=CARTESIAN_POINT('Ctrl Pts',(7.03789509308127,-0.399589635450545,
4.49010738789885));
#30304=CARTESIAN_POINT('Ctrl Pts',(7.08561092914412,-0.628355913977057,
3.92896656470948));
#30305=CARTESIAN_POINT('Ctrl Pts',(7.13332676520695,-0.280093617253323,
3.43305676608093));
#30306=CARTESIAN_POINT('Ctrl Pts',(7.1810426012698,0.325383132256395,3.45777970086456));
#30307=CARTESIAN_POINT('Ctrl Pts',(7.22875843733263,0.632055452459012,3.98043185926557));
#30308=CARTESIAN_POINT('Ctrl Pts',(7.27647427339546,0.358301574124045,4.52105375310108));
#30309=CARTESIAN_POINT('Ctrl Pts',(7.32419010945831,-0.244486178793781,
4.58318396235269));
#30310=CARTESIAN_POINT('Ctrl Pts',(7.37190594552114,-0.622758498112341,
4.10976736853928));
#30311=CARTESIAN_POINT('Ctrl Pts',(7.41962178158399,-0.42914211350377,3.53554970961824));
#30312=CARTESIAN_POINT('Ctrl Pts',(7.46733761764681,0.158562080980748,3.38784389968312));
#30313=CARTESIAN_POINT('Ctrl Pts',(7.51505345370967,0.600656274672958,3.80229045545538));
#30314=CARTESIAN_POINT('Ctrl Pts',(7.56276928977248,0.491158570126743,4.3982967283715));
#30315=CARTESIAN_POINT('Ctrl Pts',(7.61048512583535,-0.0693776073840611,
4.62854098691609));
#30316=CARTESIAN_POINT('Ctrl Pts',(7.65820096189817,-0.566203260219877,
4.28158638589565));
#30317=CARTESIAN_POINT('Ctrl Pts',(7.70591679796101,-0.543075747198986,
3.67604667390869));
#30318=CARTESIAN_POINT('Ctrl Pts',(7.75363263402386,-0.0212334191459514,
3.36799828595259));
#30319=CARTESIAN_POINT('Ctrl Pts',(7.80134847008666,0.520107884382028,3.64032679659274));
#30320=CARTESIAN_POINT('Ctrl Pts',(7.84906430614954,0.583826114817312,4.24294874421058));
#30321=CARTESIAN_POINT('Ctrl Pts',(7.89678014221235,0.111407840683781,4.62246712177016));
#30322=CARTESIAN_POINT('Ctrl Pts',(7.94449597827521,-0.463317967772962,
4.43036436352186));
#30323=CARTESIAN_POINT('Ctrl Pts',(7.99221181433803,-0.612571757364041,
3.84305138824375));
#30324=CARTESIAN_POINT('Ctrl Pts',(8.03992765040088,-0.199291476537812,
3.39986673810663));
#30325=CARTESIAN_POINT('Ctrl Pts',(8.08764348646372,0.397001233685627,3.50779369660314));
#30326=CARTESIAN_POINT('Ctrl Pts',(8.13535932252656,0.628721602366905,4.06772127707659));
#30327=CARTESIAN_POINT('Ctrl Pts',(8.18307515858938,0.283077249469033,4.56545936678474));
#30328=CARTESIAN_POINT('Ctrl Pts',(8.23079099465223,-0.32252129731946,4.54392741926377));
#30329=CARTESIAN_POINT('Ctrl Pts',(8.27850683071506,-0.631943574151527,
4.02289855323374));
#30330=CARTESIAN_POINT('Ctrl Pts',(8.32622266677791,-0.361042343138453,
3.48084159342964));
#30331=CARTESIAN_POINT('Ctrl Pts',(8.37393850284074,0.241409626929164,3.41553578665797));
#30332=CARTESIAN_POINT('Ctrl Pts',(8.42165433890358,0.622171422023167,3.88695246013618));
#30333=CARTESIAN_POINT('Ctrl Pts',(8.46937017496642,0.431583626935426,4.46218242893131));
#30334=CARTESIAN_POINT('Ctrl Pts',(8.51708601102927,-0.155334053534803,
4.61298316164806));
#30335=CARTESIAN_POINT('Ctrl Pts',(8.56480184709209,-0.599606082522386,
4.20087202506506));
#30336=CARTESIAN_POINT('Ctrl Pts',(8.61251768315494,-0.493250619804184,
3.60429701705146));
#30337=CARTESIAN_POINT('Ctrl Pts',(8.66023351921777,0.0660644767165412,
3.37110214695249));
#30338=CARTESIAN_POINT('Ctrl Pts',(8.70794935528061,0.564711547735832,3.71543385214437));
#30339=CARTESIAN_POINT('Ctrl Pts',(8.75566519134344,0.544775315265253,4.32108702952508));
#30340=CARTESIAN_POINT('Ctrl Pts',(8.80338102740629,0.0245635283409047,
4.6318810471339));
#30341=CARTESIAN_POINT('Ctrl Pts',(8.85109686346912,-0.518205324617361,
4.36240897642002));
#30342=CARTESIAN_POINT('Ctrl Pts',(8.89881269953197,-0.585098254365674,
3.76013116628075));
#30343=CARTESIAN_POINT('Ctrl Pts',(8.9465285355948,-0.114686454236133,3.3781285970023));
#30344=CARTESIAN_POINT('Ctrl Pts',(8.99424437165764,0.461043681496376,3.56720010581811));
#30345=CARTESIAN_POINT('Ctrl Pts',(9.04196020772047,0.613390310441866,4.15371841694351));
#30346=CARTESIAN_POINT('Ctrl Pts',(9.08967604378332,0.202451179085494,4.59907474052783));
#30347=CARTESIAN_POINT('Ctrl Pts',(9.13739187984615,-0.394401985136886,
4.49429151193569));
#30348=CARTESIAN_POINT('Ctrl Pts',(9.18510771590899,-0.629069737753471,
3.93559278228048));
#30349=CARTESIAN_POINT('Ctrl Pts',(9.23282355197184,-0.28605307070895,3.43604019168954));
#30350=CARTESIAN_POINT('Ctrl Pts',(9.28053938803466,0.319650532659854,3.45438057070715));
#30351=CARTESIAN_POINT('Ctrl Pts',(9.32825522409751,0.631814133431458,3.97377166707843));
#30352=CARTESIAN_POINT('Ctrl Pts',(9.37597106016033,0.363773093762905,4.51724864514637));
#30353=CARTESIAN_POINT('Ctrl Pts',(9.4236868962232,-0.238326375276645,4.58572823348297));
#30354=CARTESIAN_POINT('Ctrl Pts',(9.47140273228601,-0.621567066777005,
4.11632457242483));
#30355=CARTESIAN_POINT('Ctrl Pts',(9.51911856834886,-0.434013156817378,
3.54009826662536));
#30356=CARTESIAN_POINT('Ctrl Pts',(9.5668344044117,0.152101713198456,3.38620679908157));
#30357=CARTESIAN_POINT('Ctrl Pts',(9.61455024047453,0.598539239598464,3.79597107236355));
#30358=CARTESIAN_POINT('Ctrl Pts',(9.66226607653739,0.495328972565208,4.39309824928265));
#30359=CARTESIAN_POINT('Ctrl Pts',(9.7099819126002,-0.0627495115905886,
4.62923725529147));
#30360=CARTESIAN_POINT('Ctrl Pts',(9.75769774866305,-0.563204153727404,
4.28753800770644));
#30361=CARTESIAN_POINT('Ctrl Pts',(9.80541358472588,-0.54645975548653,3.68178818330365));
#30362=CARTESIAN_POINT('Ctrl Pts',(9.85312942078873,-0.027892955418244,
3.36825716649128));
#30363=CARTESIAN_POINT('Ctrl Pts',(9.90084525685157,0.516288374798902,3.63486531430293));
#30364=CARTESIAN_POINT('Ctrl Pts',(9.9485610929144,0.58635414632045,4.2367822623095));
#30365=CARTESIAN_POINT('Ctrl Pts',(9.99627692897723,0.117961883057689,4.62125841547385));
#30366=CARTESIAN_POINT('Ctrl Pts',(10.0439927650401,-0.458756592493822,
4.4352234064191));
#30367=CARTESIAN_POINT('Ctrl Pts',(10.0917086011029,-0.614191830280748,
3.8495160464768));
#30368=CARTESIAN_POINT('Ctrl Pts',(10.1394244371658,-0.205605259764808,
3.40200041654811));
#30369=CARTESIAN_POINT('Ctrl Pts',(10.1871402732286,0.391791784436726,3.5036370055096));
#30370=CARTESIAN_POINT('Ctrl Pts',(10.2348561092915,0.629400404498524,4.06109136983801));
#30371=CARTESIAN_POINT('Ctrl Pts',(10.2825719453542,0.289020948539269,4.56244458923262));
#30372=CARTESIAN_POINT('Ctrl Pts',(10.3302877814171,-0.316770891622519,
4.54729628801251));
#30373=CARTESIAN_POINT('Ctrl Pts',(10.3780036174799,-0.631667147860668,
4.02955738427466));
#30374=CARTESIAN_POINT('Ctrl Pts',(10.4257194535428,-0.366493742769977,
3.48467547975859));
#30375=CARTESIAN_POINT('Ctrl Pts',(10.4734352896056,0.235236505537468,3.41302401146715));
#30376=CARTESIAN_POINT('Ctrl Pts',(10.5211511256685,0.620945451230968,3.88040162523195));
#30377=CARTESIAN_POINT('Ctrl Pts',(10.5688669617313,0.436430634585191,4.45760826680378));
#30378=CARTESIAN_POINT('Ctrl Pts',(10.6165827977941,-0.148865149148659,
4.61458619576145));
#30379=CARTESIAN_POINT('Ctrl Pts',(10.664298633857,-0.597455775834545,4.20718016452724));
#30380=CARTESIAN_POINT('Ctrl Pts',(10.7120144699198,-0.497393570532806,
3.60951740033105));
#30381=CARTESIAN_POINT('Ctrl Pts',(10.7597303059826,0.059432803973042,3.37044081575797));
#30382=CARTESIAN_POINT('Ctrl Pts',(10.8074461420455,0.56168112009921,3.70949811708754));
#30383=CARTESIAN_POINT('Ctrl Pts',(10.8551619781083,0.548129021063343,4.31532776744164));
#30384=CARTESIAN_POINT('Ctrl Pts',(10.9028778141712,0.0312216079359222,
4.63158707701274));
#30385=CARTESIAN_POINT('Ctrl Pts',(10.950593650234,-0.514357088165242,4.36785025554668));
#30386=CARTESIAN_POINT('Ctrl Pts',(10.9983094862968,-0.587593755803164,
3.7663108843084));
#30387=CARTESIAN_POINT('Ctrl Pts',(11.0460253223597,-0.12123403619496,3.37937182377895));
#30388=CARTESIAN_POINT('Ctrl Pts',(11.0937411584225,0.456456764276497,3.56236516706526));
#30389=CARTESIAN_POINT('Ctrl Pts',(11.1414569944854,0.61497629462275,4.14724531131301));
#30390=CARTESIAN_POINT('Ctrl Pts',(11.1891728305482,0.208753630990335,4.59690782052167));
#30391=CARTESIAN_POINT('Ctrl Pts',(11.236888666611,-0.389170704067994,4.49842069353791));
#30392=CARTESIAN_POINT('Ctrl Pts',(11.2846045026739,-0.629713593419695,
3.94222617449013));
#30393=CARTESIAN_POINT('Ctrl Pts',(11.3323203387367,-0.291980800545002,
3.43908624837263));
#30394=CARTESIAN_POINT('Ctrl Pts',(11.3800361747996,0.313882454172263,3.45104205114199));
#30395=CARTESIAN_POINT('Ctrl Pts',(11.4277520108624,0.631502621520784,3.96711438515144));
#30396=CARTESIAN_POINT('Ctrl Pts',(11.4754678469252,0.369204214609944,4.51338608528654));
#30397=CARTESIAN_POINT('Ctrl Pts',(11.5231836829881,-0.232140103514266,
4.58820744384271));
#30398=CARTESIAN_POINT('Ctrl Pts',(11.5708995190509,-0.620306592646703,
4.12286885598323));
#30399=CARTESIAN_POINT('Ctrl Pts',(11.6186153551137,-0.438835993107895,
3.54469790709399));
#30400=CARTESIAN_POINT('Ctrl Pts',(11.6663311911766,0.145624451261577,3.38463787584353));
#30401=CARTESIAN_POINT('Ctrl Pts',(11.7140470272394,0.596355721317347,3.78967435176932));
#30402=CARTESIAN_POINT('Ctrl Pts',(11.7617628633022,0.499444356375145,4.38785610674141));
#30403=CARTESIAN_POINT('Ctrl Pts',(11.8094786993651,-0.0561144459655822,
4.62986363095956));
#30404=CARTESIAN_POINT('Ctrl Pts',(11.8571945354279,-0.560142489144378,
4.29345769116983));
#30405=CARTESIAN_POINT('Ctrl Pts',(11.9049103714908,-0.549783065641843,
3.68756503815187));
#30406=CARTESIAN_POINT('Ctrl Pts',(11.9526262075536,-0.0345493934605723,
3.36858621802886));
#30407=CARTESIAN_POINT('Ctrl Pts',(12.0003420436164,0.512411518346294,3.62944438943981));
#30408=CARTESIAN_POINT('Ctrl Pts',(12.0480578796793,0.588817048391095,4.23058947975914));
#30409=CARTESIAN_POINT('Ctrl Pts',(12.0957737157421,0.1245028227835,4.61998070274044));
#30410=CARTESIAN_POINT('Ctrl Pts',(12.1434895518049,-0.454144260708352,
4.44003410676589));
#30411=CARTESIAN_POINT('Ctrl Pts',(12.1912053878678,-0.615743681684068,
3.85599741975318));
#30412=CARTESIAN_POINT('Ctrl Pts',(12.2389212239306,-0.211896205334937,
3.40420051794564));
#30413=CARTESIAN_POINT('Ctrl Pts',(12.2866370599935,0.386538816815474,3.49953544806202));
#30414=CARTESIAN_POINT('Ctrl Pts',(12.3343528960563,0.63000929582004,4.05445467686));
#30415=CARTESIAN_POINT('Ctrl Pts',(12.3820687321191,0.294932544534008,4.55936733800455));
#30416=CARTESIAN_POINT('Ctrl Pts',(12.429784568182,-0.310985300518122,4.55060436568669));
#30417=CARTESIAN_POINT('Ctrl Pts',(12.4775004042448,-0.631320558980542,
4.0362129322216));
#30418=CARTESIAN_POINT('Ctrl Pts',(12.5252162403077,-0.371904434015698,
3.48856660588983));
#30419=CARTESIAN_POINT('Ctrl Pts',(12.5729320763705,0.229037255191033,3.41057743478371));
#30420=CARTESIAN_POINT('Ctrl Pts',(12.6206479124333,0.619650508764677,3.87386407474765));
#30421=CARTESIAN_POINT('Ctrl Pts',(12.6683637484962,0.44122916559109,4.4529832757215));
#30422=CARTESIAN_POINT('Ctrl Pts',(12.716079584559,-0.142379709528176,4.61612096455669));
#30423=CARTESIAN_POINT('Ctrl Pts',(12.7637954206218,-0.595239106594286,
4.21346529139986));
#30424=CARTESIAN_POINT('Ctrl Pts',(12.8115112566847,-0.501481273143938,
3.61478115656484));
#30425=CARTESIAN_POINT('Ctrl Pts',(12.8592270927475,0.0527945297157079,
3.36984941301012));
#30426=CARTESIAN_POINT('Ctrl Pts',(12.9069429288104,0.558588303589165,3.70359464960132));
#30427=CARTESIAN_POINT('Ctrl Pts',(12.9546587648732,0.551421843290858,4.30953348024615));
#30428=CARTESIAN_POINT('Ctrl Pts',(13.002374600936,0.0378762195828894,4.63122295319618));
#30429=CARTESIAN_POINT('Ctrl Pts',(13.0500904369989,-0.510451719368595,
4.37325067561256));
#30430=CARTESIAN_POINT('Ctrl Pts',(13.0978062730617,-0.590023990114621,
3.77251655941407));
#30431=CARTESIAN_POINT('Ctrl Pts',(13.1455221091246,-0.127768152052348,
3.38068398698829));
#30432=CARTESIAN_POINT('Ctrl Pts',(13.1932379451874,0.451819146005312,3.55757883871291));
#30433=CARTESIAN_POINT('Ctrl Pts',(13.2409537812502,0.616493970155128,4.14075585037205));
#30434=CARTESIAN_POINT('Ctrl Pts',(13.2886696173131,0.215032895532453,4.59467459882739));
#30435=CARTESIAN_POINT('Ctrl Pts',(13.3363854533759,-0.383896195764066,
4.50249451293469));
#30436=CARTESIAN_POINT('Ctrl Pts',(13.3841012894387,-0.630287503488198,
3.94886598394213));
#30437=CARTESIAN_POINT('Ctrl Pts',(13.4318171255016,-0.297876098539286,
3.4421946086935));
#30438=CARTESIAN_POINT('Ctrl Pts',(13.4795329615644,0.308079511111167,3.44776450722078));
#30439=CARTESIAN_POINT('Ctrl Pts',(13.5272487976272,0.631120965295637,3.96046075600252));
#30440=CARTESIAN_POINT('Ctrl Pts',(13.5749646336901,0.374594326004835,4.50946650093658));
#30441=CARTESIAN_POINT('Ctrl Pts',(13.6226804697529,-0.225928046730791,
4.59062131891086));
#30442=CARTESIAN_POINT('Ctrl Pts',(13.6703963058158,-0.618977217803688,
4.12939949185215));
#30443=CARTESIAN_POINT('Ctrl Pts',(13.7181121418786,-0.443610085578744,
3.54934812035851));
#30444=CARTESIAN_POINT('Ctrl Pts',(13.7658279779415,0.139131014051702,3.38313730411011));
#30445=CARTESIAN_POINT('Ctrl Pts',(13.8135438140043,0.594105962672646,3.78340099315002));
#30446=CARTESIAN_POINT('Ctrl Pts',(13.8612596500671,0.503504264276035,4.38257088298437));
#30447=CARTESIAN_POINT('Ctrl Pts',(13.90897548613,-0.0494731474142026,4.63042004436449));
#30448=CARTESIAN_POINT('Ctrl Pts',(13.9566913221928,-0.557018606591754,
4.29934477874546));
#30449=CARTESIAN_POINT('Ctrl Pts',(14.0044071582556,-0.553045308503159,
3.69337659679301));
#30450=CARTESIAN_POINT('Ctrl Pts',(14.0521229943185,-0.0412019939202257,
3.36898540401303));
#30451=CARTESIAN_POINT('Ctrl Pts',(14.0998388303813,0.50847774565382,3.62406462413548));
#30452=CARTESIAN_POINT('Ctrl Pts',(14.1475546664442,0.591214547458171,4.22437108442359));
#30453=CARTESIAN_POINT('Ctrl Pts',(14.195270502507,0.131029933326566,4.61863412549262));
#30454=CARTESIAN_POINT('Ctrl Pts',(14.2429863385698,-0.4494814847335,4.44479593021223));
#30455=CARTESIAN_POINT('Ctrl Pts',(14.2907021746327,-0.617227139201166,
3.86249478815283));
#30456=CARTESIAN_POINT('Ctrl Pts',(14.3384180106955,-0.218163614480107,
3.40646679792233));
#30457=CARTESIAN_POINT('Ctrl Pts',(14.3861338467583,0.381242914296727,3.49548947984197));
#30458=CARTESIAN_POINT('Ctrl Pts',(14.4338496828212,0.630548208698617,4.0478119353149));
#30459=CARTESIAN_POINT('Ctrl Pts',(14.481565518884,0.300811380821271,4.55622795490698));
#30460=CARTESIAN_POINT('Ctrl Pts',(14.5292813549469,-0.305165166642291,
4.55385128484077));
#30461=CARTESIAN_POINT('Ctrl Pts',(14.5769971910097,-0.630903846008588,
4.04286445780787));
#30462=CARTESIAN_POINT('Ctrl Pts',(14.6247130270726,-0.37727381588172,3.49251453961553));
#30463=CARTESIAN_POINT('Ctrl Pts',(14.6724288631354,0.222812564473163,3.40819632836178));
#30464=CARTESIAN_POINT('Ctrl Pts',(14.7201446991982,0.618286738460357,3.86734053484336));
#30465=CARTESIAN_POINT('Ctrl Pts',(14.7678605352611,0.44597868695508,4.44830796940654));
#30466=CARTESIAN_POINT('Ctrl Pts',(14.8155763713239,-0.135878455045208,
4.6175872975589));
#30467=CARTESIAN_POINT('Ctrl Pts',(14.8632922073867,-0.592956321018707,
4.2197267075609));
#30468=CARTESIAN_POINT('Ctrl Pts',(14.9110080434496,-0.505513273594975,
3.62008770107973));
#30469=CARTESIAN_POINT('Ctrl Pts',(14.9587238795124,0.0461503912925444,
3.36932800439917));
#30470=CARTESIAN_POINT('Ctrl Pts',(15.0064397155752,0.555433441741075,3.69772410541485));
#30471=CARTESIAN_POINT('Ctrl Pts',(15.0541555516381,0.554653416196733,4.30370481154056));
#30472=CARTESIAN_POINT('Ctrl Pts',(15.1018713877009,0.0445266241191229,
4.63078871612938));
#30473=CARTESIAN_POINT('Ctrl Pts',(15.1495872237638,-0.506489652017253,
4.37860963676461));
#30474=CARTESIAN_POINT('Ctrl Pts',(15.1973030598266,-0.592388687361149,
3.77874750230084));
#30475=CARTESIAN_POINT('Ctrl Pts',(15.2450188958894,-0.134288076029725,
3.38206494088146));
#30476=CARTESIAN_POINT('Ctrl Pts',(15.2927347319523,0.447131341807447,3.5528416524037));
#30477=CARTESIAN_POINT('Ctrl Pts',(15.3404505680151,0.617943168462805,4.13425075493917));
#30478=CARTESIAN_POINT('Ctrl Pts',(15.3881664040779,0.221288275240951,4.59237532350063));
#30479=CARTESIAN_POINT('Ctrl Pts',(15.4358822401408,-0.378579046092452,
4.50651251762549));
#30480=CARTESIAN_POINT('Ctrl Pts',(15.4835980762036,-0.630791404211772,
3.95551147311801));
#30481=CARTESIAN_POINT('Ctrl Pts',(15.5313139122665,-0.303738309870084,
3.44536492739022));
#30482=CARTESIAN_POINT('Ctrl Pts',(15.5790297483293,0.302242348039936,3.44454830299756));
#30483=CARTESIAN_POINT('Ctrl Pts',(15.6267455843921,0.630669207148581,3.95381151868517));
#30484=CARTESIAN_POINT('Ctrl Pts',(15.674461420455,0.379942829239589,4.50549032746533));
#30485=CARTESIAN_POINT('Ctrl Pts',(15.7221772565178,-0.219690894932002,
4.59296959056563));
#30486=CARTESIAN_POINT('Ctrl Pts',(15.7698930925806,-0.617579089908608,
4.13591575463957));
#30487=CARTESIAN_POINT('Ctrl Pts',(15.8176089286435,-0.448334903946386,
3.5540483898953));
#30488=CARTESIAN_POINT('Ctrl Pts',(15.8653247647063,0.13262212282903,3.3817052505577));
#30489=CARTESIAN_POINT('Ctrl Pts',(15.9130406007692,0.591790213556878,3.77715169332057));
#30490=CARTESIAN_POINT('Ctrl Pts',(15.960756436832,0.507508245312566,4.37724316506909));
#30491=CARTESIAN_POINT('Ctrl Pts',(16.0084722728949,-0.0428263536203826,
4.63090643370248));
#30492=CARTESIAN_POINT('Ctrl Pts',(16.0561881089577,-0.553832853055588,
4.30519861652357));
#30493=CARTESIAN_POINT('Ctrl Pts',(16.1039039450205,-0.556246121716014,
3.69922221370673));
#30494=CARTESIAN_POINT('Ctrl Pts',(16.1516197810833,-0.0478500178579074,
3.36945468010413));
#30495=CARTESIAN_POINT('Ctrl Pts',(16.1993356171462,0.504487493666278,3.61872661594874));
#30496=CARTESIAN_POINT('Ctrl Pts',(16.247051453209,0.593546377218863,4.21812776701271));
#30497=CARTESIAN_POINT('Ctrl Pts',(16.2947672892719,0.137542489686435,4.61721883330181));
#30498=CARTESIAN_POINT('Ctrl Pts',(16.3424831253347,-0.444768782488292,
4.44950834783736));
#30499=CARTESIAN_POINT('Ctrl Pts',(16.3901989613976,-0.618642038056621,
3.86900742997889));
#30500=CARTESIAN_POINT('Ctrl Pts',(16.4379147974604,-0.224406791046256,
3.40879900475058));
#30501=CARTESIAN_POINT('Ctrl Pts',(16.4856306335233,0.375904665124208,3.49149955025639));
#30502=CARTESIAN_POINT('Ctrl Pts',(16.533346469586,0.631017083274371,4.04116388304691));
#30503=CARTESIAN_POINT('Ctrl Pts',(16.5810623056489,0.306656804407812,4.55302678864769));
#30504=CARTESIAN_POINT('Ctrl Pts',(16.6287781417117,-0.29931113646787,4.55703668482238));
#30505=CARTESIAN_POINT('Ctrl Pts',(16.6764939777746,-0.630417055231307,
4.04951122221356));
#30506=CARTESIAN_POINT('Ctrl Pts',(16.7242098138374,-0.382601291962586,
3.49651884241796));
#30507=CARTESIAN_POINT('Ctrl Pts',(16.7719256499003,0.216563124792967,3.40588095668335));
#30508=CARTESIAN_POINT('Ctrl Pts',(16.8196414859631,0.616854291799135,3.86083173012294));
#30509=CARTESIAN_POINT('Ctrl Pts',(16.8673573220259,0.450678671122871,4.44358286716973));
#30510=CARTESIAN_POINT('Ctrl Pts',(16.9150731580887,-0.129362107828251,
4.61898503189482));
#30511=CARTESIAN_POINT('Ctrl Pts',(16.9627889941516,-0.590607672668797,
4.22596371752193));
#30512=CARTESIAN_POINT('Ctrl Pts',(17.0105048302144,-0.509489124030439,
3.62543644444997));
#30513=CARTESIAN_POINT('Ctrl Pts',(17.0582206662773,0.0395011267029154,
3.3688766478407));
#30514=CARTESIAN_POINT('Ctrl Pts',(17.1059365023401,0.552216884982031,3.69188713660034));
#30515=CARTESIAN_POINT('Ctrl Pts',(17.153652338403,0.557823380833178,4.29784240874569));
#30516=CARTESIAN_POINT('Ctrl Pts',(17.2013681744658,0.0511720828492506,
4.63028441404532));
#30517=CARTESIAN_POINT('Ctrl Pts',(17.2490840105287,-0.502471326198846,
4.38392654375487));
#30518=CARTESIAN_POINT('Ctrl Pts',(17.2967998465914,-0.594687584883411,
3.78500302086511));
#30519=CARTESIAN_POINT('Ctrl Pts',(17.3445156826543,-0.140793083924855,
3.38351453206865));
#30520=CARTESIAN_POINT('Ctrl Pts',(17.3922315187171,0.442393872381948,3.5481541343218));
#30521=CARTESIAN_POINT('Ctrl Pts',(17.43994735478,0.61932372857571,4.1277307475695));
#30522=CARTESIAN_POINT('Ctrl Pts',(17.4876631908428,0.227519075297936,4.590010249934));
#30523=CARTESIAN_POINT('Ctrl Pts',(17.5353790269057,-0.373219845656906,
4.51047426130944));
#30524=CARTESIAN_POINT('Ctrl Pts',(17.5830948629685,-0.631225239619516,
3.96216190386831));
#30525=CARTESIAN_POINT('Ctrl Pts',(17.6308106990313,-0.309566783390781,
3.44859685231885));
#30526=CARTESIAN_POINT('Ctrl Pts',(17.6785265350942,0.29637161332294,3.44139379571298));
#30527=CARTESIAN_POINT('Ctrl Pts',(17.726242371157,0.630147397258769,3.94716741176515));
#30528=CARTESIAN_POINT('Ctrl Pts',(17.7739582072198,0.385249130227842,4.50145800652724));
#30529=CARTESIAN_POINT('Ctrl Pts',(17.8216740432827,-0.213429340911116,
4.59525199797214));
#30530=CARTESIAN_POINT('Ctrl Pts',(17.8693898793456,-0.616112364258878,
4.14241692054995));
#30531=CARTESIAN_POINT('Ctrl Pts',(17.9171057154084,-0.453009923400427,
3.55879819362073));
#30532=CARTESIAN_POINT('Ctrl Pts',(17.9648215514712,0.126098500570276,3.38034187425201));
#30533=CARTESIAN_POINT('Ctrl Pts',(18.012537387534,0.589408731192455,3.77092714642348));
#30534=CARTESIAN_POINT('Ctrl Pts',(18.0602532235969,0.511455854741549,4.3718735447732));
#30535=CARTESIAN_POINT('Ctrl Pts',(18.1079690596597,-0.0361748028784226,
4.6313227449477));
#30536=CARTESIAN_POINT('Ctrl Pts',(18.1556848957226,-0.55058558239424,4.31101855428765));
#30537=CARTESIAN_POINT('Ctrl Pts',(18.2034007317854,-0.559385149749292,
3.70510123958967));
#30538=CARTESIAN_POINT('Ctrl Pts',(18.2511165678482,-0.0544927268426965,
3.36999399417717));
#30539=CARTESIAN_POINT('Ctrl Pts',(18.2988324039111,0.500441205601937,3.6134309578002));
#30540=CARTESIAN_POINT('Ctrl Pts',(18.3465482399739,0.595812278664582,4.21186022100458));
#30541=CARTESIAN_POINT('Ctrl Pts',(18.3942640760367,0.144039768479226,4.61573498337195));
#30542=CARTESIAN_POINT('Ctrl Pts',(18.4419799120996,-0.440006677437314,
4.4541708362083));
#30543=CARTESIAN_POINT('Ctrl Pts',(18.4896957481624,-0.619988221090196,
3.87553462183804));
#30544=CARTESIAN_POINT('Ctrl Pts',(18.5374115842252,-0.230625041570952,
3.41119687937986));
#30545=CARTESIAN_POINT('Ctrl Pts',(18.5851274202881,0.370524662245315,3.48756610248778));
#30546=CARTESIAN_POINT('Ctrl Pts',(18.6328432563509,0.631415867466904,4.03451125849008));
#30547=CARTESIAN_POINT('Ctrl Pts',(18.6805590924138,0.31246816601179,4.54976419479712));
#30548=CARTESIAN_POINT('Ctrl Pts',(18.7282749284766,-0.293423860232864,
4.56016021181225));
#30549=CARTESIAN_POINT('Ctrl Pts',(18.7759907645394,-0.629860240718928,
4.05615248714788));
#30550=CARTESIAN_POINT('Ctrl Pts',(18.8237066006023,-0.387886270507855,
3.50057906951772));
#30551=CARTESIAN_POINT('Ctrl Pts',(18.8714224366651,0.210289630309142,3.40363157692976));
#30552=CARTESIAN_POINT('Ctrl Pts',(18.919138272728,0.615353327889266,3.85433838355196));
#30553=CARTESIAN_POINT('Ctrl Pts',(18.9668541087908,0.455328596044662,4.43880849385601));
#30554=CARTESIAN_POINT('Ctrl Pts',(19.0145699448537,-0.122831391686292,
4.62031401230505));
#30555=CARTESIAN_POINT('Ctrl Pts',(19.0622857809165,-0.588193422413584,
4.2321756285162));
#30556=CARTESIAN_POINT('Ctrl Pts',(19.1100016169793,-0.513408382846255,
3.63082679254236));
#30557=CARTESIAN_POINT('Ctrl Pts',(19.1577174530421,0.0328474745430158,
3.36849539350727));
#30558=CARTESIAN_POINT('Ctrl Pts',(19.205433289105,0.548938990540088,3.68608439142882));
#30559=CARTESIAN_POINT('Ctrl Pts',(19.2531491251678,0.560931385193363,4.2919469231649));
#30560=CARTESIAN_POINT('Ctrl Pts',(19.3008649612307,0.0578118574426247,
4.62971010270368));
#30561=CARTESIAN_POINT('Ctrl Pts',(19.3485807972935,-0.498397187901359,
4.38920080648958));
#30562=CARTESIAN_POINT('Ctrl Pts',(19.3962966333563,-0.596920427988996,
3.79128241936144));
#30563=CARTESIAN_POINT('Ctrl Pts',(19.4440124694192,-0.147282451949449,
3.38503260125846));
#30564=CARTESIAN_POINT('Ctrl Pts',(19.491728305482,0.437607261597584,3.54351680188243));
#30565=CARTESIAN_POINT('Ctrl Pts',(19.5394441415449,0.620635501579114,4.12119655861503));
#30566=CARTESIAN_POINT('Ctrl Pts',(19.5871599776077,0.233724595248439,4.58757962923414));
#30567=CARTESIAN_POINT('Ctrl Pts',(19.6348758136705,-0.367819173932889,
4.51437932582758));
#30568=CARTESIAN_POINT('Ctrl Pts',(19.6825916497334,-0.631588991354928,
3.96881649615688));
#30569=CARTESIAN_POINT('Ctrl Pts',(19.7303074857962,-0.315360815373557,
3.4518901025469));
#30570=CARTESIAN_POINT('Ctrl Pts',(19.778023321859,0.290467852693633,3.43830118837221));
#30571=CARTESIAN_POINT('Ctrl Pts',(19.8257391579219,0.629555794415491,3.94052945152661));
#30572=CARTESIAN_POINT('Ctrl Pts',(19.8734549939847,0.390512260364629,4.49736946054851));
#30573=CARTESIAN_POINT('Ctrl Pts',(19.9211708300476,-0.207143364153331,
4.59746927979605));
#30574=CARTESIAN_POINT('Ctrl Pts',(19.9688866661104,-0.61457855576007,4.14890039401813));
#30575=CARTESIAN_POINT('Ctrl Pts',(20.0166025021732,-0.45763207183192,3.5636005413983));
#30576=CARTESIAN_POINT('Ctrl Pts',(20.0643183382361,0.119556051622903,3.37904064719698));
#30577=CARTESIAN_POINT('Ctrl Pts',(20.1120341742989,0.586970881772813,3.7647406560623));
#30578=CARTESIAN_POINT('Ctrl Pts',(20.1597500103618,0.515329468049299,4.36643880344312));
#30579=CARTESIAN_POINT('Ctrl Pts',(20.2074658464246,-0.029486781418557,
4.63171390504007));
#30580=CARTESIAN_POINT('Ctrl Pts',(20.2551816824874,-0.547338447674763,
4.31671898245684));
#30581=CARTESIAN_POINT('Ctrl Pts',(20.3028975185503,-0.562346186529673,
3.71117381387971));
#30582=CARTESIAN_POINT('Ctrl Pts',(20.3506133546131,-0.0613491664957494,
3.37029669484294));
#30583=CARTESIAN_POINT('Ctrl Pts',(20.398329190676,0.496762641213801,3.60878154740643));
#30584=CARTESIAN_POINT('Ctrl Pts',(20.4380923873949,0.580417208789547,4.10498761157686));
#30585=CARTESIAN_POINT('Ctrl Pts',(20.4699029447702,0.374745574175769,4.41137453781958));
#30586=CARTESIAN_POINT('Ctrl Pts',(20.4937608628016,0.13332385162888,4.54159545884303));
#30587=CARTESIAN_POINT('Ctrl Pts',(20.517618780833,-0.143293564288956,4.53872805560682));
#30588=CARTESIAN_POINT('Ctrl Pts',(20.5414766988645,-0.38346854803195,4.40448715909776));
#30589=CARTESIAN_POINT('Ctrl Pts',(20.5653346168959,-0.530621786340447,
4.17114564603877));
#30590=CARTESIAN_POINT('Ctrl Pts',(20.5891925349273,-0.547627617499454,
3.89605651468078));
#30591=CARTESIAN_POINT('Ctrl Pts',(20.6130504529587,-0.430933317123153,
3.64633026976583));
#30592=CARTESIAN_POINT('Ctrl Pts',(20.6369083709901,-0.208752997660079,
3.48311457674551));
#30593=CARTESIAN_POINT('Ctrl Pts',(20.6607662890215,0.0644142843662171,
3.4462762657402));
#30594=CARTESIAN_POINT('Ctrl Pts',(20.684624207053,0.321861676845817,3.54484653226013));
#30595=CARTESIAN_POINT('Ctrl Pts',(20.7084821250844,0.500588620804837,3.75470996102831));
#30596=CARTESIAN_POINT('Ctrl Pts',(20.7323400431158,0.556916750317041,4.02455574134091));
#30597=CARTESIAN_POINT('Ctrl Pts',(20.7561979611472,0.47705893600668,4.28839577951569));
#30598=CARTESIAN_POINT('Ctrl Pts',(20.7800558791787,0.280549668164313,4.48171582646486));
#30599=CARTESIAN_POINT('Ctrl Pts',(20.8039137972101,0.0154370662995263,
4.55724289713534));
#30600=CARTESIAN_POINT('Ctrl Pts',(20.8277717152415,-0.253449631274377,
4.49650907789895));
#30601=CARTESIAN_POINT('Ctrl Pts',(20.8516296332729,-0.460361354274216,
4.31436517051053));
#30602=CARTESIAN_POINT('Ctrl Pts',(20.8754875513043,-0.554701993332711,
4.05535046556385));
#30603=CARTESIAN_POINT('Ctrl Pts',(20.8993454693358,-0.513402987365846,
3.78280103771366));
#30604=CARTESIAN_POINT('Ctrl Pts',(20.9232033873672,-0.346562912086465,
3.56336268648205));
#30605=CARTESIAN_POINT('Ctrl Pts',(20.9470613053986,-0.0949787932613798,
3.45069404477467));
#30606=CARTESIAN_POINT('Ctrl Pts',(20.97091922343,0.179830242856268,3.47234567582879));
#30607=CARTESIAN_POINT('Ctrl Pts',(20.9947771414614,0.410665878084123,3.62302316008453));
#30608=CARTESIAN_POINT('Ctrl Pts',(21.0186350594928,0.541082524061315,3.86588175144064));
#30609=CARTESIAN_POINT('Ctrl Pts',(21.0424929775243,0.539189751860116,4.14153590729571));
#30610=CARTESIAN_POINT('Ctrl Pts',(21.0663508955557,0.405450399288564,4.38258067876424));
#30611=CARTESIAN_POINT('Ctrl Pts',(21.0902088135871,0.172567379211795,4.53007405282339));
#30612=CARTESIAN_POINT('Ctrl Pts',(21.1140667316185,-0.102513065388571,
4.54794988212627));
#30613=CARTESIAN_POINT('Ctrl Pts',(21.1379246496499,-0.352526273278862,
4.43183703934844));
#30614=CARTESIAN_POINT('Ctrl Pts',(21.1617825676814,-0.516337204635697,
4.21012827746935));
#30615=CARTESIAN_POINT('Ctrl Pts',(21.1856404857128,-0.553889624765765,
3.93703742795684));
#30616=CARTESIAN_POINT('Ctrl Pts',(21.2094984037442,-0.456000943963824,
3.67934264238169));
#30617=CARTESIAN_POINT('Ctrl Pts',(21.2333563217756,-0.246607611160355,
3.50005731527167));
#30618=CARTESIAN_POINT('Ctrl Pts',(21.257214239807,0.0230880000356606,3.44302159274494));
#30619=CARTESIAN_POINT('Ctrl Pts',(21.2810721578385,0.287137966314551,3.52218226257825));
#30620=CARTESIAN_POINT('Ctrl Pts',(21.3049300758698,0.480974878350452,3.71818238470557));
#30621=CARTESIAN_POINT('Ctrl Pts',(21.3287879939013,0.557200331135927,3.9830945903298));
#30622=CARTESIAN_POINT('Ctrl Pts',(21.3526459119327,0.497175125126959,4.25214062911267));
#30623=CARTESIAN_POINT('Ctrl Pts',(21.3765038299641,0.31557705824565,4.45953141590455));
#30624=CARTESIAN_POINT('Ctrl Pts',(21.4003617479955,0.0568118044769688,
4.55455425412338));
#30625=CARTESIAN_POINT('Ctrl Pts',(21.424219666027,-0.215845483008899,4.51397347145443));
#30626=CARTESIAN_POINT('Ctrl Pts',(21.4480775840584,-0.435722670386138,
4.34771217465862));
#30627=CARTESIAN_POINT('Ctrl Pts',(21.4719355020898,-0.549053796006754,
4.0964257796693));
#30628=CARTESIAN_POINT('Ctrl Pts',(21.4957934201212,-0.528126312578589,
3.82156065496534));
#30629=CARTESIAN_POINT('Ctrl Pts',(21.5196513381527,-0.378057559853047,
3.59032881071252));
#30630=CARTESIAN_POINT('Ctrl Pts',(21.543509256184,-0.135543435662257,3.45927273145963));
#30631=CARTESIAN_POINT('Ctrl Pts',(21.5673671742155,0.14011475067701,3.46043919847993));
#30632=CARTESIAN_POINT('Ctrl Pts',(21.5912250922469,0.381511063826562,3.59354297881304));
#30633=CARTESIAN_POINT('Ctrl Pts',(21.6150830102783,0.529617529717794,3.8260365724933));
#30634=CARTESIAN_POINT('Ctrl Pts',(21.6389409283097,0.548218083101175,4.10106896286759));
#30635=CARTESIAN_POINT('Ctrl Pts',(21.6627988463412,0.432764382005563,4.35138723875747));
#30636=CARTESIAN_POINT('Ctrl Pts',(21.6866567643726,0.211488001244504,4.51578176317496));
#30637=CARTESIAN_POINT('Ctrl Pts',(21.710514682404,-0.0615029566383307,
4.55405359688301));
#30638=CARTESIAN_POINT('Ctrl Pts',(21.7343726004354,-0.319454766316188,
4.4568442340362));
#30639=CARTESIAN_POINT('Ctrl Pts',(21.7582305184669,-0.499291183856609,
4.24792401178047));
#30640=CARTESIAN_POINT('Ctrl Pts',(21.7820884364982,-0.557037306525311,
3.97837961532992));
#30641=CARTESIAN_POINT('Ctrl Pts',(21.8059463545297,-0.478572634356998,
3.71412199185867));
#30642=CARTESIAN_POINT('Ctrl Pts',(21.8298042725611,-0.283083917031579,
3.51976932853855));
#30643=CARTESIAN_POINT('Ctrl Pts',(21.8536621905926,-0.018373470940863,
3.44284614561161));
#30644=CARTESIAN_POINT('Ctrl Pts',(21.8775201086239,0.250829789278194,3.5021622566489));
#30645=CARTESIAN_POINT('Ctrl Pts',(21.9013780266554,0.458698333552465,3.68321325676341));
#30646=CARTESIAN_POINT('Ctrl Pts',(21.9252359446868,0.55440264058141,3.94172724469688));
#30647=CARTESIAN_POINT('Ctrl Pts',(21.9490938627182,0.514540400363477,4.21449050861997));
#30648=CARTESIAN_POINT('Ctrl Pts',(21.9729517807496,0.348859016457567,4.4348050005813));
#30649=CARTESIAN_POINT('Ctrl Pts',(21.996809698781,0.0978721002989983,4.54879782605011));
#30650=CARTESIAN_POINT('Ctrl Pts',(22.0206676168125,-0.177047210365213,
4.52859463409701));
#30651=CARTESIAN_POINT('Ctrl Pts',(22.0445255348439,-0.408673655425848,
4.3791356554785));
#30652=CARTESIAN_POINT('Ctrl Pts',(22.0683834528753,-0.540368259688198,
4.13696768164748));
#30653=CARTESIAN_POINT('Ctrl Pts',(22.0922413709067,-0.53992810512055,3.86130737872913));
#30654=CARTESIAN_POINT('Ctrl Pts',(22.1160992889381,-0.407460821505317,
3.61956119962225));
#30655=CARTESIAN_POINT('Ctrl Pts',(22.1399572069695,-0.175358268020808,
3.47084267015335));
#30656=CARTESIAN_POINT('Ctrl Pts',(22.163815125001,0.0996241586556461,3.45151752178681));
#30657=CARTESIAN_POINT('Ctrl Pts',(22.1876730430324,0.350245764837839,3.56631127970877));
#30658=CARTESIAN_POINT('Ctrl Pts',(22.2115309610638,0.51522274100534,3.78715374318048));
#30659=CARTESIAN_POINT('Ctrl Pts',(22.2353888790952,0.554213722627899,4.06004291426965));
#30660=CARTESIAN_POINT('Ctrl Pts',(22.2592467971266,0.457684352558003,4.31824995726588));
#30661=CARTESIAN_POINT('Ctrl Pts',(22.2831047151581,0.249238691275201,4.49863621678958));
#30662=CARTESIAN_POINT('Ctrl Pts',(22.3069626331895,-0.0201526192614011,
4.55709233866662));
#30663=CARTESIAN_POINT('Ctrl Pts',(22.3308205512209,-0.284616065231974,
4.47932420896945));
#30664=CARTESIAN_POINT('Ctrl Pts',(22.3546784692523,-0.479483130864429,
4.28434825342259));
#30665=CARTESIAN_POINT('Ctrl Pts',(22.3785363872838,-0.557103509392546,
4.01984140485232));
#30666=CARTESIAN_POINT('Ctrl Pts',(22.4023943053151,-0.498496906094933,
3.75048279151596));
#30667=CARTESIAN_POINT('Ctrl Pts',(22.4262522233466,-0.317994227800984,
3.542137933897));
#30668=CARTESIAN_POINT('Ctrl Pts',(22.450110141378,-0.0597333038680864,
3.44575282046209));
#30669=CARTESIAN_POINT('Ctrl Pts',(22.4739680594094,0.213134049493302,3.48489624527193));
#30670=CARTESIAN_POINT('Ctrl Pts',(22.4978259774408,0.433884304103661,3.6499965589521));
#30671=CARTESIAN_POINT('Ctrl Pts',(22.5216838954723,0.548538061567711,3.90068226732924));
#30672=CARTESIAN_POINT('Ctrl Pts',(22.5455418135037,0.529059256943919,4.17565382996358));
#30673=CARTESIAN_POINT('Ctrl Pts',(22.5693997315351,0.380211173855379,4.40767331583304));
#30674=CARTESIAN_POINT('Ctrl Pts',(22.5932576495665,0.138390873272415,4.54000544018811));
#30675=CARTESIAN_POINT('Ctrl Pts',(22.6171155675979,-0.137269333605106,
4.54029177230974));
#30676=CARTESIAN_POINT('Ctrl Pts',(22.6409734856293,-0.379364264814148,
4.40846158181013));
#30677=CARTESIAN_POINT('Ctrl Pts',(22.6648314036608,-0.528692759685234,
4.17675229015827));
#30678=CARTESIAN_POINT('Ctrl Pts',(22.6886893216921,-0.54874438127821,3.90182058373076));
#30679=CARTESIAN_POINT('Ctrl Pts',(22.7125472397236,-0.434607562942265,
3.65089956353622));
#30680=CARTESIAN_POINT('Ctrl Pts',(22.736405157755,-0.214207731687487,3.48533716867003));
#30681=CARTESIAN_POINT('Ctrl Pts',(22.7602630757864,0.0585913648593265,
3.44563509732658));
#30682=CARTESIAN_POINT('Ctrl Pts',(22.7841209938179,0.31702578011682,3.5414689143437));
#30683=CARTESIAN_POINT('Ctrl Pts',(22.8079789118493,0.498012898707086,3.74946820019106));
#30684=CARTESIAN_POINT('Ctrl Pts',(22.8238841905369,0.537376264140017,3.92891364167179));
#30685=CARTESIAN_POINT('Ctrl Pts',(22.8318368298807,0.534391234777113,4.01792167950194));
#30686=CARTESIAN_POINT('Ctrl Pts',(3.99999999999998,0.254694598474614,4.53673594206822));
#30687=CARTESIAN_POINT('Ctrl Pts',(4.00795263934379,0.165296026927429,4.57915779516171));
#30688=CARTESIAN_POINT('Ctrl Pts',(4.0238579180314,-0.0350146299391769,
4.61842892627033));
#30689=CARTESIAN_POINT('Ctrl Pts',(4.04771583606282,-0.327086058023631,
4.5259865276721));
#30690=CARTESIAN_POINT('Ctrl Pts',(4.07157375409423,-0.539100294705402,
4.30498302442502));
#30691=CARTESIAN_POINT('Ctrl Pts',(4.09543167212566,-0.619328256935644,
4.00937412827253));
#30692=CARTESIAN_POINT('Ctrl Pts',(4.11928959015708,-0.548093442686671,
3.71148804617917));
#30693=CARTESIAN_POINT('Ctrl Pts',(4.1431475081885,-0.342845496867427,3.48414304986991));
#30694=CARTESIAN_POINT('Ctrl Pts',(4.16700542621991,-0.0537568536316998,
3.38294333505492));
#30695=CARTESIAN_POINT('Ctrl Pts',(4.19086334425134,0.248473820944083,3.43262855616194));
#30696=CARTESIAN_POINT('Ctrl Pts',(4.21472126228276,0.489947458130694,3.62105272953394));
#30697=CARTESIAN_POINT('Ctrl Pts',(4.23857918031417,0.611614759069978,3.90213920826301));
#30698=CARTESIAN_POINT('Ctrl Pts',(4.26243709834559,0.583726034554802,4.20715564703007));
#30699=CARTESIAN_POINT('Ctrl Pts',(4.28629501637702,0.413100159498109,4.46151671210738));
#30700=CARTESIAN_POINT('Ctrl Pts',(4.31015293440843,0.141460167127662,4.60302446238992));
#30701=CARTESIAN_POINT('Ctrl Pts',(4.33401085243986,-0.164770755236008,
4.59707625642582));
#30702=CARTESIAN_POINT('Ctrl Pts',(4.35786877047126,-0.430710704813839,
4.44512666775742));
#30703=CARTESIAN_POINT('Ctrl Pts',(4.38172668850269,-0.59133017320549,4.18433147003372));
#30704=CARTESIAN_POINT('Ctrl Pts',(4.40558460653411,-0.607353296958831,
3.87846221409715));
#30705=CARTESIAN_POINT('Ctrl Pts',(4.42944252456553,-0.474862000813124,
3.60231225357117));
#30706=CARTESIAN_POINT('Ctrl Pts',(4.45330044259694,-0.226254007744579,
3.42340778189093));
#30707=CARTESIAN_POINT('Ctrl Pts',(4.47715836062837,0.0776792518003291,
3.38549581251083));
#30708=CARTESIAN_POINT('Ctrl Pts',(4.50101627865978,0.362617819109035,3.49784685630402));
#30709=CARTESIAN_POINT('Ctrl Pts',(4.5248741966912,0.558886451727075,3.73298802180378));
#30710=CARTESIAN_POINT('Ctrl Pts',(4.54873211472262,0.618492123352341,4.03342088939383));
#30711=CARTESIAN_POINT('Ctrl Pts',(4.57259003275404,0.5268596233165,4.32568143907503));
#30712=CARTESIAN_POINT('Ctrl Pts',(4.59644795078546,0.306395594072305,4.5383040055633));
#30713=CARTESIAN_POINT('Ctrl Pts',(4.62030586881688,0.0110094959969652,
4.61929657956068));
#30714=CARTESIAN_POINT('Ctrl Pts',(4.6441637868483,-0.287068723725306,4.54885427056805));
#30715=CARTESIAN_POINT('Ctrl Pts',(4.66802170487971,-0.514950820910697,
4.34420214192463));
#30716=CARTESIAN_POINT('Ctrl Pts',(4.69187962291114,-0.616913415399932,
4.05538321370614));
#30717=CARTESIAN_POINT('Ctrl Pts',(4.71573754094255,-0.568023875442366,
3.75302158112612));
#30718=CARTESIAN_POINT('Ctrl Pts',(4.73959545897398,-0.380237025278099,
3.51105289951885));
#30719=CARTESIAN_POINT('Ctrl Pts',(4.76345337700539,-0.0994718649854296,
3.38864510263028));
#30720=CARTESIAN_POINT('Ctrl Pts',(4.78731129503681,0.205616875855751,3.41573023112194));
#30721=CARTESIAN_POINT('Ctrl Pts',(4.81116921306823,0.460426689658758,3.5856852332931));
#30722=CARTESIAN_POINT('Ctrl Pts',(4.83502713109965,0.60264963606909,3.85695148163183));
#30723=CARTESIAN_POINT('Ctrl Pts',(4.85888504913107,0.597508330613982,4.16319698927494));
#30724=CARTESIAN_POINT('Ctrl Pts',(4.88274296716248,0.446259962523644,4.42953638764361));
#30725=CARTESIAN_POINT('Ctrl Pts',(4.90660088519391,0.185888877718945,4.59084243889714));
#30726=CARTESIAN_POINT('Ctrl Pts',(4.93045880322533,-0.119937101199393,
4.60767141961541));
#30727=CARTESIAN_POINT('Ctrl Pts',(4.95431672125674,-0.396435191853442,
4.47590818560059));
#30728=CARTESIAN_POINT('Ctrl Pts',(4.97817463928816,-0.575994079421511,
4.22777243672773));
#30729=CARTESIAN_POINT('Ctrl Pts',(5.00203255731958,-0.614706724807315,
3.92394012267834));
#30730=CARTESIAN_POINT('Ctrl Pts',(5.025890475351,-0.503106831702736,3.63870652046354));
#30731=CARTESIAN_POINT('Ctrl Pts',(5.04974839338242,-0.268483613891896,
3.44181901543221));
#30732=CARTESIAN_POINT('Ctrl Pts',(5.07360631141384,0.0317911608623165,
3.38142196567243));
#30733=CARTESIAN_POINT('Ctrl Pts',(5.09746422944526,0.32429213081186,3.47228409503311));
#30734=CARTESIAN_POINT('Ctrl Pts',(5.12132214747667,0.537494841237617,3.69218713785082));
#30735=CARTESIAN_POINT('Ctrl Pts',(5.1451800655081,0.619265421915264,3.98735881011802));
#30736=CARTESIAN_POINT('Ctrl Pts',(5.16903798353952,0.549608738483219,4.28562159765047));
#30737=CARTESIAN_POINT('Ctrl Pts',(5.19289590157094,0.34555774745058,4.51404212438126));
#30738=CARTESIAN_POINT('Ctrl Pts',(5.21675381960235,0.0570084743622218,
4.61676534947452));
#30739=CARTESIAN_POINT('Ctrl Pts',(5.24061173763377,-0.245480923587363,
4.56867264627043));
#30740=CARTESIAN_POINT('Ctrl Pts',(5.26446965566519,-0.487943548953736,
4.38152399072137));
#30741=CARTESIAN_POINT('Ctrl Pts',(5.28832757369661,-0.611090685285508,
4.10108232693608));
#30742=CARTESIAN_POINT('Ctrl Pts',(5.31218549172803,-0.584809503288917,
3.79592328078761));
#30743=CARTESIAN_POINT('Ctrl Pts',(5.33604340975945,-0.415526467847156,
3.5406665514248));
#30744=CARTESIAN_POINT('Ctrl Pts',(5.35990132779088,-0.144635892303038,
3.39772936223054));
#30745=CARTESIAN_POINT('Ctrl Pts',(5.38375924582228,0.161622098711782,3.40206374949372));
#30746=CARTESIAN_POINT('Ctrl Pts',(5.40761716385371,0.428359084093981,3.55260983746209));
#30747=CARTESIAN_POINT('Ctrl Pts',(5.43147508188512,0.590350605148055,3.81255500683439));
#30748=CARTESIAN_POINT('Ctrl Pts',(5.45533299991655,0.607985322415754,4.11833558293467));
#30749=CARTESIAN_POINT('Ctrl Pts',(5.47919091794796,0.476951067165249,4.39517988561105));
#30750=CARTESIAN_POINT('Ctrl Pts',(5.50304883597938,0.2292892841064,4.57539194177126));
#30751=CARTESIAN_POINT('Ctrl Pts',(5.5269067540108,-0.0744399746307492,
4.61490499480714));
#30752=CARTESIAN_POINT('Ctrl Pts',(5.55076467204222,-0.359966631867259,
4.5040570269359));
#30753=CARTESIAN_POINT('Ctrl Pts',(5.57462259007364,-0.55747164231658,4.26995338574299));
#30754=CARTESIAN_POINT('Ctrl Pts',(5.59848050810506,-0.618659650999605,
3.96983878834977));
#30755=CARTESIAN_POINT('Ctrl Pts',(5.62233842613648,-0.528568523057477,
3.67709942878664));
#30756=CARTESIAN_POINT('Ctrl Pts',(5.6461963441679,-0.309227993320144,3.46331805450751));
#30757=CARTESIAN_POINT('Ctrl Pts',(5.67005426219932,-0.0142727959960426,
3.38077003484781));
#30758=CARTESIAN_POINT('Ctrl Pts',(5.69391218023074,0.284172488697173,3.4496406091084));
#30759=CARTESIAN_POINT('Ctrl Pts',(5.71777009826216,0.513129859266986,3.65308904601577));
#30760=CARTESIAN_POINT('Ctrl Pts',(5.74162801629357,0.616613001744231,3.94136666067651));
#30761=CARTESIAN_POINT('Ctrl Pts',(5.765485934325,0.569317469330215,4.24398172424487));
#30762=CARTESIAN_POINT('Ctrl Pts',(5.78934385235641,0.382808307322586,4.48693660973462));
#30763=CARTESIAN_POINT('Ctrl Pts',(5.81320177038783,0.102692087527565,4.61082223133738));
#30764=CARTESIAN_POINT('Ctrl Pts',(5.83705968841925,-0.202535146533943,
4.58534517687525));
#30765=CARTESIAN_POINT('Ctrl Pts',(5.86091760645067,-0.458237017319611,
4.41673528603543));
#30766=CARTESIAN_POINT('Ctrl Pts',(5.88477552448209,-0.601887460912657,
4.14622225884759));
#30767=CARTESIAN_POINT('Ctrl Pts',(5.9086334425135,-0.598360014525416,3.83995392008642));
#30768=CARTESIAN_POINT('Ctrl Pts',(5.93249136054493,-0.448517265794504,
3.57282118150817));
#30769=CARTESIAN_POINT('Ctrl Pts',(5.95634927857635,-0.188999790056246,
3.41014534911766));
#30770=CARTESIAN_POINT('Ctrl Pts',(5.98020719660777,0.116733210556207,3.39170495376011));
#30771=CARTESIAN_POINT('Ctrl Pts',(6.00406511463918,0.393921897475357,3.52200944135141));
#30772=CARTESIAN_POINT('Ctrl Pts',(6.02792303267061,0.574785693380153,3.76919531120668));
#30773=CARTESIAN_POINT('Ctrl Pts',(6.05178095070201,0.61509921541814,4.07281983667942));
#30774=CARTESIAN_POINT('Ctrl Pts',(6.07563886873346,0.505003308517799,4.35863675364492));
#30775=CARTESIAN_POINT('Ctrl Pts',(6.09949678676485,0.27142206589204,4.55675943366228));
#30776=CARTESIAN_POINT('Ctrl Pts',(6.12335470479629,-0.0285325303540597,
4.61873507756083));
#30777=CARTESIAN_POINT('Ctrl Pts',(6.14721262282769,-0.321503980505702,
4.52942105023226));
#30778=CARTESIAN_POINT('Ctrl Pts',(6.17107054085913,-0.535870591003297,
4.31063422072759));
#30779=CARTESIAN_POINT('Ctrl Pts',(6.19492845889052,-0.619180264299368,
4.01591706164003));
#30780=CARTESIAN_POINT('Ctrl Pts',(6.21878637692196,-0.551125001039776,
3.71725450231754));
#30781=CARTESIAN_POINT('Ctrl Pts',(6.24264429495337,-0.348226295733882,
3.48783145534908));
#30782=CARTESIAN_POINT('Ctrl Pts',(6.2665022129848,-0.0603247367796791,
3.38345774569467));
#30783=CARTESIAN_POINT('Ctrl Pts',(6.29036013101621,0.242607149567705,3.43020375417728));
#30784=CARTESIAN_POINT('Ctrl Pts',(6.31421804904763,0.485688404846908,3.61560451082823));
#30785=CARTESIAN_POINT('Ctrl Pts',(6.33807596707905,0.61099356578022,3.89627130770405));
#30786=CARTESIAN_POINT('Ctrl Pts',(6.36193388511046,0.585080291527744,4.19994745529594));
#30787=CARTESIAN_POINT('Ctrl Pts',(6.3937444424857,0.363797450650833,4.54512657044717));
#30788=CARTESIAN_POINT('Ctrl Pts',(6.43350763920472,-0.178959141669374,
4.67939801199369));
#30789=CARTESIAN_POINT('Ctrl Pts',(6.48122347526757,-0.668951848353412,
4.21606826543601));
#30790=CARTESIAN_POINT('Ctrl Pts',(6.5289393113304,-0.543175254381078,3.55462676401443));
#30791=CARTESIAN_POINT('Ctrl Pts',(6.57665514739324,0.0806513803028556,
3.30201433154981));
#30792=CARTESIAN_POINT('Ctrl Pts',(6.62437098345608,0.630812951656228,3.69045991683978));
#30793=CARTESIAN_POINT('Ctrl Pts',(6.67208681951892,0.601478580142798,4.36311480674272));
#30794=CARTESIAN_POINT('Ctrl Pts',(6.71980265558175,0.0199087309838695,
4.70234020845997));
#30795=CARTESIAN_POINT('Ctrl Pts',(6.76751849164459,-0.580002689552455,
4.39658285339385));
#30796=CARTESIAN_POINT('Ctrl Pts',(6.81523432770743,-0.64725742864426,3.72664421308375));
#30797=CARTESIAN_POINT('Ctrl Pts',(6.86295016377027,-0.120142281411799,
3.30772876957018));
#30798=CARTESIAN_POINT('Ctrl Pts',(6.91066599983311,0.517310146858294,3.52453857056345));
#30799=CARTESIAN_POINT('Ctrl Pts',(6.95838183589594,0.679704059947864,4.17797090041396));
#30800=CARTESIAN_POINT('Ctrl Pts',(7.00609767195879,0.217917737520193,4.66797035296266));
#30801=CARTESIAN_POINT('Ctrl Pts',(7.05381350802161,-0.443987099894697,
4.54456206689342));
#30802=CARTESIAN_POINT('Ctrl Pts',(7.10152934408447,-0.698171061503544,
3.92107420680554));
#30803=CARTESIAN_POINT('Ctrl Pts',(7.14924518014729,-0.311214160204793,
3.3700650369752));
#30804=CARTESIAN_POINT('Ctrl Pts',(7.19696101621015,0.361535686685884,3.39753487888718));
#30805=CARTESIAN_POINT('Ctrl Pts',(7.24467685227297,0.702281647003851,3.97825768917858));
#30806=CARTESIAN_POINT('Ctrl Pts',(7.29239268833582,0.398111619195611,4.5789468099385));
#30807=CARTESIAN_POINT('Ctrl Pts',(7.34010852439865,-0.271650463017158,
4.64798016059173));
#30808=CARTESIAN_POINT('Ctrl Pts',(7.38782436046149,-0.691951729928866,
4.1219633626529));
#30809=CARTESIAN_POINT('Ctrl Pts',(7.43554019652432,-0.476823084268312,
3.48394573037578));
#30810=CARTESIAN_POINT('Ctrl Pts',(7.48325603258717,0.17617954081454,3.31982867534575));
#30811=CARTESIAN_POINT('Ctrl Pts',(7.53097186865001,0.667393780433987,3.78032341303133));
#30812=CARTESIAN_POINT('Ctrl Pts',(7.57868770471284,0.545730043505963,4.44255054095139));
#30813=CARTESIAN_POINT('Ctrl Pts',(7.62640354077568,-0.077085990144297,
4.69837669746149));
#30814=CARTESIAN_POINT('Ctrl Pts',(7.67411937683852,-0.629112772588521,
4.31287278685955));
#30815=CARTESIAN_POINT('Ctrl Pts',(7.72183521290136,-0.603415615998442,
3.64005298187887));
#30816=CARTESIAN_POINT('Ctrl Pts',(7.76955104896419,-0.0235926144000291,
3.29777806215626));
#30817=CARTESIAN_POINT('Ctrl Pts',(7.81726688502703,0.577895847971041,3.60036435301798));
#30818=CARTESIAN_POINT('Ctrl Pts',(7.86498272108987,0.648693661106154,4.26994220769392));
#30819=CARTESIAN_POINT('Ctrl Pts',(7.9126985571527,0.123786103798515,4.6916279794467));
#30820=CARTESIAN_POINT('Ctrl Pts',(7.96041439321555,-0.514796137313916,
4.47818113561083));
#30821=CARTESIAN_POINT('Ctrl Pts',(8.00813022927838,-0.680633164378164,
3.82561319718015));
#30822=CARTESIAN_POINT('Ctrl Pts',(8.05584606534123,-0.221434283704469,
3.33318734306526));
#30823=CARTESIAN_POINT('Ctrl Pts',(8.10356190140405,0.441111106898351,3.45310581204486));
#30824=CARTESIAN_POINT('Ctrl Pts',(8.1512777374669,0.698577380670183,4.07524562887252));
#30825=CARTESIAN_POINT('Ctrl Pts',(8.19899357352974,0.314529296777622,4.62828622690367));
#30826=CARTESIAN_POINT('Ctrl Pts',(8.24670940959258,-0.358355880000973,
4.60436191534297));
#30827=CARTESIAN_POINT('Ctrl Pts',(8.29442524565541,-0.70215733816079,4.02544275761943));
#30828=CARTESIAN_POINT('Ctrl Pts',(8.34214108171825,-0.401156908608127,
3.42315912408683));
#30829=CARTESIAN_POINT('Ctrl Pts',(8.3898569177811,0.268232082711808,3.35059734274305));
#30830=CARTESIAN_POINT('Ctrl Pts',(8.43757275384392,0.691299425196396,3.8743920139026));
#30831=CARTESIAN_POINT('Ctrl Pts',(8.48528858990677,0.479535868514212,4.51353443142269));
#30832=CARTESIAN_POINT('Ctrl Pts',(8.53300442596961,-0.172592854832336,
4.68109027882443));
#30833=CARTESIAN_POINT('Ctrl Pts',(8.58072026203244,-0.66622690390392,4.22319044326068));
#30834=CARTESIAN_POINT('Ctrl Pts',(8.62843609809529,-0.548054535901959,
3.56033138942427));
#30835=CARTESIAN_POINT('Ctrl Pts',(8.67615193415812,0.0734047453217555,
3.30122678585069));
#30836=CARTESIAN_POINT('Ctrl Pts',(8.72386777022095,0.627455319439314,3.68381637683837));
#30837=CARTESIAN_POINT('Ctrl Pts',(8.7715836062838,0.605304019074675,4.35676225408577));
#30838=CARTESIAN_POINT('Ctrl Pts',(8.81929944234663,0.0272927241942496,
4.70208786391332));
#30839=CARTESIAN_POINT('Ctrl Pts',(8.86701527840948,-0.575781899266294,
4.40267538529889));
#30840=CARTESIAN_POINT('Ctrl Pts',(8.9147311144723,-0.650107145087294,3.73347990440727));
#30841=CARTESIAN_POINT('Ctrl Pts',(8.96244695053515,-0.127428996390418,
3.30903392823725));
#30842=CARTESIAN_POINT('Ctrl Pts',(9.01016278659798,0.512269160438921,3.51911272764658));
#30843=CARTESIAN_POINT('Ctrl Pts',(9.05787862266082,0.681542664962993,4.17079770865984));
#30844=CARTESIAN_POINT('Ctrl Pts',(9.10559445872366,0.224945053369686,4.66563652575022));
#30845=CARTESIAN_POINT('Ctrl Pts',(9.1533102947865,-0.438223061957547,4.54921107910972));
#30846=CARTESIAN_POINT('Ctrl Pts',(9.20102613084934,-0.698964196560635,
3.92843664782408));
#30847=CARTESIAN_POINT('Ctrl Pts',(9.24874196691217,-0.317835754515511,
3.3733799439853));
#30848=CARTESIAN_POINT('Ctrl Pts',(9.29645780297501,0.355166151432911,3.39375807937372));
#30849=CARTESIAN_POINT('Ctrl Pts',(9.34417363903786,0.702013515586798,3.97085749870423));
#30850=CARTESIAN_POINT('Ctrl Pts',(9.39188947510068,0.404191066510942,4.57471892538967));
#30851=CARTESIAN_POINT('Ctrl Pts',(9.43960531116354,-0.264806258220881,
4.65080711970243));
#30852=CARTESIAN_POINT('Ctrl Pts',(9.48732114722635,-0.690627921460452,
4.12924912203773));
#30853=CARTESIAN_POINT('Ctrl Pts',(9.53503698328922,-0.482235337746388,
3.48899966685243));
#30854=CARTESIAN_POINT('Ctrl Pts',(9.58275281935202,0.169001376764621,3.31800968034731));
#30855=CARTESIAN_POINT('Ctrl Pts',(9.63046865541491,0.665041526572246,3.77330189814918));
#30856=CARTESIAN_POINT('Ctrl Pts',(9.6781844914777,0.550363809549371,4.43677447107931));
#30857=CARTESIAN_POINT('Ctrl Pts',(9.72590032754056,-0.0697214622184181,
4.69915032657822));
#30858=CARTESIAN_POINT('Ctrl Pts',(9.7736161636034,-0.625780442428439,4.31948567936979));
#30859=CARTESIAN_POINT('Ctrl Pts',(9.82133199966623,-0.607175613486645,
3.64643241687702));
#30860=CARTESIAN_POINT('Ctrl Pts',(9.86904783572907,-0.030992076082374,
3.29806570630264));
#30861=CARTESIAN_POINT('Ctrl Pts',(9.91676367179191,0.573651961662729,3.59429605827795));
#30862=CARTESIAN_POINT('Ctrl Pts',(9.96447950785474,0.651502576242943,4.26309058249416));
#30863=CARTESIAN_POINT('Ctrl Pts',(10.0121953439176,0.131068350403577,4.69028497663703));
#30864=CARTESIAN_POINT('Ctrl Pts',(10.0599111799804,-0.50972795835719,4.48358005533451));
#30865=CARTESIAN_POINT('Ctrl Pts',(10.1076270160433,-0.682433239785766,
3.83279612838271));
#30866=CARTESIAN_POINT('Ctrl Pts',(10.1553428521061,-0.228449576533966,
3.33555808949935));
#30867=CARTESIAN_POINT('Ctrl Pts',(10.2030586881689,0.435322847997542,3.44848728078164));
#30868=CARTESIAN_POINT('Ctrl Pts',(10.2507745242318,0.699331602909907,4.06787908823615));
#30869=CARTESIAN_POINT('Ctrl Pts',(10.2984903602946,0.321133386270249,4.62493648450936));
#30870=CARTESIAN_POINT('Ctrl Pts',(10.3462061963575,-0.351966560253669,
4.60810509117381));
#30871=CARTESIAN_POINT('Ctrl Pts',(10.3939220324203,-0.701850198794989,
4.03284143571381));
#30872=CARTESIAN_POINT('Ctrl Pts',(10.4416378684831,-0.407214000429435,
3.42741898450738));
#30873=CARTESIAN_POINT('Ctrl Pts',(10.489353704546,0.261373080323254,3.34780649011919));
#30874=CARTESIAN_POINT('Ctrl Pts',(10.5370695406088,0.689937239673316,3.86711333114163));
#30875=CARTESIAN_POINT('Ctrl Pts',(10.5847853766716,0.484921415782374,4.50845204490092));
#30876=CARTESIAN_POINT('Ctrl Pts',(10.6325012127345,-0.165405205696588,
4.68287142228737));
#30877=CARTESIAN_POINT('Ctrl Pts',(10.6802170487973,-0.66383768169814,4.23019946525991));
#30878=CARTESIAN_POINT('Ctrl Pts',(10.7279328848602,-0.552657800140614,
3.5661317972102));
#30879=CARTESIAN_POINT('Ctrl Pts',(10.775648720923,0.0660362430193439,3.30049197570278));
#30880=CARTESIAN_POINT('Ctrl Pts',(10.8233645569858,0.624088188116435,3.67722113622194));
#30881=CARTESIAN_POINT('Ctrl Pts',(10.8710803930487,0.609030347235101,4.3503630939397));
#30882=CARTESIAN_POINT('Ctrl Pts',(10.9187962291115,0.0346905673513346,
4.70176123146349));
#30883=CARTESIAN_POINT('Ctrl Pts',(10.9665120651743,-0.57150609431415,4.40872123214985));
#30884=CARTESIAN_POINT('Ctrl Pts',(11.0142279012372,-0.65287991581936,3.74034623636848));
#30885=CARTESIAN_POINT('Ctrl Pts',(11.0619437373,-0.134704064778877,3.31041528701663));
#30886=CARTESIAN_POINT('Ctrl Pts',(11.1096595733629,0.507172601636502,3.51374059022208));
#30887=CARTESIAN_POINT('Ctrl Pts',(11.1573754094257,0.68330486411552,4.16360539148934));
#30888=CARTESIAN_POINT('Ctrl Pts',(11.2050912454885,0.231947755880478,4.66322884435941));
#30889=CARTESIAN_POINT('Ctrl Pts',(11.2528070815514,-0.432410545554582,
4.55379904436673));
#30890=CARTESIAN_POINT('Ctrl Pts',(11.3005229176142,-0.699679589515398,
3.93580706063847));
#30891=CARTESIAN_POINT('Ctrl Pts',(11.348238753677,-0.324422100469907,3.37676444086124));
#30892=CARTESIAN_POINT('Ctrl Pts',(11.3959545897399,0.348757195312759,3.39004862475285));
#30893=CARTESIAN_POINT('Ctrl Pts',(11.4436704258027,0.701667392320496,3.9634605418422));
#30894=CARTESIAN_POINT('Ctrl Pts',(11.4913862618656,0.410225626419724,4.57042720558968));
#30895=CARTESIAN_POINT('Ctrl Pts',(11.5391020979284,-0.257932644354891,
4.65356178929341));
#30896=CARTESIAN_POINT('Ctrl Pts',(11.5868179339912,-0.689227399014534,
4.13652052554825));
#30897=CARTESIAN_POINT('Ctrl Pts',(11.6345337700541,-0.487594028032435,
3.49411036255383));
#30898=CARTESIAN_POINT('Ctrl Pts',(11.6822496061169,0.161804441490335,3.31626643773886));
#30899=CARTESIAN_POINT('Ctrl Pts',(11.7299654421798,0.662615402711184,3.76630556374144));
#30900=CARTESIAN_POINT('Ctrl Pts',(11.7776812782426,0.554936443973853,4.43094988641136));
#30901=CARTESIAN_POINT('Ctrl Pts',(11.8253971143054,-0.062349190059417,
4.69984629737339));
#30902=CARTESIAN_POINT('Ctrl Pts',(11.8731129503683,-0.622378603495518,
4.32606308493799));
#30903=CARTESIAN_POINT('Ctrl Pts',(11.9208287864311,-0.610868168815925,
3.65285112447858));
#30904=CARTESIAN_POINT('Ctrl Pts',(11.9685446224939,-0.0383880952977111,
3.29843131798253));
#30905=CARTESIAN_POINT('Ctrl Pts',(12.0162604585568,0.569344356809164,3.58827282720487));
#30906=CARTESIAN_POINT('Ctrl Pts',(12.0639762946196,0.654239125569198,4.25620973444184));
#30907=CARTESIAN_POINT('Ctrl Pts',(12.1116921306825,0.138336038556134,4.68886530024737));
#30908=CARTESIAN_POINT('Ctrl Pts',(12.1594079667453,-0.50460316123658,4.48892526128066));
#30909=CARTESIAN_POINT('Ctrl Pts',(12.2071238028081,-0.684157513748105,
3.83999763179777));
#30910=CARTESIAN_POINT('Ctrl Pts',(12.254839638871,-0.235439494268261,3.33800263898788));
#30911=CARTESIAN_POINT('Ctrl Pts',(12.3025554749338,0.429486235500398,3.44393000893412));
#30912=CARTESIAN_POINT('Ctrl Pts',(12.3502713109967,0.700008146713868,4.06050500791278));
#30913=CARTESIAN_POINT('Ctrl Pts',(12.3979871470595,0.327701805790174,4.62151732713591));
#30914=CARTESIAN_POINT('Ctrl Pts',(12.4457029831223,-0.345538145731053,
4.61178072157682));
#30915=CARTESIAN_POINT('Ctrl Pts',(12.4934188191852,-0.701465101239671,
4.04023646593735));
#30916=CARTESIAN_POINT('Ctrl Pts',(12.541134655248,-0.413225860851952,3.43174244451));
#30917=CARTESIAN_POINT('Ctrl Pts',(12.5888504913108,0.254485045853264,3.34508808005552));
#30918=CARTESIAN_POINT('Ctrl Pts',(12.6365663273737,0.688498419195676,3.85984940880123));
#30919=CARTESIAN_POINT('Ctrl Pts',(12.6842821634365,0.490253100280801,4.50331318193882));
#30920=CARTESIAN_POINT('Ctrl Pts',(12.7319979994994,-0.158199184135511,
4.68457671563321));
#30921=CARTESIAN_POINT('Ctrl Pts',(12.7797138355622,-0.661374723552845,
4.23718291779492));
#30922=CARTESIAN_POINT('Ctrl Pts',(12.827429671625,-0.557199677773407,3.57198039701723));
#30923=CARTESIAN_POINT('Ctrl Pts',(12.8751455076879,0.058660405724426,3.29983486358678));
#30924=CARTESIAN_POINT('Ctrl Pts',(12.9228613437507,0.62065173603916,3.67066174834999));
#30925=CARTESIAN_POINT('Ctrl Pts',(12.9705771798135,0.612689027194643,4.34392501712378));
#30926=CARTESIAN_POINT('Ctrl Pts',(13.0182930158764,0.0420845572448178,
4.7013566507062));
#30927=CARTESIAN_POINT('Ctrl Pts',(13.0660088519392,-0.567166809177069,
4.4147216801859));
#30928=CARTESIAN_POINT('Ctrl Pts',(13.1137246880021,-0.655580167748548,
3.74724140943759));
#30929=CARTESIAN_POINT('Ctrl Pts',(13.1614405240649,-0.141964170879043,
3.31187324159358));
#30930=CARTESIAN_POINT('Ctrl Pts',(13.2091563601277,0.502019708508231,3.50842246418533));
#30931=CARTESIAN_POINT('Ctrl Pts',(13.2568721961906,0.684991165006287,4.15639490180834));
#30932=CARTESIAN_POINT('Ctrl Pts',(13.3045880322534,0.238924694735218,4.66074749465585));
#30933=CARTESIAN_POINT('Ctrl Pts',(13.3523038683163,-0.426549999040181,
4.55832549625387));
#30934=CARTESIAN_POINT('Ctrl Pts',(13.4000197043791,-0.700317265381609,
3.94318460369993));
#30935=CARTESIAN_POINT('Ctrl Pts',(13.4477355404419,-0.330972411156884,
3.38021816378559));
#30936=CARTESIAN_POINT('Ctrl Pts',(13.4954513765048,0.342309500898352,3.3864069206363));
#30937=CARTESIAN_POINT('Ctrl Pts',(13.5431672125676,0.70124333116994,3.95606764360979));
#30938=CARTESIAN_POINT('Ctrl Pts',(13.5908830486304,0.416214620412595,4.5660721254426));
#30939=CARTESIAN_POINT('Ctrl Pts',(13.6385988846933,-0.251030380554765,
4.65624386434224));
#30940=CARTESIAN_POINT('Ctrl Pts',(13.6863147207561,-0.687750320459788,
4.14377676500662));
#30941=CARTESIAN_POINT('Ctrl Pts',(13.734030556819,-0.492898558687668,3.49927725007553));
#30942=CARTESIAN_POINT('Ctrl Pts',(13.7817463928818,0.15458953374652,3.31459914100992));
#30943=CARTESIAN_POINT('Ctrl Pts',(13.8294622289446,0.660115678675556,3.75933518700271));
#30944=CARTESIAN_POINT('Ctrl Pts',(13.8771780650075,0.559447438691528,4.42507743387505));
#30945=CARTESIAN_POINT('Ctrl Pts',(13.9248939010703,-0.0549699924482557,
4.7004645325629));
#30946=CARTESIAN_POINT('Ctrl Pts',(13.9726097371331,-0.61890763370075,4.33260427296601));
#30947=CARTESIAN_POINT('Ctrl Pts',(14.020325573196,-0.614492871807821,3.65930839172987));
#30948=CARTESIAN_POINT('Ctrl Pts',(14.0680414092588,-0.0457798505455885,
3.29887485658241));
#30949=CARTESIAN_POINT('Ctrl Pts',(14.1157572453217,0.564973511886205,3.58229532883235));
#30950=CARTESIAN_POINT('Ctrl Pts',(14.1634730813845,0.656903005118004,4.24930042782804));
#30951=CARTESIAN_POINT('Ctrl Pts',(14.2111889174473,0.145588360997982,4.6873691079691));
#30952=CARTESIAN_POINT('Ctrl Pts',(14.2589047535102,-0.499422315191365,
4.49421615972892));
#30953=CARTESIAN_POINT('Ctrl Pts',(14.306620589573,-0.685805794740406,3.8472169075166));
#30954=CARTESIAN_POINT('Ctrl Pts',(14.3543364256359,-0.242403260500786,
3.34052072000184));
#30955=CARTESIAN_POINT('Ctrl Pts',(14.4020522616987,0.423601917710294,3.43943450270243));
#30956=CARTESIAN_POINT('Ctrl Pts',(14.4497680977615,0.700606936934704,4.05312420698026));
#30957=CARTESIAN_POINT('Ctrl Pts',(14.4974839338244,0.334233825748585,4.61802913456711));
#30958=CARTESIAN_POINT('Ctrl Pts',(14.5451997698872,-0.339071350470923,
4.61538839828042));
#30959=CARTESIAN_POINT('Ctrl Pts',(14.59291560595,-0.701002088269634,4.04762702688518));
#30960=CARTESIAN_POINT('Ctrl Pts',(14.6406314420129,-0.419191822106764,
3.43612902386528));
#30961=CARTESIAN_POINT('Ctrl Pts',(14.6883472780757,0.24756874439201,3.34244241450009));
#30962=CARTESIAN_POINT('Ctrl Pts',(14.7360631141386,0.686983123580828,3.85260105372344));
#30963=CARTESIAN_POINT('Ctrl Pts',(14.7837789502014,0.495530329791292,4.49811841333687));
#30964=CARTESIAN_POINT('Ctrl Pts',(14.8314947862642,-0.150975590559777,
4.68620596944608));
#30965=CARTESIAN_POINT('Ctrl Pts',(14.8792106223271,-0.658838303041738,
4.24414002517693));
#30966=CARTESIAN_POINT('Ctrl Pts',(14.9269264583899,-0.561679664310124,
3.57787653921065));
#30967=CARTESIAN_POINT('Ctrl Pts',(14.9746422944528,0.0512780527100071,
3.29925552249156));
#30968=CARTESIAN_POINT('Ctrl Pts',(15.0223581305156,0.617146344912281,3.6641389418082));
#30969=CARTESIAN_POINT('Ctrl Pts',(15.0700739665784,0.616279652564493,4.337448738749));
#30970=CARTESIAN_POINT('Ctrl Pts',(15.1177898026413,0.0494738725853903,
4.70087416658037));
#30971=CARTESIAN_POINT('Ctrl Pts',(15.1655056387041,-0.562764525842253,
4.42067606290572));
#30972=CARTESIAN_POINT('Ctrl Pts',(15.2132214747669,-0.658207600943685,
3.75416465773151));
#30973=CARTESIAN_POINT('Ctrl Pts',(15.2609373108298,-0.14920850827279,3.31340763002542));
#30974=CARTESIAN_POINT('Ctrl Pts',(15.3086531468926,0.496811053413015,3.50315894024854));
#30975=CARTESIAN_POINT('Ctrl Pts',(15.3563689829554,0.686601380328997,4.14916704052379));
#30976=CARTESIAN_POINT('Ctrl Pts',(15.4040848190183,0.245875094968658,4.6581927522561));
#30977=CARTESIAN_POINT('Ctrl Pts',(15.4518006550811,-0.420642073376032,
4.56278993199436));
#30978=CARTESIAN_POINT('Ctrl Pts',(15.499516491144,-0.700877153329261,3.95056845754601));
#30979=CARTESIAN_POINT('Ctrl Pts',(15.5472323272068,-0.337485958999024,
3.3837407291352));
#30980=CARTESIAN_POINT('Ctrl Pts',(15.5949481632696,0.335823784368978,3.38283337152726));
#30981=CARTESIAN_POINT('Ctrl Pts',(15.6426639993325,0.70074137923783,3.94867962517506));
#30982=CARTESIAN_POINT('Ctrl Pts',(15.6903798353953,0.422157383260532,4.56165416869007));
#30983=CARTESIAN_POINT('Ctrl Pts',(15.7380956714582,-0.244100233491204,
4.65885304693675));
#30984=CARTESIAN_POINT('Ctrl Pts',(15.785811507521,-0.686196849863089,4.15101703442422));
#30985=CARTESIAN_POINT('Ctrl Pts',(15.8335273435838,-0.498148340509996,
3.50449975550414));
#30986=CARTESIAN_POINT('Ctrl Pts',(15.8812431796467,0.147357454930898,3.3130079753559));
#30987=CARTESIAN_POINT('Ctrl Pts',(15.9289590157095,0.657542632122849,3.75239154216938));
#30988=CARTESIAN_POINT('Ctrl Pts',(15.9766748517723,0.563896292642505,4.41915776575455));
#30989=CARTESIAN_POINT('Ctrl Pts',(16.0243906878352,-0.0475846890311933,
4.70100496347609));
#30990=CARTESIAN_POINT('Ctrl Pts',(16.072106523898,-0.615367918582998,4.33910851688972));
#30991=CARTESIAN_POINT('Ctrl Pts',(16.1198223599609,-0.618049319847516,
3.66580350138828));
#30992=CARTESIAN_POINT('Ctrl Pts',(16.1675381960237,-0.0531665207849041,
3.29939627283611));
#30993=CARTESIAN_POINT('Ctrl Pts',(16.2152540320865,0.560539912386559,3.57636422711252));
#30994=CARTESIAN_POINT('Ctrl Pts',(16.2629698681494,0.659493918998266,4.24236343010572));
#30995=CARTESIAN_POINT('Ctrl Pts',(16.3106857042122,0.152824512175573,4.68579656599215));
#30996=CARTESIAN_POINT('Ctrl Pts',(16.358401540275,-0.494185995685336,4.49945216299141));
#30997=CARTESIAN_POINT('Ctrl Pts',(16.4061173763379,-0.687377899679438,
3.85445315365633));
#30998=CARTESIAN_POINT('Ctrl Pts',(16.4538332124007,-0.249340101729437,
3.34311205284473));
#30999=CARTESIAN_POINT('Ctrl Pts',(16.5015490484636,0.417670548229327,3.43500126142608));
#31000=CARTESIAN_POINT('Ctrl Pts',(16.5492648845264,0.701127907061643,4.04573750526291));
#31001=CARTESIAN_POINT('Ctrl Pts',(16.5969807205892,0.340728720599694,4.61447229425484));
#31002=CARTESIAN_POINT('Ctrl Pts',(16.6446965566521,-0.3325668927742,4.61892772056098));
#31003=CARTESIAN_POINT('Ctrl Pts',(16.6924123927149,-0.700461211314163,
4.05501229764889));
#31004=CARTESIAN_POINT('Ctrl Pts',(16.7401282287777,-0.425111221523205,
3.4405782353328));
#31005=CARTESIAN_POINT('Ctrl Pts',(16.7878440648406,0.240624944169445,3.3398697873209));
#31006=CARTESIAN_POINT('Ctrl Pts',(16.8355599009034,0.685391521140609,3.84536907102113));
#31007=CARTESIAN_POINT('Ctrl Pts',(16.8832757369663,0.500752518144239,4.49286831610534));
#31008=CARTESIAN_POINT('Ctrl Pts',(16.9309915730291,-0.143735227331884,
4.68775900275617));
#31009=CARTESIAN_POINT('Ctrl Pts',(16.978707409092,-0.656228701898373,4.25107001464348));
#31010=CARTESIAN_POINT('Ctrl Pts',(17.0264232451548,-0.566097262135119,
3.58381956887496));
#31011=CARTESIAN_POINT('Ctrl Pts',(17.0741390812176,0.0438900039728252,
3.29875401676759));
#31012=CARTESIAN_POINT('Ctrl Pts',(17.1218549172805,0.613572404098014,3.65765344111895));
#31013=CARTESIAN_POINT('Ctrl Pts',(17.1695707533433,0.619801824515016,4.33093497816967));
#31014=CARTESIAN_POINT('Ctrl Pts',(17.2172865894061,0.0568576926029748,
4.70031383267802));
#31015=CARTESIAN_POINT('Ctrl Pts',(17.265002425469,-0.558299733294432,4.42658371892475));
#31016=CARTESIAN_POINT('Ctrl Pts',(17.3127182615318,-0.66076192356197,3.76111521224867));
#31017=CARTESIAN_POINT('Ctrl Pts',(17.3604340975947,-0.156436272293483,
3.31501828187956));
#31018=CARTESIAN_POINT('Ctrl Pts',(17.4081499336575,0.491547214903555,3.49795060305896));
#31019=CARTESIAN_POINT('Ctrl Pts',(17.4558657697204,0.688135331228569,4.14192261047223));
#31020=CARTESIAN_POINT('Ctrl Pts',(17.5035816057831,0.252798184563325,4.65556490092881));
#31021=CARTESIAN_POINT('Ctrl Pts',(17.551297441846,-0.414687424786488,4.56719185569987));
#31022=CARTESIAN_POINT('Ctrl Pts',(17.5990132779088,-0.701359191168653,
3.95795780201324));
#31023=CARTESIAN_POINT('Ctrl Pts',(17.6467291139717,-0.343962020502345,
3.38733174564023));
#31024=CARTESIAN_POINT('Ctrl Pts',(17.6944449500345,0.329300766127249,3.37932837435862));
#31025=CARTESIAN_POINT('Ctrl Pts',(17.7421607860974,0.700161592278611,3.94129730716402));
#31026=CARTESIAN_POINT('Ctrl Pts',(17.7898766221602,0.428053254869629,4.55717382605774));
#31027=CARTESIAN_POINT('Ctrl Pts',(17.837592458223,-0.23714297293205,4.66138904726133));
#31028=CARTESIAN_POINT('Ctrl Pts',(17.8853082942859,-0.684567159776581,
4.15824052958626));
#31029=CARTESIAN_POINT('Ctrl Pts',(17.9330241303487,-0.503342790378573,
3.50977729874859));
#31030=CARTESIAN_POINT('Ctrl Pts',(17.9807399664116,0.140109008348428,3.31149311751593));
#31031=CARTESIAN_POINT('Ctrl Pts',(18.0284558024744,0.654896548854854,3.7454754005085));
#31032=CARTESIAN_POINT('Ctrl Pts',(18.0761716385372,0.568282511669218,4.41319153957849));
#31033=CARTESIAN_POINT('Ctrl Pts',(18.1238874746001,-0.040194100132671,
4.70146753008449));
#31034=CARTESIAN_POINT('Ctrl Pts',(18.1716033106629,-0.611759851316993,
4.34557509424858));
#31035=CARTESIAN_POINT('Ctrl Pts',(18.2193191467258,-0.621537117901666,
3.67233573200791));
#31036=CARTESIAN_POINT('Ctrl Pts',(18.2670349827885,-0.0605472855394143,
3.29999550882718));
#31037=CARTESIAN_POINT('Ctrl Pts',(18.3147508188514,0.556044050773433,3.57048018084402));
#31038=CARTESIAN_POINT('Ctrl Pts',(18.3624666549143,0.662011579423562,4.23539951180373));
#31039=CARTESIAN_POINT('Ctrl Pts',(18.4101824909771,0.160043688331546,4.684147848987));
#31040=CARTESIAN_POINT('Ctrl Pts',(18.4578983270399,-0.488894784343999,
4.50463268947774));
#31041=CARTESIAN_POINT('Ctrl Pts',(18.5056141631028,-0.68887365394326,3.86170556644909));
#31042=CARTESIAN_POINT('Ctrl Pts',(18.5533299991656,-0.256249247442801,
3.34577634968359));
#31043=CARTESIAN_POINT('Ctrl Pts',(18.6010458352284,0.41169278588589,3.4306307775285));
#31044=CARTESIAN_POINT('Ctrl Pts',(18.6487616712913,0.701570999227752,4.03834572324048));
#31045=CARTESIAN_POINT('Ctrl Pts',(18.6964775073541,0.347185768921481,4.6108472012761));
#31046=CARTESIAN_POINT('Ctrl Pts',(18.744193343417,-0.326025495125306,4.62239829528727));
#31047=CARTESIAN_POINT('Ctrl Pts',(18.7919091794798,-0.699842530451103,
4.06239145790787));
#31048=CARTESIAN_POINT('Ctrl Pts',(18.8396250155426,-0.430983401602837,
3.44508958471478));
#31049=CARTESIAN_POINT('Ctrl Pts',(18.8873408516055,0.233654416470602,3.33737048427408));
#31050=CARTESIAN_POINT('Ctrl Pts',(18.9350566876683,0.683723788661416,3.83815426398688));
#31051=CARTESIAN_POINT('Ctrl Pts',(18.9827725237312,0.505919085286118,4.48756347340344));
#31052=CARTESIAN_POINT('Ctrl Pts',(19.030488359794,-0.136478898681533,4.68923564305365));
#31053=CARTESIAN_POINT('Ctrl Pts',(19.0782041958568,-0.653546209976322,
4.2579721164561));
#31054=CARTESIAN_POINT('Ctrl Pts',(19.1259200319197,-0.570451980578726,
3.58980882586423));
#31055=CARTESIAN_POINT('Ctrl Pts',(19.1736358679825,0.0364970801727598,
3.29833040216201));
#31056=CARTESIAN_POINT('Ctrl Pts',(19.2213517040453,0.609930310515188,3.65120596658116));
#31057=CARTESIAN_POINT('Ctrl Pts',(19.2690675401082,0.623255151928734,4.32438445905389));
#31058=CARTESIAN_POINT('Ctrl Pts',(19.316783376171,0.0642351969327414,4.69967571095415));
#31059=CARTESIAN_POINT('Ctrl Pts',(19.3644992122339,-0.553772927074266,
4.43244399258532));
#31060=CARTESIAN_POINT('Ctrl Pts',(19.4122150482967,-0.663242852612724,
3.76809229994096));
#31061=CARTESIAN_POINT('Ctrl Pts',(19.4599308843595,-0.163646658734412,
3.3167050201661));
#31062=CARTESIAN_POINT('Ctrl Pts',(19.5076467204224,0.486228775054438,3.49279802752061));
#31063=CARTESIAN_POINT('Ctrl Pts',(19.5553625564852,0.689592852244711,4.13466242315333));
#31064=CARTESIAN_POINT('Ctrl Pts',(19.6030783925481,0.259693185238344,4.65286421968052));
#31065=CARTESIAN_POINT('Ctrl Pts',(19.6507942286109,-0.408686697131164,
4.57153080275077));
#31066=CARTESIAN_POINT('Ctrl Pts',(19.6985100646738,-0.701763358503738,
3.96535177039745));
#31067=CARTESIAN_POINT('Ctrl Pts',(19.7462259007365,-0.350399813749482,
3.39099090115443));
#31068=CARTESIAN_POINT('Ctrl Pts',(19.7939417367994,0.322741052541778,3.37589215469092));
#31069=CARTESIAN_POINT('Ctrl Pts',(19.8416575728622,0.699504257835039,3.93392181877779));
#31070=CARTESIAN_POINT('Ctrl Pts',(19.8893734089251,0.433901159015506,4.55263101135276));
#31071=CARTESIAN_POINT('Ctrl Pts',(19.9370892449879,-0.23015857608315,4.663852686053));
#31072=CARTESIAN_POINT('Ctrl Pts',(19.9848050810507,-0.682862933423436,
4.16544436654047));
#31073=CARTESIAN_POINT('Ctrl Pts',(20.0325209171136,-0.508478494849655,
3.51511322409123));
#31074=CARTESIAN_POINT('Ctrl Pts',(20.0802367531764,0.132839643288252,3.31004731418368));
#31075=CARTESIAN_POINT('Ctrl Pts',(20.1279525892393,0.652187835720725,3.73860154375571));
#31076=CARTESIAN_POINT('Ctrl Pts',(20.1756684253021,0.572586513039731,4.4071529569233));
#31077=CARTESIAN_POINT('Ctrl Pts',(20.2233842613649,-0.0327629883405684,
4.70190215105461));
#31078=CARTESIAN_POINT('Ctrl Pts',(20.2711000974278,-0.608151935097038,
4.35190888358257));
#31079=CARTESIAN_POINT('Ctrl Pts',(20.3188159334906,-0.624827148513498,
3.67908301574286));
#31080=CARTESIAN_POINT('Ctrl Pts',(20.3665317695535,-0.0681655280739813,
3.30033184185188));
#31081=CARTESIAN_POINT('Ctrl Pts',(20.4142476056163,0.551956769749184,3.56531418539817));
#31082=CARTESIAN_POINT('Ctrl Pts',(20.4540108023353,0.644905999548395,4.11665253813788));
#31083=CARTESIAN_POINT('Ctrl Pts',(20.4858213597105,0.416382673412033,4.45708139504444));
#31084=CARTESIAN_POINT('Ctrl Pts',(20.509679277742,0.148137151166912,4.60177085628536));
#31085=CARTESIAN_POINT('Ctrl Pts',(20.5335371957734,-0.159214575149101,
4.59858486262053));
#31086=CARTESIAN_POINT('Ctrl Pts',(20.5573951138048,-0.426074836374489,
4.44942877587387));
#31087=CARTESIAN_POINT('Ctrl Pts',(20.5812530318362,-0.589577924844292,
4.19016123618585));
#31088=CARTESIAN_POINT('Ctrl Pts',(20.6051109498677,-0.608473233900696,
3.88450759853215));
#31089=CARTESIAN_POINT('Ctrl Pts',(20.6289688678991,-0.478813304308425,
3.60703485797333));
#31090=CARTESIAN_POINT('Ctrl Pts',(20.6528267859305,-0.231947052182395,
3.42568465323223));
#31091=CARTESIAN_POINT('Ctrl Pts',(20.6766847039619,0.0715712039811096,
3.38475332414555));
#31092=CARTESIAN_POINT('Ctrl Pts',(20.7005426219933,0.357622970648114,3.49427550111266));
#31093=CARTESIAN_POINT('Ctrl Pts',(20.7244005400248,0.556207844932749,3.72745636179159));
#31094=CARTESIAN_POINT('Ctrl Pts',(20.7482584580561,0.618794460414918,4.02728407199912));
#31095=CARTESIAN_POINT('Ctrl Pts',(20.7721163760876,0.530063832205264,4.32043875618714));
#31096=CARTESIAN_POINT('Ctrl Pts',(20.7959742941189,0.311720881859749,4.53523813880796));
#31097=CARTESIAN_POINT('Ctrl Pts',(20.8198322121505,0.01715224242355,4.619156844639));
#31098=CARTESIAN_POINT('Ctrl Pts',(20.8436901301818,-0.281609823618225,
4.55167503361081));
#31099=CARTESIAN_POINT('Ctrl Pts',(20.8675480482133,-0.511511021444125,
4.34929354512778));
#31100=CARTESIAN_POINT('Ctrl Pts',(20.8914059662447,-0.616333626991818,
4.06150032559224));
#31101=CARTESIAN_POINT('Ctrl Pts',(20.9152638842761,-0.570445985619195,
3.75866857192897));
#31102=CARTESIAN_POINT('Ctrl Pts',(20.9391218023075,-0.385068702031786,
3.51484894167474));
#31103=CARTESIAN_POINT('Ctrl Pts',(20.9629797203389,-0.105531663562905,
3.38966195221662));
#31104=CARTESIAN_POINT('Ctrl Pts',(20.9868376383704,0.199810758127152,3.41371924506628));
#31105=CARTESIAN_POINT('Ctrl Pts',(21.0106955564018,0.456293997792742,3.58113815016051));
#31106=CARTESIAN_POINT('Ctrl Pts',(21.0345534744332,0.60120093052663,3.85098018832832));
#31107=CARTESIAN_POINT('Ctrl Pts',(21.0584113924646,0.599097856858477,4.15726162902184));
#31108=CARTESIAN_POINT('Ctrl Pts',(21.082269310496,0.450499039416452,4.42508831804098));
#31109=CARTESIAN_POINT('Ctrl Pts',(21.1061272285275,0.191740934787398,4.58896933394457));
#31110=CARTESIAN_POINT('Ctrl Pts',(21.1299851465589,-0.113903050943465,
4.60883130459215));
#31111=CARTESIAN_POINT('Ctrl Pts',(21.1538430645903,-0.391694638258801,
4.47981743698434));
#31112=CARTESIAN_POINT('Ctrl Pts',(21.1777009826217,-0.573706216867813,
4.23347513609622));
#31113=CARTESIAN_POINT('Ctrl Pts',(21.2015589006531,-0.615430998064313,
3.9300418046833));
#31114=CARTESIAN_POINT('Ctrl Pts',(21.2254168186846,-0.506666136201032,
3.64371515765586));
#31115=CARTESIAN_POINT('Ctrl Pts',(21.2492747367159,-0.27400760274365,3.44450985958179));
#31116=CARTESIAN_POINT('Ctrl Pts',(21.2731326547474,0.0256532534100022,
3.38113703208972));
#31117=CARTESIAN_POINT('Ctrl Pts',(21.2969905727788,0.319041190319967,3.46909305773936));
#31118=CARTESIAN_POINT('Ctrl Pts',(21.3208484908102,0.534414865691478,3.68687029238709));
#31119=CARTESIAN_POINT('Ctrl Pts',(21.3447064088416,0.619109549231529,3.98121627002784));
#31120=CARTESIAN_POINT('Ctrl Pts',(21.3685643268731,0.552415083779586,4.28015538130547));
#31121=CARTESIAN_POINT('Ctrl Pts',(21.3924222449044,0.350640082858436,4.51058887057447));
#31122=CARTESIAN_POINT('Ctrl Pts',(21.4162801629359,0.0631240304344945,
4.61616947282646));
#31123=CARTESIAN_POINT('Ctrl Pts',(21.4401380809673,-0.239827566894842,
4.57107985485291));
#31124=CARTESIAN_POINT('Ctrl Pts',(21.4639959989987,-0.484134791346583,
4.38634565646493));
#31125=CARTESIAN_POINT('Ctrl Pts',(21.4878539170302,-0.610057871747176,
4.10713942122688));
#31126=CARTESIAN_POINT('Ctrl Pts',(21.5117118350615,-0.586805184862796,
3.80173467907963));
#31127=CARTESIAN_POINT('Ctrl Pts',(21.535569753093,-0.420062646027161,3.5448112085363));
#31128=CARTESIAN_POINT('Ctrl Pts',(21.5594276711244,-0.150603347961132,
3.39919379659958));
#31129=CARTESIAN_POINT('Ctrl Pts',(21.5832855891558,0.155682571034224,3.40048986702667));
#31130=CARTESIAN_POINT('Ctrl Pts',(21.6071435071872,0.423899860703612,3.54838249529388));
#31131=CARTESIAN_POINT('Ctrl Pts',(21.6310014252187,0.588462087630599,3.80670790527556));
#31132=CARTESIAN_POINT('Ctrl Pts',(21.6548593432501,0.609129304746478,4.11229849758833));
#31133=CARTESIAN_POINT('Ctrl Pts',(21.6787172612815,0.480847814502724,4.39042904829107));
#31134=CARTESIAN_POINT('Ctrl Pts',(21.7025751793129,0.234985935581564,4.57308906161293));
#31135=CARTESIAN_POINT('Ctrl Pts',(21.7264330973443,-0.0683364054776661,
4.61561318873779));
#31136=CARTESIAN_POINT('Ctrl Pts',(21.7502910153758,-0.35494863395129,4.5076031222497));
#31137=CARTESIAN_POINT('Ctrl Pts',(21.7741489334072,-0.554766252817153,
4.2754702655401));
#31138=CARTESIAN_POINT('Ctrl Pts',(21.7980068514386,-0.618928411339905,
3.9759774252466));
#31139=CARTESIAN_POINT('Ctrl Pts',(21.82186476947,-0.531745714018629,3.68235875884208));
#31140=CARTESIAN_POINT('Ctrl Pts',(21.8457226875014,-0.314536705157368,
3.46641202827438));
#31141=CARTESIAN_POINT('Ctrl Pts',(21.8695806055329,-0.0204149040773093,
3.3809420914381));
#31142=CARTESIAN_POINT('Ctrl Pts',(21.8934385235643,0.278698897140474,3.44684867604406));
#31143=CARTESIAN_POINT('Ctrl Pts',(21.9172964415957,0.509663226401888,3.6480158268968));
#31144=CARTESIAN_POINT('Ctrl Pts',(21.9411543596271,0.616001013860485,3.93525269592965));
#31145=CARTESIAN_POINT('Ctrl Pts',(21.9650122776585,0.571709773899469,4.23832204448885));
#31146=CARTESIAN_POINT('Ctrl Pts',(21.98887019569,0.387619921158457,4.48311516140836));
#31147=CARTESIAN_POINT('Ctrl Pts',(22.0127281137213,0.108746439139576,4.60977346157076));
#31148=CARTESIAN_POINT('Ctrl Pts',(22.0365860317528,-0.196718509442517,
4.5873255404835));
#31149=CARTESIAN_POINT('Ctrl Pts',(22.0604439497842,-0.454080423961193,
4.42126052632156));
#31150=CARTESIAN_POINT('Ctrl Pts',(22.0843018678156,-0.600407305919173,
4.15218583856754));
#31151=CARTESIAN_POINT('Ctrl Pts',(22.1081597858471,-0.599918246812857,
3.84589756782496));
#31152=CARTESIAN_POINT('Ctrl Pts',(22.1320177038785,-0.452732834916613,
3.57729153941473));
#31153=CARTESIAN_POINT('Ctrl Pts',(22.1558756219099,-0.194841912687001,
3.41204924396571));
#31154=CARTESIAN_POINT('Ctrl Pts',(22.1797335399413,0.110693164578993,3.39057692382254));
#31155=CARTESIAN_POINT('Ctrl Pts',(22.2035914579728,0.389160747889314,3.51812514615901));
#31156=CARTESIAN_POINT('Ctrl Pts',(22.2274493760041,0.572467927805029,3.76350489626149));
#31157=CARTESIAN_POINT('Ctrl Pts',(22.2513072940356,0.615791105677536,4.06671414123586));
#31158=CARTESIAN_POINT('Ctrl Pts',(22.2751652120669,0.508536584364246,4.35360996140145));
#31159=CARTESIAN_POINT('Ctrl Pts',(22.2990231300984,0.276931015980992,4.55403851389998));
#31160=CARTESIAN_POINT('Ctrl Pts',(22.3228810481298,-0.0223917293827815,
4.61898955797298));
#31161=CARTESIAN_POINT('Ctrl Pts',(22.3467389661613,-0.31623908674035,4.53258079431836));
#31162=CARTESIAN_POINT('Ctrl Pts',(22.3705968841927,-0.532757373651304,
4.31594151899069));
#31163=CARTESIAN_POINT('Ctrl Pts',(22.3944548022241,-0.619001969851995,
4.02204593667267));
#31164=CARTESIAN_POINT('Ctrl Pts',(22.4183127202555,-0.553883724721699,
3.72275952141814));
#31165=CARTESIAN_POINT('Ctrl Pts',(22.4421706382869,-0.35332581843718,3.49126595675675));
#31166=CARTESIAN_POINT('Ctrl Pts',(22.4660285563184,-0.0663701307507445,
3.38417172009386));
#31167=CARTESIAN_POINT('Ctrl Pts',(22.4898864743497,0.236814872379406,3.42766427875767));
#31168=CARTESIAN_POINT('Ctrl Pts',(22.5137443923812,0.482092168510832,3.61110849992699));
#31169=CARTESIAN_POINT('Ctrl Pts',(22.5376023104126,0.609484835267769,3.88964730767638));
#31170=CARTESIAN_POINT('Ctrl Pts',(22.561460228444,0.587841786482003,4.19517031382209));
#31171=CARTESIAN_POINT('Ctrl Pts',(22.5853181464754,0.422455543015367,4.45296893898932));
#31172=CARTESIAN_POINT('Ctrl Pts',(22.6091760645069,0.153767157666155,4.60000417439789));
#31173=CARTESIAN_POINT('Ctrl Pts',(22.6330339825383,-0.152521006364708,
4.60032232020799));
#31174=CARTESIAN_POINT('Ctrl Pts',(22.6568919005697,-0.421514535902825,
4.45384478734481));
#31175=CARTESIAN_POINT('Ctrl Pts',(22.6807498186011,-0.587434568575047,
4.19639082134502));
#31176=CARTESIAN_POINT('Ctrl Pts',(22.7046077366325,-0.60971407867596,3.89091209973551));
#31177=CARTESIAN_POINT('Ctrl Pts',(22.728465654664,-0.482895786937606,3.61211183522625));
#31178=CARTESIAN_POINT('Ctrl Pts',(22.7523235726954,-0.23800784887647,3.4281541921173));
#31179=CARTESIAN_POINT('Ctrl Pts',(22.7761814907268,0.0651013135850054,
3.38404091701771));
#31180=CARTESIAN_POINT('Ctrl Pts',(22.8000394087582,0.352249768808992,3.49052260401466));
#31181=CARTESIAN_POINT('Ctrl Pts',(22.8238973267896,0.553345940411564,3.72163220123786));
#31182=CARTESIAN_POINT('Ctrl Pts',(22.8398026054772,0.597082876783669,3.92101540361374));
#31183=CARTESIAN_POINT('Ctrl Pts',(22.847755244821,0.593766187829899,4.01991291515446));
#31184=CARTESIAN_POINT('',(22.8,0.337479661717902,3.51106003648017));
#31185=CARTESIAN_POINT('Ctrl Pts',(22.8,0.337504360408405,3.51101527402275));
#31186=CARTESIAN_POINT('Ctrl Pts',(22.8,0.337610992569967,3.51114843896934));
#31187=CARTESIAN_POINT('Ctrl Pts',(22.8,0.337717562131928,3.51128164981369));
#31188=CARTESIAN_POINT('Ctrl Pts',(22.8,0.337824069051012,3.51141490653789));
#31189=CARTESIAN_POINT('Ctrl Pts',(22.8,0.354145371784291,3.53183539523119));
#31190=CARTESIAN_POINT('Ctrl Pts',(22.8,0.368999739942303,3.55333386321799));
#31191=CARTESIAN_POINT('Ctrl Pts',(22.8,0.382262544471458,3.57576050230915));
#31192=CARTESIAN_POINT('Ctrl Pts',(22.8,0.395177725624396,3.59759933027929));
#31193=CARTESIAN_POINT('Ctrl Pts',(22.8,0.406583379369087,3.62031953557487));
#31194=CARTESIAN_POINT('Ctrl Pts',(22.8,0.416319965152677,3.64376476659274));
#31195=CARTESIAN_POINT('Ctrl Pts',(22.8,0.420499854003763,3.65382973822867));
#31196=CARTESIAN_POINT('Ctrl Pts',(22.8,0.424371599987778,3.66402799385056));
#31197=CARTESIAN_POINT('Ctrl Pts',(22.8,0.42792023461967,3.67434527679585));
#31198=CARTESIAN_POINT('Ctrl Pts',(22.8,0.430015882150509,3.68043815216119));
#31199=CARTESIAN_POINT('Ctrl Pts',(22.8,0.431995626466768,3.68656321156818));
#31200=CARTESIAN_POINT('Ctrl Pts',(22.8,0.433857425300493,3.69271766785326));
#31201=CARTESIAN_POINT('Ctrl Pts',(22.8,0.440667704273582,3.71523007009016));
#31202=CARTESIAN_POINT('Ctrl Pts',(22.8,0.445903532435623,3.73813926926309));
#31203=CARTESIAN_POINT('Ctrl Pts',(22.8,0.449441836754149,3.76130640751661));
#31204=CARTESIAN_POINT('Ctrl Pts',(22.8,0.450038513826676,3.76521316594877));
#31205=CARTESIAN_POINT('Ctrl Pts',(22.8,0.450586822418701,3.76912718643627));
#31206=CARTESIAN_POINT('Ctrl Pts',(22.8,0.451086059471329,3.77304770583064));
#31207=CARTESIAN_POINT('Ctrl Pts',(22.8,0.453684096906641,3.79345015011803));
#31208=CARTESIAN_POINT('Ctrl Pts',(22.8,0.454954433743694,3.81403106227893));
#31209=CARTESIAN_POINT('Ctrl Pts',(22.8,0.45484641916779,3.83463783350426));
#31210=CARTESIAN_POINT('Ctrl Pts',(22.8,0.454808390965019,3.84189276616533));
#31211=CARTESIAN_POINT('Ctrl Pts',(22.8,0.454599381710613,3.84915061719132));
#31212=CARTESIAN_POINT('Ctrl Pts',(22.8,0.454216814112443,3.8564037154462));
#31213=CARTESIAN_POINT('Ctrl Pts',(22.8,0.453866695925276,3.86304160538904));
#31214=CARTESIAN_POINT('Ctrl Pts',(22.8,0.453371644107099,3.86966645154658));
#31215=CARTESIAN_POINT('Ctrl Pts',(22.8,0.452731182295137,3.87626933737115));
#31216=CARTESIAN_POINT('Ctrl Pts',(22.8,0.450713457978438,3.89707120727158));
#31217=CARTESIAN_POINT('Ctrl Pts',(22.8,0.447253508643,3.9176725514372));
#31218=CARTESIAN_POINT('Ctrl Pts',(22.8,0.442312061254715,3.9379035771693));
#31219=CARTESIAN_POINT('Ctrl Pts',(22.8,0.437564183511961,3.95734209977996));
#31220=CARTESIAN_POINT('Ctrl Pts',(22.8,0.431447509288203,3.97643919003209));
#31221=CARTESIAN_POINT('Ctrl Pts',(22.8,0.423915075143768,3.9949978423605));
#31222=CARTESIAN_POINT('Ctrl Pts',(22.8,0.421325190817866,4.00137888225459));
#31223=CARTESIAN_POINT('Ctrl Pts',(22.8,0.418567902041021,4.00769582483512));
#31224=CARTESIAN_POINT('Ctrl Pts',(22.8,0.415641328671541,4.01393920819689));
#31225=CARTESIAN_POINT('Ctrl Pts',(22.6211545887425,-1.51173456864708E-7,
4.59404872180247));
#31226=CARTESIAN_POINT('Ctrl Pts',(22.6251143866744,-0.0492822808754852,
4.59404929162283));
#31227=CARTESIAN_POINT('Ctrl Pts',(22.6290741846063,-0.0985642856931001,
4.58798571459226));
#31228=CARTESIAN_POINT('Ctrl Pts',(22.6330339825383,-0.14630523394925,4.57585637376244));
#31229=CARTESIAN_POINT('Ctrl Pts',(22.6409866218821,-0.242185516210759,
4.55149647592026));
#31230=CARTESIAN_POINT('Ctrl Pts',(22.6489392612259,-0.331850026056775,
4.50267063163255));
#31231=CARTESIAN_POINT('Ctrl Pts',(22.6568919005697,-0.404335619758509,
4.43534871515538));
#31232=CARTESIAN_POINT('Ctrl Pts',(22.6648445399135,-0.476821213460227,
4.36802679867822));
#31233=CARTESIAN_POINT('Ctrl Pts',(22.6727971792573,-0.532127891017642,
4.28220881001161));
#31234=CARTESIAN_POINT('Ctrl Pts',(22.6807498186011,-0.563494481479829,
4.18838669541007));
#31235=CARTESIAN_POINT('Ctrl Pts',(22.6887024579449,-0.594861071942019,
4.09456458080851));
#31236=CARTESIAN_POINT('Ctrl Pts',(22.6966550972887,-0.602287575308989,
3.99273834027202));
#31237=CARTESIAN_POINT('Ctrl Pts',(22.7046077366325,-0.584864445036083,
3.89535850925222));
#31238=CARTESIAN_POINT('Ctrl Pts',(22.7125603759763,-0.567441314763176,
3.79797867823242));
#31239=CARTESIAN_POINT('Ctrl Pts',(22.7205130153201,-0.525168550850394,
3.70504525672934));
#31240=CARTESIAN_POINT('Ctrl Pts',(22.7284656546639,-0.463217512550482,
3.62791893879298));
#31241=CARTESIAN_POINT('Ctrl Pts',(22.7364182940078,-0.401266474250563,
3.5507926208566));
#31242=CARTESIAN_POINT('Ctrl Pts',(22.7443709333516,-0.319637161563486,
3.48947340648693));
#31243=CARTESIAN_POINT('Ctrl Pts',(22.7523235726954,-0.228304311476372,
3.45146158678551));
#31244=CARTESIAN_POINT('Ctrl Pts',(22.7602762120392,-0.136971461389268,
3.41344976708409));
#31245=CARTESIAN_POINT('Ctrl Pts',(22.768228851383,-0.0359350739021178,
3.3987453420509));
#31246=CARTESIAN_POINT('Ctrl Pts',(22.7761814907268,0.062441195712126,3.40914007736714));
#31247=CARTESIAN_POINT('Ctrl Pts',(22.7841209938178,0.160654966376612,3.41951764255099));
#31248=CARTESIAN_POINT('Ctrl Pts',(22.7920604969089,0.256217399931083,3.45491151845628));
#31249=CARTESIAN_POINT('Ctrl Pts',(22.8,0.337504360408238,3.51101527402264));
#31250=CARTESIAN_POINT('Ctrl Pts',(4.,-0.219914231356244,4.35301468169996));
#31251=CARTESIAN_POINT('Ctrl Pts',(4.00793950309107,-0.278596966840389,
4.31645650682028));
#31252=CARTESIAN_POINT('Ctrl Pts',(4.02383164552594,-0.377405665439666,
4.21337674819164));
#31253=CARTESIAN_POINT('Ctrl Pts',(4.04767642730463,-0.433534992178268,
4.00656196868444));
#31254=CARTESIAN_POINT('Ctrl Pts',(4.07153434533603,-0.383670022685343,
3.79803920418254));
#31255=CARTESIAN_POINT('Ctrl Pts',(4.09539226336747,-0.239994733226421,
3.63889579340969));
#31256=CARTESIAN_POINT('Ctrl Pts',(4.11925018139887,-0.0376302499649443,
3.56805514133307));
#31257=CARTESIAN_POINT('Ctrl Pts',(4.1431080994303,0.173933765839147,3.60283521426327));
#31258=CARTESIAN_POINT('Ctrl Pts',(4.16696601746172,0.342967344134064,3.73473372141871));
#31259=CARTESIAN_POINT('Ctrl Pts',(4.19082393549313,0.428135478754777,3.93149662217858));
#31260=CARTESIAN_POINT('Ctrl Pts',(4.21468185352456,0.40861313688017,4.1450106963618));
#31261=CARTESIAN_POINT('Ctrl Pts',(4.23853977155597,0.289173588337559,4.32306558264197));
#31262=CARTESIAN_POINT('Ctrl Pts',(4.25811226835493,0.13317859508208,4.40432939198872));
#31263=CARTESIAN_POINT('Ctrl Pts',(4.26973212581007,0.0319512750557707,
4.41584666103033));
#31264=CARTESIAN_POINT('Ctrl Pts',(4.2733993439214,2.51014653359152E-6,
4.41583996132385));
#31265=CARTESIAN_POINT('Origin',(3.42660065607856,0.,4.));
#31266=CARTESIAN_POINT('Ctrl Pts',(4.,-0.219892372743211,3.64701365460636));
#31267=CARTESIAN_POINT('Ctrl Pts',(4.00795263934381,-0.161099076858729,
3.61038844940468));
#31268=CARTESIAN_POINT('Ctrl Pts',(4.02385791803142,-0.0249198690254346,
3.56711791692558));
#31269=CARTESIAN_POINT('Ctrl Pts',(4.04771583606284,0.185569069288609,3.60813812632505));
#31270=CARTESIAN_POINT('Ctrl Pts',(4.07157375409426,0.350624105231944,3.74494568050885));
#31271=CARTESIAN_POINT('Ctrl Pts',(4.09543167212568,0.429971014252744,3.94413788601839));
#31272=CARTESIAN_POINT('Ctrl Pts',(4.1192895901571,0.40416308778273,4.15698104289539));
#31273=CARTESIAN_POINT('Ctrl Pts',(4.14314750818851,0.279534313346206,4.3314427366163));
#31274=CARTESIAN_POINT('Ctrl Pts',(4.16225119682902,0.125004509401131,4.40624063703925));
#31275=CARTESIAN_POINT('Ctrl Pts',(4.1734022461257,0.0278694809177792,4.41585864517498));
#31276=CARTESIAN_POINT('Ctrl Pts',(4.17660065607858,5.88453344126799E-6,
4.41584444980552));
#31277=CARTESIAN_POINT('Ctrl Pts',(3.95224475517896,-0.314128184302177,
3.49573985500833));
#31278=CARTESIAN_POINT('Ctrl Pts',(3.96019739452277,-0.230138771413741,
3.44341876234755));
#31279=CARTESIAN_POINT('Ctrl Pts',(3.97610267321038,-0.0355993848822847,
3.38160445914153));
#31280=CARTESIAN_POINT('Ctrl Pts',(3.9999605912418,0.265095483172694,3.44020405374152));
#31281=CARTESIAN_POINT('Ctrl Pts',(4.02381850927322,0.500885556761892,3.63564106712445));
#31282=CARTESIAN_POINT('Ctrl Pts',(4.04767642730465,0.614236921112272,3.92019793948569));
#31283=CARTESIAN_POINT('Ctrl Pts',(4.07153434533605,0.577368897990231,4.22425593648149));
#31284=CARTESIAN_POINT('Ctrl Pts',(4.09539226336749,0.399329932212592,4.47348393104611));
#31285=CARTESIAN_POINT('Ctrl Pts',(4.11925018139889,0.123637843932736,4.60692867011962));
#31286=CARTESIAN_POINT('Ctrl Pts',(4.14310809943032,-0.182283847264271,
4.59196468982869));
#31287=CARTESIAN_POINT('Ctrl Pts',(4.16696601746173,-0.443633876576525,
4.43224822622665));
#31288=CARTESIAN_POINT('Ctrl Pts',(4.19082393549315,-0.596502436238336,
4.16683582239239));
#31289=CARTESIAN_POINT('Ctrl Pts',(4.21468185352458,-0.603510379797736,
3.86062723727387));
#31290=CARTESIAN_POINT('Ctrl Pts',(4.23853977155598,-0.462943343075553,
3.58849923641164));
#31291=CARTESIAN_POINT('Ctrl Pts',(4.26239768958742,-0.209174182705692,
3.41699430327496));
#31292=CARTESIAN_POINT('Ctrl Pts',(4.28625560761882,0.0957438341235747,
3.38805018506757));
#31293=CARTESIAN_POINT('Ctrl Pts',(4.31011352565025,0.377249837899377,3.50874444390425));
#31294=CARTESIAN_POINT('Ctrl Pts',(4.33397144368167,0.566508000142931,3.7495640793295));
#31295=CARTESIAN_POINT('Ctrl Pts',(4.35782936171309,0.617239514437223,4.05162211295782));
#31296=CARTESIAN_POINT('Ctrl Pts',(4.3816872797445,0.517039159770137,4.34105713706075));
#31297=CARTESIAN_POINT('Ctrl Pts',(4.40554519777592,0.290408643717306,4.54709439922074));
#31298=CARTESIAN_POINT('Ctrl Pts',(4.42940311580735,-0.00723469473045889,
4.61935217913086));
#31299=CARTESIAN_POINT('Ctrl Pts',(4.45326103383876,-0.303108954077165,
4.54016147994594));
#31300=CARTESIAN_POINT('Ctrl Pts',(4.47711895187019,-0.524864817190473,
4.3288865854667));
#31301=CARTESIAN_POINT('Ctrl Pts',(4.5009768699016,-0.618276935702851,4.03718996201469));
#31302=CARTESIAN_POINT('Ctrl Pts',(4.52483478793302,-0.560503501787052,
3.7363993798876));
#31303=CARTESIAN_POINT('Ctrl Pts',(4.54869270596444,-0.365671693940747,
3.50006632967672));
#31304=CARTESIAN_POINT('Ctrl Pts',(4.57255062399586,-0.0814231961944085,
3.38598067979976));
#31305=CARTESIAN_POINT('Ctrl Pts',(4.59640854202727,0.222735490926488,3.42203947925158));
#31306=CARTESIAN_POINT('Ctrl Pts',(4.6202664600587,0.472429283332598,3.59942536936051));
#31307=CARTESIAN_POINT('Ctrl Pts',(4.64412437809011,0.606601247243452,3.87476266809168));
#31308=CARTESIAN_POINT('Ctrl Pts',(4.66798229612153,0.592442682719785,4.18072390587243));
#31309=CARTESIAN_POINT('Ctrl Pts',(4.69184021415295,0.433415744455024,4.44249322584619));
#31310=CARTESIAN_POINT('Ctrl Pts',(4.71569813218437,0.168406850663934,4.59606089882753));
#31311=CARTESIAN_POINT('Ctrl Pts',(4.7395560502158,-0.1377821054254,4.60387544567241));
#31312=CARTESIAN_POINT('Ctrl Pts',(4.7634139682472,-0.410279583628813,4.46402599681362));
#31313=CARTESIAN_POINT('Ctrl Pts',(4.78727188627863,-0.582452527843622,
4.21070955191949));
#31314=CARTESIAN_POINT('Ctrl Pts',(4.81112980431005,-0.612199963312297,
3.9058688819681));
#31315=CARTESIAN_POINT('Ctrl Pts',(4.83498772234147,-0.492247831758966,
3.62404583445569));
#31316=CARTESIAN_POINT('Ctrl Pts',(4.85884564037289,-0.251927696778831,
3.4341538212047));
#31317=CARTESIAN_POINT('Ctrl Pts',(4.88270355840431,0.0499956224363984,
3.38262661200963));
#31318=CARTESIAN_POINT('Ctrl Pts',(4.90656147643572,0.339693650112522,3.48206401309162));
#31319=CARTESIAN_POINT('Ctrl Pts',(4.93041939446714,0.546327327266884,3.70815087126575));
#31320=CARTESIAN_POINT('Ctrl Pts',(4.95427731249857,0.619369091246891,4.00560279122603));
#31321=CARTESIAN_POINT('Ctrl Pts',(4.97813523052998,0.540958241141728,4.3016846761146));
#31322=CARTESIAN_POINT('Ctrl Pts',(5.00199314856141,0.330268365670778,4.52399643996756));
#31323=CARTESIAN_POINT('Ctrl Pts',(5.02585106659282,0.0388188784636707,
4.61817680087201));
#31324=CARTESIAN_POINT('Ctrl Pts',(5.04970898462424,-0.262122881932824,
4.56119609516527));
#31325=CARTESIAN_POINT('Ctrl Pts',(5.07356690265566,-0.498968457612796,
4.36698765751594));
#31326=CARTESIAN_POINT('Ctrl Pts',(5.09742482068708,-0.613802653778546,
4.08304074106085));
#31327=CARTESIAN_POINT('Ctrl Pts',(5.12128273871849,-0.578545381446849,
3.77878810143205));
#31328=CARTESIAN_POINT('Ctrl Pts',(5.14514065674992,-0.40181800409162,3.52862779669421));
#31329=CARTESIAN_POINT('Ctrl Pts',(5.16899857478133,-0.126835179433317,
3.39373083558568));
#31330=CARTESIAN_POINT('Ctrl Pts',(5.19285649281276,0.179162301517353,3.4070831996169));
#31331=CARTESIAN_POINT('Ctrl Pts',(5.21671441084417,0.441349719463922,3.56541987207117));
#31332=CARTESIAN_POINT('Ctrl Pts',(5.24057232887559,0.595615108876583,3.83002322352904));
#31333=CARTESIAN_POINT('Ctrl Pts',(5.26443024690701,0.604236379939102,4.13619052690848));
#31334=CARTESIAN_POINT('Ctrl Pts',(5.28828816493843,0.465105397037983,4.40905553670335));
#31335=CARTESIAN_POINT('Ctrl Pts',(5.31214608296985,0.21224347534444,4.58189532532512));
#31336=CARTESIAN_POINT('Ctrl Pts',(5.33600400100126,-0.0925177574670201,
4.61244585639451));
#31337=CARTESIAN_POINT('Ctrl Pts',(5.35986191903269,-0.37465587844466,4.49323669288525));
#31338=CARTESIAN_POINT('Ctrl Pts',(5.3837198370641,-0.565180431721392,4.25341772246777));
#31339=CARTESIAN_POINT('Ctrl Pts',(5.40757775509553,-0.617502974236318,
3.95163121594683));
#31340=CARTESIAN_POINT('Ctrl Pts',(5.43143567312694,-0.518829219107294,
3.66167219466597));
#31341=CARTESIAN_POINT('Ctrl Pts',(5.45529359115837,-0.293287587282116,
3.45444353765392));
#31342=CARTESIAN_POINT('Ctrl Pts',(5.47915150918978,0.00397084862654925,
3.38061829634467));
#31343=CARTESIAN_POINT('Ctrl Pts',(5.50300942722121,0.300258303883157,3.45824875319892));
#31344=CARTESIAN_POINT('Ctrl Pts',(5.52686734525262,0.523124424966688,3.66835214690199));
#31345=CARTESIAN_POINT('Ctrl Pts',(5.55072526328404,0.618072374525773,3.95955247459688));
#31346=CARTESIAN_POINT('Ctrl Pts',(5.57458318131546,0.561884792553919,4.26064332401524));
#31347=CARTESIAN_POINT('Ctrl Pts',(5.59844109934688,0.368301073379394,4.49799978094171));
#31348=CARTESIAN_POINT('Ctrl Pts',(5.62229901737829,0.0846577094226282,
4.61358172616469));
#31349=CARTESIAN_POINT('Ctrl Pts',(5.64615693540972,-0.219686770477705,
4.57912622575047));
#31350=CARTESIAN_POINT('Ctrl Pts',(5.67001485344113,-0.470311850924231,
4.40305858798173));
#31351=CARTESIAN_POINT('Ctrl Pts',(5.69387277147256,-0.605932872639677,
4.12843214650112));
#31352=CARTESIAN_POINT('Ctrl Pts',(5.71773068950397,-0.593386801983745,
3.82240054650545));
#31353=CARTESIAN_POINT('Ctrl Pts',(5.74158860753539,-0.435741494202748,
3.55979685111874));
#31354=CARTESIAN_POINT('Ctrl Pts',(5.76544652556682,-0.171545522688555,
3.40483481554927));
#31355=CARTESIAN_POINT('Ctrl Pts',(5.78930444359822,0.134598003740687,3.39540688139736));
#31356=CARTESIAN_POINT('Ctrl Pts',(5.81316236162965,0.407828648458881,3.53381843004554));
#31357=CARTESIAN_POINT('Ctrl Pts',(5.83702027966106,0.58133408605803,3.78622407765735));
#31358=CARTESIAN_POINT('Ctrl Pts',(5.86087819769249,0.612687492198482,4.09090374899912));
#31359=CARTESIAN_POINT('Ctrl Pts',(5.8847361157239,0.494222140250734,4.3733550009975));
#31360=CARTESIAN_POINT('Ctrl Pts',(5.90859403375532,0.254905969192102,4.56451074097759));
#31361=CARTESIAN_POINT('Ctrl Pts',(5.93245195178675,-0.0467415727364197,
4.61762831145024));
#31362=CARTESIAN_POINT('Ctrl Pts',(5.95630986981815,-0.336959681931401,
4.51971877801409));
#31363=CARTESIAN_POINT('Ctrl Pts',(5.98016778784959,-0.544781677596122,
4.29472414464893));
#31364=CARTESIAN_POINT('Ctrl Pts',(6.00402570588099,-0.61939026621187,3.99766086682344));
#31365=CARTESIAN_POINT('Ctrl Pts',(6.02788362391242,-0.542540019317823,
3.70117063377655));
#31366=CARTESIAN_POINT('Ctrl Pts',(6.05174154194384,-0.333025929677459,
3.47775031355921));
#31367=CARTESIAN_POINT('Ctrl Pts',(6.07559945997526,-0.042074208138152,
3.38203805739984));
#31368=CARTESIAN_POINT('Ctrl Pts',(6.09945737800668,0.259158778028439,3.43742717299816));
#31369=CARTESIAN_POINT('Ctrl Pts',(6.12331529603809,0.497033648893269,3.63039418124561));
#31370=CARTESIAN_POINT('Ctrl Pts',(6.14717321406952,0.613345206175343,3.91371436613889));
#31371=CARTESIAN_POINT('Ctrl Pts',(6.17103113210093,0.579724447951105,4.21818191418763));
#31372=CARTESIAN_POINT('Ctrl Pts',(6.19488905013236,0.40425597056565,4.46920707734689));
#31373=CARTESIAN_POINT('Ctrl Pts',(6.21874696816377,0.13010450107023,4.60567007851858));
#31374=CARTESIAN_POINT('Ctrl Pts',(6.24260488619519,-0.176179318911185,
4.59370602015056));
#31375=CARTESIAN_POINT('Ctrl Pts',(6.26646280422661,-0.438782409775579,
4.43717629804221));
#31376=CARTESIAN_POINT('Ctrl Pts',(6.29032072225803,-0.595217424383659,
4.17259489198797));
#31377=CARTESIAN_POINT('Ctrl Pts',(6.31417864028945,-0.604035436411749,
3.86794272465182));
#31378=CARTESIAN_POINT('Ctrl Pts',(6.34598919766468,-0.423477061217623,
3.4998212904071));
#31379=CARTESIAN_POINT('Ctrl Pts',(6.3857523943837,0.100470573235224,3.30464850830547));
#31380=CARTESIAN_POINT('Ctrl Pts',(6.43346823044655,0.640013163212275,3.70919899990029));
#31381=CARTESIAN_POINT('Ctrl Pts',(6.48118406650937,0.590335835129396,4.3806576914582));
#31382=CARTESIAN_POINT('Ctrl Pts',(6.52889990257223,-0.000686065451295705,
4.70262946694599));
#31383=CARTESIAN_POINT('Ctrl Pts',(6.57661573863505,-0.591483599613884,
4.37932465573422));
#31384=CARTESIAN_POINT('Ctrl Pts',(6.6243315746979,-0.638898060441451,3.70770201230499));
#31385=CARTESIAN_POINT('Ctrl Pts',(6.67204741076074,-0.0997162142428727,
3.30448953810453));
#31386=CARTESIAN_POINT('Ctrl Pts',(6.71976324682356,0.531096731682035,3.53998115137447));
#31387=CARTESIAN_POINT('Ctrl Pts',(6.76747908288643,0.674163513320998,4.19791190586338));
#31388=CARTESIAN_POINT('Ctrl Pts',(6.81519491894923,0.19815244237474,4.67409883091767));
#31389=CARTESIAN_POINT('Ctrl Pts',(6.86291075501209,-0.459834002450772,
4.53124951681343));
#31390=CARTESIAN_POINT('Ctrl Pts',(6.91062659107492,-0.695543074258338,
3.90054607923755));
#31391=CARTESIAN_POINT('Ctrl Pts',(6.95834242713776,-0.292526745343327,
3.36117245204842));
#31392=CARTESIAN_POINT('Ctrl Pts',(7.00605826320061,0.379122722467859,3.40844412700009));
#31393=CARTESIAN_POINT('Ctrl Pts',(7.05377409926343,0.702617257610868,3.99895059076549));
#31394=CARTESIAN_POINT('Ctrl Pts',(7.10148993532628,0.380887926283931,4.59042078110798));
#31395=CARTESIAN_POINT('Ctrl Pts',(7.14920577138911,-0.290616845661789,
4.63969846327979));
#31396=CARTESIAN_POINT('Ctrl Pts',(7.19692160745196,-0.695243592084394,
4.10153121423426));
#31397=CARTESIAN_POINT('Ctrl Pts',(7.24463744351478,-0.461417505508394,
3.47012628326466));
#31398=CARTESIAN_POINT('Ctrl Pts',(7.29235327957764,0.196135405489393,3.32531254251214));
#31399=CARTESIAN_POINT('Ctrl Pts',(7.34006911564046,0.673574140181709,3.80007467379138));
#31400=CARTESIAN_POINT('Ctrl Pts',(7.38778495170331,0.532459385890787,4.45843130921146));
#31401=CARTESIAN_POINT('Ctrl Pts',(7.43550078776614,-0.0976210197556089,
4.69580341906706));
#31402=CARTESIAN_POINT('Ctrl Pts',(7.48321662382899,-0.638054538563543,
4.29420854311633));
#31403=CARTESIAN_POINT('Ctrl Pts',(7.53093245989182,-0.592552758097988,
3.62243743491725));
#31404=CARTESIAN_POINT('Ctrl Pts',(7.57864829595465,-0.00290066162856385,
3.29738783984629));
#31405=CARTESIAN_POINT('Ctrl Pts',(7.6263641320175,0.589415156704478,3.61755780248734));
#31406=CARTESIAN_POINT('Ctrl Pts',(7.67407996808033,0.64046196749915,4.28893031975233));
#31407=CARTESIAN_POINT('Ctrl Pts',(7.72179580414318,0.103362698669259,4.69497367861456));
#31408=CARTESIAN_POINT('Ctrl Pts',(7.769511640206,-0.528656126737314,4.46281201486565));
#31409=CARTESIAN_POINT('Ctrl Pts',(7.81722747626886,-0.675201896567852,
3.80564295658466));
#31410=CARTESIAN_POINT('Ctrl Pts',(7.86494331233168,-0.201699375449268,
3.32695496184095));
#31411=CARTESIAN_POINT('Ctrl Pts',(7.91265914839452,0.457026785680635,3.46633458176699));
#31412=CARTESIAN_POINT('Ctrl Pts',(7.96037498445737,0.696058217263005,4.09578736675475));
#31413=CARTESIAN_POINT('Ctrl Pts',(8.0080908205202,0.295888677698302,4.63727713897333));
#31414=CARTESIAN_POINT('Ctrl Pts',(8.05580665658303,-0.375999987428149,
4.59354550870361));
#31415=CARTESIAN_POINT('Ctrl Pts',(8.10352249264589,-0.702602078596463,
4.00475190491975));
#31416=CARTESIAN_POINT('Ctrl Pts',(8.1512383287087,-0.383993870066737,3.41159455373064));
#31417=CARTESIAN_POINT('Ctrl Pts',(8.19895416477156,0.287241817850264,3.35877897763223));
#31418=CARTESIAN_POINT('Ctrl Pts',(8.24667000083438,0.694698924651979,3.89480653282778));
#31419=CARTESIAN_POINT('Ctrl Pts',(8.29438583689724,0.464203319628796,4.52743486753713));
#31420=CARTESIAN_POINT('Ctrl Pts',(8.34210167296006,-0.192577336495663,
4.67571164775853));
#31421=CARTESIAN_POINT('Ctrl Pts',(8.3898175090229,-0.672511261332963,4.20347202468314));
#31422=CARTESIAN_POINT('Ctrl Pts',(8.43753334508575,-0.534867746972347,
3.54438091052171));
#31423=CARTESIAN_POINT('Ctrl Pts',(8.48524918114857,0.0939530494311211,
3.303691816829));
#31424=CARTESIAN_POINT('Ctrl Pts',(8.53296501721143,0.636495314888509,3.70243324182078));
#31425=CARTESIAN_POINT('Ctrl Pts',(8.58068085327425,0.594534138944492,4.37443479950165));
#31426=CARTESIAN_POINT('Ctrl Pts',(8.6283966893371,0.00660311512414562,
4.7025871193802));
#31427=CARTESIAN_POINT('Ctrl Pts',(8.67611252539993,-0.58739165091669,4.3855428768395));
#31428=CARTESIAN_POINT('Ctrl Pts',(8.72382836146277,-0.64197562573843,3.71444867815739));
#31429=CARTESIAN_POINT('Ctrl Pts',(8.77154419752561,-0.107023505379864,
3.30558065209521));
#31430=CARTESIAN_POINT('Ctrl Pts',(8.81926003358845,0.526209946737336,3.53440859822909));
#31431=CARTESIAN_POINT('Ctrl Pts',(8.86697586965128,0.676216707984864,4.19079629265377));
#31432=CARTESIAN_POINT('Ctrl Pts',(8.91469170571413,0.20524326135842,4.67197281575615));
#31433=CARTESIAN_POINT('Ctrl Pts',(8.96240754177695,-0.45420823024697,4.53606636251889));
#31434=CARTESIAN_POINT('Ctrl Pts',(9.0101233778398,-0.69655331512461,3.90788192013928));
#31435=CARTESIAN_POINT('Ctrl Pts',(9.05783921390263,-0.299242772872918,
3.36429092791464));
#31436=CARTESIAN_POINT('Ctrl Pts',(9.10555504996548,0.37286701214988,3.40448135822736));
#31437=CARTESIAN_POINT('Ctrl Pts',(9.15327088602831,0.702567282619003,3.99154572051203));
#31438=CARTESIAN_POINT('Ctrl Pts',(9.20098672209116,0.387089207071907,4.58637377773631));
#31439=CARTESIAN_POINT('Ctrl Pts',(9.24870255815397,-0.28385884346236,4.64272577234503));
#31440=CARTESIAN_POINT('Ctrl Pts',(9.29641839421684,-0.694134950315416,
4.10885280060212));
#31441=CARTESIAN_POINT('Ctrl Pts',(9.34413423027966,-0.46697625165475,3.47501862715065));
#31442=CARTESIAN_POINT('Ctrl Pts',(9.39185006634251,0.189013924253689,3.32328292626348));
#31443=CARTESIAN_POINT('Ctrl Pts',(9.43956590240535,0.671429705166911,3.79298692681914));
#31444=CARTESIAN_POINT('Ctrl Pts',(9.48728173846818,0.537261256551386,4.45279421778236));
#31445=CARTESIAN_POINT('Ctrl Pts',(9.53499757453101,-0.090282470782305,
4.69679361142145));
#31446=CARTESIAN_POINT('Ctrl Pts',(9.58271341059386,-0.634918416022234,
4.30091671014441));
#31447=CARTESIAN_POINT('Ctrl Pts',(9.63042924665669,-0.596499010353368,
3.62870336374299));
#31448=CARTESIAN_POINT('Ctrl Pts',(9.67814508271953,-0.0103053851599677,
3.29745743154951));
#31449=CARTESIAN_POINT('Ctrl Pts',(9.72586091878236,0.585351833794561,3.61136714997101));
#31450=CARTESIAN_POINT('Ctrl Pts',(9.77357675484522,0.643471456979869,4.28216439445919));
#31451=CARTESIAN_POINT('Ctrl Pts',(9.82129259090803,0.110681340139534,4.69384573385819));
#31452=CARTESIAN_POINT('Ctrl Pts',(9.8690084269709,-0.523749154402255,4.46835785966634));
#31453=CARTESIAN_POINT('Ctrl Pts',(9.91672426303372,-0.677212741539845,
3.81276975633088));
#31454=CARTESIAN_POINT('Ctrl Pts',(9.96444009909655,-0.208781447863971,
3.32911806666439));
#31455=CARTESIAN_POINT('Ctrl Pts',(10.0121559351594,0.451377061900895,3.4615475792254));
#31456=CARTESIAN_POINT('Ctrl Pts',(10.0598717712222,0.697029070393332,4.08844623493918));
#31457=CARTESIAN_POINT('Ctrl Pts',(10.1075876072851,0.302588558372737,4.63412335218805));
#31458=CARTESIAN_POINT('Ctrl Pts',(10.1553034433479,-0.369723682724971,
4.5974752378807));
#31459=CARTESIAN_POINT('Ctrl Pts',(10.2030192794108,-0.702512977046242,
4.01215641928927));
#31460=CARTESIAN_POINT('Ctrl Pts',(10.2507351154736,-0.390173794994359,
3.41567417381395));
#31461=CARTESIAN_POINT('Ctrl Pts',(10.2984509515364,0.280467986596366,3.3557873255338));
#31462=CARTESIAN_POINT('Ctrl Pts',(10.3461667875993,0.693551700540965,3.8874908887021));
#31463=CARTESIAN_POINT('Ctrl Pts',(10.3938826236621,0.469736216214169,4.52251329995044));
#31464=CARTESIAN_POINT('Ctrl Pts',(10.441598459725,-0.185445263282835,4.67770370795377));
#31465=CARTESIAN_POINT('Ctrl Pts',(10.4893142957878,-0.670329504065059,
4.21054837313121));
#31466=CARTESIAN_POINT('Ctrl Pts',(10.5370301318506,-0.539639846919137,
3.55004322755915));
#31467=CARTESIAN_POINT('Ctrl Pts',(10.5847459679134,0.0866093850789692,
3.30274030959437));
#31468=CARTESIAN_POINT('Ctrl Pts',(10.6324618039763,0.633323886102378,3.69574169404847));
#31469=CARTESIAN_POINT('Ctrl Pts',(10.6801776400391,0.598447317577389,4.36814816247366));
#31470=CARTESIAN_POINT('Ctrl Pts',(10.727893476102,0.0140073690254923,4.70247850861168));
#31471=CARTESIAN_POINT('Ctrl Pts',(10.7756093121648,-0.583295762033595,
4.39171203127037));
#31472=CARTESIAN_POINT('Ctrl Pts',(10.8233251482277,-0.644949419658282,
3.72123036834915));
#31473=CARTESIAN_POINT('Ctrl Pts',(10.8710409842905,-0.114336101388361,
3.30674714759503));
#31474=CARTESIAN_POINT('Ctrl Pts',(10.9187568203533,0.521273818073547,3.52888868827067));
#31475=CARTESIAN_POINT('Ctrl Pts',(10.9664726564162,0.678189969569843,4.18365899548663));
#31476=CARTESIAN_POINT('Ctrl Pts',(11.014188492479,0.212313836716152,4.66977242119035));
#31477=CARTESIAN_POINT('Ctrl Pts',(11.0619043285418,-0.44853335926228,4.54082352674158));
#31478=CARTESIAN_POINT('Ctrl Pts',(11.1096201646047,-0.697485469857315,
3.91522806604643));
#31479=CARTESIAN_POINT('Ctrl Pts',(11.1573360006675,-0.305925941288932,
3.36747997668469));
#31480=CARTESIAN_POINT('Ctrl Pts',(11.2050518367303,0.36657008644075,3.40058475730499));
#31481=CARTESIAN_POINT('Ctrl Pts',(11.2527676727932,0.702439163386103,3.98414177848112));
#31482=CARTESIAN_POINT('Ctrl Pts',(11.300483508856,0.393247548178179,4.58226164848818));
#31483=CARTESIAN_POINT('Ctrl Pts',(11.3481993449189,-0.277069341413063,
4.64568168744144));
#31484=CARTESIAN_POINT('Ctrl Pts',(11.3959151809817,-0.692949191524882,
4.11616229772746));
#31485=CARTESIAN_POINT('Ctrl Pts',(11.4436310170446,-0.47248313666557,3.47996928262364));
#31486=CARTESIAN_POINT('Ctrl Pts',(11.4913468531074,0.181871452681271,3.32132847698764));
#31487=CARTESIAN_POINT('Ctrl Pts',(11.5390626891702,0.669210688578896,3.78592217363756));
#31488=CARTESIAN_POINT('Ctrl Pts',(11.586778525233,0.54200345202451,4.44710683224685));
#31489=CARTESIAN_POINT('Ctrl Pts',(11.6344943612959,-0.082933894319074,
4.69770640718098));
#31490=CARTESIAN_POINT('Ctrl Pts',(11.6822101973587,-0.631711769407458,
4.30759145280778));
#31491=CARTESIAN_POINT('Ctrl Pts',(11.7299260334216,-0.600379006513997,
3.63501053441836));
#31492=CARTESIAN_POINT('Ctrl Pts',(11.7776418694844,-0.0177089639202829,
3.29760505835735));
#31493=CARTESIAN_POINT('Ctrl Pts',(11.8253577055473,0.581223492728864,3.60521966494218));
#31494=CARTESIAN_POINT('Ctrl Pts',(11.8730735416101,0.646409472732109,4.27536712768685));
#31495=CARTESIAN_POINT('Ctrl Pts',(11.9207893776729,0.11798768763725,4.69264072000881));
#31496=CARTESIAN_POINT('Ctrl Pts',(11.9685052137358,-0.518784006488825,
4.4738516814993));
#31497=CARTESIAN_POINT('Ctrl Pts',(12.0162210497986,-0.679148364938221,
3.81991735272367));
#31498=CARTESIAN_POINT('Ctrl Pts',(12.0639368858614,-0.215840329824027,
3.33135568986959));
#31499=CARTESIAN_POINT('Ctrl Pts',(12.1116527219243,0.445677201297934,3.45682038542343));
#31500=CARTESIAN_POINT('Ctrl Pts',(12.1593685579871,0.697922500842799,4.08109527893561));
#31501=CARTESIAN_POINT('Ctrl Pts',(12.2070843940499,0.309254828945687,4.63089912998995));
#31502=CARTESIAN_POINT('Ctrl Pts',(12.2548002301128,-0.36340631086944,4.60133860234362));
#31503=CARTESIAN_POINT('Ctrl Pts',(12.3025160661756,-0.702345843688318,
4.0195595833814));
#31504=CARTESIAN_POINT('Ctrl Pts',(12.3502319022385,-0.396310381268302,
3.41981869803717));
#31505=CARTESIAN_POINT('Ctrl Pts',(12.3979477383013,0.273663002289436,3.35286722952223));
#31506=CARTESIAN_POINT('Ctrl Pts',(12.4456635743641,0.69232743999824,3.88018774155459));
#31507=CARTESIAN_POINT('Ctrl Pts',(12.493379410427,0.475216936729713,4.51753369406595));
#31508=CARTESIAN_POINT('Ctrl Pts',(12.5410952464898,-0.178292591690169,
4.67962049203707));
#31509=CARTESIAN_POINT('Ctrl Pts',(12.5888110825527,-0.66807328977682,4.21760133486514));
#31510=CARTESIAN_POINT('Ctrl Pts',(12.6365269186155,-0.544352006232531,
3.55575552365962));
#31511=CARTESIAN_POINT('Ctrl Pts',(12.6842427546784,0.0792561005673328,
3.3018662506574));
#31512=CARTESIAN_POINT('Ctrl Pts',(12.7319585907411,0.630082110704352,3.68908394184497));
#31513=CARTESIAN_POINT('Ctrl Pts',(12.779674426804,0.60229402352211,4.36182063329482));
#31514=CARTESIAN_POINT('Ctrl Pts',(12.8273902628668,0.0214100670547408,
4.70229186986395));
#31515=CARTESIAN_POINT('Ctrl Pts',(12.8751060989297,-0.579135083425219,
4.39783767618763));
#31516=CARTESIAN_POINT('Ctrl Pts',(12.9228219349925,-0.647851575657132,
3.7280430229487));
#31517=CARTESIAN_POINT('Ctrl Pts',(12.9705377710554,-0.121635997485283,
3.30799064633195));
#31518=CARTESIAN_POINT('Ctrl Pts',(13.0182536071182,0.516279788787698,3.52342110712114));
#31519=CARTESIAN_POINT('Ctrl Pts',(13.065969443181,0.68008790103128,4.17650129834983));
#31520=CARTESIAN_POINT('Ctrl Pts',(13.1136852792439,0.219360829260397,4.66749763148232));
#31521=CARTESIAN_POINT('Ctrl Pts',(13.1614011153067,-0.44280866732052,4.54552061885334));
#31522=CARTESIAN_POINT('Ctrl Pts',(13.2091169513696,-0.698340151213866,
3.92258362801769));
#31523=CARTESIAN_POINT('Ctrl Pts',(13.2568327874324,-0.31257512890311,3.37073928277739));
#31524=CARTESIAN_POINT('Ctrl Pts',(13.3045486234952,0.36023244386594,3.39675473658331));
#31525=CARTESIAN_POINT('Ctrl Pts',(13.3522644595581,0.702233020544282,3.97673959790624));
#31526=CARTESIAN_POINT('Ctrl Pts',(13.3999802956209,0.39936220921291,4.57808484437918));
#31527=CARTESIAN_POINT('Ctrl Pts',(13.4476961316837,-0.270249063816132,
4.64856588328003));
#31528=CARTESIAN_POINT('Ctrl Pts',(13.4954119677466,-0.691686463226468,
4.123458892096));
#31529=CARTESIAN_POINT('Ctrl Pts',(13.5431278038094,-0.47793754049168,3.48497770064095));
#31530=CARTESIAN_POINT('Ctrl Pts',(13.5908436398723,0.174708779690948,3.31944941132403));
#31531=CARTESIAN_POINT('Ctrl Pts',(13.6385594759351,0.666917339243262,3.77888119920505));
#31532=CARTESIAN_POINT('Ctrl Pts',(13.6862753119979,0.54668544432619,4.44136978420615));
#31533=CARTESIAN_POINT('Ctrl Pts',(13.7339911480608,-0.075576105952426,
4.69854170502367));
#31534=CARTESIAN_POINT('Ctrl Pts',(13.7817069841236,-0.62843495524706,4.31423202967224));
#31535=CARTESIAN_POINT('Ctrl Pts',(13.8294228201864,-0.604192315423611,
3.64135824639153));
#31536=CARTESIAN_POINT('Ctrl Pts',(13.8771386562493,-0.025110575652917,
3.29783070386218));
#31537=CARTESIAN_POINT('Ctrl Pts',(13.9248544923121,0.577030592115723,3.59911603023956));
#31538=CARTESIAN_POINT('Ctrl Pts',(13.972570328375,0.649275688387581,4.26853927444071));
#31539=CARTESIAN_POINT('Ctrl Pts',(14.0202861644378,0.125280929622514,4.69135877091509));
#31540=CARTESIAN_POINT('Ctrl Pts',(14.0680020005006,-0.513761234509794,
4.47929287013608));
#31541=CARTESIAN_POINT('Ctrl Pts',(14.1157178365635,-0.681008551759042,
3.82708495184235));
#31542=CARTESIAN_POINT('Ctrl Pts',(14.1634336726263,-0.222875237264486,
3.33366758291179));
#31543=CARTESIAN_POINT('Ctrl Pts',(14.2111495086891,0.439927836986373,3.45215352543546));
#31544=CARTESIAN_POINT('Ctrl Pts',(14.258865344752,0.698738409372782,4.07373531525328));
#31545=CARTESIAN_POINT('Ctrl Pts',(14.3065811808148,0.315886748959774,4.62760483051036));
#31546=CARTESIAN_POINT('Ctrl Pts',(14.3542970168777,-0.357048573565392,
4.60513517296818));
#31547=CARTESIAN_POINT('Ctrl Pts',(14.4020128529405,-0.702100697086982,
4.02696057488784));
#31548=CARTESIAN_POINT('Ctrl Pts',(14.4497286890033,-0.402402947265751,
3.42402766604624));
#31549=CARTESIAN_POINT('Ctrl Pts',(14.4974445250662,0.266827620794843,3.35001901394789));
#31550=CARTESIAN_POINT('Ctrl Pts',(14.545160361129,0.691026279008849,3.87289790258421));
#31551=CARTESIAN_POINT('Ctrl Pts',(14.5928761971919,0.480644872403009,4.51249660299459));
#31552=CARTESIAN_POINT('Ctrl Pts',(14.6405920332547,-0.171120116202498,
4.6814617871012));
#31553=CARTESIAN_POINT('Ctrl Pts',(14.6883078693176,-0.665742869077823,
4.22463012647536));
#31554=CARTESIAN_POINT('Ctrl Pts',(14.7360237053803,-0.549003701508229,
3.56151716432844));
#31555=CARTESIAN_POINT('Ctrl Pts',(14.7837395414432,0.0718940126641393,
3.30106973710437));
#31556=CARTESIAN_POINT('Ctrl Pts',(14.831455377506,0.626770348775451,3.68246072472179));
#31557=CARTESIAN_POINT('Ctrl Pts',(14.8791712135689,0.606073829504824,4.35545291479698));
#31558=CARTESIAN_POINT('Ctrl Pts',(14.9268870496317,0.0288103869553486,
4.70202722386799));
#31559=CARTESIAN_POINT('Ctrl Pts',(14.9746028856946,-0.574910077240004,
4.4039191311837));
#31560=CARTESIAN_POINT('Ctrl Pts',(15.0223187217574,-0.650681771377263,
3.73488588523872));
#31561=CARTESIAN_POINT('Ctrl Pts',(15.0700345578202,-0.128922382832804,
3.30931101018402));
#31562=CARTESIAN_POINT('Ctrl Pts',(15.1177503938831,0.511228413592865,3.51800646209349));
#31563=CARTESIAN_POINT('Ctrl Pts',(15.1654662299459,0.681910291555949,4.16932399628639));
#31564=CARTESIAN_POINT('Ctrl Pts',(15.2131820660088,0.226383456244684,4.6651486993049));
#31565=CARTESIAN_POINT('Ctrl Pts',(15.2608979020716,-0.437034790293287,
4.55015711712348));
#31566=CARTESIAN_POINT('Ctrl Pts',(15.3086137381344,-0.699117264260319,
3.92994778903219));
#31567=CARTESIAN_POINT('Ctrl Pts',(15.3563295741972,-0.319189597155267,
3.37406848416447));
#31568=CARTESIAN_POINT('Ctrl Pts',(15.4040454102601,0.353854788380711,3.39299172148285));
#31569=CARTESIAN_POINT('Ctrl Pts',(15.4517612463229,0.70194887699091,3.96934000098645));
#31570=CARTESIAN_POINT('Ctrl Pts',(15.4994770823858,0.40543251098856,4.57384382934891));
#31571=CARTESIAN_POINT('Ctrl Pts',(15.5471929184486,-0.263398768235635,
4.65137803949801));
#31572=CARTESIAN_POINT('Ctrl Pts',(15.5949087545115,-0.690346905678043,
4.13074177323664));
#31573=CARTESIAN_POINT('Ctrl Pts',(15.6426245905743,-0.483338857283784,
3.4900433248913));
#31574=CARTESIAN_POINT('Ctrl Pts',(15.6903404266371,0.167526700878456,3.31764593799033));
#31575=CARTESIAN_POINT('Ctrl Pts',(15.7380562627,0.664549911894371,3.77186478559966));
#31576=CARTESIAN_POINT('Ctrl Pts',(15.7857720987628,0.551306713402943,4.43558371090429));
#31577=CARTESIAN_POINT('Ctrl Pts',(15.8334879348256,-0.0682099229505586,
4.69929941216862));
#31578=CARTESIAN_POINT('Ctrl Pts',(15.8812037708885,-0.625088337514006,
4.32083770313399));
#31579=CARTESIAN_POINT('Ctrl Pts',(15.9289196069513,-0.607938513517956,
3.64774579458877));
#31580=CARTESIAN_POINT('Ctrl Pts',(15.9766354430142,-0.0325093982219456,
3.29813434300035));
#31581=CARTESIAN_POINT('Ctrl Pts',(16.024351279077,0.572773597682653,3.59305692382598));
#31582=CARTESIAN_POINT('Ctrl Pts',(16.0720671151399,0.652069785580651,4.2616815931263));
#31583=CARTESIAN_POINT('Ctrl Pts',(16.1197829512026,0.132560255996602,4.69000002896988));
#31584=CARTESIAN_POINT('Ctrl Pts',(16.1674987872655,-0.508681396370837,
4.48468082119526));
#31585=CARTESIAN_POINT('Ctrl Pts',(16.2152146233283,-0.682793095381579,
3.83427175754402));
#31586=CARTESIAN_POINT('Ctrl Pts',(16.2629304593912,-0.229885388781225,
3.33605348899688));
#31587=CARTESIAN_POINT('Ctrl Pts',(16.310646295454,0.434129607578297,3.44754751763412));
#31588=CARTESIAN_POINT('Ctrl Pts',(16.3583621315168,0.699476705356048,4.06636716140204));
#31589=CARTESIAN_POINT('Ctrl Pts',(16.4060779675797,0.322483581772784,4.62424081966442));
#31590=CARTESIAN_POINT('Ctrl Pts',(16.4537938036425,-0.350651177000141,
4.60886452804932));
#31591=CARTESIAN_POINT('Ctrl Pts',(16.5015096397054,-0.701777564471952,
4.03435857174156));
#31592=CARTESIAN_POINT('Ctrl Pts',(16.5492254757682,-0.408450816253369,
3.42830061032894));
#31593=CARTESIAN_POINT('Ctrl Pts',(16.596941311831,0.259962601354342,3.34724299517707));
#31594=CARTESIAN_POINT('Ctrl Pts',(16.6446571478939,0.689648362099571,3.86562218151166));
#31595=CARTESIAN_POINT('Ctrl Pts',(16.6923729839567,0.486019420324727,4.50740258623259));
#31596=CARTESIAN_POINT('Ctrl Pts',(16.7400888200196,-0.163928633504336,
4.6832273886238));
#31597=CARTESIAN_POINT('Ctrl Pts',(16.7878046560824,-0.663338500820136,
4.23163396723712));
#31598=CARTESIAN_POINT('Ctrl Pts',(16.8355204921452,-0.553594416058007,
3.56732750958986));
#31599=CARTESIAN_POINT('Ctrl Pts',(16.8832363282081,0.064523939115192,3.30035085740826));
#31600=CARTESIAN_POINT('Ctrl Pts',(16.9309521642709,0.623388968170475,3.67587277835446));
#31601=CARTESIAN_POINT('Ctrl Pts',(16.9786680003338,0.609786315682611,4.34904571427615));
#31602=CARTESIAN_POINT('Ctrl Pts',(17.0263838363966,0.0362075067348799,
4.70168460001938));
#31603=CARTESIAN_POINT('Ctrl Pts',(17.0740996724594,-0.570621212771584,
4.40995572075944));
#31604=CARTESIAN_POINT('Ctrl Pts',(17.1218155085223,-0.653439692453966,
3.74175819514654));
#31605=CARTESIAN_POINT('Ctrl Pts',(17.1695313445851,-0.136194448093839,
3.31070809249149));
#31606=CARTESIAN_POINT('Ctrl Pts',(17.2172471806479,0.50612025357182,3.51264535462077));
#31607=CARTESIAN_POINT('Ctrl Pts',(17.2649630167108,0.683656938721366,4.16212788651693));
#31608=CARTESIAN_POINT('Ctrl Pts',(17.3126788527736,0.233380937628925,4.66272588556639));
#31609=CARTESIAN_POINT('Ctrl Pts',(17.3603946888365,-0.431212369515449,
4.55473250655174));
#31610=CARTESIAN_POINT('Ctrl Pts',(17.4081105248993,-0.699816722678643,
3.93731973111387));
#31611=CARTESIAN_POINT('Ctrl Pts',(17.4558263609621,-0.325768611341644,
3.37746721105403));
#31612=CARTESIAN_POINT('Ctrl Pts',(17.503542197025,0.347437828384778,3.38929612998149));
#31613=CARTESIAN_POINT('Ctrl Pts',(17.5512580330878,0.701586764287296,3.96194380963385));
#31614=CARTESIAN_POINT('Ctrl Pts',(17.5989738691507,0.411457779244836,4.56953907446917));
#31615=CARTESIAN_POINT('Ctrl Pts',(17.6466897052135,-0.256519215569882,
4.65411784373439));
#31616=CARTESIAN_POINT('Ctrl Pts',(17.6944055412764,-0.688930667671302,
4.13801013220155));
#31617=CARTESIAN_POINT('Ctrl Pts',(17.7421213773391,-0.488686487089258,
3.49516559270919));
#31618=CARTESIAN_POINT('Ctrl Pts',(17.789837213402,0.160326013994967,3.3159182573078));
#31619=CARTESIAN_POINT('Ctrl Pts',(17.8375530494648,0.662108669494809,3.76487371217125));
#31620=CARTESIAN_POINT('Ctrl Pts',(17.8852688855277,0.555866745946156,4.42974925503083));
#31621=CARTESIAN_POINT('Ctrl Pts',(17.9329847215905,-0.060836163514142,
4.69997944445332));
#31622=CARTESIAN_POINT('Ctrl Pts',(17.9807005576534,-0.621672287934692,
4.32740773946617));
#31623=CARTESIAN_POINT('Ctrl Pts',(18.0284163937162,-0.611617184687133,
3.65417246951162));
#31624=CARTESIAN_POINT('Ctrl Pts',(18.0761322297791,-0.0399046098013318,
3.29851594204507));
#31625=CARTESIAN_POINT('Ctrl Pts',(18.1238480658419,0.568452982276385,3.58704301871817));
#31626=CARTESIAN_POINT('Ctrl Pts',(18.1715639019047,0.65479145395626,4.25479484546229));
#31627=CARTESIAN_POINT('Ctrl Pts',(18.2192797379675,0.139824858206545,4.68856464509573));
#31628=CARTESIAN_POINT('Ctrl Pts',(18.2669955740304,-0.503545056316242,
4.49001493620888));
#31629=CARTESIAN_POINT('Ctrl Pts',(18.3147114100932,-0.684501797587214,
3.84147697155243));
#31630=CARTESIAN_POINT('Ctrl Pts',(18.3624272461561,-0.236870005719869,
3.33851314310973));
#31631=CARTESIAN_POINT('Ctrl Pts',(18.4101430822189,0.42828315711354,3.44300287363294));
#31632=CARTESIAN_POINT('Ctrl Pts',(18.4578589182817,0.70013730678616,4.05899163580144));
#31633=CARTESIAN_POINT('Ctrl Pts',(18.5055747543446,0.32904459463985,4.62080747111051));
#31634=CARTESIAN_POINT('Ctrl Pts',(18.5532905904074,-0.34421483176614,4.61252625334797));
#31635=CARTESIAN_POINT('Ctrl Pts',(18.6010064264702,-0.701376481735239,
4.0417527522082));
#31636=CARTESIAN_POINT('Ctrl Pts',(18.6487222625331,-0.414453316462639,
3.43263705626685));
#31637=CARTESIAN_POINT('Ctrl Pts',(18.6964380985959,0.253068706501803,3.34453948155689));
#31638=CARTESIAN_POINT('Ctrl Pts',(18.7441539346588,0.68819384232267,3.85836138648927));
#31639=CARTESIAN_POINT('Ctrl Pts',(18.7918697707216,0.491339983515996,4.50225220959958));
#31640=CARTESIAN_POINT('Ctrl Pts',(18.8395856067844,-0.156718942392259,
4.68491710048942));
#31641=CARTESIAN_POINT('Ctrl Pts',(18.8873014428473,-0.660860452068119,
4.23861207919858));
#31642=CARTESIAN_POINT('Ctrl Pts',(18.9350172789101,-0.558123639969822,
3.57318591405529));
#31643=CARTESIAN_POINT('Ctrl Pts',(18.9827331149729,0.0571466985584877,
3.29970969142451));
#31644=CARTESIAN_POINT('Ctrl Pts',(19.0304489510358,0.619938344467307,3.66932083449001));
#31645=CARTESIAN_POINT('Ctrl Pts',(19.0781647870986,0.613431069708698,4.3425997434341));
#31646=CARTESIAN_POINT('Ctrl Pts',(19.1258806231615,0.0436006047213211,
4.70126403633668));
#31647=CARTESIAN_POINT('Ctrl Pts',(19.1735964592243,-0.566268966340429,
4.41594677447179));
#31648=CARTESIAN_POINT('Ctrl Pts',(19.2213122952871,-0.656125032675529,
3.74865918919138));
#31649=CARTESIAN_POINT('Ctrl Pts',(19.26902813135,-0.143451385285705,3.31218173833215));
#31650=CARTESIAN_POINT('Ctrl Pts',(19.3167439674128,0.500955875668841,3.50733837970023));
#31651=CARTESIAN_POINT('Ctrl Pts',(19.3644598034757,0.68532764936022,4.15491376927485));
#31652=CARTESIAN_POINT('Ctrl Pts',(19.4121756395385,0.240352494576274,4.66022945763735));
#31653=CARTESIAN_POINT('Ctrl Pts',(19.4598914756013,-0.425342048711971,
4.55924628221868));
#31654=CARTESIAN_POINT('Ctrl Pts',(19.5076073116642,-0.700438454444525,
3.94469862920436));
#31655=CARTESIAN_POINT('Ctrl Pts',(19.555323147727,-0.332311429993836,3.3809350976725));
#31656=CARTESIAN_POINT('Ctrl Pts',(19.6030389837899,0.340982256434611,3.38566835039883));
#31657=CARTESIAN_POINT('Ctrl Pts',(19.6507548198527,0.701146760813864,3.95455188724214));
#31658=CARTESIAN_POINT('Ctrl Pts',(19.6984706559155,0.417437272672218,4.56517097885182));
#31659=CARTESIAN_POINT('Ctrl Pts',(19.7461864919784,-0.249611033919464,
4.6567851409082));
#31660=CARTESIAN_POINT('Ctrl Pts',(19.7939023280412,-0.687438163400574,
4.14526287985386));
#31661=CARTESIAN_POINT('Ctrl Pts',(19.841618164104,-0.493979350866992,3.5003444672369));
#31662=CARTESIAN_POINT('Ctrl Pts',(19.8893340001669,0.153106602982307,3.31426555646693));
#31663=CARTESIAN_POINT('Ctrl Pts',(19.9370498362297,0.659595612567133,3.75791065255607));
#31664=CARTESIAN_POINT('Ctrl Pts',(19.9847656722925,0.560361770063263,4.42386348253578));
#31665=CARTESIAN_POINT('Ctrl Pts',(20.0324815083554,-0.0534494809679074,
4.70058849011268));
#31666=CARTESIAN_POINT('Ctrl Pts',(20.0801973444182,-0.618198828117398,
4.33392863744107));
#31667=CARTESIAN_POINT('Ctrl Pts',(20.1279131804811,-0.615205937201001,
3.66066167313574));
#31668=CARTESIAN_POINT('Ctrl Pts',(20.1756290165439,-0.0473369003220797,
3.29892991724937));
#31669=CARTESIAN_POINT('Ctrl Pts',(20.2233448526068,0.564147630203746,3.58116102158214));
#31670=CARTESIAN_POINT('Ctrl Pts',(20.2710606886696,0.657292163719816,4.24771695100806));
#31671=CARTESIAN_POINT('Ctrl Pts',(20.3187765247324,0.147355317357748,4.68736342730055));
#31672=CARTESIAN_POINT('Ctrl Pts',(20.3664923607953,-0.498896366832293,
4.49468216892218));
#31673=CARTESIAN_POINT('Ctrl Pts',(20.4062555575143,-0.653992183610565,
3.9575054511282));
#31674=CARTESIAN_POINT('Ctrl Pts',(20.4380661148895,-0.465699721472375,
3.59327933193152));
#31675=CARTESIAN_POINT('Ctrl Pts',(20.461924032921,-0.215665100260693,3.41899970433759));
#31676=CARTESIAN_POINT('Ctrl Pts',(20.4857819509523,0.0900520562992202,
3.38718375849312));
#31677=CARTESIAN_POINT('Ctrl Pts',(20.5096398689838,0.372154449079436,3.50499792242313));
#31678=CARTESIAN_POINT('Ctrl Pts',(20.5334977870152,0.564103623124681,3.74397162737493));
#31679=CARTESIAN_POINT('Ctrl Pts',(20.5573557050466,0.61766411855396,4.04548854604559));
#31680=CARTESIAN_POINT('Ctrl Pts',(20.581213623078,0.520427284318709,4.33591550271974));
#31681=CARTESIAN_POINT('Ctrl Pts',(20.6050715411094,0.295805552416038,4.5441843692251));
#31682=CARTESIAN_POINT('Ctrl Pts',(20.6289294591409,-0.00108183093298003,
4.61939465531364));
#31683=CARTESIAN_POINT('Ctrl Pts',(20.6527873771723,-0.297740088546312,
4.543141139652));
#31684=CARTESIAN_POINT('Ctrl Pts',(20.6766452952037,-0.521574030203058,
4.33407743490148));
#31685=CARTESIAN_POINT('Ctrl Pts',(20.7005032132351,-0.617878846294169,
4.04332131262121));
#31686=CARTESIAN_POINT('Ctrl Pts',(20.7243611312665,-0.563090193646282,
3.74197268265107));
#31687=CARTESIAN_POINT('Ctrl Pts',(20.748219049298,-0.370613436173077,3.50371837193987));
#31688=CARTESIAN_POINT('Ctrl Pts',(20.7720769673294,-0.0875101228827464,
3.38681864340431));
#31689=CARTESIAN_POINT('Ctrl Pts',(20.7959348853608,0.216991017820888,3.41985835035499));
#31690=CARTESIAN_POINT('Ctrl Pts',(20.8197928033922,0.468432357761717,3.59475855107288));
#31691=CARTESIAN_POINT('Ctrl Pts',(20.8436507214236,0.605329007232586,3.86875129405724));
#31692=CARTESIAN_POINT('Ctrl Pts',(20.8675086394551,0.594206341669864,4.17483793696784));
#31693=CARTESIAN_POINT('Ctrl Pts',(20.8913665574864,0.437783978244149,4.43817193323088));
#31694=CARTESIAN_POINT('Ctrl Pts',(20.9152244755179,0.174311539695801,4.5943609607934));
#31695=CARTESIAN_POINT('Ctrl Pts',(20.9390823935493,-0.13178483570001,4.60521254097096));
#31696=CARTESIAN_POINT('Ctrl Pts',(20.9629403115808,-0.405656219889506,
4.46807317049539));
#31697=CARTESIAN_POINT('Ctrl Pts',(20.9867982296121,-0.580333613298163,
4.21647715910241));
#31698=CARTESIAN_POINT('Ctrl Pts',(21.0106561476436,-0.613103627724174,
3.91194658594648));
#31699=CARTESIAN_POINT('Ctrl Pts',(21.034514065675,-0.495953105920446,3.62894747086441));
#31700=CARTESIAN_POINT('Ctrl Pts',(21.0583719837064,-0.257528539509485,
3.43668080652407));
#31701=CARTESIAN_POINT('Ctrl Pts',(21.0822299017379,0.0438687693677006,
3.38216102944232));
#31702=CARTESIAN_POINT('Ctrl Pts',(21.1060878197692,0.334538969374667,3.47871971028568));
#31703=CARTESIAN_POINT('Ctrl Pts',(21.1299457378007,0.543405278604256,3.7027456213393));
#31704=CARTESIAN_POINT('Ctrl Pts',(21.153803655832,0.619394195209021,3.99945832503004));
#31705=CARTESIAN_POINT('Ctrl Pts',(21.1776615738635,0.543924359096133,4.29630348300169));
#31706=CARTESIAN_POINT('Ctrl Pts',(21.2015194918949,0.33545020099803,4.52069436823682));
#31707=CARTESIAN_POINT('Ctrl Pts',(21.2253774099264,0.0449493312674926,
4.61776129700707));
#31708=CARTESIAN_POINT('Ctrl Pts',(21.2492353279577,-0.256542874348706,
4.56376876117982));
#31709=CARTESIAN_POINT('Ctrl Pts',(21.2730932459892,-0.495303359101402,
4.37191940649105));
#31710=CARTESIAN_POINT('Ctrl Pts',(21.2969511640206,-0.612948680759938,
4.08912562603418));
#31711=CARTESIAN_POINT('Ctrl Pts',(21.320809082052,-0.580711353586496,3.78453820227854));
#31712=CARTESIAN_POINT('Ctrl Pts',(21.3446670000834,-0.406474282201139,
3.53263705712739));
#31713=CARTESIAN_POINT('Ctrl Pts',(21.3685249181149,-0.132843176680646,
3.39501888221951));
#31714=CARTESIAN_POINT('Ctrl Pts',(21.3923828361463,0.17327170411384,3.40533506996376));
#31715=CARTESIAN_POINT('Ctrl Pts',(21.4162407541777,0.437016933425986,3.56106303144932));
#31716=CARTESIAN_POINT('Ctrl Pts',(21.4400986722091,0.593899618413251,3.82412303814848));
#31717=CARTESIAN_POINT('Ctrl Pts',(21.4639565902405,0.605557669197671,4.13018975281259));
#31718=CARTESIAN_POINT('Ctrl Pts',(21.4878145082719,0.469140374803543,4.40442152661638));
#31719=CARTESIAN_POINT('Ctrl Pts',(21.5116724263034,0.218005479642704,4.57976122094124));
#31720=CARTESIAN_POINT('Ctrl Pts',(21.5355303443348,-0.0864376936408111,
4.61333350436739));
#31721=CARTESIAN_POINT('Ctrl Pts',(21.5593882623662,-0.369744496313637,
4.49692903910649));
#31722=CARTESIAN_POINT('Ctrl Pts',(21.5832461803976,-0.562638697999917,
4.2590118877088));
#31723=CARTESIAN_POINT('Ctrl Pts',(21.607104098429,-0.617952412054802,3.95775927442416));
#31724=CARTESIAN_POINT('Ctrl Pts',(21.6309620164605,-0.522159928676552,
3.66683566915707));
#31725=CARTESIAN_POINT('Ctrl Pts',(21.6548199344919,-0.298685119385998,
3.45737981799522));
#31726=CARTESIAN_POINT('Ctrl Pts',(21.6786778525233,-0.00217366238626178,
3.38060938201055));
#31727=CARTESIAN_POINT('Ctrl Pts',(21.7025357705547,0.294869314276287,3.45529682398599));
#31728=CARTESIAN_POINT('Ctrl Pts',(21.7263936885862,0.519808711519421,3.66317902991346));
#31729=CARTESIAN_POINT('Ctrl Pts',(21.7502516066175,0.617640719491047,3.95342313784609));
#31730=CARTESIAN_POINT('Ctrl Pts',(21.774109524649,0.564442747351711,4.25505655730362));
#31731=CARTESIAN_POINT('Ctrl Pts',(21.7979674426804,0.373223148373148,4.49432170089927));
#31732=CARTESIAN_POINT('Ctrl Pts',(21.8218253607118,0.0907403232229101,
4.61271172357229));
#31733=CARTESIAN_POINT('Ctrl Pts',(21.8456832787432,-0.213930982672105,
4.58127703989962));
#31734=CARTESIAN_POINT('Ctrl Pts',(21.8695411967746,-0.466290335940828,
4.40770428630285));
#31735=CARTESIAN_POINT('Ctrl Pts',(21.8933991148061,-0.604629000578284,
4.13443672906324));
#31736=CARTESIAN_POINT('Ctrl Pts',(21.9172570328375,-0.595119404811066,
3.82829572958469));
#31737=CARTESIAN_POINT('Ctrl Pts',(21.9411149508689,-0.440086903840403,
3.56414110135311));
#31738=CARTESIAN_POINT('Ctrl Pts',(21.9649728689003,-0.177441167154219,
3.40656584639871));
#31739=CARTESIAN_POINT('Ctrl Pts',(21.9888307869318,0.128593768301574,3.39410140682164));
#31740=CARTESIAN_POINT('Ctrl Pts',(22.0126887049631,0.403184024583593,3.52979567762293));
#31741=CARTESIAN_POINT('Ctrl Pts',(22.0365466229946,0.579184804342829,3.7804677133541));
#31742=CARTESIAN_POINT('Ctrl Pts',(22.060404541026,0.613559122762511,4.08482137310942));
#31743=CARTESIAN_POINT('Ctrl Pts',(22.0842624590574,0.497901522652627,4.36843389665204));
#31744=CARTESIAN_POINT('Ctrl Pts',(22.1081203770888,0.260493437687466,4.56195429652472));
#31745=CARTESIAN_POINT('Ctrl Pts',(22.1319782951203,-0.0406123884881684,
4.61806156357065));
#31746=CARTESIAN_POINT('Ctrl Pts',(22.1558362131517,-0.33178737942464,4.52303594266224));
#31747=CARTESIAN_POINT('Ctrl Pts',(22.1796941311831,-0.541831318374727,
4.30011378656432));
#31748=CARTESIAN_POINT('Ctrl Pts',(22.2035520492145,-0.619382740812877,
4.00380563470766));
#31749=CARTESIAN_POINT('Ctrl Pts',(22.2274099672459,-0.545478211438426,
3.70656690151735));
#31750=CARTESIAN_POINT('Ctrl Pts',(22.2512678852774,-0.338189400908512,
3.48108055383335));
#31751=CARTESIAN_POINT('Ctrl Pts',(22.2751258033088,-0.0482040696311437,
3.38248414587532));
#31752=CARTESIAN_POINT('Ctrl Pts',(22.2989837213402,0.253568469476171,3.43488718493857));
#31753=CARTESIAN_POINT('Ctrl Pts',(22.3228416393716,0.493336611197201,3.62547570084914));
#31754=CARTESIAN_POINT('Ctrl Pts',(22.346699557403,0.612470512379129,3.90764560936005));
#31755=CARTESIAN_POINT('Ctrl Pts',(22.3705574754344,0.581838691587799,4.21239868278141));
#31756=CARTESIAN_POINT('Ctrl Pts',(22.3944153934659,0.408931458591185,4.46521449128699));
#31757=CARTESIAN_POINT('Ctrl Pts',(22.4182733114973,0.13602935083686,4.60427268703701));
#31758=CARTESIAN_POINT('Ctrl Pts',(22.4421312295287,-0.170135649772668,
4.59556974592947));
#31759=CARTESIAN_POINT('Ctrl Pts',(22.4659891475601,-0.434697828443077,
4.44123378804823));
#31760=CARTESIAN_POINT('Ctrl Pts',(22.4898470655916,-0.592964587096883,
4.17900413283907));
#31761=CARTESIAN_POINT('Ctrl Pts',(22.513704983623,-0.606235276705168,3.87300312362118));
#31762=CARTESIAN_POINT('Ctrl Pts',(22.5375629016543,-0.471265070143009,
3.59805624874041));
#31763=CARTESIAN_POINT('Ctrl Pts',(22.5614208196858,-0.22105744785653,3.4213956854475));
#31764=CARTESIAN_POINT('Ctrl Pts',(22.5852787377172,0.0832042338527798,
3.38621941950615));
#31765=CARTESIAN_POINT('Ctrl Pts',(22.6091366557487,0.36712117327337,3.50112963696785));
#31766=CARTESIAN_POINT('Ctrl Pts',(22.63299457378,0.561265174232679,3.7380264683998));
#31767=CARTESIAN_POINT('Ctrl Pts',(22.6568524918115,0.618167971965146,4.03898443479498));
#31768=CARTESIAN_POINT('Ctrl Pts',(22.6807104098429,0.523905402647805,4.33040686810369));
#31769=CARTESIAN_POINT('Ctrl Pts',(22.7045683278744,0.301545895245711,4.54104106792393));
#31770=CARTESIAN_POINT('Ctrl Pts',(22.7284262459057,0.00542710047790416,
4.61936606261506));
#31771=CARTESIAN_POINT('Ctrl Pts',(22.7522841639372,-0.291974666000346,
4.54625809930836));
#31772=CARTESIAN_POINT('Ctrl Pts',(22.7761420819686,-0.518067845615496,
4.33953802216683));
#31773=CARTESIAN_POINT('Ctrl Pts',(22.7920473606562,-0.584213376873476,
4.14642833911731));
#31774=CARTESIAN_POINT('Ctrl Pts',(22.8,-0.592174260192535,4.04779597854866));
#31775=CARTESIAN_POINT('Ctrl Pts',(3.96816317011931,-0.282716247115855,
3.54616445487434));
#31776=CARTESIAN_POINT('Ctrl Pts',(3.97611580946312,-0.207125539895404,
3.49907532469992));
#31777=CARTESIAN_POINT('Ctrl Pts',(3.99202108815073,-0.0320395462633344,
3.44344227840288));
#31778=CARTESIAN_POINT('Ctrl Pts',(4.01587900618214,0.238586678544665,3.49618207793602));
#31779=CARTESIAN_POINT('Ctrl Pts',(4.03973692421357,0.450798406251909,3.67207593825259));
#31780=CARTESIAN_POINT('Ctrl Pts',(4.06359484224498,0.552814952159096,3.92817792166325));
#31781=CARTESIAN_POINT('Ctrl Pts',(4.0874527602764,0.519633627921064,4.20183097195279));
#31782=CARTESIAN_POINT('Ctrl Pts',(4.11131067830782,0.359398059257131,4.42613686623617));
#31783=CARTESIAN_POINT('Ctrl Pts',(4.13516859633924,0.11127440638865,4.54623750576341));
#31784=CARTESIAN_POINT('Ctrl Pts',(4.15902651437066,-0.164055973910312,
4.53276988152218));
#31785=CARTESIAN_POINT('Ctrl Pts',(4.18288443240208,-0.399271733473279,
4.38902461621758));
#31786=CARTESIAN_POINT('Ctrl Pts',(4.2067423504335,-0.536853866020863,4.15015270818839));
#31787=CARTESIAN_POINT('Ctrl Pts',(4.23060026846491,-0.543161034884179,
3.87456412255522));
#31788=CARTESIAN_POINT('Ctrl Pts',(4.25445818649634,-0.416650307492554,
3.62964815836115));
#31789=CARTESIAN_POINT('Ctrl Pts',(4.27831610452775,-0.188257351244862,
3.47529323740438));
#31790=CARTESIAN_POINT('Ctrl Pts',(4.30217402255918,0.0861697193074588,
3.44924344981891));
#31791=CARTESIAN_POINT('Ctrl Pts',(4.32603194059059,0.339525912432458,3.55786862136322));
#31792=CARTESIAN_POINT('Ctrl Pts',(4.34988985862202,0.509858789389686,3.77460696883261));
#31793=CARTESIAN_POINT('Ctrl Pts',(4.37374777665342,0.555517294574929,4.0464600464808));
#31794=CARTESIAN_POINT('Ctrl Pts',(4.39760569468486,0.465336694276122,4.30695238014399));
#31795=CARTESIAN_POINT('Ctrl Pts',(4.42146361271626,0.261368594047533,4.4923864940975));
#31796=CARTESIAN_POINT('Ctrl Pts',(4.4453215307477,-0.00651124555331369,
4.55741869872598));
#31797=CARTESIAN_POINT('Ctrl Pts',(4.4691794487791,-0.272798909000308,4.48614684730087));
#31798=CARTESIAN_POINT('Ctrl Pts',(4.49303736681053,-0.472379807908186,
4.29599884956661));
#31799=CARTESIAN_POINT('Ctrl Pts',(4.51689528484195,-0.55645097662433,4.03347107014466));
#31800=CARTESIAN_POINT('Ctrl Pts',(4.54075320287336,-0.504454724024634,
3.76275870240323));
#31801=CARTESIAN_POINT('Ctrl Pts',(4.56461112090479,-0.329105550388866,
3.55005829421323));
#31802=CARTESIAN_POINT('Ctrl Pts',(4.5884690389362,-0.0732811049967102,
3.44738088927219));
#31803=CARTESIAN_POINT('Ctrl Pts',(4.61232695696762,0.200462566687888,3.47983390993684));
#31804=CARTESIAN_POINT('Ctrl Pts',(4.63618487499904,0.425187680335341,3.63948170866684));
#31805=CARTESIAN_POINT('Ctrl Pts',(4.66004279303046,0.54594282425631,3.88728604994618));
#31806=CARTESIAN_POINT('Ctrl Pts',(4.68390071106188,0.533200076465109,4.16265202228146));
#31807=CARTESIAN_POINT('Ctrl Pts',(4.7077586290933,0.390075385898422,4.39824514461603));
#31808=CARTESIAN_POINT('Ctrl Pts',(4.73161654712472,0.151566638040082,4.53645648111246));
#31809=CARTESIAN_POINT('Ctrl Pts',(4.75547446515614,-0.124004281411749,
4.54348959519552));
#31810=CARTESIAN_POINT('Ctrl Pts',(4.77933238318755,-0.369252776249408,
4.41762469889406));
#31811=CARTESIAN_POINT('Ctrl Pts',(4.80319030121898,-0.524208909050512,
4.18963918784455));
#31812=CARTESIAN_POINT('Ctrl Pts',(4.82704821925039,-0.550981684424725,
3.91528172969931));
#31813=CARTESIAN_POINT('Ctrl Pts',(4.85090613728181,-0.443024429517375,
3.66164019632193));
#31814=CARTESIAN_POINT('Ctrl Pts',(4.87476405531323,-0.226735633849849,
3.49073685167984));
#31815=CARTESIAN_POINT('Ctrl Pts',(4.89862197334465,0.0449962004486201,
3.44436221885167));
#31816=CARTESIAN_POINT('Ctrl Pts',(4.92247989137607,0.305725238065515,3.53385615878353));
#31817=CARTESIAN_POINT('Ctrl Pts',(4.94633780940749,0.491696127187109,3.73733496539613));
#31818=CARTESIAN_POINT('Ctrl Pts',(4.9701957274389,0.557433919677865,4.00504252782125));
#31819=CARTESIAN_POINT('Ctrl Pts',(4.99405364547033,0.486863934612277,4.27151705483839));
#31820=CARTESIAN_POINT('Ctrl Pts',(5.01791156350174,0.297242455626679,4.47159826597145));
#31821=CARTESIAN_POINT('Ctrl Pts',(5.04176948153317,0.0349370995184326,
4.55636085499566));
#31822=CARTESIAN_POINT('Ctrl Pts',(5.06562739956458,-0.235911329089554,
4.505078060008));
#31823=CARTESIAN_POINT('Ctrl Pts',(5.08948531759601,-0.449073011639563,
4.33028992129829));
#31824=CARTESIAN_POINT('Ctrl Pts',(5.11334323562741,-0.552424110340463,
4.07473689991432));
#31825=CARTESIAN_POINT('Ctrl Pts',(5.13720115365885,-0.520692466332485,
3.80090867070902));
#31826=CARTESIAN_POINT('Ctrl Pts',(5.16105907169026,-0.361637330928202,
3.57576369465428));
#31827=CARTESIAN_POINT('Ctrl Pts',(5.18491698972168,-0.114152017308863,
3.45435605122152));
#31828=CARTESIAN_POINT('Ctrl Pts',(5.2087749077531,0.161246573981014,3.46637321630784));
#31829=CARTESIAN_POINT('Ctrl Pts',(5.23263282578452,0.397215985664045,3.60887666570863));
#31830=CARTESIAN_POINT('Ctrl Pts',(5.25649074381594,0.536055268906009,3.84702042432939));
#31831=CARTESIAN_POINT('Ctrl Pts',(5.28034866184735,0.543814437048104,4.12257185628156));
#31832=CARTESIAN_POINT('Ctrl Pts',(5.30420657987878,0.418596162124088,4.3681511305826));
#31833=CARTESIAN_POINT('Ctrl Pts',(5.32806449791019,0.191019723230217,4.5237074252207));
#31834=CARTESIAN_POINT('Ctrl Pts',(5.35192241594161,-0.0832662412662402,
4.55120298888854));
#31835=CARTESIAN_POINT('Ctrl Pts',(5.37578033397303,-0.337191341646214,
4.44391440730515));
#31836=CARTESIAN_POINT('Ctrl Pts',(5.39963825200445,-0.508663974085987,
4.22807666114996));
#31837=CARTESIAN_POINT('Ctrl Pts',(5.42349617003587,-0.555754409133215,
3.95646795866016));
#31838=CARTESIAN_POINT('Ctrl Pts',(5.4473540880673,-0.466947752701331,3.69550402606682));
#31839=CARTESIAN_POINT('Ctrl Pts',(5.47121200609871,-0.263959651332346,
3.50899765340418));
#31840=CARTESIAN_POINT('Ctrl Pts',(5.49506992413013,0.00357377490351851,
3.44255472911916));
#31841=CARTESIAN_POINT('Ctrl Pts',(5.51892784216155,0.270233315828591,3.51242235806964));
#31842=CARTESIAN_POINT('Ctrl Pts',(5.54278576019296,0.470813450024345,3.70151600181885));
#31843=CARTESIAN_POINT('Ctrl Pts',(5.56664367822439,0.556266870991092,3.96359711366712));
#31844=CARTESIAN_POINT('Ctrl Pts',(5.5905015962558,0.505697889589837,4.23457972281303));
#31845=CARTESIAN_POINT('Ctrl Pts',(5.61435951428722,0.331471999260015,4.4482011999181));
#31846=CARTESIAN_POINT('Ctrl Pts',(5.63821743231864,0.0761921759760934,
4.55222527486821));
#31847=CARTESIAN_POINT('Ctrl Pts',(5.66207535035006,-0.197718709731212,
4.52121522783523));
#31848=CARTESIAN_POINT('Ctrl Pts',(5.68593326838148,-0.423281985227643,
4.3627538599096));
#31849=CARTESIAN_POINT('Ctrl Pts',(5.70979118641289,-0.545341285237878,
4.11558929214995));
#31850=CARTESIAN_POINT('Ctrl Pts',(5.73364910444432,-0.534049786451273,
3.84015999362387));
#31851=CARTESIAN_POINT('Ctrl Pts',(5.75750702247573,-0.392168567195948,
3.6038159310769));
#31852=CARTESIAN_POINT('Ctrl Pts',(5.78136494050716,-0.154391451667357,
3.46434966433946));
#31853=CARTESIAN_POINT('Ctrl Pts',(5.80522285853857,0.121138580962943,3.45586449715393));
#31854=CARTESIAN_POINT('Ctrl Pts',(5.82908077656999,0.367046927720705,3.58043527923202));
#31855=CARTESIAN_POINT('Ctrl Pts',(5.85293869460141,0.523202308305842,3.80760107017232));
#31856=CARTESIAN_POINT('Ctrl Pts',(5.87679661263283,0.551420461789987,4.08181362911724));
#31857=CARTESIAN_POINT('Ctrl Pts',(5.90065453066425,0.44480131269862,4.33602054829434));
#31858=CARTESIAN_POINT('Ctrl Pts',(5.92451244869567,0.229416087376931,4.50806125053784));
#31859=CARTESIAN_POINT('Ctrl Pts',(5.94837036672709,-0.042067546589846,
4.55586721297736));
#31860=CARTESIAN_POINT('Ctrl Pts',(5.97222828475851,-0.30326465903273,4.46774835821298));
#31861=CARTESIAN_POINT('Ctrl Pts',(5.99608620278993,-0.490305038147314,
4.26525255699254));
#31862=CARTESIAN_POINT('Ctrl Pts',(6.01994412082133,-0.557452977205748,
3.99789477357902));
#31863=CARTESIAN_POINT('Ctrl Pts',(6.04380203885278,-0.488287539408226,
3.73105273207384));
#31864=CARTESIAN_POINT('Ctrl Pts',(6.06765995688417,-0.299724270968661,
3.52997381710292));
#31865=CARTESIAN_POINT('Ctrl Pts',(6.09151787491561,-0.0378669053578504,
3.44383251805177));
#31866=CARTESIAN_POINT('Ctrl Pts',(6.11537579294702,0.233243627260218,3.49368287747685));
#31867=CARTESIAN_POINT('Ctrl Pts',(6.13923371097844,0.447331678364145,3.6673537262422));
#31868=CARTESIAN_POINT('Ctrl Pts',(6.16309162900986,0.552012406214274,3.92234268746235));
#31869=CARTESIAN_POINT('Ctrl Pts',(6.18694954704127,0.521753629494025,4.19636433484848));
#31870=CARTESIAN_POINT('Ctrl Pts',(6.2108074650727,0.363831507594212,4.42228768590875));
#31871=CARTESIAN_POINT('Ctrl Pts',(6.23466538310411,0.117094415953721,4.54510476979165));
#31872=CARTESIAN_POINT('Ctrl Pts',(6.25852330113554,-0.158561881267111,
4.53433708369694));
#31873=CARTESIAN_POINT('Ctrl Pts',(6.28238121916695,-0.394905399742298,
4.39345989467659));
#31874=CARTESIAN_POINT('Ctrl Pts',(6.30623913719837,-0.535697351746728,
4.1553358869807));
#31875=CARTESIAN_POINT('Ctrl Pts',(6.33009705522979,-0.543633587309765,
3.88114808171798));
#31876=CARTESIAN_POINT('Ctrl Pts',(6.36190761260502,-0.381130543103143,
3.54983775818315));
#31877=CARTESIAN_POINT('Ctrl Pts',(6.40167080932404,0.0904237977681596,
3.37418170676098));
#31878=CARTESIAN_POINT('Ctrl Pts',(6.4493866453869,0.576013642360818,3.73827828410759));
#31879=CARTESIAN_POINT('Ctrl Pts',(6.49710248144972,0.531303907723303,4.34259299019566));
#31880=CARTESIAN_POINT('Ctrl Pts',(6.54481831751257,-0.000617460830772086,
4.63236849138271));
#31881=CARTESIAN_POINT('Ctrl Pts',(6.5925341535754,-0.532336898979176,4.34139325430452));
#31882=CARTESIAN_POINT('Ctrl Pts',(6.64024998963824,-0.575010046738857,
3.73693099107234));
#31883=CARTESIAN_POINT('Ctrl Pts',(6.68796582570108,-0.0897448725589052,
3.37403863313417));
#31884=CARTESIAN_POINT('Ctrl Pts',(6.73568166176391,0.477988548433368,3.58598174571673));
#31885=CARTESIAN_POINT('Ctrl Pts',(6.78339749782676,0.606749053262868,4.17812127049189));
#31886=CARTESIAN_POINT('Ctrl Pts',(6.83111333388958,0.178337754027021,4.60669083891839));
#31887=CARTESIAN_POINT('Ctrl Pts',(6.87882916995244,-0.413851892207341,
4.47812605548031));
#31888=CARTESIAN_POINT('Ctrl Pts',(6.92654500601527,-0.625990718083913,
3.91049119230943));
#31889=CARTESIAN_POINT('Ctrl Pts',(6.97426084207811,-0.263274891453005,
3.42505341469988));
#31890=CARTESIAN_POINT('Ctrl Pts',(7.02197667814094,0.341211513798207,3.46759805477058));
#31891=CARTESIAN_POINT('Ctrl Pts',(7.06969251420378,0.63235750294684,3.99905552874491));
#31892=CARTESIAN_POINT('Ctrl Pts',(7.11740835026662,0.342800202184808,4.53138035934227));
#31893=CARTESIAN_POINT('Ctrl Pts',(7.16512418632946,-0.261555976381552,
4.57573041153878));
#31894=CARTESIAN_POINT('Ctrl Pts',(7.2128400223923,-0.625721183287191,4.0913783776429));
#31895=CARTESIAN_POINT('Ctrl Pts',(7.26055585845514,-0.41527704940159,3.52311216844965));
#31896=CARTESIAN_POINT('Ctrl Pts',(7.30827169451797,0.176522415171576,3.39277939551711));
#31897=CARTESIAN_POINT('Ctrl Pts',(7.35598753058081,0.606218615784068,3.8200666455489));
#31898=CARTESIAN_POINT('Ctrl Pts',(7.40370336664364,0.479214941044062,4.4125894643569));
#31899=CARTESIAN_POINT('Ctrl Pts',(7.4514192027065,-0.0878591916424711,
4.62622502914213));
#31900=CARTESIAN_POINT('Ctrl Pts',(7.49913503876932,-0.574250874682306,
4.26478851416677));
#31901=CARTESIAN_POINT('Ctrl Pts',(7.54685087483217,-0.53329914461431,3.6601926322252));
#31902=CARTESIAN_POINT('Ctrl Pts',(7.594566710895,-0.00261060360317682,
3.36764708477891));
#31903=CARTESIAN_POINT('Ctrl Pts',(7.64228254695784,0.530475294557976,3.65580094934904));
#31904=CARTESIAN_POINT('Ctrl Pts',(7.68999838302067,0.576417567478113,4.26003809833172));
#31905=CARTESIAN_POINT('Ctrl Pts',(7.73771421908353,0.093026718772369,4.62547826040714));
#31906=CARTESIAN_POINT('Ctrl Pts',(7.78543005514634,-0.475791997136335,
4.41653211173522));
#31907=CARTESIAN_POINT('Ctrl Pts',(7.8331458912092,-0.607683601098078,3.82507811568403));
#31908=CARTESIAN_POINT('Ctrl Pts',(7.88086172727203,-0.181530003744534,
3.39425757752065));
#31909=CARTESIAN_POINT('Ctrl Pts',(7.92857756333487,0.411325389238953,3.51969962646458));
#31910=CARTESIAN_POINT('Ctrl Pts',(7.97629339939771,0.626454348233276,4.08620889879763));
#31911=CARTESIAN_POINT('Ctrl Pts',(8.02400923546054,0.266300640003926,4.57355121287022));
#31912=CARTESIAN_POINT('Ctrl Pts',(8.07172507152339,-0.338401043502061,
4.5341926229444));
#31913=CARTESIAN_POINT('Ctrl Pts',(8.11944090758622,-0.632343841791292,
4.00427672775865));
#31914=CARTESIAN_POINT('Ctrl Pts',(8.16715674364906,-0.345595560302635,
3.47043344766624));
#31915=CARTESIAN_POINT('Ctrl Pts',(8.2148725797119,0.258518441882999,3.42289928101069));
#31916=CARTESIAN_POINT('Ctrl Pts',(8.26258841577473,0.625230981070026,3.90532558443901));
#31917=CARTESIAN_POINT('Ctrl Pts',(8.31030425183758,0.417784289925175,4.47469286043008));
#31918=CARTESIAN_POINT('Ctrl Pts',(8.35802008790041,-0.173320143095541,
4.60814237859973));
#31919=CARTESIAN_POINT('Ctrl Pts',(8.40573592396325,-0.605262021838435,
4.18312539302794));
#31920=CARTESIAN_POINT('Ctrl Pts',(8.45345176002609,-0.481382472773795,
3.58994154129225));
#31921=CARTESIAN_POINT('Ctrl Pts',(8.50116759608892,0.0845580080604409,
3.37332068174828));
#31922=CARTESIAN_POINT('Ctrl Pts',(8.54888343215178,0.572847569000584,3.73218908285563));
#31923=CARTESIAN_POINT('Ctrl Pts',(8.59659926821459,0.535082392934658,4.33699236997728));
#31924=CARTESIAN_POINT('Ctrl Pts',(8.64431510427745,0.00594282213592907,
4.6323303784547));
#31925=CARTESIAN_POINT('Ctrl Pts',(8.69203094034027,-0.528654133672296,
4.34698967074364));
#31926=CARTESIAN_POINT('Ctrl Pts',(8.73974677640312,-0.577779864139828,
3.74300300926635));
#31927=CARTESIAN_POINT('Ctrl Pts',(8.78746261246595,-0.0963214550818077,
3.37502063878676));
#31928=CARTESIAN_POINT('Ctrl Pts',(8.8351784485288,0.473590428273928,3.58096643225285));
#31929=CARTESIAN_POINT('Ctrl Pts',(8.88289428459164,0.608596934220305,4.17171719864135));
#31930=CARTESIAN_POINT('Ctrl Pts',(8.93061012065447,0.184719511004659,4.60477741930878));
#31931=CARTESIAN_POINT('Ctrl Pts',(8.97832595671731,-0.408788681441581,
4.48246123012823));
#31932=CARTESIAN_POINT('Ctrl Pts',(9.02604179278014,-0.626899937697651,
3.91709346970068));
#31933=CARTESIAN_POINT('Ctrl Pts',(9.07375762884299,-0.269319335070538,
3.42786005172794));
#31934=CARTESIAN_POINT('Ctrl Pts',(9.12147346490582,0.335581356962483,3.46403155175812));
#31935=CARTESIAN_POINT('Ctrl Pts',(9.16918930096866,0.632312525313962,3.99239112474344));
#31936=CARTESIAN_POINT('Ctrl Pts',(9.21690513703149,0.348381372290835,4.52773804495445));
#31937=CARTESIAN_POINT('Ctrl Pts',(9.26462097309434,-0.255473755443411,
4.5784549981902));
#31938=CARTESIAN_POINT('Ctrl Pts',(9.31233680915717,-0.624723402584967,
4.09796782591368));
#31939=CARTESIAN_POINT('Ctrl Pts',(9.36005264522002,-0.420279936527615,
3.52751529167185));
#31940=CARTESIAN_POINT('Ctrl Pts',(9.40776848128285,0.170113062081096,3.39095273519949));
#31941=CARTESIAN_POINT('Ctrl Pts',(9.45548431734569,0.604288618254829,3.81368765339017));
#31942=CARTESIAN_POINT('Ctrl Pts',(9.50320015340853,0.483536638109595,4.40751606625661));
#31943=CARTESIAN_POINT('Ctrl Pts',(9.55091598947137,-0.0812544769791981,
4.62711620503893));
#31944=CARTESIAN_POINT('Ctrl Pts',(9.5986318255342,-0.571428355597161,4.27082588331087));
#31945=CARTESIAN_POINT('Ctrl Pts',(9.64634766159704,-0.536850782714826,
3.66583198574659));
#31946=CARTESIAN_POINT('Ctrl Pts',(9.69406349765987,-0.0092748755543832,
3.36770971750703));
#31947=CARTESIAN_POINT('Ctrl Pts',(9.74177933372272,0.52681829253995,3.65022934471732));
#31948=CARTESIAN_POINT('Ctrl Pts',(9.78949516978555,0.579126116453474,4.253948746587));
#31949=CARTESIAN_POINT('Ctrl Pts',(9.83721100584839,0.099613516627068,4.62446310696212));
#31950=CARTESIAN_POINT('Ctrl Pts',(9.88492684191123,-0.471375708268938,
4.42152338761395));
#31951=CARTESIAN_POINT('Ctrl Pts',(9.93264267797408,-0.609493367214024,
3.83149225544889));
#31952=CARTESIAN_POINT('Ctrl Pts',(9.9803585140369,-0.187903888785556,3.39620437793004));
#31953=CARTESIAN_POINT('Ctrl Pts',(10.0280743500997,0.406240621987656,3.51539131074786));
#31954=CARTESIAN_POINT('Ctrl Pts',(10.0757901861626,0.627328118774167,4.07960185956908));
#31955=CARTESIAN_POINT('Ctrl Pts',(10.1235060222254,0.27233055140652,4.57071279591595));
#31956=CARTESIAN_POINT('Ctrl Pts',(10.1712218582883,-0.332752351661881,
4.5377293902281));
#31957=CARTESIAN_POINT('Ctrl Pts',(10.2189376943511,-0.632263650146131,
4.01094081146358));
#31958=CARTESIAN_POINT('Ctrl Pts',(10.2666535304139,-0.351157510074434,
3.47410511718603));
#31959=CARTESIAN_POINT('Ctrl Pts',(10.3143693664768,0.252421974751429,3.42020678572945));
#31960=CARTESIAN_POINT('Ctrl Pts',(10.3620852025396,0.624198476151732,3.89874148420283));
#31961=CARTESIAN_POINT('Ctrl Pts',(10.4098010386024,0.422763912373798,4.47026343579529));
#31962=CARTESIAN_POINT('Ctrl Pts',(10.4575168746653,-0.166901257195935,
4.60993523836389));
#31963=CARTESIAN_POINT('Ctrl Pts',(10.5052327107281,-0.603298434176698,
4.18949412648294));
#31964=CARTESIAN_POINT('Ctrl Pts',(10.552948546791,-0.485677376113382,3.5950376425108));
#31965=CARTESIAN_POINT('Ctrl Pts',(10.6006643828538,0.0779486895418537,
3.3724643225678));
#31966=CARTESIAN_POINT('Ctrl Pts',(10.6483802189166,0.569993274196054,3.72616667108832));
#31967=CARTESIAN_POINT('Ctrl Pts',(10.6960960549795,0.538604264682155,4.3313343790158));
#31968=CARTESIAN_POINT('Ctrl Pts',(10.7438118910423,0.0126066714187673,
4.63223262845832));
#31969=CARTESIAN_POINT('Ctrl Pts',(10.7915277271052,-0.524967822187051,
4.35254192703816));
#31970=CARTESIAN_POINT('Ctrl Pts',(10.839243563168,-0.580456287010268,3.74910654946403));
#31971=CARTESIAN_POINT('Ctrl Pts',(10.8869593992308,-0.102902812003948,
3.37607048800905));
#31972=CARTESIAN_POINT('Ctrl Pts',(10.9346752352937,0.469147898628881,3.5759984978049));
#31973=CARTESIAN_POINT('Ctrl Pts',(10.9823910713565,0.610372875182502,4.16529361116822));
#31974=CARTESIAN_POINT('Ctrl Pts',(11.0301069074193,0.191083048662156,4.60279705802663));
#31975=CARTESIAN_POINT('Ctrl Pts',(11.0778227434822,-0.403681281635282,
4.48674269127424));
#31976=CARTESIAN_POINT('Ctrl Pts',(11.125538579545,-0.627738879572117,3.92370502162571));
#31977=CARTESIAN_POINT('Ctrl Pts',(11.1732544156079,-0.275334205393669,
3.43073020456744));
#31978=CARTESIAN_POINT('Ctrl Pts',(11.2209702516707,0.329914106159097,3.46052459999659));
#31979=CARTESIAN_POINT('Ctrl Pts',(11.2686860877335,0.632197217644931,3.98572755614488));
#31980=CARTESIAN_POINT('Ctrl Pts',(11.3164019237964,0.353923896562866,4.52403711709511));
#31981=CARTESIAN_POINT('Ctrl Pts',(11.3641177598592,-0.24936318455202,4.58111533006939));
#31982=CARTESIAN_POINT('Ctrl Pts',(11.411833595922,-0.623656216347001,4.10454639383227));
#31983=CARTESIAN_POINT('Ctrl Pts',(11.4595494319849,-0.425236148486169,
3.53197089548594));
#31984=CARTESIAN_POINT('Ctrl Pts',(11.5072652680477,0.163684817628688,3.3891937253683));
#31985=CARTESIAN_POINT('Ctrl Pts',(11.5549811041106,0.602291497100466,3.80732935570755));
#31986=CARTESIAN_POINT('Ctrl Pts',(11.6026969401734,0.487804627338989,4.40239740331947));
#31987=CARTESIAN_POINT('Ctrl Pts',(11.6504127762363,-0.0746407375468588,
4.62793772378323));
#31988=CARTESIAN_POINT('Ctrl Pts',(11.6981286122991,-0.568542364648052,
4.276833170433));
#31989=CARTESIAN_POINT('Ctrl Pts',(11.7458444483619,-0.540342790144192,
3.67150845704832));
#31990=CARTESIAN_POINT('Ctrl Pts',(11.7935602844247,-0.0159381172083995,
3.36784258204823));
#31991=CARTESIAN_POINT('Ctrl Pts',(11.8412761204876,0.523102773999324,3.64469659094542));
#31992=CARTESIAN_POINT('Ctrl Pts',(11.8889919565504,0.581770338872691,4.24783118742311));
#31993=CARTESIAN_POINT('Ctrl Pts',(11.9367077926133,0.106189249871976,4.62337859111715));
#31994=CARTESIAN_POINT('Ctrl Pts',(11.9844236286761,-0.466907061217805,
4.4264678426758));
#31995=CARTESIAN_POINT('Ctrl Pts',(12.0321394647389,-0.611235433702689,
3.83792511225401));
#31996=CARTESIAN_POINT('Ctrl Pts',(12.0798553008018,-0.19425690235234,3.39821824509208));
#31997=CARTESIAN_POINT('Ctrl Pts',(12.1275711368646,0.401110731454808,3.51113682306459));
#31998=CARTESIAN_POINT('Ctrl Pts',(12.1752869729275,0.628132208685083,4.07298597854376));
#31999=CARTESIAN_POINT('Ctrl Pts',(12.2230028089903,0.27833021362349,4.56781098689255));
#32000=CARTESIAN_POINT('Ctrl Pts',(12.2707186450531,-0.327066699269377,
4.54120642908287));
#32001=CARTESIAN_POINT('Ctrl Pts',(12.3184344811159,-0.632113229655128,
4.01760367991507));
#32002=CARTESIAN_POINT('Ctrl Pts',(12.3661503171788,-0.356680454936339,
3.47783520061383));
#32003=CARTESIAN_POINT('Ctrl Pts',(12.4138661532416,0.246297469784735,3.4175786911271));
#32004=CARTESIAN_POINT('Ctrl Pts',(12.4615819893045,0.623096638228782,3.89216863128209));
#32005=CARTESIAN_POINT('Ctrl Pts',(12.5092978253673,0.427696576213203,4.46578177652963));
#32006=CARTESIAN_POINT('Ctrl Pts',(12.5570136614302,-0.16046383269669,4.61166034941614));
#32007=CARTESIAN_POINT('Ctrl Pts',(12.604729497493,-0.601267834987779,4.1958418118296));
#32008=CARTESIAN_POINT('Ctrl Pts',(12.6524453335558,-0.489918332714758,
3.60017872502631));
#32009=CARTESIAN_POINT('Ctrl Pts',(12.7001611696187,0.0713307128527425,
3.37167766707246));
#32010=CARTESIAN_POINT('Ctrl Pts',(12.7478770056815,0.56707566724347,3.72017467542775));
#32011=CARTESIAN_POINT('Ctrl Pts',(12.7955928417444,0.542066310823814,4.32563958500381));
#32012=CARTESIAN_POINT('Ctrl Pts',(12.8433086778072,0.0192691204123526,
4.63206465306178));
#32013=CARTESIAN_POINT('Ctrl Pts',(12.89102451387,-0.521223199767296,4.35805502464836));
#32014=CARTESIAN_POINT('Ctrl Pts',(12.9387403499329,-0.583068235550835,
3.7552379577156));
#32015=CARTESIAN_POINT('Ctrl Pts',(12.9864561859957,-0.109472738970043,
3.37718964036075));
#32016=CARTESIAN_POINT('Ctrl Pts',(13.0341720220585,0.464653258261548,3.57107765943178));
#32017=CARTESIAN_POINT('Ctrl Pts',(13.0818878581214,0.612081018822183,4.15885166366515));
#32018=CARTESIAN_POINT('Ctrl Pts',(13.1296036941842,0.197425361721354,4.6007497409078));
#32019=CARTESIAN_POINT('Ctrl Pts',(13.177319530247,-0.398529042827853,4.49097008735187));
#32020=CARTESIAN_POINT('Ctrl Pts',(13.2250353663099,-0.628508095190705,
3.93032504803489));
#32021=CARTESIAN_POINT('Ctrl Pts',(13.2727512023727,-0.281318492899819,
3.4336635891944));
#32022=CARTESIAN_POINT('Ctrl Pts',(13.3204670384356,0.324210210062374,3.45707757060249));
#32023=CARTESIAN_POINT('Ctrl Pts',(13.3681828744984,0.632011688508986,3.97906557286167));
#32024=CARTESIAN_POINT('Ctrl Pts',(13.4158987105612,0.359427108647973,4.52027798167956));
#32025=CARTESIAN_POINT('Ctrl Pts',(13.4636145466241,-0.243224915581421,
4.58371111441534));
#32026=CARTESIAN_POINT('Ctrl Pts',(13.5113303826869,-0.622519757336015,
4.11111334923356));
#32027=CARTESIAN_POINT('Ctrl Pts',(13.5590462187498,-0.430145127231255,
3.53647848575196));
#32028=CARTESIAN_POINT('Ctrl Pts',(13.6067620548126,0.157238391843492,3.38750256099959));
#32029=CARTESIAN_POINT('Ctrl Pts',(13.6544778908755,0.600227476264717,3.8009924589658));
#32030=CARTESIAN_POINT('Ctrl Pts',(13.7021937269383,0.492018433545193,4.39723404398833));
#32031=CARTESIAN_POINT('Ctrl Pts',(13.7499095630011,-0.0680187073756014,
4.62868949418496));
#32032=CARTESIAN_POINT('Ctrl Pts',(13.797625399064,-0.565593222711038,4.28280970824024));
#32033=CARTESIAN_POINT('Ctrl Pts',(13.8453412351268,-0.543774778860562,
3.67722141563181));
#32034=CARTESIAN_POINT('Ctrl Pts',(13.8930570711896,-0.0225995885319848,
3.36804566363559));
#32035=CARTESIAN_POINT('Ctrl Pts',(13.9407729072525,0.519329151684885,3.63920330259016));
#32036=CARTESIAN_POINT('Ctrl Pts',(13.9884887433153,0.584349941003394,4.24168610034696));
#32037=CARTESIAN_POINT('Ctrl Pts',(14.0362045793781,0.112753188118911,4.62222483333648));
#32038=CARTESIAN_POINT('Ctrl Pts',(14.083920415441,-0.462386552345973,4.43136492771341));
#32039=CARTESIAN_POINT('Ctrl Pts',(14.1316362515038,-0.612909607059929,
3.84437597156854));
#32040=CARTESIAN_POINT('Ctrl Pts',(14.1793520875667,-0.200588338784227,
3.40029895531576));
#32041=CARTESIAN_POINT('Ctrl Pts',(14.2270679236295,0.395936287445344,3.50693663598317));
#32042=CARTESIAN_POINT('Ctrl Pts',(14.2747837596923,0.628866528650988,4.06636199058228));
#32043=CARTESIAN_POINT('Ctrl Pts',(14.3224995957552,0.284298960241116,4.5648461081192));
#32044=CARTESIAN_POINT('Ctrl Pts',(14.370215431818,-0.321344717859966,4.54462335329573));
#32045=CARTESIAN_POINT('Ctrl Pts',(14.4179312678809,-0.631892597026201,
4.02426459303334));
#32046=CARTESIAN_POINT('Ctrl Pts',(14.4656471039437,-0.362163781425906,
3.48162328362967));
#32047=CARTESIAN_POINT('Ctrl Pts',(14.5133629400065,0.240145607263868,3.41501528911991));
#32048=CARTESIAN_POINT('Ctrl Pts',(14.5610787760693,0.6219255896881,3.8856077557581));
#32049=CARTESIAN_POINT('Ctrl Pts',(14.6087946121322,0.432581733546503,4.46124838043455));
#32050=CARTESIAN_POINT('Ctrl Pts',(14.656510448195,-0.154008584636381,4.61331752013935));
#32051=CARTESIAN_POINT('Ctrl Pts',(14.7042262842579,-0.599170449821005,
4.20216774399712));
#32052=CARTESIAN_POINT('Ctrl Pts',(14.7519421203207,-0.494104871512583,
3.60536421779174));
#32053=CARTESIAN_POINT('Ctrl Pts',(14.7996579563836,0.0647048130865326,
3.37096080264023));
#32054=CARTESIAN_POINT('Ctrl Pts',(14.8473737924464,0.564095072216763,3.71421376143635));
#32055=CARTESIAN_POINT('Ctrl Pts',(14.8950896285093,0.545468146811986,4.319908620492));
#32056=CARTESIAN_POINT('Ctrl Pts',(14.942805464572,0.0259294290834894,4.63182647092298));
#32057=CARTESIAN_POINT('Ctrl Pts',(14.9905213006349,-0.517420682347921,
4.36352835120552));
#32058=CARTESIAN_POINT('Ctrl Pts',(15.0382371366977,-0.585615419638682,
3.76139655297334));
#32059=CARTESIAN_POINT('Ctrl Pts',(15.0859529727606,-0.116030506223773,
3.3783779715317));
#32060=CARTESIAN_POINT('Ctrl Pts',(15.1336688088234,0.460107006415252,3.56620446371685));
#32061=CARTESIAN_POINT('Ctrl Pts',(15.1813846448862,0.613721175406852,4.15239207167311));
#32062=CARTESIAN_POINT('Ctrl Pts',(15.2291004809491,0.203745745708236,4.59863569535852));
#32063=CARTESIAN_POINT('Ctrl Pts',(15.2768163170119,-0.393332537305518,
4.49514294880206));
#32064=CARTESIAN_POINT('Ctrl Pts',(15.3245321530748,-0.629207499112597,
3.93695281360709));
#32065=CARTESIAN_POINT('Ctrl Pts',(15.3722479891376,-0.287271532882751,
3.43665987978239));
#32066=CARTESIAN_POINT('Ctrl Pts',(15.4199638252004,0.318470302234025,3.45369084645546));
#32067=CARTESIAN_POINT('Ctrl Pts',(15.4676796612633,0.631755958513824,3.97240591487529));
#32068=CARTESIAN_POINT('Ctrl Pts',(15.5153954973261,0.364890397275464,4.51646105625472));
#32069=CARTESIAN_POINT('Ctrl Pts',(15.563111333389,-0.237059630341402,4.58624206290064));
#32070=CARTESIAN_POINT('Ctrl Pts',(15.6108271694518,-0.621314151784485,
4.11766796269128));
#32071=CARTESIAN_POINT('Ctrl Pts',(15.6585430055147,-0.435006327496808,
3.54103756178819));
#32072=CARTESIAN_POINT('Ctrl Pts',(15.7062588415774,0.150774500763906,3.38587942993986));
#32073=CARTESIAN_POINT('Ctrl Pts',(15.7539746776403,0.598096785009218,3.79467766703735));
#32074=CARTESIAN_POINT('Ctrl Pts',(15.8016905137032,0.496177588678611,4.39202656178461));
#32075=CARTESIAN_POINT('Ctrl Pts',(15.849406349766,-0.0613891220090978,
4.62937143274106));
#32076=CARTESIAN_POINT('Ctrl Pts',(15.8971221858288,-0.562581257362808,
4.28875483288714));
#32077=CARTESIAN_POINT('Ctrl Pts',(15.9448380218917,-0.547146367654922,
3.68297022692873));
#32078=CARTESIAN_POINT('Ctrl Pts',(15.9925538579545,-0.0292585496004989,
3.36831893971177));
#32079=CARTESIAN_POINT('Ctrl Pts',(16.0402696940173,0.515497844752703,3.63375008981994));
#32080=CARTESIAN_POINT('Ctrl Pts',(16.0879855300802,0.586864636315616,4.23551416792571));
#32081=CARTESIAN_POINT('Ctrl Pts',(16.135701366143,0.119304602276749,4.62100196177401));
#32082=CARTESIAN_POINT('Ctrl Pts',(16.1834172022059,-0.457814683770117,
4.43621409878185));
#32083=CARTESIAN_POINT('Ctrl Pts',(16.2311330382687,-0.614515701326505,
3.85084411686165));
#32084=CARTESIAN_POINT('Ctrl Pts',(16.2788488743316,-0.206897494815317,
3.40244627748567));
#32085=CARTESIAN_POINT('Ctrl Pts',(16.3265647103943,0.390717864711932,3.50279121604045));
#32086=CARTESIAN_POINT('Ctrl Pts',(16.3742805464572,0.629530997107116,4.05973063144581));
#32087=CARTESIAN_POINT('Ctrl Pts',(16.42199638252,0.290236128279341,4.56181848892059));
#32088=CARTESIAN_POINT('Ctrl Pts',(16.4697122185829,-0.315587043004215,
4.54797978333095));
#32089=CARTESIAN_POINT('Ctrl Pts',(16.5174280546457,-0.631601776766168,
4.03092281095576));
#32090=CARTESIAN_POINT('Ctrl Pts',(16.5651438907086,-0.367606880481235,
3.48546894547127));
#32091=CARTESIAN_POINT('Ctrl Pts',(16.6128597267714,0.233967070508539,3.41251686443844));
#32092=CARTESIAN_POINT('Ctrl Pts',(16.6605755628343,0.620685460604191,3.87905958638177));
#32093=CARTESIAN_POINT('Ctrl Pts',(16.7082913988971,0.437418841753611,4.45666375105816));
#32094=CARTESIAN_POINT('Ctrl Pts',(16.7560072349599,-0.147536230033309,
4.61490656646286));
#32095=CARTESIAN_POINT('Ctrl Pts',(16.8037230710227,-0.597006511643959,
4.20847122033102));
#32096=CARTESIAN_POINT('Ctrl Pts',(16.8514389070856,-0.498236527486006,
3.61059354482716));
#32097=CARTESIAN_POINT('Ctrl Pts',(16.8991547431484,0.058071726216741,3.37031380889701));
#32098=CARTESIAN_POINT('Ctrl Pts',(16.9468705792113,0.561051820186282,3.70828459122417));
#32099=CARTESIAN_POINT('Ctrl Pts',(16.9945864152741,0.548809394786867,4.31414212204871));
#32100=CARTESIAN_POINT('Ctrl Pts',(17.0423022513369,0.0325868576366809,
4.63151810849805));
#32101=CARTESIAN_POINT('Ctrl Pts',(17.0900180873998,-0.513560692294518,
4.3689612987585));
#32102=CARTESIAN_POINT('Ctrl Pts',(17.1377339234626,-0.588097556344686,
3.76758165116972));
#32103=CARTESIAN_POINT('Ctrl Pts',(17.1854497595255,-0.122575385359494,
3.37963534952775));
#32104=CARTESIAN_POINT('Ctrl Pts',(17.2331655955883,0.455509648066065,3.56137945195155));
#32105=CARTESIAN_POINT('Ctrl Pts',(17.2808814316511,0.615293162755707,4.14591555269289));
#32106=CARTESIAN_POINT('Ctrl Pts',(17.328597267714,0.210043498584534,4.59645515619697));
#32107=CARTESIAN_POINT('Ctrl Pts',(17.3763131037768,-0.388092342271454,
4.49926081212312));
#32108=CARTESIAN_POINT('Ctrl Pts',(17.4240289398397,-0.629837013651323,
3.94358758216158));
#32109=CARTESIAN_POINT('Ctrl Pts',(17.4717447759025,-0.293192664107019,
3.43971874351766));
#32110=CARTESIAN_POINT('Ctrl Pts',(17.5194606119653,0.312695020235776,3.45036480373676));
#32111=CARTESIAN_POINT('Ctrl Pts',(17.5671764480282,0.631430056064715,3.96574932190893));
#32112=CARTESIAN_POINT('Ctrl Pts',(17.614892284091,0.370313155609181,4.51258676478657));
#32113=CARTESIAN_POINT('Ctrl Pts',(17.6626081201539,-0.230868013642575,
4.58870789439952));
#32114=CARTESIAN_POINT('Ctrl Pts',(17.7103239562166,-0.620039533605355,
4.12420950615009));
#32115=CARTESIAN_POINT('Ctrl Pts',(17.7580397922796,-0.43981920932378,3.54564761719411));
#32116=CARTESIAN_POINT('Ctrl Pts',(17.8057556283423,0.144293862368219,3.38432451247882));
#32117=CARTESIAN_POINT('Ctrl Pts',(17.8534714644052,0.595899660001039,3.78838568133928));
#32118=CARTESIAN_POINT('Ctrl Pts',(17.901187300468,0.500281630760053,4.38677553513073));
#32119=CARTESIAN_POINT('Ctrl Pts',(17.9489031365309,-0.0547527178302441,
4.62998346370502));
#32120=CARTESIAN_POINT('Ctrl Pts',(17.9966189725937,-0.559506803158163,
4.29466788401745));
#32121=CARTESIAN_POINT('Ctrl Pts',(18.0443348086565,-0.550457182027191,
3.68875425238845));
#32122=CARTESIAN_POINT('Ctrl Pts',(18.0920506447194,-0.0359142607682062,
3.36866237992255));
#32123=CARTESIAN_POINT('Ctrl Pts',(18.1397664807822,0.511609278766163,3.62833755835171));
#32124=CARTESIAN_POINT('Ctrl Pts',(18.187482316845,0.589314145488933,4.22931607570827));
#32125=CARTESIAN_POINT('Ctrl Pts',(18.2351981529079,0.12584276464555,4.61971011226051));
#32126=CARTESIAN_POINT('Ctrl Pts',(18.2829139889707,-0.453191963311679,
4.44101481725822));
#32127=CARTESIAN_POINT('Ctrl Pts',(18.3306298250336,-0.616053538105107,
3.85732882968247));
#32128=CARTESIAN_POINT('Ctrl Pts',(18.3783456610964,-0.213183669654489,
3.40465997308746));
#32129=CARTESIAN_POINT('Ctrl Pts',(18.4260614971592,0.385456042892229,3.49870102369));
#32130=CARTESIAN_POINT('Ctrl Pts',(18.4737773332221,0.630125540247444,4.05309263771424));
#32131=CARTESIAN_POINT('Ctrl Pts',(18.5214931692849,0.296141058265729,4.55872846559028));
#32132=CARTESIAN_POINT('Ctrl Pts',(18.5692090053478,-0.309794314237323,
4.55127534637221));
#32133=CARTESIAN_POINT('Ctrl Pts',(18.6169248414106,-0.631240801177943,
4.0375775941191));
#32134=CARTESIAN_POINT('Ctrl Pts',(18.6646406774734,-0.373009147508776,
3.4893717589807));
#32135=CARTESIAN_POINT('Ctrl Pts',(18.7123565135363,0.227762545801372,3.41008369459593));
#32136=CARTESIAN_POINT('Ctrl Pts',(18.7600723495991,0.619376388724522,3.87252485049244));
#32137=CARTESIAN_POINT('Ctrl Pts',(18.8077881856619,0.442207363551868,4.45202839763978));
#32138=CARTESIAN_POINT('Ctrl Pts',(18.8555040217248,-0.141047487806633,
4.61642731188217));
#32139=CARTESIAN_POINT('Ctrl Pts',(18.9032198577876,-0.594776260815313,
4.21475154067248));
#32140=CARTESIAN_POINT('Ctrl Pts',(18.9509356938505,-0.502312841712761,
3.615866125281));
#32141=CARTESIAN_POINT('Ctrl Pts',(18.9986515299133,0.0514321890198641,
3.36973675771293));
#32142=CARTESIAN_POINT('Ctrl Pts',(19.0463673659762,0.557946249173174,3.70238782336559));
#32143=CARTESIAN_POINT('Ctrl Pts',(19.0940832020389,0.552089683635207,4.30834073020757));
#32144=CARTESIAN_POINT('Ctrl Pts',(19.1417990381018,0.0392406665648073,
4.63113960000379));
#32145=CARTESIAN_POINT('Ctrl Pts',(19.1895148741646,-0.509643658296843,
4.3743532639067));
#32146=CARTESIAN_POINT('Ctrl Pts',(19.2372307102275,-0.590514370077448,
3.77379256516987));
#32147=CARTESIAN_POINT('Ctrl Pts',(19.2849465462903,-0.129106649190522,
3.38096163491845));
#32148=CARTESIAN_POINT('Ctrl Pts',(19.3326623823532,0.450861693465423,3.55660315963506));
#32149=CARTESIAN_POINT('Ctrl Pts',(19.380378218416,0.616796807017627,4.1394228269368));
#32150=CARTESIAN_POINT('Ctrl Pts',(19.4280940544789,0.216317919394901,4.59420836405745));
#32151=CARTESIAN_POINT('Ctrl Pts',(19.4758098905416,-0.382809037079938,
4.50332322288615));
#32152=CARTESIAN_POINT('Ctrl Pts',(19.5235257266046,-0.630396573984801,
3.95022861114352));
#32153=CARTESIAN_POINT('Ctrl Pts',(19.5712415626673,-0.299081219248977,
3.44283985120298));
#32154=CARTESIAN_POINT('Ctrl Pts',(19.6189573987302,0.306884987370396,3.44709979193512));
#32155=CARTESIAN_POINT('Ctrl Pts',(19.666673234793,0.631034051704256,3.95909657101937));
#32156=CARTESIAN_POINT('Ctrl Pts',(19.7143890708559,0.375694716468479,4.50865546647685));
#32157=CARTESIAN_POINT('Ctrl Pts',(19.7621049069187,-0.224650630777236,
4.59110846933868));
#32158=CARTESIAN_POINT('Ctrl Pts',(19.8098207429815,-0.618696275574682,
4.13073699938377));
#32159=CARTESIAN_POINT('Ctrl Pts',(19.8575365790444,-0.44458280157215,3.55030861879767));
#32160=CARTESIAN_POINT('Ctrl Pts',(19.9052524151072,0.13779637220375,3.3828370770856));
#32161=CARTESIAN_POINT('Ctrl Pts',(19.9529682511701,0.593637901716091,3.7821189081517));
#32162=CARTESIAN_POINT('Ctrl Pts',(20.0006840872329,0.504327165075627,4.38147832337345));
#32163=CARTESIAN_POINT('Ctrl Pts',(20.0483999232957,-0.0481046828163007,
4.63053160650705));
#32164=CARTESIAN_POINT('Ctrl Pts',(20.0961157593586,-0.556380679578279,
4.30053671048834));
#32165=CARTESIAN_POINT('Ctrl Pts',(20.1438315954214,-0.553687069357429,
3.69459455385474));
#32166=CARTESIAN_POINT('Ctrl Pts',(20.1915474314843,-0.0426033430871586,
3.36903495876776));
#32167=CARTESIAN_POINT('Ctrl Pts',(20.2392632675471,0.507734449822709,3.62304374442814));
#32168=CARTESIAN_POINT('Ctrl Pts',(20.2869791036099,0.591564791291533,4.22294595084339));
#32169=CARTESIAN_POINT('Ctrl Pts',(20.3346949396728,0.132620199007312,4.618629012875));
#32170=CARTESIAN_POINT('Ctrl Pts',(20.3824107757356,-0.449008129734859,
4.44521533979349));
#32171=CARTESIAN_POINT('Ctrl Pts',(20.4221739724547,-0.588594799935545,
3.96175478680276));
#32172=CARTESIAN_POINT('Ctrl Pts',(20.4539845298298,-0.419131055782338,
3.63395025773895));
#32173=CARTESIAN_POINT('Ctrl Pts',(20.4778424478613,-0.194099195253748,
3.47709810398663));
#32174=CARTESIAN_POINT('Ctrl Pts',(20.5017003658927,0.0810471032980313,
3.44846366347126));
#32175=CARTESIAN_POINT('Ctrl Pts',(20.5255582839241,0.334940048200093,3.55449674151986));
#32176=CARTESIAN_POINT('Ctrl Pts',(20.5494162019556,0.507694843328107,3.76957374638464));
#32177=CARTESIAN_POINT('Ctrl Pts',(20.5732741199869,0.555899439471162,4.04093981905292));
#32178=CARTESIAN_POINT('Ctrl Pts',(20.5971320380184,0.468386015874758,4.30232489481291));
#32179=CARTESIAN_POINT('Ctrl Pts',(20.6209899560498,0.266225827016684,4.48976745893774));
#32180=CARTESIAN_POINT('Ctrl Pts',(20.6448478740812,-0.000973650874560818,
4.55745692740964));
#32181=CARTESIAN_POINT('Ctrl Pts',(20.6687057921126,-0.267966914960919,
4.48882854939535));
#32182=CARTESIAN_POINT('Ctrl Pts',(20.6925637101441,-0.469418090387657,
4.30067062862012));
#32183=CARTESIAN_POINT('Ctrl Pts',(20.7164216281755,-0.556092695039732,
4.03898930289119));
#32184=CARTESIAN_POINT('Ctrl Pts',(20.7402795462069,-0.506782753954552,
3.7677746905255));
#32185=CARTESIAN_POINT('Ctrl Pts',(20.7641374642383,-0.333553132261349,
3.55334514249538));
#32186=CARTESIAN_POINT('Ctrl Pts',(20.7879953822697,-0.0787593560922578,
3.44813505886707));
#32187=CARTESIAN_POINT('Ctrl Pts',(20.8118533003012,0.19529252477751,3.47787088781106));
#32188=CARTESIAN_POINT('Ctrl Pts',(20.8357112183325,0.421590436108717,3.63528155911584));
#32189=CARTESIAN_POINT('Ctrl Pts',(20.859569136364,0.544797804677434,3.8818757964511));
#32190=CARTESIAN_POINT('Ctrl Pts',(20.8834270543954,0.534787374467886,4.15735463375504));
#32191=CARTESIAN_POINT('Ctrl Pts',(20.9072849724269,0.394006808563119,4.39435596913946));
#32192=CARTESIAN_POINT('Ctrl Pts',(20.9311428904582,0.156880874733563,4.53492653211281));
#32193=CARTESIAN_POINT('Ctrl Pts',(20.9550008084897,-0.118606721834374,
4.54469298471526));
#32194=CARTESIAN_POINT('Ctrl Pts',(20.9788587265211,-0.365091735913813,
4.42126716656144));
#32195=CARTESIAN_POINT('Ctrl Pts',(21.0027166445525,-0.522301880015273,
4.19483005048941));
#32196=CARTESIAN_POINT('Ctrl Pts',(21.0265745625839,-0.55179498493052,3.92075168033001));
#32197=CARTESIAN_POINT('Ctrl Pts',(21.0504324806153,-0.446359186657349,
3.66605168284066));
#32198=CARTESIAN_POINT('Ctrl Pts',(21.0742903986468,-0.231776408019839,
3.49301114555638));
#32199=CARTESIAN_POINT('Ctrl Pts',(21.0981483166782,0.0394820154987394,
3.44394319323497));
#32200=CARTESIAN_POINT('Ctrl Pts',(21.1220062347096,0.301086010940692,3.5308462768762));
#32201=CARTESIAN_POINT('Ctrl Pts',(21.145864152741,0.489066275193333,3.73247022529863));
#32202=CARTESIAN_POINT('Ctrl Pts',(21.1697220707724,0.557456513314207,3.9995124910074));
#32203=CARTESIAN_POINT('Ctrl Pts',(21.1935799888039,0.489533449092281,4.26667396594056));
#32204=CARTESIAN_POINT('Ctrl Pts',(21.2174379068352,0.30190612195814,4.46862639215028));
#32205=CARTESIAN_POINT('Ctrl Pts',(21.2412958248667,0.0404545242400231,
4.55598690035157));
#32206=CARTESIAN_POINT('Ctrl Pts',(21.2651537428981,-0.230889306609896,
4.50739346663836));
#32207=CARTESIAN_POINT('Ctrl Pts',(21.2890116609295,-0.445774412697373,
4.33472850921124));
#32208=CARTESIAN_POINT('Ctrl Pts',(21.312869578961,-0.551655532228011,4.08021331346062));
#32209=CARTESIAN_POINT('Ctrl Pts',(21.3367274969923,-0.522641847334507,
3.80608377760199));
#32210=CARTESIAN_POINT('Ctrl Pts',(21.3605854150238,-0.365827994289322,
3.57937204029158));
#32211=CARTESIAN_POINT('Ctrl Pts',(21.3844433330552,-0.119559231686077,
3.45551529680541));
#32212=CARTESIAN_POINT('Ctrl Pts',(21.4083012510867,0.155945019792583,3.46479989471587));
#32213=CARTESIAN_POINT('Ctrl Pts',(21.432159169118,0.393316466074861,3.60495549692644));
#32214=CARTESIAN_POINT('Ctrl Pts',(21.4560170871495,0.534511322676435,3.84171024093472));
#32215=CARTESIAN_POINT('Ctrl Pts',(21.4798750051809,0.545003601087511,4.11717114276091));
#32216=CARTESIAN_POINT('Ctrl Pts',(21.5037329232123,0.422227653432673,4.36398050850424));
#32217=CARTESIAN_POINT('Ctrl Pts',(21.5275908412437,0.196205543263173,4.52178672528827));
#32218=CARTESIAN_POINT('Ctrl Pts',(21.5514487592751,-0.0777941667658609,
4.5520018745543));
#32219=CARTESIAN_POINT('Ctrl Pts',(21.5753066773066,-0.332771083950078,
4.44723752926263));
#32220=CARTESIAN_POINT('Ctrl Pts',(21.5991645953379,-0.506376406606172,
4.23311142556056));
#32221=CARTESIAN_POINT('Ctrl Pts',(21.6230225133694,-0.556158904430687,
3.96198322848119));
#32222=CARTESIAN_POINT('Ctrl Pts',(21.6468804314008,-0.469945400657515,
3.70015116759423));
#32223=CARTESIAN_POINT('Ctrl Pts',(21.6707383494323,-0.268817445367881,
3.51164031394868));
#32224=CARTESIAN_POINT('Ctrl Pts',(21.6945962674636,-0.00195630224560004,
3.44254670619344));
#32225=CARTESIAN_POINT('Ctrl Pts',(21.7184541854951,0.26538321006433,3.50976561349676));
#32226=CARTESIAN_POINT('Ctrl Pts',(21.7423121035264,0.467829298620023,3.6968601820167));
#32227=CARTESIAN_POINT('Ctrl Pts',(21.766170021558,0.555878380248887,3.95808069339639));
#32228=CARTESIAN_POINT('Ctrl Pts',(21.7900279395893,0.508000056083844,4.22955161709966));
#32229=CARTESIAN_POINT('Ctrl Pts',(21.8138858576208,0.335901880562604,4.44489091756156));
#32230=CARTESIAN_POINT('Ctrl Pts',(21.8377437756521,0.0816665454602928,
4.55144227009437));
#32231=CARTESIAN_POINT('Ctrl Pts',(21.8616016936836,-0.192538484559094,
4.52315096660328));
#32232=CARTESIAN_POINT('Ctrl Pts',(21.885459611715,-0.419662610460766,4.36693500143146));
#32233=CARTESIAN_POINT('Ctrl Pts',(21.9093175297464,-0.544167796724789,
4.12099343330092));
#32234=CARTESIAN_POINT('Ctrl Pts',(21.9331754477779,-0.535609133856441,
3.84546567493331));
#32235=CARTESIAN_POINT('Ctrl Pts',(21.9570333658092,-0.396079448060293,
3.60772576847503));
#32236=CARTESIAN_POINT('Ctrl Pts',(21.9808912838407,-0.159697548225882,
3.46590759696012));
#32237=CARTESIAN_POINT('Ctrl Pts',(22.0047492018721,0.115734752223676,3.45468956637345));
#32238=CARTESIAN_POINT('Ctrl Pts',(22.0286071199035,0.362866753203085,3.5768147907664));
#32239=CARTESIAN_POINT('Ctrl Pts',(22.0524650379349,0.521267948732644,3.80242032615069));
#32240=CARTESIAN_POINT('Ctrl Pts',(22.0763229559664,0.552204931742854,4.07633947375325));
#32241=CARTESIAN_POINT('Ctrl Pts',(22.1001808739978,0.448112767182329,4.33159154057792));
#32242=CARTESIAN_POINT('Ctrl Pts',(22.1240387920292,0.23444482469764,4.5057604433585));
#32243=CARTESIAN_POINT('Ctrl Pts',(22.1478967100606,-0.0365512635718279,
4.55625714110116));
#32244=CARTESIAN_POINT('Ctrl Pts',(22.171754628092,-0.298609572266455,4.47073381570218));
#32245=CARTESIAN_POINT('Ctrl Pts',(22.1956125461234,-0.487649706571227,
4.2701032498363));
#32246=CARTESIAN_POINT('Ctrl Pts',(22.2194704641549,-0.557446204325542,
4.00342508191314));
#32247=CARTESIAN_POINT('Ctrl Pts',(22.2433283821863,-0.490931920559466,
3.73590938817905));
#32248=CARTESIAN_POINT('Ctrl Pts',(22.2671863002177,-0.304371409562025,
3.53297104269219));
#32249=CARTESIAN_POINT('Ctrl Pts',(22.2910442182491,-0.0433837978980346,
3.44423399893113));
#32250=CARTESIAN_POINT('Ctrl Pts',(22.3149021362806,0.228212333880327,3.49139688109763));
#32251=CARTESIAN_POINT('Ctrl Pts',(22.3387600543119,0.444004334066149,3.66292708008725));
#32252=CARTESIAN_POINT('Ctrl Pts',(22.3626179723434,0.551225179343846,3.91688078933633));
#32253=CARTESIAN_POINT('Ctrl Pts',(22.3864758903748,0.523656454698273,4.19115941035881));
#32254=CARTESIAN_POINT('Ctrl Pts',(22.4103338084062,0.368039459933637,4.41869434725418));
#32255=CARTESIAN_POINT('Ctrl Pts',(22.4341917264376,0.122426797365049,4.54384711353805));
#32256=CARTESIAN_POINT('Ctrl Pts',(22.458049644469,-0.153122562087755,4.53601444212637));
#32257=CARTESIAN_POINT('Ctrl Pts',(22.4819075625005,-0.391229265084309,
4.39711164706476));
#32258=CARTESIAN_POINT('Ctrl Pts',(22.5057654805319,-0.533669791868601,
4.16110422172694));
#32259=CARTESIAN_POINT('Ctrl Pts',(22.5296233985633,-0.545613449745194,
3.88570245498666));
#32260=CARTESIAN_POINT('Ctrl Pts',(22.5534813165947,-0.424139885198736,
3.63824949626794));
#32261=CARTESIAN_POINT('Ctrl Pts',(22.5773392346261,-0.198952323217499,
3.47925449370713));
#32262=CARTESIAN_POINT('Ctrl Pts',(22.6011971526576,0.0748840438856019,
3.44759575567767));
#32263=CARTESIAN_POINT('Ctrl Pts',(22.625055070689,0.330410085854462,3.55101527375816));
#32264=CARTESIAN_POINT('Ctrl Pts',(22.6489129887204,0.505140231362423,3.7642230866287));
#32265=CARTESIAN_POINT('Ctrl Pts',(22.6727709067518,0.556352908954721,4.03508610068096));
#32266=CARTESIAN_POINT('Ctrl Pts',(22.6966288247833,0.471516332128332,4.29736710820476));
#32267=CARTESIAN_POINT('Ctrl Pts',(22.7204867428146,0.27139215166714,4.48693847894857));
#32268=CARTESIAN_POINT('Ctrl Pts',(22.7443446608461,0.00488440565515616,
4.55743119390072));
#32269=CARTESIAN_POINT('Ctrl Pts',(22.7682025788775,-0.262778018495442,
4.49163382183027));
#32270=CARTESIAN_POINT('Ctrl Pts',(22.7920604969089,-0.466262514422727,
4.30558517247789));
#32271=CARTESIAN_POINT('Ctrl Pts',(22.8079657755965,-0.525793678117208,
4.1317859159904));
#32272=CARTESIAN_POINT('Ctrl Pts',(22.8159184149403,-0.532958495437544,
4.04301651477895));
#32273=CARTESIAN_POINT('Ctrl Pts',(3.98408158505965,-0.251304309929533,
3.59658905474035));
#32274=CARTESIAN_POINT('Ctrl Pts',(3.99203422440346,-0.184112308377066,
3.5547318870523));
#32275=CARTESIAN_POINT('Ctrl Pts',(4.00793950309107,-0.0284797076443847,
3.50528009766423));
#32276=CARTESIAN_POINT('Ctrl Pts',(4.03179742112249,0.212077873916637,3.55216010213054));
#32277=CARTESIAN_POINT('Ctrl Pts',(4.05565533915392,0.400711255741927,3.70851080938071));
#32278=CARTESIAN_POINT('Ctrl Pts',(4.07951325718533,0.49139298320592,3.93615790384083));
#32279=CARTESIAN_POINT('Ctrl Pts',(4.10337117521676,0.461898357851897,4.17940600742409));
#32280=CARTESIAN_POINT('Ctrl Pts',(4.12722909324816,0.319466186301668,4.37878980142624));
#32281=CARTESIAN_POINT('Ctrl Pts',(4.15108701127959,0.0989109688445654,
4.48554634140719));
#32282=CARTESIAN_POINT('Ctrl Pts',(4.174944929311,-0.145828100556353,4.47357507321567));
#32283=CARTESIAN_POINT('Ctrl Pts',(4.19880284734243,-0.354909590370033,
4.34580100620849));
#32284=CARTESIAN_POINT('Ctrl Pts',(4.22266076537384,-0.477205295803391,
4.13346959398438));
#32285=CARTESIAN_POINT('Ctrl Pts',(4.24651868340526,-0.482811689970624,
3.88850100783657));
#32286=CARTESIAN_POINT('Ctrl Pts',(4.27037660143669,-0.370357271909554,
3.67079708031066));
#32287=CARTESIAN_POINT('Ctrl Pts',(4.2942345194681,-0.167340519784032,3.53359217153378));
#32288=CARTESIAN_POINT('Ctrl Pts',(4.31809243749953,0.0765956044913427,
3.51043671457025));
#32289=CARTESIAN_POINT('Ctrl Pts',(4.34195035553093,0.301801986965541,3.60699279882218));
#32290=CARTESIAN_POINT('Ctrl Pts',(4.36580827356237,0.453209578636439,3.79964985833574));
#32291=CARTESIAN_POINT('Ctrl Pts',(4.38966619159377,0.493795074712635,4.04129798000377));
#32292=CARTESIAN_POINT('Ctrl Pts',(4.4135241096252,0.413634228782107,4.27284762322724));
#32293=CARTESIAN_POINT('Ctrl Pts',(4.43738202765661,0.23232854437776,4.43767858897425));
#32294=CARTESIAN_POINT('Ctrl Pts',(4.46123994568804,-0.00578779637616802,
4.49548521832112));
#32295=CARTESIAN_POINT('Ctrl Pts',(4.48509786371945,-0.242488863923451,
4.43213221465579));
#32296=CARTESIAN_POINT('Ctrl Pts',(4.50895578175088,-0.419894798625899,
4.26311111366653));
#32297=CARTESIAN_POINT('Ctrl Pts',(4.53281369978229,-0.494625017545811,
4.02975217827461));
#32298=CARTESIAN_POINT('Ctrl Pts',(4.55667161781372,-0.448405946262215,
3.78911802491887));
#32299=CARTESIAN_POINT('Ctrl Pts',(4.58052953584513,-0.292539406836986,
3.60005025874973));
#32300=CARTESIAN_POINT('Ctrl Pts',(4.60438745387655,-0.0651390137990107,
3.50878109874461));
#32301=CARTESIAN_POINT('Ctrl Pts',(4.62824537190797,0.178189642449287,3.53762834062211));
#32302=CARTESIAN_POINT('Ctrl Pts',(4.65210328993938,0.377946077338085,3.67953804797316));
#32303=CARTESIAN_POINT('Ctrl Pts',(4.67596120797081,0.485284401269169,3.89980943180067));
#32304=CARTESIAN_POINT('Ctrl Pts',(4.69981912600222,0.473957470210434,4.14458013869048));
#32305=CARTESIAN_POINT('Ctrl Pts',(4.72367704403364,0.34673502734182,4.35399706338589));
#32306=CARTESIAN_POINT('Ctrl Pts',(4.74753496206506,0.134726425416229,4.47685206339739));
#32307=CARTESIAN_POINT('Ctrl Pts',(4.77139288009648,-0.110226457398098,
4.48310374471865));
#32308=CARTESIAN_POINT('Ctrl Pts',(4.7952507981279,-0.328225968870003,4.37122340097448));
#32309=CARTESIAN_POINT('Ctrl Pts',(4.81910871615932,-0.465965290257402,
4.16856882376961));
#32310=CARTESIAN_POINT('Ctrl Pts',(4.84296663419074,-0.489763405537152,
3.92469457743051));
#32311=CARTESIAN_POINT('Ctrl Pts',(4.86682455222216,-0.393801027275785,
3.69923455818817));
#32312=CARTESIAN_POINT('Ctrl Pts',(4.89068247025357,-0.201543570920867,
3.54731988215497));
#32313=CARTESIAN_POINT('Ctrl Pts',(4.914540388285,0.039996778460842,3.50609782569371));
#32314=CARTESIAN_POINT('Ctrl Pts',(4.93839830631641,0.271756826018508,3.58564830447545));
#32315=CARTESIAN_POINT('Ctrl Pts',(4.96225622434784,0.437064927107334,3.76651905952651));
#32316=CARTESIAN_POINT('Ctrl Pts',(4.98611414237925,0.495498748108838,4.00448226441646));
#32317=CARTESIAN_POINT('Ctrl Pts',(5.00997206041068,0.432769628082826,4.24134943356216));
#32318=CARTESIAN_POINT('Ctrl Pts',(5.03382997844209,0.26421654558258,4.41920009197534));
#32319=CARTESIAN_POINT('Ctrl Pts',(5.05768789647352,0.031055320573195,4.49454490911931));
#32320=CARTESIAN_POINT('Ctrl Pts',(5.08154581450493,-0.209699776246285,
4.44896002485074));
#32321=CARTESIAN_POINT('Ctrl Pts',(5.10540373253635,-0.399177565666329,
4.29359218508065));
#32322=CARTESIAN_POINT('Ctrl Pts',(5.12926165056777,-0.491045566902382,
4.06643305876778));
#32323=CARTESIAN_POINT('Ctrl Pts',(5.15311956859918,-0.462839551218119,
3.823029239986));
#32324=CARTESIAN_POINT('Ctrl Pts',(5.17697748663061,-0.321456657764784,
3.62289959261435));
#32325=CARTESIAN_POINT('Ctrl Pts',(5.20083540466202,-0.101468855184408,
3.51498126685736));
#32326=CARTESIAN_POINT('Ctrl Pts',(5.22469332269345,0.143330846444675,3.52566323299877));
#32327=CARTESIAN_POINT('Ctrl Pts',(5.24855124072486,0.353082251864168,3.6523334593461));
#32328=CARTESIAN_POINT('Ctrl Pts',(5.27240915875629,0.476495428935435,3.86401762512973));
#32329=CARTESIAN_POINT('Ctrl Pts',(5.2962670767877,0.483392494157105,4.10895318565465));
#32330=CARTESIAN_POINT('Ctrl Pts',(5.32012499481913,0.372086927210194,4.32724672446184));
#32331=CARTESIAN_POINT('Ctrl Pts',(5.34398291285054,0.169795971115995,4.46551952511629));
#32332=CARTESIAN_POINT('Ctrl Pts',(5.36784083088196,-0.0740147250654609,
4.48996012138256));
#32333=CARTESIAN_POINT('Ctrl Pts',(5.39169874891337,-0.299726804847767,
4.39459212172504));
#32334=CARTESIAN_POINT('Ctrl Pts',(5.4155566669448,-0.452147516450583,4.20273559983216));
#32335=CARTESIAN_POINT('Ctrl Pts',(5.43941458497621,-0.494005844030112,
3.96130470137348));
#32336=CARTESIAN_POINT('Ctrl Pts',(5.46327250300764,-0.415066286295368,
3.72933585746768));
#32337=CARTESIAN_POINT('Ctrl Pts',(5.48713042103905,-0.234631715382576,
3.56355176915442));
#32338=CARTESIAN_POINT('Ctrl Pts',(5.51098833907048,0.00317670118048804,
3.50449116189365));
#32339=CARTESIAN_POINT('Ctrl Pts',(5.53484625710188,0.240208327774024,3.56659596294035));
#32340=CARTESIAN_POINT('Ctrl Pts',(5.55870417513332,0.418502475082003,3.73467985673571));
#32341=CARTESIAN_POINT('Ctrl Pts',(5.58256209316472,0.494461367456411,3.96764175273735));
#32342=CARTESIAN_POINT('Ctrl Pts',(5.60642001119615,0.449510986625754,4.20851612161082));
#32343=CARTESIAN_POINT('Ctrl Pts',(5.63027792922757,0.294642925140636,4.39840261889448));
#32344=CARTESIAN_POINT('Ctrl Pts',(5.65413584725899,0.0677266425295592,
4.49086882357174));
#32345=CARTESIAN_POINT('Ctrl Pts',(5.6779937652904,-0.17575064898472,4.46330422991997));
#32346=CARTESIAN_POINT('Ctrl Pts',(5.70185168332183,-0.376252119531055,
4.32244913183746));
#32347=CARTESIAN_POINT('Ctrl Pts',(5.72570960135325,-0.48474969783608,4.10274643779879));
#32348=CARTESIAN_POINT('Ctrl Pts',(5.74956751938466,-0.474712770918799,
3.85791944074229));
#32349=CARTESIAN_POINT('Ctrl Pts',(5.77342543741608,-0.348595640189148,
3.64783501103505));
#32350=CARTESIAN_POINT('Ctrl Pts',(5.7972833554475,-0.13723738064616,3.52386451312966));
#32351=CARTESIAN_POINT('Ctrl Pts',(5.82114127347893,0.1076791581852,3.5163221129105));
#32352=CARTESIAN_POINT('Ctrl Pts',(5.84499919151033,0.326265206982528,3.62705212841851));
#32353=CARTESIAN_POINT('Ctrl Pts',(5.86885710954176,0.465070530553655,3.82897806268729));
#32354=CARTESIAN_POINT('Ctrl Pts',(5.89271502757317,0.490153431381492,4.07272350923538));
#32355=CARTESIAN_POINT('Ctrl Pts',(5.9165729456046,0.395380485146506,4.29868609559117));
#32356=CARTESIAN_POINT('Ctrl Pts',(5.94043086363601,0.203926205561759,4.45161176009809));
#32357=CARTESIAN_POINT('Ctrl Pts',(5.96428878166744,-0.0373935204432717,
4.49410611450448));
#32358=CARTESIAN_POINT('Ctrl Pts',(5.98814669969885,-0.26956963613406,4.41577793841189));
#32359=CARTESIAN_POINT('Ctrl Pts',(6.01200461773027,-0.435828398698505,
4.23578096933615));
#32360=CARTESIAN_POINT('Ctrl Pts',(6.0358625357617,-0.495515688199628,3.99812868033461));
#32361=CARTESIAN_POINT('Ctrl Pts',(6.0597204537931,-0.434035059498629,3.76093483037113));
#32362=CARTESIAN_POINT('Ctrl Pts',(6.08357837182454,-0.266422612259865,
3.58219732064663));
#32363=CARTESIAN_POINT('Ctrl Pts',(6.10743628985594,-0.0336596025775484,
3.50562697870369));
#32364=CARTESIAN_POINT('Ctrl Pts',(6.13129420788738,0.207328476491996,3.54993858195554));
#32365=CARTESIAN_POINT('Ctrl Pts',(6.15515212591877,0.397629707835022,3.70431327123879));
#32366=CARTESIAN_POINT('Ctrl Pts',(6.17901004395022,0.490679606253205,3.93097100878581));
#32367=CARTESIAN_POINT('Ctrl Pts',(6.20286796198161,0.463782811036945,4.17454675550933));
#32368=CARTESIAN_POINT('Ctrl Pts',(6.22672588001306,0.323407044622774,4.3753682944706));
#32369=CARTESIAN_POINT('Ctrl Pts',(6.25058379804445,0.104084330837213,4.48453946106473));
#32370=CARTESIAN_POINT('Ctrl Pts',(6.27444171607588,-0.140944443623038,
4.4749681472433));
#32371=CARTESIAN_POINT('Ctrl Pts',(6.29829963410731,-0.351028389709017,
4.349743491311));
#32372=CARTESIAN_POINT('Ctrl Pts',(6.32215755213872,-0.476177279109797,
4.13807688197341));
#32373=CARTESIAN_POINT('Ctrl Pts',(6.34601547017014,-0.483231738207782,
3.89435343878414));
#32374=CARTESIAN_POINT('Ctrl Pts',(6.37782602754537,-0.338784024988664,
3.5998542259592));
#32375=CARTESIAN_POINT('Ctrl Pts',(6.41758922426439,0.0803770223010952,
3.44371490521648));
#32376=CARTESIAN_POINT('Ctrl Pts',(6.46530506032724,0.512014121509362,3.7673575683149));
#32377=CARTESIAN_POINT('Ctrl Pts',(6.51302089639006,0.472271980317209,4.30452828893312));
#32378=CARTESIAN_POINT('Ctrl Pts',(6.56073673245292,-0.000548856210248058,
4.56210751581942));
#32379=CARTESIAN_POINT('Ctrl Pts',(6.60845256851575,-0.473190198344468,
4.30346185287483));
#32380=CARTESIAN_POINT('Ctrl Pts',(6.65616840457859,-0.511122033036262,
3.76615996983968));
#32381=CARTESIAN_POINT('Ctrl Pts',(6.70388424064142,-0.0797735308749388,
3.44358772816382));
#32382=CARTESIAN_POINT('Ctrl Pts',(6.75160007670426,0.424880365184703,3.63198234005898));
#32383=CARTESIAN_POINT('Ctrl Pts',(6.7993159127671,0.539334593204737,4.15833063512042));
#32384=CARTESIAN_POINT('Ctrl Pts',(6.84703174882994,0.158523065679302,4.53928284691909));
#32385=CARTESIAN_POINT('Ctrl Pts',(6.89474758489278,-0.367869781963911,
4.42500259414721));
#32386=CARTESIAN_POINT('Ctrl Pts',(6.94246342095561,-0.556438361909488,
3.92043630538129));
#32387=CARTESIAN_POINT('Ctrl Pts',(6.99017925701846,-0.234023037562683,
3.48893437735136));
#32388=CARTESIAN_POINT('Ctrl Pts',(7.03789509308128,0.303300305128555,3.52675198254107));
#32389=CARTESIAN_POINT('Ctrl Pts',(7.08561092914413,0.562097748282813,3.99916046672433));
#32390=CARTESIAN_POINT('Ctrl Pts',(7.13332676520696,0.304712478085684,4.47233993757656));
#32391=CARTESIAN_POINT('Ctrl Pts',(7.18104260126981,-0.232495107101315,
4.51176235979777));
#32392=CARTESIAN_POINT('Ctrl Pts',(7.22875843733264,-0.556198774489988,
4.08122554105153));
#32393=CARTESIAN_POINT('Ctrl Pts',(7.27647427339549,-0.369136593294786,
3.57609805363465));
#32394=CARTESIAN_POINT('Ctrl Pts',(7.32419010945832,0.156909424853758,3.46024624852207));
#32395=CARTESIAN_POINT('Ctrl Pts',(7.37190594552116,0.538863091386428,3.84005861730642));
#32396=CARTESIAN_POINT('Ctrl Pts',(7.41962178158399,0.425970496197337,4.36674761950234));
#32397=CARTESIAN_POINT('Ctrl Pts',(7.46733761764684,-0.0780973635293338,
4.55664663921719));
#32398=CARTESIAN_POINT('Ctrl Pts',(7.51505345370967,-0.510447210801067,
4.2353684852172));
#32399=CARTESIAN_POINT('Ctrl Pts',(7.56276928977251,-0.474045531130633,
3.69794782953315));
#32400=CARTESIAN_POINT('Ctrl Pts',(7.61048512583535,-0.00232054557778912,
3.43790632971152));
#32401=CARTESIAN_POINT('Ctrl Pts',(7.65820096189818,0.471535432411473,3.69404409621074));
#32402=CARTESIAN_POINT('Ctrl Pts',(7.70591679796103,0.512373167457076,4.23114587691112));
#32403=CARTESIAN_POINT('Ctrl Pts',(7.75363263402387,0.0826907388754792,
4.55598284219971));
#32404=CARTESIAN_POINT('Ctrl Pts',(7.80134847008669,-0.422927867535356,
4.3702522086048));
#32405=CARTESIAN_POINT('Ctrl Pts',(7.84906430614955,-0.540165305628305,
3.84451327478339));
#32406=CARTESIAN_POINT('Ctrl Pts',(7.89678014221237,-0.161360632039799,
3.46156019320034));
#32407=CARTESIAN_POINT('Ctrl Pts',(7.94449597827521,0.365623992797271,3.57306467116217));
#32408=CARTESIAN_POINT('Ctrl Pts',(7.99221181433806,0.556850479203549,4.07663043084052));
#32409=CARTESIAN_POINT('Ctrl Pts',(8.03992765040089,0.236712602309549,4.50982528676712));
#32410=CARTESIAN_POINT('Ctrl Pts',(8.08764348646373,-0.300802099575971,
4.47483973718518));
#32411=CARTESIAN_POINT('Ctrl Pts',(8.13535932252656,-0.562085604986122,
4.00380155059756));
#32412=CARTESIAN_POINT('Ctrl Pts',(8.18307515858941,-0.307197250538534,
3.52927234160183));
#32413=CARTESIAN_POINT('Ctrl Pts',(8.23079099465223,0.229795065915734,3.48701958438918));
#32414=CARTESIAN_POINT('Ctrl Pts',(8.27850683071509,0.555763037488074,3.91584463605021));
#32415=CARTESIAN_POINT('Ctrl Pts',(8.32622266677791,0.371365260221553,4.42195085332305));
#32416=CARTESIAN_POINT('Ctrl Pts',(8.37393850284076,-0.154062949695418,
4.54057310944092));
#32417=CARTESIAN_POINT('Ctrl Pts',(8.4216543389036,-0.538012782343907,4.16277876137275));
#32418=CARTESIAN_POINT('Ctrl Pts',(8.46937017496643,-0.427897198575242,
3.6355021720628));
#32419=CARTESIAN_POINT('Ctrl Pts',(8.51708601102927,0.0751629666897603,
3.44294954666756));
#32420=CARTESIAN_POINT('Ctrl Pts',(8.56480184709211,0.50919982311266,3.76194492389047));
#32421=CARTESIAN_POINT('Ctrl Pts',(8.61251768315494,0.475630646924824,4.29954994045293));
#32422=CARTESIAN_POINT('Ctrl Pts',(8.66023351921779,0.00528252914771292,
4.56207363752918));
#32423=CARTESIAN_POINT('Ctrl Pts',(8.70794935528062,-0.469916616427902,
4.30843646464781));
#32424=CARTESIAN_POINT('Ctrl Pts',(8.75566519134346,-0.513584102541225,
3.7715573403753));
#32425=CARTESIAN_POINT('Ctrl Pts',(8.8033810274063,-0.0856194047837525,
3.44446062547832));
#32426=CARTESIAN_POINT('Ctrl Pts',(8.85109686346913,0.420970909810523,3.6275242662766));
#32427=CARTESIAN_POINT('Ctrl Pts',(8.89881269953199,0.540977160455745,4.15263810462895));
#32428=CARTESIAN_POINT('Ctrl Pts',(8.9465285355948,0.1641957606509,4.5375820228614));
#32429=CARTESIAN_POINT('Ctrl Pts',(8.99424437165766,-0.363369132636193,
4.42885609773758));
#32430=CARTESIAN_POINT('Ctrl Pts',(9.04196020772048,-0.557246560270691,
3.92630501926208));
#32431=CARTESIAN_POINT('Ctrl Pts',(9.08967604378333,-0.239395897268157,
3.49142917554125));
#32432=CARTESIAN_POINT('Ctrl Pts',(9.13739187984617,0.298295701775085,3.52358174528888));
#32433=CARTESIAN_POINT('Ctrl Pts',(9.18510771590899,0.562057768008922,3.99323652897485));
#32434=CARTESIAN_POINT('Ctrl Pts',(9.23282355197185,0.309673537509763,4.46910231217259));
#32435=CARTESIAN_POINT('Ctrl Pts',(9.28053938803466,-0.227088667424462,
4.51418422403538));
#32436=CARTESIAN_POINT('Ctrl Pts',(9.32825522409753,-0.555311854854516,
4.08708285122523));
#32437=CARTESIAN_POINT('Ctrl Pts',(9.37597106016035,-0.373583621400482,
3.58001195619306));
#32438=CARTESIAN_POINT('Ctrl Pts',(9.4236868962232,0.151212199908504,3.45862254413551));
#32439=CARTESIAN_POINT('Ctrl Pts',(9.47140273228603,0.537147531342748,3.83438837996121));
#32440=CARTESIAN_POINT('Ctrl Pts',(9.51911856834887,0.429812019667804,4.36223791473086));
#32441=CARTESIAN_POINT('Ctrl Pts',(9.5668344044117,-0.0722264831760907,
4.5574387986564));
#32442=CARTESIAN_POINT('Ctrl Pts',(9.61455024047456,-0.507938295172089,
4.24073505647735));
#32443=CARTESIAN_POINT('Ctrl Pts',(9.66226607653738,-0.477202555076283,
3.70296060775017));
#32444=CARTESIAN_POINT('Ctrl Pts',(9.70998191260023,-0.00824436594879979,
3.43796200346455));
#32445=CARTESIAN_POINT('Ctrl Pts',(9.75769774866306,0.46828475128534,3.68909153946361));
#32446=CARTESIAN_POINT('Ctrl Pts',(9.80541358472589,0.514780775927077,4.22573309871483));
#32447=CARTESIAN_POINT('Ctrl Pts',(9.85312942078874,0.0885456931146035,
4.55508048006603));
#32448=CARTESIAN_POINT('Ctrl Pts',(9.90084525685159,-0.419002262135622,
4.37468891556157));
#32449=CARTESIAN_POINT('Ctrl Pts',(9.9485610929144,-0.541773992888202,3.8502147545669));
#32450=CARTESIAN_POINT('Ctrl Pts',(9.99627692897727,-0.167026329707142,
3.46329068919569));
#32451=CARTESIAN_POINT('Ctrl Pts',(10.0439927650401,0.361104182074418,3.56923504227033));
#32452=CARTESIAN_POINT('Ctrl Pts',(10.0917086011029,0.557627167155001,4.07075748419897));
#32453=CARTESIAN_POINT('Ctrl Pts',(10.1394244371657,0.242072544440304,4.50730223964386));
#32454=CARTESIAN_POINT('Ctrl Pts',(10.1871402732286,-0.295781020598791,
4.47798354257549));
#32455=CARTESIAN_POINT('Ctrl Pts',(10.2348561092914,-0.56201432324602,4.00972520363789));
#32456=CARTESIAN_POINT('Ctrl Pts',(10.2825719453543,-0.312141225154507,
3.53253606055812));
#32457=CARTESIAN_POINT('Ctrl Pts',(10.3302877814171,0.224375962906492,3.48462624592509));
#32458=CARTESIAN_POINT('Ctrl Pts',(10.37800361748,0.554845251762499,3.90999207970357));
#32459=CARTESIAN_POINT('Ctrl Pts',(10.4257194535428,0.375791608533427,4.41801357164013));
#32460=CARTESIAN_POINT('Ctrl Pts',(10.4734352896056,-0.148357251109035,
4.54216676877402));
#32461=CARTESIAN_POINT('Ctrl Pts',(10.5211511256685,-0.536267364288337,
4.16843987983467));
#32462=CARTESIAN_POINT('Ctrl Pts',(10.5688669617313,-0.431714905307627,
3.64003205746247));
#32463=CARTESIAN_POINT('Ctrl Pts',(10.6165827977942,0.0692879940047382,
3.44218833554121));
#32464=CARTESIAN_POINT('Ctrl Pts',(10.664298633857,0.50666266228973,3.75659164812817));
#32465=CARTESIAN_POINT('Ctrl Pts',(10.7120144699198,0.478761211786921,4.29452059555793));
#32466=CARTESIAN_POINT('Ctrl Pts',(10.7597303059827,0.0112059738120427,
4.56198674830498));
#32467=CARTESIAN_POINT('Ctrl Pts',(10.8074461420455,-0.466639882340508,
4.31337182280594));
#32468=CARTESIAN_POINT('Ctrl Pts',(10.8551619781083,-0.515963154362253,
3.77698273057893));
#32469=CARTESIAN_POINT('Ctrl Pts',(10.9028778141712,-0.0914695226195351,
3.44539382842306));
#32470=CARTESIAN_POINT('Ctrl Pts',(10.950593650234,0.417021979184216,3.62310830733915));
#32471=CARTESIAN_POINT('Ctrl Pts',(10.9983094862969,0.542555780795161,4.14692822684982));
#32472=CARTESIAN_POINT('Ctrl Pts',(11.0460253223597,0.169852260608159,4.53582169486292));
#32473=CARTESIAN_POINT('Ctrl Pts',(11.0937411584225,-0.358829204008283,
4.43266185580689));
#32474=CARTESIAN_POINT('Ctrl Pts',(11.1414569944853,-0.55799228928692,3.93218197720501));
#32475=CARTESIAN_POINT('Ctrl Pts',(11.1891728305482,-0.244742469498405,
3.49398043245019));
#32476=CARTESIAN_POINT('Ctrl Pts',(11.236888666611,0.293258125877444,3.5204644426882));
#32477=CARTESIAN_POINT('Ctrl Pts',(11.2846045026739,0.561955271903759,3.98731333380864));
#32478=CARTESIAN_POINT('Ctrl Pts',(11.3323203387367,0.314600244947554,4.46581258570203));
#32479=CARTESIAN_POINT('Ctrl Pts',(11.3800361747996,-0.221657027690976,
4.51654897269734));
#32480=CARTESIAN_POINT('Ctrl Pts',(11.4277520108624,-0.554363241169119,
4.0929304899371));
#32481=CARTESIAN_POINT('Ctrl Pts',(11.4754678469252,-0.377989160306769,
3.58397250834823));
#32482=CARTESIAN_POINT('Ctrl Pts',(11.5231836829881,0.145498182576105,3.45705897374896));
#32483=CARTESIAN_POINT('Ctrl Pts',(11.5708995190509,0.535372305622036,3.82873653777755));
#32484=CARTESIAN_POINT('Ctrl Pts',(11.6186153551137,0.43360580265347,4.35768797439208));
#32485=CARTESIAN_POINT('Ctrl Pts',(11.6663311911766,-0.0663475807746441,
4.55816904038548));
#32486=CARTESIAN_POINT('Ctrl Pts',(11.7140470272394,-0.505372959888646,
4.24607488805821));
#32487=CARTESIAN_POINT('Ctrl Pts',(11.7617628633023,-0.480306573774387,
3.70800637967828));
#32488=CARTESIAN_POINT('Ctrl Pts',(11.8094786993651,-0.0141672704965164,
3.43808010573911));
#32489=CARTESIAN_POINT('Ctrl Pts',(11.8571945354279,0.464982055269784,3.68417351694868));
#32490=CARTESIAN_POINT('Ctrl Pts',(11.9049103714908,0.517131205013274,4.22029524715934));
#32491=CARTESIAN_POINT('Ctrl Pts',(11.9526262075536,0.0943908121067024,
4.55411646222552));
#32492=CARTESIAN_POINT('Ctrl Pts',(12.0003420436165,-0.415030115946784,
4.37908400385228));
#32493=CARTESIAN_POINT('Ctrl Pts',(12.0480578796793,-0.543322502467158,
3.85593287178435));
#32494=CARTESIAN_POINT('Ctrl Pts',(12.0957737157421,-0.172673474880652,
3.46508080031456));
#32495=CARTESIAN_POINT('Ctrl Pts',(12.143489551805,0.356544261611682,3.56545326070575));
#32496=CARTESIAN_POINT('Ctrl Pts',(12.1912053878678,0.558341916527368,4.06487667815191));
#32497=CARTESIAN_POINT('Ctrl Pts',(12.2389212239306,0.247405598301292,4.50472284379514));
#32498=CARTESIAN_POINT('Ctrl Pts',(12.2866370599935,-0.290727087669313,
4.48107425582212));
#32499=CARTESIAN_POINT('Ctrl Pts',(12.3343528960563,-0.56188061562194,4.01564777644873));
#32500=CARTESIAN_POINT('Ctrl Pts',(12.3820687321191,-0.317050528604376,
3.5358517031905));
#32501=CARTESIAN_POINT('Ctrl Pts',(12.429784568182,0.218931937280033,3.48229015273196));
#32502=CARTESIAN_POINT('Ctrl Pts',(12.4775004042448,0.553865836459325,3.90414952100961));
#32503=CARTESIAN_POINT('Ctrl Pts',(12.5252162403077,0.380176215696692,4.4140298589933));
#32504=CARTESIAN_POINT('Ctrl Pts',(12.5729320763705,-0.142635073703209,
4.54370020679522));
#32505=CARTESIAN_POINT('Ctrl Pts',(12.6206479124333,-0.53446238019874,4.17408228879405));
#32506=CARTESIAN_POINT('Ctrl Pts',(12.6683637484962,-0.435484659196984,
3.644601926393));
#32507=CARTESIAN_POINT('Ctrl Pts',(12.716079584559,0.0634053251381518,3.44148908348752));
#32508=CARTESIAN_POINT('Ctrl Pts',(12.7637954206219,0.504069223782589,3.75126540901054));
#32509=CARTESIAN_POINT('Ctrl Pts',(12.8115112566847,0.481838598125516,4.2894585367128));
#32510=CARTESIAN_POINT('Ctrl Pts',(12.8592270927475,0.0171281737699642,
4.56183743625962));
#32511=CARTESIAN_POINT('Ctrl Pts',(12.9069429288104,-0.463311316109371,
4.31827237310907));
#32512=CARTESIAN_POINT('Ctrl Pts',(12.9546587648732,-0.518284895444539,
3.78243289248252));
#32513=CARTESIAN_POINT('Ctrl Pts',(13.0023746009361,-0.0973094804548018,
3.44638863438952));
#32514=CARTESIAN_POINT('Ctrl Pts',(13.0500904369989,0.413026727735397,3.61873421174243));
#32515=CARTESIAN_POINT('Ctrl Pts',(13.0978062730617,0.544074136613086,4.14120202898048));
#32516=CARTESIAN_POINT('Ctrl Pts',(13.1455221091246,0.17548989418231,4.53400185033327));
#32517=CARTESIAN_POINT('Ctrl Pts',(13.1932379451874,-0.354249418335187,
4.4364195558504));
#32518=CARTESIAN_POINT('Ctrl Pts',(13.2409537812502,-0.558676039167545,
3.93806646805208));
#32519=CARTESIAN_POINT('Ctrl Pts',(13.2886696173131,-0.250061856896528,
3.49658789561142));
#32520=CARTESIAN_POINT('Ctrl Pts',(13.3363854533759,0.288187976258808,3.51740040462167));
#32521=CARTESIAN_POINT('Ctrl Pts',(13.3841012894388,0.56179035647369,3.9813915478171));
#32522=CARTESIAN_POINT('Ctrl Pts',(13.4318171255016,0.319492008083037,4.46247111897993));
#32523=CARTESIAN_POINT('Ctrl Pts',(13.4795329615644,-0.21620076734671,4.51885634555065));
#32524=CARTESIAN_POINT('Ctrl Pts',(13.5272487976273,-0.553353051445561,
4.09876780637113));
#32525=CARTESIAN_POINT('Ctrl Pts',(13.5749646336901,-0.382352713970831,
3.58797927086295));
#32526=CARTESIAN_POINT('Ctrl Pts',(13.6226804697529,0.139768003996038,3.45555571067516));
#32527=CARTESIAN_POINT('Ctrl Pts',(13.6703963058158,0.53353761328617,3.82310371872654));
#32528=CARTESIAN_POINT('Ctrl Pts',(13.7181121418786,0.437351422764197,4.35309830377052));
#32529=CARTESIAN_POINT('Ctrl Pts',(13.7658279779415,-0.0604613087987784,
4.55883728334624));
#32530=CARTESIAN_POINT('Ctrl Pts',(13.8135438140043,-0.502751490175015,
4.25138738680826));
#32531=CARTESIAN_POINT('Ctrl Pts',(13.8612596500671,-0.483357242297515,
3.71308458487209));
#32532=CARTESIAN_POINT('Ctrl Pts',(13.90897548613,-0.0200886014110514,3.43826062340902));
#32533=CARTESIAN_POINT('Ctrl Pts',(13.9566913221928,0.461627711254046,3.67929057494076));
#32534=CARTESIAN_POINT('Ctrl Pts',(14.0044071582557,0.519424193619207,4.21483292625321));
#32535=CARTESIAN_POINT('Ctrl Pts',(14.0521229943185,0.100225446615308,4.55309089575788));
#32536=CARTESIAN_POINT('Ctrl Pts',(14.0998388303813,-0.411011870182152,
4.38343698529073));
#32537=CARTESIAN_POINT('Ctrl Pts',(14.1475546664441,-0.544810662360815,
3.86166699129474));
#32538=CARTESIAN_POINT('Ctrl Pts',(14.195270502507,-0.178301440303968,3.46693032771971));
#32539=CARTESIAN_POINT('Ctrl Pts',(14.2429863385698,0.351944737904315,3.5617197465309));
#32540=CARTESIAN_POINT('Ctrl Pts',(14.2907021746327,0.558994647929194,4.05898866591129));
#32541=CARTESIAN_POINT('Ctrl Pts',(14.3384180106955,0.252711171522458,4.50208738572805));
#32542=CARTESIAN_POINT('Ctrl Pts',(14.3861338467583,-0.28564086215454,4.48411153362329));
#32543=CARTESIAN_POINT('Ctrl Pts',(14.4338496828212,-0.561684496965419,
4.02156861117883));
#32544=CARTESIAN_POINT('Ctrl Pts',(14.481565518884,-0.321924615586062,3.53921890121312));
#32545=CARTESIAN_POINT('Ctrl Pts',(14.5292813549469,0.213463593732893,3.48001156429194));
#32546=CARTESIAN_POINT('Ctrl Pts',(14.5769971910097,0.552824900367352,3.89831760893199));
#32547=CARTESIAN_POINT('Ctrl Pts',(14.6247130270725,0.384518594689996,4.4100001578745));
#32548=CARTESIAN_POINT('Ctrl Pts',(14.6724288631354,-0.136897053070264,
4.54517325317752));
#32549=CARTESIAN_POINT('Ctrl Pts',(14.7201446991982,-0.532598030564186,
4.17970536151887));
#32550=CARTESIAN_POINT('Ctrl Pts',(14.7678605352611,-0.439206041516937,
3.64921127125505));
#32551=CARTESIAN_POINT('Ctrl Pts',(14.8155763713239,0.0575156135089261,
3.44085186817608));
#32552=CARTESIAN_POINT('Ctrl Pts',(14.8632922073868,0.501419795658073,3.74596679815093));
#32553=CARTESIAN_POINT('Ctrl Pts',(14.9110080434496,0.484862464119148,4.284364326187));
#32554=CARTESIAN_POINT('Ctrl Pts',(14.9587238795124,0.0230484712116303,
4.56162571797798));
#32555=CARTESIAN_POINT('Ctrl Pts',(15.0064397155752,-0.459931287455839,
4.32313757122732));
#32556=CARTESIAN_POINT('Ctrl Pts',(15.0541555516381,-0.5205490679001,3.78790722070797));
#32557=CARTESIAN_POINT('Ctrl Pts',(15.1018713877009,-0.103138629614742,
3.44744493287938));
#32558=CARTESIAN_POINT('Ctrl Pts',(15.1495872237638,0.40898559923764,3.61440246534021));
#32559=CARTESIAN_POINT('Ctrl Pts',(15.1973030598266,0.545532059257757,4.13546014705983));
#32560=CARTESIAN_POINT('Ctrl Pts',(15.2450188958894,0.181108035171788,4.53212269141213));
#32561=CARTESIAN_POINT('Ctrl Pts',(15.2927347319523,-0.349630284317748,
4.44012878048063));
#32562=CARTESIAN_POINT('Ctrl Pts',(15.3404505680151,-0.559297733964875,
3.94395783818199));
#32563=CARTESIAN_POINT('Ctrl Pts',(15.3881664040779,-0.255353468610234,
3.49925127540033));
#32564=CARTESIAN_POINT('Ctrl Pts',(15.4358822401408,0.283085816087337,3.51438997142805));
#32565=CARTESIAN_POINT('Ctrl Pts',(15.4835980762036,0.561563040036739,3.97547182876414));
#32566=CARTESIAN_POINT('Ctrl Pts',(15.5313139122665,0.324348283562367,4.45907828316053));
#32567=CARTESIAN_POINT('Ctrl Pts',(15.5790297483293,-0.210720492447169,
4.52110608630326));
#32568=CARTESIAN_POINT('Ctrl Pts',(15.6267455843921,-0.552281397890927,
4.10459415214592));
#32569=CARTESIAN_POINT('Ctrl Pts',(15.674461420455,-0.386673797709831,3.59203179868507));
#32570=CARTESIAN_POINT('Ctrl Pts',(15.7221772565178,0.134022300649356,3.45411292188939));
#32571=CARTESIAN_POINT('Ctrl Pts',(15.7698930925807,0.531643658124066,3.81749054847505));
#32572=CARTESIAN_POINT('Ctrl Pts',(15.8176089286435,0.441048463954279,4.34846941266494));
#32573=CARTESIAN_POINT('Ctrl Pts',(15.8653247647064,-0.054568321067637,
4.5594434533135));
#32574=CARTESIAN_POINT('Ctrl Pts',(15.9130406007692,-0.500074177211609,
4.25667196264028));
#32575=CARTESIAN_POINT('Ctrl Pts',(15.960756436832,-0.486354221791887,3.71819465926869));
#32576=CARTESIAN_POINT('Ctrl Pts',(16.0084722728949,-0.0260077009790528,
3.4385035364232));
#32577=CARTESIAN_POINT('Ctrl Pts',(16.0561881089577,0.458222091822753,3.6744432558139));
#32578=CARTESIAN_POINT('Ctrl Pts',(16.1039039450206,0.52165948705058,4.2093467427251));
#32579=CARTESIAN_POINT('Ctrl Pts',(16.1516197810833,0.106048948556897,4.55200389457816));
#32580=CARTESIAN_POINT('Ctrl Pts',(16.1993356171462,-0.406947971169398,
4.38774737636841));
#32581=CARTESIAN_POINT('Ctrl Pts',(16.247051453209,-0.546238307271431,3.86741647617928));
#32582=CARTESIAN_POINT('Ctrl Pts',(16.2947672892719,-0.183909600849411,
3.46883906597446));
#32583=CARTESIAN_POINT('Ctrl Pts',(16.3424831253347,0.347306121845567,3.55803491444678));
#32584=CARTESIAN_POINT('Ctrl Pts',(16.3901989613975,0.559585288858183,4.05309410148958));
#32585=CARTESIAN_POINT('Ctrl Pts',(16.4379147974604,0.257988674785898,4.49939615817675));
#32586=CARTESIAN_POINT('Ctrl Pts',(16.4856306335232,-0.280522909008289,
4.4870950386126));
#32587=CARTESIAN_POINT('Ctrl Pts',(16.5333464695861,-0.561425989060384,
4.02748705016995));
#32588=CARTESIAN_POINT('Ctrl Pts',(16.5810623056489,-0.326762944709103,
3.54263728061361));
#32589=CARTESIAN_POINT('Ctrl Pts',(16.6287781417117,0.207971539662738,3.4777907336998));
#32590=CARTESIAN_POINT('Ctrl Pts',(16.6764939777746,0.551722559108811,3.89249699125187));
#32591=CARTESIAN_POINT('Ctrl Pts',(16.7242098138374,0.388818263182495,4.40592491588375));
#32592=CARTESIAN_POINT('Ctrl Pts',(16.7719256499003,-0.131143826562283,
4.54658574430191));
#32593=CARTESIAN_POINT('Ctrl Pts',(16.8196414859631,-0.53067452246778,4.18530847342493));
#32594=CARTESIAN_POINT('Ctrl Pts',(16.8673573220259,-0.442878638914007,
3.65385958006445));
#32595=CARTESIAN_POINT('Ctrl Pts',(16.9150731580888,0.0516195133182915,
3.44027676038576));
#32596=CARTESIAN_POINT('Ctrl Pts',(16.9627889941516,0.498714672202087,3.74069640409388));
#32597=CARTESIAN_POINT('Ctrl Pts',(17.0105048302145,0.487832473891125,4.27923852982128));
#32598=CARTESIAN_POINT('Ctrl Pts',(17.0582206662773,0.0289662085384809,
4.56135161697672));
#32599=CARTESIAN_POINT('Ctrl Pts',(17.1059365023401,-0.456500171817451,
4.32796687675757));
#32600=CARTESIAN_POINT('Ctrl Pts',(17.1536523384029,-0.522755420235406,
3.79340510719289));
#32601=CARTESIAN_POINT('Ctrl Pts',(17.2013681744658,-0.108956322625149,
3.44856260656401));
#32602=CARTESIAN_POINT('Ctrl Pts',(17.2490840105286,0.404899042560309,3.61011354928233));
#32603=CARTESIAN_POINT('Ctrl Pts',(17.2967998465915,0.54692938679005,4.12970321886885));
#32604=CARTESIAN_POINT('Ctrl Pts',(17.3445156826543,0.186706059540143,4.53018442682757));
#32605=CARTESIAN_POINT('Ctrl Pts',(17.3922315187172,-0.344972315027459,
4.4437891176945));
#32606=CARTESIAN_POINT('Ctrl Pts',(17.43994735478,-0.559857304624004,3.94985543320929));
#32607=CARTESIAN_POINT('Ctrl Pts',(17.4876631908428,-0.260616716872392,
3.5019702759813));
#32608=CARTESIAN_POINT('Ctrl Pts',(17.5353790269057,0.277952212086773,3.51143347749201));
#32609=CARTESIAN_POINT('Ctrl Pts',(17.5830948629685,0.561273347842132,3.96955483418404));
#32610=CARTESIAN_POINT('Ctrl Pts',(17.6308106990313,0.329168531973526,4.45563445510394));
#32611=CARTESIAN_POINT('Ctrl Pts',(17.6785265350942,-0.205216811715269,
4.52329794506467));
#32612=CARTESIAN_POINT('Ctrl Pts',(17.726242371157,-0.551148399539408,4.11040888009862));
#32613=CARTESIAN_POINT('Ctrl Pts',(17.7739582072198,-0.390951931558304,
3.59612964167903));
#32614=CARTESIAN_POINT('Ctrl Pts',(17.8216740432827,0.128261710741471,3.45273076764982));
#32615=CARTESIAN_POINT('Ctrl Pts',(17.8693898793456,0.529690650507269,3.81189765050732));
#32616=CARTESIAN_POINT('Ctrl Pts',(17.9171057154083,0.44469651557395,4.34380181523062));
#32617=CARTESIAN_POINT('Ctrl Pts',(17.9648215514712,-0.0486692721463468,
4.55998748295674));
#32618=CARTESIAN_POINT('Ctrl Pts',(18.012537387534,-0.497341318381634,4.26192802856871));
#32619=CARTESIAN_POINT('Ctrl Pts',(18.0602532235969,-0.489297179367249,
3.72333603526529));
#32620=CARTESIAN_POINT('Ctrl Pts',(18.1079690596597,-0.0319239117350811,
3.43880881780002));
#32621=CARTESIAN_POINT('Ctrl Pts',(18.1556848957225,0.454765575255941,3.66963209798526));
#32622=CARTESIAN_POINT('Ctrl Pts',(18.2034007317854,0.523836837021606,4.20383730595423));
#32623=CARTESIAN_POINT('Ctrl Pts',(18.2511165678483,0.111860671084556,4.5508555794253));
#32624=CARTESIAN_POINT('Ctrl Pts',(18.298832403911,-0.402838870307115,4.39201469830757));
#32625=CARTESIAN_POINT('Ctrl Pts',(18.346548239974,-0.547605278623001,3.87318068781251));
#32626=CARTESIAN_POINT('Ctrl Pts',(18.3942640760367,-0.189497333589109,
3.47080680306518));
#32627=CARTESIAN_POINT('Ctrl Pts',(18.4419799120997,0.342628928670919,3.55439917374707));
#32628=CARTESIAN_POINT('Ctrl Pts',(18.4896957481624,0.560113773708727,4.04719363962704));
#32629=CARTESIAN_POINT('Ctrl Pts',(18.5374115842253,0.263237521891608,4.49664946007004));
#32630=CARTESIAN_POINT('Ctrl Pts',(18.5851274202881,-0.275373796708506,
4.49002443939646));
#32631=CARTESIAN_POINT('Ctrl Pts',(18.632843256351,-0.561105120620647,4.03340243603));
#32632=CARTESIAN_POINT('Ctrl Pts',(18.6805590924138,-0.331564978554912,
3.54610646169455));
#32633=CARTESIAN_POINT('Ctrl Pts',(18.7282749284766,0.202456385100939,3.47562790763498));
#32634=CARTESIAN_POINT('Ctrl Pts',(18.7759907645394,0.550558935126376,3.8866883144956));
#32635=CARTESIAN_POINT('Ctrl Pts',(18.8237066006023,0.393074743587739,4.40180458567998));
#32636=CARTESIAN_POINT('Ctrl Pts',(18.8714224366651,-0.125376033221007,
4.54793752327491));
#32637=CARTESIAN_POINT('Ctrl Pts',(18.919138272728,-0.528692069562509,4.19089100214638));
#32638=CARTESIAN_POINT('Ctrl Pts',(18.9668541087908,-0.4465020434557,3.6585463365067));
#32639=CARTESIAN_POINT('Ctrl Pts',(19.0145699448537,0.0457176794812401,
3.43976382400136));
#32640=CARTESIAN_POINT('Ctrl Pts',(19.0622857809165,0.495954153879041,3.73545481224116));
#32641=CARTESIAN_POINT('Ctrl Pts',(19.1100016169793,0.490748297561716,4.27408171698104));
#32642=CARTESIAN_POINT('Ctrl Pts',(19.1577174530421,0.0348807284082936,
4.5610151636709));
#32643=CARTESIAN_POINT('Ctrl Pts',(19.205433289105,-0.453018350253257,4.33275975334162));
#32644=CARTESIAN_POINT('Ctrl Pts',(19.2531491251678,-0.524903707479367,
3.79892594114836));
#32645=CARTESIAN_POINT('Ctrl Pts',(19.3008649612307,-0.11476191309534,3.44974153150476));
#32646=CARTESIAN_POINT('Ctrl Pts',(19.3485807972935,0.400767511262006,3.60586793956989));
#32647=CARTESIAN_POINT('Ctrl Pts',(19.3962966333564,0.548265964675035,4.12393188459875));
#32648=CARTESIAN_POINT('Ctrl Pts',(19.4440124694192,0.192283344213529,4.52818727047755));
#32649=CARTESIAN_POINT('Ctrl Pts',(19.491728305482,-0.340276025447905,4.44740016355363));
#32650=CARTESIAN_POINT('Ctrl Pts',(19.5394441415448,-0.560354693525076,
3.95575859308266));
#32651=CARTESIAN_POINT('Ctrl Pts',(19.5871599776077,-0.265851008504119,
3.50474460473346));
#32652=CARTESIAN_POINT('Ctrl Pts',(19.6348758136705,0.272787718306182,3.5085312334714));
#32653=CARTESIAN_POINT('Ctrl Pts',(19.6825916497334,0.560921342594646,3.96364125479661));
#32654=CARTESIAN_POINT('Ctrl Pts',(19.7303074857962,0.33395216026474,4.45213995410186));
#32655=CARTESIAN_POINT('Ctrl Pts',(19.7780233218591,-0.199690227635008,
4.52543179776919));
#32656=CARTESIAN_POINT('Ctrl Pts',(19.8257391579219,-0.549954387748789,
4.11621111891367));
#32657=CARTESIAN_POINT('Ctrl Pts',(19.8734549939848,-0.395186252277308,
3.60027277035845));
#32658=CARTESIAN_POINT('Ctrl Pts',(19.9211708300475,0.122486141425193,3.45140859770427));
#32659=CARTESIAN_POINT('Ctrl Pts',(19.9688866661104,0.527680190865048,3.80632716374734));
#32660=CARTESIAN_POINT('Ctrl Pts',(20.0166025021732,0.448292560087992,4.33909316421112));
#32661=CARTESIAN_POINT('Ctrl Pts',(20.0643183382361,-0.0427598846646947,
4.56047472290141));
#32662=CARTESIAN_POINT('Ctrl Pts',(20.1120341742989,-0.49456253103916,4.26714478353561));
#32663=CARTESIAN_POINT('Ctrl Pts',(20.1597500103618,-0.492168201513856,
3.72852743457374));
#32664=CARTESIAN_POINT('Ctrl Pts',(20.2074658464246,-0.0378697858522375,
3.43914000028616));
#32665=CARTESIAN_POINT('Ctrl Pts',(20.2551816824874,0.451321269441671,3.66492646727415));
#32666=CARTESIAN_POINT('Ctrl Pts',(20.3028975185503,0.52583741886325,4.1981749506787));
#32667=CARTESIAN_POINT('Ctrl Pts',(20.3506133546131,0.117885080656874,4.54989459844945));
#32668=CARTESIAN_POINT('Ctrl Pts',(20.398329190676,-0.399119892637424,4.39574851066478));
#32669=CARTESIAN_POINT('Ctrl Pts',(20.438092387395,-0.523197416260526,3.96600412247733));
#32670=CARTESIAN_POINT('Ctrl Pts',(20.4699029447702,-0.3725623900923,3.67462118354637));
#32671=CARTESIAN_POINT('Ctrl Pts',(20.4937608628016,-0.172533290246804,
3.53519650363565));
#32672=CARTESIAN_POINT('Ctrl Pts',(20.5176187808331,0.0720421502968434,
3.50974356844941));
#32673=CARTESIAN_POINT('Ctrl Pts',(20.5414766988645,0.297725647320748,3.60399556061657));
#32674=CARTESIAN_POINT('Ctrl Pts',(20.5653346168959,0.451286063531533,3.79517586539437));
#32675=CARTESIAN_POINT('Ctrl Pts',(20.5891925349273,0.494134760388362,4.03639109206021));
#32676=CARTESIAN_POINT('Ctrl Pts',(20.6130504529587,0.416344747430809,4.26873428690612));
#32677=CARTESIAN_POINT('Ctrl Pts',(20.6369083709901,0.23664610161733,4.43535054865035));
#32678=CARTESIAN_POINT('Ctrl Pts',(20.6607662890216,-0.000865470816140784,
4.49551919950567));
#32679=CARTESIAN_POINT('Ctrl Pts',(20.684624207053,-0.238193741375527,4.43451595913869));
#32680=CARTESIAN_POINT('Ctrl Pts',(20.7084821250844,-0.417262150572256,
4.26726382233879));
#32681=CARTESIAN_POINT('Ctrl Pts',(20.7323400431158,-0.494306543785295,
4.03465729316116));
#32682=CARTESIAN_POINT('Ctrl Pts',(20.7561979611472,-0.45047531426282,3.79357669839993));
#32683=CARTESIAN_POINT('Ctrl Pts',(20.7800558791787,-0.296492828349621,
3.60297191305088));
#32684=CARTESIAN_POINT('Ctrl Pts',(20.80391379721,-0.0700085893017688,3.50945147432983));
#32685=CARTESIAN_POINT('Ctrl Pts',(20.8277717152415,0.173594031734132,3.53588342526713));
#32686=CARTESIAN_POINT('Ctrl Pts',(20.8516296332729,0.374748514455718,3.6758045671588));
#32687=CARTESIAN_POINT('Ctrl Pts',(20.8754875513043,0.484266602122282,3.89500029884494));
#32688=CARTESIAN_POINT('Ctrl Pts',(20.8993454693358,0.475368407265908,4.13987133054223));
#32689=CARTESIAN_POINT('Ctrl Pts',(20.9232033873671,0.350229638882089,4.35054000504804));
#32690=CARTESIAN_POINT('Ctrl Pts',(20.9470613053986,0.139450209771325,4.47549210343221));
#32691=CARTESIAN_POINT('Ctrl Pts',(20.97091922343,-0.105428607968738,4.48417342845956));
#32692=CARTESIAN_POINT('Ctrl Pts',(20.9947771414615,-0.324527251938122,
4.37446116262749));
#32693=CARTESIAN_POINT('Ctrl Pts',(21.0186350594928,-0.464270146732381,
4.17318294187641));
#32694=CARTESIAN_POINT('Ctrl Pts',(21.0424929775243,-0.490486342136868,
3.92955677471355));
#32695=CARTESIAN_POINT('Ctrl Pts',(21.0663508955557,-0.396765267394252,
3.7031558948169));
#32696=CARTESIAN_POINT('Ctrl Pts',(21.0902088135871,-0.206024276530194,
3.54934148458869));
#32697=CARTESIAN_POINT('Ctrl Pts',(21.1140667316185,0.0350952616297792,
3.50572535702762));
#32698=CARTESIAN_POINT('Ctrl Pts',(21.1379246496499,0.267633052506714,3.58297284346672));
#32699=CARTESIAN_POINT('Ctrl Pts',(21.1617825676814,0.434727271782411,3.76219482925797));
#32700=CARTESIAN_POINT('Ctrl Pts',(21.1856404857128,0.495518831419392,3.99956665698474));
#32701=CARTESIAN_POINT('Ctrl Pts',(21.2094984037442,0.43514253908843,4.23704444887943));
#32702=CARTESIAN_POINT('Ctrl Pts',(21.2333563217756,0.268362042918248,4.41655841606373));
#32703=CARTESIAN_POINT('Ctrl Pts',(21.257214239807,0.0359597172125542,4.49421250369607));
#32704=CARTESIAN_POINT('Ctrl Pts',(21.2810721578384,-0.205235738871087,
4.45101817209691));
#32705=CARTESIAN_POINT('Ctrl Pts',(21.3049300758699,-0.396245466293343,
4.29753761193144));
#32706=CARTESIAN_POINT('Ctrl Pts',(21.3287879939013,-0.490362383696085,
4.07130100088706));
#32707=CARTESIAN_POINT('Ctrl Pts',(21.3526459119327,-0.464572341082516,
3.82762935292545));
#32708=CARTESIAN_POINT('Ctrl Pts',(21.3765038299641,-0.325181706377507,
3.62610702345576));
#32709=CARTESIAN_POINT('Ctrl Pts',(21.4003617479955,-0.106275286691508,
3.51601171139131));
#32710=CARTESIAN_POINT('Ctrl Pts',(21.424219666027,0.138618335471326,3.52426471946798));
#32711=CARTESIAN_POINT('Ctrl Pts',(21.4480775840584,0.349615998723735,3.64884796240357));
#32712=CARTESIAN_POINT('Ctrl Pts',(21.4719355020898,0.475123026939619,3.85929744372095));
#32713=CARTESIAN_POINT('Ctrl Pts',(21.4957934201212,0.484449532977353,4.10415253270923));
#32714=CARTESIAN_POINT('Ctrl Pts',(21.5196513381527,0.375314932061802,4.32353949039209));
#32715=CARTESIAN_POINT('Ctrl Pts',(21.543509256184,0.174405606883644,4.4638122296353));
#32716=CARTESIAN_POINT('Ctrl Pts',(21.5673671742155,-0.069150639890911,
4.49067024474121));
#32717=CARTESIAN_POINT('Ctrl Pts',(21.5912250922469,-0.29579767158652,4.39754601941878));
#32718=CARTESIAN_POINT('Ctrl Pts',(21.6150830102783,-0.450114115212426,
4.20721096341231));
#32719=CARTESIAN_POINT('Ctrl Pts',(21.6389409283097,-0.494365396806572,
3.96620718253823));
#32720=CARTESIAN_POINT('Ctrl Pts',(21.6627988463412,-0.417730872638478,
3.73346666603139));
#32721=CARTESIAN_POINT('Ctrl Pts',(21.6866567643726,-0.238949771349764,
3.56590080990214));
#32722=CARTESIAN_POINT('Ctrl Pts',(21.710514682404,-0.00173894210493873,
3.50448403037633));
#32723=CARTESIAN_POINT('Ctrl Pts',(21.7343726004354,0.235897105852373,3.56423440300754));
#32724=CARTESIAN_POINT('Ctrl Pts',(21.7582305184669,0.415849885720624,3.73054133411992));
#32725=CARTESIAN_POINT('Ctrl Pts',(21.7820884364982,0.49411604100673,3.96273824894669));
#32726=CARTESIAN_POINT('Ctrl Pts',(21.8059463545297,0.451557364815975,4.20404667689569));
#32727=CARTESIAN_POINT('Ctrl Pts',(21.8298042725611,0.29858061275206,4.39546013422383));
#32728=CARTESIAN_POINT('Ctrl Pts',(21.8536621905925,0.0725927676976751,
4.49017281661646));
#32729=CARTESIAN_POINT('Ctrl Pts',(21.8775201086239,-0.171145986446082,
4.46502489330693));
#32730=CARTESIAN_POINT('Ctrl Pts',(21.9013780266554,-0.373034884980705,
4.32616571656009));
#32731=CARTESIAN_POINT('Ctrl Pts',(21.9252359446868,-0.483706592871294,
4.10755013753858));
#32732=CARTESIAN_POINT('Ctrl Pts',(21.9490938627182,-0.476098862901817,
3.86263562028194));
#32733=CARTESIAN_POINT('Ctrl Pts',(21.9729517807496,-0.352071992280181,
3.65131043559696));
#32734=CARTESIAN_POINT('Ctrl Pts',(21.996809698781,-0.141953929297546,3.52524934752154));
#32735=CARTESIAN_POINT('Ctrl Pts',(22.0206676168125,0.102875736145779,3.51527772592526));
#32736=CARTESIAN_POINT('Ctrl Pts',(22.0445255348438,0.322549481822576,3.62383390390986));
#32737=CARTESIAN_POINT('Ctrl Pts',(22.0683834528753,0.46335109312246,3.82437293894729));
#32738=CARTESIAN_POINT('Ctrl Pts',(22.0922413709067,0.490850740723195,4.06785757439707));
#32739=CARTESIAN_POINT('Ctrl Pts',(22.1160992889381,0.398324011712033,4.29474918450382));
#32740=CARTESIAN_POINT('Ctrl Pts',(22.1399572069695,0.208396211707814,4.44956659019228));
#32741=CARTESIAN_POINT('Ctrl Pts',(22.163815125001,-0.0324901386554863,
4.49445271863166));
#32742=CARTESIAN_POINT('Ctrl Pts',(22.1876730430324,-0.265431765108271,
4.41843168874211));
#32743=CARTESIAN_POINT('Ctrl Pts',(22.2115309610638,-0.433468094767725,
4.24009271310828));
#32744=CARTESIAN_POINT('Ctrl Pts',(22.2353888790952,-0.495509667838209,
4.00304452911861));
#32745=CARTESIAN_POINT('Ctrl Pts',(22.2592467971266,-0.436385629680506,
3.76525187484075));
#32746=CARTESIAN_POINT('Ctrl Pts',(22.2831047151581,-0.270553418215538,
3.58486153155103));
#32747=CARTESIAN_POINT('Ctrl Pts',(22.3069626331895,-0.0385635261649252,
3.50598385198694));
#32748=CARTESIAN_POINT('Ctrl Pts',(22.3308205512209,0.202856198284482,3.54790657725669));
#32749=CARTESIAN_POINT('Ctrl Pts',(22.3546784692523,0.394672056935096,3.70037845932536));
#32750=CARTESIAN_POINT('Ctrl Pts',(22.3785363872837,0.489979846308564,3.9261159693126));
#32751=CARTESIAN_POINT('Ctrl Pts',(22.4023943053151,0.465474217808745,4.1699201379362));
#32752=CARTESIAN_POINT('Ctrl Pts',(22.4262522233466,0.327147461276091,4.37217420322137));
#32753=CARTESIAN_POINT('Ctrl Pts',(22.450110141378,0.108824243893236,4.4834215400391));
#32754=CARTESIAN_POINT('Ctrl Pts',(22.4739680594094,-0.136109474402841,
4.47645913832327));
#32755=CARTESIAN_POINT('Ctrl Pts',(22.4978259774408,-0.347760701725541,
4.3529895060813));
#32756=CARTESIAN_POINT('Ctrl Pts',(22.5216838954723,-0.474374996640319,
4.1432043106148));
#32757=CARTESIAN_POINT('Ctrl Pts',(22.5455418135036,-0.484991622785221,
3.89840178635216));
#32758=CARTESIAN_POINT('Ctrl Pts',(22.5693997315351,-0.377014700254462,
3.67844274379546));
#32759=CARTESIAN_POINT('Ctrl Pts',(22.5932576495665,-0.176847198578467,
3.53711330196678));
#32760=CARTESIAN_POINT('Ctrl Pts',(22.6171155675979,0.0665638539184235,
3.50897209184919));
#32761=CARTESIAN_POINT('Ctrl Pts',(22.6409734856293,0.293698998435555,3.60090091054846));
#32762=CARTESIAN_POINT('Ctrl Pts',(22.6648314036608,0.449015288492166,3.79041970485759));
#32763=CARTESIAN_POINT('Ctrl Pts',(22.6886893216922,0.494537845944295,4.03118776656693));
#32764=CARTESIAN_POINT('Ctrl Pts',(22.7125472397236,0.419127261608858,4.26432734830583));
#32765=CARTESIAN_POINT('Ctrl Pts',(22.736405157755,0.241238408088568,4.43283588997321));
#32766=CARTESIAN_POINT('Ctrl Pts',(22.7602630757865,0.00434171083240793,
4.49549632518638));
#32767=CARTESIAN_POINT('Ctrl Pts',(22.7841209938178,-0.233581370990537,
4.43700954435219));
#32768=CARTESIAN_POINT('Ctrl Pts',(22.8079789118493,-0.414457183229959,
4.27163232278894));
#32769=CARTESIAN_POINT('Ctrl Pts',(22.8238841905369,-0.46737397936094,4.11714349286348));
#32770=CARTESIAN_POINT('Ctrl Pts',(22.8318368298807,-0.473742730682552,
4.03823705100924));
#32771=CARTESIAN_POINT('Ctrl Pts',(4.,-0.219892372743211,3.64701365460636));
#32772=CARTESIAN_POINT('Ctrl Pts',(4.00795263934381,-0.161099076858729,
3.61038844940468));
#32773=CARTESIAN_POINT('Ctrl Pts',(4.02385791803142,-0.0249198690254346,
3.56711791692558));
#32774=CARTESIAN_POINT('Ctrl Pts',(4.04771583606284,0.185569069288609,3.60813812632505));
#32775=CARTESIAN_POINT('Ctrl Pts',(4.07157375409426,0.350624105231944,3.74494568050885));
#32776=CARTESIAN_POINT('Ctrl Pts',(4.09543167212568,0.429971014252744,3.94413788601839));
#32777=CARTESIAN_POINT('Ctrl Pts',(4.1192895901571,0.40416308778273,4.15698104289539));
#32778=CARTESIAN_POINT('Ctrl Pts',(4.14314750818851,0.279534313346206,4.3314427366163));
#32779=CARTESIAN_POINT('Ctrl Pts',(4.16700542621994,0.0865475313004802,
4.42485517705098));
#32780=CARTESIAN_POINT('Ctrl Pts',(4.19086334425134,-0.127600227202394,
4.41438026490915));
#32781=CARTESIAN_POINT('Ctrl Pts',(4.21472126228278,-0.310547447266788,
4.30257739619942));
#32782=CARTESIAN_POINT('Ctrl Pts',(4.23857918031418,-0.417556725585918,
4.11678647978038));
#32783=CARTESIAN_POINT('Ctrl Pts',(4.26243709834561,-0.422462345057068,
3.90243789311793));
#32784=CARTESIAN_POINT('Ctrl Pts',(4.28629501637703,-0.324064236326554,
3.71194600226016));
#32785=CARTESIAN_POINT('Ctrl Pts',(4.31015293440845,-0.146423688323203,
3.59189110566319));
#32786=CARTESIAN_POINT('Ctrl Pts',(4.33401085243986,0.0670214896752265,
3.5716299793216));
#32787=CARTESIAN_POINT('Ctrl Pts',(4.35786877047129,0.264078061498623,3.65611697628114));
#32788=CARTESIAN_POINT('Ctrl Pts',(4.38172668850271,0.396560367883193,3.82469274783887));
#32789=CARTESIAN_POINT('Ctrl Pts',(4.40558460653412,0.432072854850341,4.03613591352675));
#32790=CARTESIAN_POINT('Ctrl Pts',(4.42944252456555,0.361931763288092,4.23874286631049));
#32791=CARTESIAN_POINT('Ctrl Pts',(4.45330044259696,0.203288494707987,4.382970683851));
#32792=CARTESIAN_POINT('Ctrl Pts',(4.47715836062838,-0.00506434719902249,
4.43355173791626));
#32793=CARTESIAN_POINT('Ctrl Pts',(4.5010162786598,-0.212178818846594,4.37811758201071));
#32794=CARTESIAN_POINT('Ctrl Pts',(4.52487419669122,-0.367409789343613,
4.23022337776645));
#32795=CARTESIAN_POINT('Ctrl Pts',(4.54873211472264,-0.432799058467291,
4.02603328640456));
#32796=CARTESIAN_POINT('Ctrl Pts',(4.57259003275406,-0.392357168499796,
3.8154773474345));
#32797=CARTESIAN_POINT('Ctrl Pts',(4.59644795078547,-0.255973263285106,
3.65004222328625));
#32798=CARTESIAN_POINT('Ctrl Pts',(4.6203058688169,-0.0569969226013119,
3.57018130821703));
#32799=CARTESIAN_POINT('Ctrl Pts',(4.64416378684831,0.155916718210686,3.59542277130738));
#32800=CARTESIAN_POINT('Ctrl Pts',(4.66802170487973,0.330704474340828,3.71959438727947));
#32801=CARTESIAN_POINT('Ctrl Pts',(4.69187962291115,0.424625978282027,3.91233281365517));
#32802=CARTESIAN_POINT('Ctrl Pts',(4.71573754094257,0.41471486395576,4.1265082550995));
#32803=CARTESIAN_POINT('Ctrl Pts',(4.73959545897399,0.303394668785218,4.30974898215573));
#32804=CARTESIAN_POINT('Ctrl Pts',(4.76345337700541,0.117886212792376,4.41724764568232));
#32805=CARTESIAN_POINT('Ctrl Pts',(4.78731129503683,-0.0964486333844469,
4.42271789424177));
#32806=CARTESIAN_POINT('Ctrl Pts',(4.81116921306824,-0.287199161490599,
4.32482210305491));
#32807=CARTESIAN_POINT('Ctrl Pts',(4.83502713109967,-0.407721671464292,
4.14749845969467));
#32808=CARTESIAN_POINT('Ctrl Pts',(4.85888504913109,-0.42854512664958,3.93410742516172));
#32809=CARTESIAN_POINT('Ctrl Pts',(4.8827429671625,-0.344577625034195,3.73682892005441));
#32810=CARTESIAN_POINT('Ctrl Pts',(4.90660088519393,-0.176351507991885,
3.60390291263011));
#32811=CARTESIAN_POINT('Ctrl Pts',(4.93045880322534,0.0349973564730633,
3.56783343253575));
#32812=CARTESIAN_POINT('Ctrl Pts',(4.95431672125677,0.237788413971502,3.63744045016736));
#32813=CARTESIAN_POINT('Ctrl Pts',(4.97817463928818,0.382433727027559,3.79570315365689));
#32814=CARTESIAN_POINT('Ctrl Pts',(5.0020325573196,0.433563576539811,4.00392200101168));
#32815=CARTESIAN_POINT('Ctrl Pts',(5.02589047535102,0.378675321553375,4.21118181228595));
#32816=CARTESIAN_POINT('Ctrl Pts',(5.04974839338244,0.231190635538481,4.36680191797922));
#32817=CARTESIAN_POINT('Ctrl Pts',(5.07360631141386,0.0271735416279573,
4.43272896324296));
#32818=CARTESIAN_POINT('Ctrl Pts',(5.09746422944527,-0.183488223403015,
4.39284198969348));
#32819=CARTESIAN_POINT('Ctrl Pts',(5.1213221474767,-0.349282119693095,4.256894448863));
#32820=CARTESIAN_POINT('Ctrl Pts',(5.1451800655081,-0.4296670234643,4.05812921762123));
#32821=CARTESIAN_POINT('Ctrl Pts',(5.16903798353954,-0.404986636103755,
3.84514980926298));
#32822=CARTESIAN_POINT('Ctrl Pts',(5.19289590157095,-0.281275984601366,
3.67003549057442));
#32823=CARTESIAN_POINT('Ctrl Pts',(5.21675381960238,-0.0887856930599551,
3.5756064824932));
#32824=CARTESIAN_POINT('Ctrl Pts',(5.24061173763379,0.125415118908336,3.58495324968971));
#32825=CARTESIAN_POINT('Ctrl Pts',(5.26446965566521,0.308948518064291,3.69579025298356));
#32826=CARTESIAN_POINT('Ctrl Pts',(5.28832757369662,0.416935588964862,3.88101482593007));
#32827=CARTESIAN_POINT('Ctrl Pts',(5.31218549172805,0.422970551266107,4.09533451502773));
#32828=CARTESIAN_POINT('Ctrl Pts',(5.33604340975946,0.325577692296299,4.28634231834109));
#32829=CARTESIAN_POINT('Ctrl Pts',(5.35990132779089,0.148572219001774,4.40733162501188));
#32830=CARTESIAN_POINT('Ctrl Pts',(5.3837592458223,-0.0647632088646815,
4.42871725387658));
#32831=CARTESIAN_POINT('Ctrl Pts',(5.40761716385372,-0.26226226804932,4.34526983614494));
#32832=CARTESIAN_POINT('Ctrl Pts',(5.43147508188515,-0.395631058815178,
4.17739453851434));
#32833=CARTESIAN_POINT('Ctrl Pts',(5.45533299991656,-0.432257278927009,
3.96614144408682));
#32834=CARTESIAN_POINT('Ctrl Pts',(5.47919091794798,-0.363184819889405,
3.76316768886851));
#32835=CARTESIAN_POINT('Ctrl Pts',(5.5030488359794,-0.205303779432806,3.61810588490468));
#32836=CARTESIAN_POINT('Ctrl Pts',(5.52690675401082,0.00277962745745752,
3.56642759466814));
#32837=CARTESIAN_POINT('Ctrl Pts',(5.55076467204224,0.210183339719457,3.62076956781107));
#32838=CARTESIAN_POINT('Ctrl Pts',(5.57462259007365,0.36619150013966,3.76784371165257));
#32839=CARTESIAN_POINT('Ctrl Pts',(5.59848050810508,0.432655863921731,3.97168639180759));
#32840=CARTESIAN_POINT('Ctrl Pts',(5.62233842613649,0.393324083661671,4.18245252040861));
#32841=CARTESIAN_POINT('Ctrl Pts',(5.64619634416792,0.257813851021257,4.34860403787086));
#32842=CARTESIAN_POINT('Ctrl Pts',(5.67005426219933,0.0592611090830247,
4.42951237227525));
#32843=CARTESIAN_POINT('Ctrl Pts',(5.69391218023075,-0.153782588238227,
4.40539323200473));
#32844=CARTESIAN_POINT('Ctrl Pts',(5.71777009826218,-0.329222253834466,
4.28214440376531));
#32845=CARTESIAN_POINT('Ctrl Pts',(5.74162801629359,-0.424158110434281,
4.08990358344764));
#32846=CARTESIAN_POINT('Ctrl Pts',(5.76548593432501,-0.415375755386326,
3.8756788878607));
#32847=CARTESIAN_POINT('Ctrl Pts',(5.78934385235642,-0.305022713182347,
3.69185409099321));
#32848=CARTESIAN_POINT('Ctrl Pts',(5.81320177038785,-0.120083309624962,
3.58337936191985));
#32849=CARTESIAN_POINT('Ctrl Pts',(5.83705968841926,0.0942197354074567,
3.57677972866706));
#32850=CARTESIAN_POINT('Ctrl Pts',(5.86091760645069,0.285483486244351,3.673668977605));
#32851=CARTESIAN_POINT('Ctrl Pts',(5.8847755244821,0.406938752801468,3.85035505520226));
#32852=CARTESIAN_POINT('Ctrl Pts',(5.90863344251353,0.428886400972996,4.06363338935351));
#32853=CARTESIAN_POINT('Ctrl Pts',(5.93249136054494,0.345959657594393,4.261351642888));
#32854=CARTESIAN_POINT('Ctrl Pts',(5.95634927857636,0.178436323746589,4.39516226965834));
#32855=CARTESIAN_POINT('Ctrl Pts',(5.98020719660778,-0.0327194942966983,
4.4323450160316));
#32856=CARTESIAN_POINT('Ctrl Pts',(6.0040651146392,-0.23587461323539,4.36380751861078));
#32857=CARTESIAN_POINT('Ctrl Pts',(6.02792303267061,-0.381351759249696,
4.20630938167977));
#32858=CARTESIAN_POINT('Ctrl Pts',(6.05178095070204,-0.433578399193506,
3.9983625870902));
#32859=CARTESIAN_POINT('Ctrl Pts',(6.07563886873346,-0.379782579589031,
3.79081692866841));
#32860=CARTESIAN_POINT('Ctrl Pts',(6.09949678676487,-0.233120953551068,
3.63442082419035));
#32861=CARTESIAN_POINT('Ctrl Pts',(6.12335470479629,-0.0294522997972467,
3.5674214393556));
#32862=CARTESIAN_POINT('Ctrl Pts',(6.14721262282771,0.181413325723775,3.60619428643423));
#32863=CARTESIAN_POINT('Ctrl Pts',(6.17107054085913,0.347927737305898,3.74127281623538));
#32864=CARTESIAN_POINT('Ctrl Pts',(6.19492845889055,0.429346806292137,3.93959933010928));
#32865=CARTESIAN_POINT('Ctrl Pts',(6.21878637692197,0.405811992579865,4.15272917617017));
#32866=CARTESIAN_POINT('Ctrl Pts',(6.24264429495339,0.282982581651336,4.32844890303245));
#32867=CARTESIAN_POINT('Ctrl Pts',(6.26650221298481,0.0910742457207041,
4.42397415233781));
#32868=CARTESIAN_POINT('Ctrl Pts',(6.29036013101623,-0.123327005978964,
4.41559921078967));
#32869=CARTESIAN_POINT('Ctrl Pts',(6.31421804904765,-0.307151379675736,
4.3060270879454));
#32870=CARTESIAN_POINT('Ctrl Pts',(6.33807596707907,-0.416657206472865,
4.12081787696614));
#32871=CARTESIAN_POINT('Ctrl Pts',(6.36193388511048,-0.422829889105799,
3.9075587958503));
#32872=CARTESIAN_POINT('Ctrl Pts',(6.39374444248571,-0.296437506874183,
3.64987069373525));
#32873=CARTESIAN_POINT('Ctrl Pts',(6.43350763920474,0.0703302468340302,
3.51324810367198));
#32874=CARTESIAN_POINT('Ctrl Pts',(6.48122347526758,0.448014600657906,3.7964368525222));
#32875=CARTESIAN_POINT('Ctrl Pts',(6.52893931133042,0.413240052911115,4.26646358767058));
#32876=CARTESIAN_POINT('Ctrl Pts',(6.57665514739325,-0.000480251589724132,
4.49184654025612));
#32877=CARTESIAN_POINT('Ctrl Pts',(6.62437098345609,-0.41404349770976,4.26553045144514));
#32878=CARTESIAN_POINT('Ctrl Pts',(6.67208681951894,-0.447234019333667,
3.79538894860702));
#32879=CARTESIAN_POINT('Ctrl Pts',(6.71980265558177,-0.0698021891909718,
3.51313682319347));
#32880=CARTESIAN_POINT('Ctrl Pts',(6.76751849164461,0.371772181936036,3.67798293440124));
#32881=CARTESIAN_POINT('Ctrl Pts',(6.81523432770745,0.471920133146607,4.13853999974893));
#32882=CARTESIAN_POINT('Ctrl Pts',(6.86295016377028,0.138708377331583,4.4718748549198));
#32883=CARTESIAN_POINT('Ctrl Pts',(6.91066599983312,-0.32188767172048,4.37187913281409));
#32884=CARTESIAN_POINT('Ctrl Pts',(6.95838183589596,-0.486886005735063,
3.93038141845316));
#32885=CARTESIAN_POINT('Ctrl Pts',(7.0060976719588,-0.204771183672361,3.55281534000283));
#32886=CARTESIAN_POINT('Ctrl Pts',(7.05381350802163,0.265389096458903,3.58590591031157));
#32887=CARTESIAN_POINT('Ctrl Pts',(7.10152934408448,0.491837993618785,3.99926540470374));
#32888=CARTESIAN_POINT('Ctrl Pts',(7.14924518014731,0.266624753986561,4.41329951581085));
#32889=CARTESIAN_POINT('Ctrl Pts',(7.19696101621015,-0.203434237821079,
4.44779430805676));
#32890=CARTESIAN_POINT('Ctrl Pts',(7.24467685227299,-0.486676365692783,
4.07107270446015));
#32891=CARTESIAN_POINT('Ctrl Pts',(7.29239268833582,-0.322996137187983,
3.62908393881966));
#32892=CARTESIAN_POINT('Ctrl Pts',(7.34010852439867,0.137296434535941,3.52771310152703));
#32893=CARTESIAN_POINT('Ctrl Pts',(7.3878243604615,0.471507566988788,3.86005058906394));
#32894=CARTESIAN_POINT('Ctrl Pts',(7.43554019652434,0.372726051350611,4.32090577464778));
#32895=CARTESIAN_POINT('Ctrl Pts',(7.48325603258718,-0.0683355354161961,
4.48706824929225));
#32896=CARTESIAN_POINT('Ctrl Pts',(7.53097186865002,-0.44664354691983,4.20594845626764));
#32897=CARTESIAN_POINT('Ctrl Pts',(7.57868770471286,-0.414791917646955,
3.73570302684109));
#32898=CARTESIAN_POINT('Ctrl Pts',(7.62640354077569,-0.00203048755240202,
3.50816557464413));
#32899=CARTESIAN_POINT('Ctrl Pts',(7.67411937683853,0.412595570264971,3.73228724307244));
#32900=CARTESIAN_POINT('Ctrl Pts',(7.72183521290137,0.448328767436039,4.20225365549051));
#32901=CARTESIAN_POINT('Ctrl Pts',(7.7695510489642,0.0723547589785895,4.48648742399228));
#32902=CARTESIAN_POINT('Ctrl Pts',(7.81726688502705,-0.370063737934377,
4.32397230547438));
#32903=CARTESIAN_POINT('Ctrl Pts',(7.86498272108989,-0.472647010158531,
3.86394843388276));
#32904=CARTESIAN_POINT('Ctrl Pts',(7.91269855715272,-0.141191260335066,
3.52886280888004));
#32905=CARTESIAN_POINT('Ctrl Pts',(7.96041439321556,0.31992259635559,3.62642971585976));
#32906=CARTESIAN_POINT('Ctrl Pts',(8.0081302292784,0.48724661017382,4.0670519628834));
#32907=CARTESIAN_POINT('Ctrl Pts',(8.05584606534124,0.207124564615173,4.44609936066402));
#32908=CARTESIAN_POINT('Ctrl Pts',(8.10356190140407,-0.263203155649882,
4.41548685142597));
#32909=CARTESIAN_POINT('Ctrl Pts',(8.15127773746691,-0.491827368180951,
4.00332637343646));
#32910=CARTESIAN_POINT('Ctrl Pts',(8.19899357352975,-0.268798940774433,
3.58811123553743));
#32911=CARTESIAN_POINT('Ctrl Pts',(8.24670940959259,0.201071689948468,3.55113988776764));
#32912=CARTESIAN_POINT('Ctrl Pts',(8.29442524565542,0.486295093906121,3.92636368766143));
#32913=CARTESIAN_POINT('Ctrl Pts',(8.34214108171827,0.324946230517931,4.36920884621601));
#32914=CARTESIAN_POINT('Ctrl Pts',(8.3898569177811,-0.134805756295296,4.47300384028212));
#32915=CARTESIAN_POINT('Ctrl Pts',(8.43757275384394,-0.470763542849379,
4.14243212971755));
#32916=CARTESIAN_POINT('Ctrl Pts',(8.48528858990678,-0.37441192437669,3.68106280283335));
#32917=CARTESIAN_POINT('Ctrl Pts',(8.53300442596962,0.0657679253190804,
3.51257841158684));
#32918=CARTESIAN_POINT('Ctrl Pts',(8.58072026203246,0.445552077224736,3.79170076492532));
#32919=CARTESIAN_POINT('Ctrl Pts',(8.62843609809529,0.41617890091499,4.26210751092856));
#32920=CARTESIAN_POINT('Ctrl Pts',(8.67615193415813,0.0046222361594965,
4.49181689660367));
#32921=CARTESIAN_POINT('Ctrl Pts',(8.72386777022097,-0.411179099183508,
4.26988325855195));
#32922=CARTESIAN_POINT('Ctrl Pts',(8.7715836062838,-0.449388340942622,3.80011167148426));
#32923=CARTESIAN_POINT('Ctrl Pts',(8.81929944234665,-0.0749173544856965,
3.51390061216986));
#32924=CARTESIAN_POINT('Ctrl Pts',(8.86701527840948,0.368351391347115,3.67408210030036));
#32925=CARTESIAN_POINT('Ctrl Pts',(8.91473111447233,0.473357386691186,4.13355901061654));
#32926=CARTESIAN_POINT('Ctrl Pts',(8.96244695053515,0.14367201029714,4.47038662641401));
#32927=CARTESIAN_POINT('Ctrl Pts',(9.01016278659801,-0.317949583830803,
4.37525096534692));
#32928=CARTESIAN_POINT('Ctrl Pts',(9.05787862266083,-0.487593182843731,
3.93551656882348));
#32929=CARTESIAN_POINT('Ctrl Pts',(9.10559445872368,-0.209472459465777,
3.55499829935456));
#32930=CARTESIAN_POINT('Ctrl Pts',(9.15331029478651,0.261010046587687,3.58313193881964));
#32931=CARTESIAN_POINT('Ctrl Pts',(9.20102613084934,0.491803010703882,3.99408193320625));
#32932=CARTESIAN_POINT('Ctrl Pts',(9.2487419669122,0.270965702728691,4.41046657939073));
#32933=CARTESIAN_POINT('Ctrl Pts',(9.29645780297501,-0.198703579405513,
4.44991344988054));
#32934=CARTESIAN_POINT('Ctrl Pts',(9.34417363903789,-0.485900307124067,
4.07619787653679));
#32935=CARTESIAN_POINT('Ctrl Pts',(9.39188947510068,-0.326887306273347,
3.63250862071426));
#32936=CARTESIAN_POINT('Ctrl Pts',(9.43960531116356,0.13231133773591,3.52629235307153));
#32937=CARTESIAN_POINT('Ctrl Pts',(9.48732114722637,0.470006444430667,3.85508910653225));
#32938=CARTESIAN_POINT('Ctrl Pts',(9.53503698328922,0.376087401226012,4.31695976320512));
#32939=CARTESIAN_POINT('Ctrl Pts',(9.58275281935206,-0.0631984893729827,
4.48776139227388));
#32940=CARTESIAN_POINT('Ctrl Pts',(9.63046865541489,-0.444448234747017,
4.21064422964382));
#32941=CARTESIAN_POINT('Ctrl Pts',(9.67818449147773,-0.41755432743774,3.74008922975375));
#32942=CARTESIAN_POINT('Ctrl Pts',(9.72590032754057,-0.00721385634321597,
3.50821428942208));
#32943=CARTESIAN_POINT('Ctrl Pts',(9.77361616360341,0.40975121003073,3.72795373420991));
#32944=CARTESIAN_POINT('Ctrl Pts',(9.82133199966624,0.450435435400681,4.19751745084266));
#32945=CARTESIAN_POINT('Ctrl Pts',(9.86904783572909,0.077477869602138,4.48569785316993));
#32946=CARTESIAN_POINT('Ctrl Pts',(9.91676367179192,-0.366628816002305,
4.3278544435092));
#32947=CARTESIAN_POINT('Ctrl Pts',(9.96447950785476,-0.474054618562381,
3.8689372536849));
#32948=CARTESIAN_POINT('Ctrl Pts',(10.0121953439176,-0.146148770628728,
3.53037700046135));
#32949=CARTESIAN_POINT('Ctrl Pts',(10.0599111799804,0.315967742161179,3.62307877379278));
#32950=CARTESIAN_POINT('Ctrl Pts',(10.1076270160433,0.487926215535836,4.06191310882887));
#32951=CARTESIAN_POINT('Ctrl Pts',(10.1553428521061,0.211814537474087,4.44389168337175));
#32952=CARTESIAN_POINT('Ctrl Pts',(10.203058688169,-0.258809689535701,4.4182376949229));
#32953=CARTESIAN_POINT('Ctrl Pts',(10.2507745242318,-0.491764996345908,
4.00850959581219));
#32954=CARTESIAN_POINT('Ctrl Pts',(10.2984903602946,-0.273124940234581,
3.59096700393021));
#32955=CARTESIAN_POINT('Ctrl Pts',(10.3462061963575,0.196329951061554,3.54904570612073));
#32956=CARTESIAN_POINT('Ctrl Pts',(10.3939220324203,0.485492027373267,3.92124267520431));
#32957=CARTESIAN_POINT('Ctrl Pts',(10.4416378684831,0.328819304693055,4.36576370748498));
#32958=CARTESIAN_POINT('Ctrl Pts',(10.489353704546,-0.129813245022134,4.47439829918413));
#32959=CARTESIAN_POINT('Ctrl Pts',(10.5370695406088,-0.469236294399976,
4.14738563318641));
#32960=CARTESIAN_POINT('Ctrl Pts',(10.5847853766716,-0.377752434501872,
3.68502647241413));
#32961=CARTESIAN_POINT('Ctrl Pts',(10.6325012127345,0.0606272984676223,
3.51191234851464));
#32962=CARTESIAN_POINT('Ctrl Pts',(10.6802170487973,0.443332050383407,3.78701662516801));
#32963=CARTESIAN_POINT('Ctrl Pts',(10.7279328848602,0.418918158891686,4.25770681210006));
#32964=CARTESIAN_POINT('Ctrl Pts',(10.775648720923,0.00980527620531799,
4.49174086815163));
#32965=CARTESIAN_POINT('Ctrl Pts',(10.8233645569858,-0.408311942493964,
4.27420171857372));
#32966=CARTESIAN_POINT('Ctrl Pts',(10.8710803930487,-0.451470021714238,
3.80485891169382));
#32967=CARTESIAN_POINT('Ctrl Pts',(10.9187962291115,-0.080036233235122,
3.51471716883706));
#32968=CARTESIAN_POINT('Ctrl Pts',(10.9665120651743,0.364896059739551,3.6702181168734));
#32969=CARTESIAN_POINT('Ctrl Pts',(11.0142279012372,0.47473868640782,4.1285628425314));
#32970=CARTESIAN_POINT('Ctrl Pts',(11.0619437373,0.148621472554162,4.46884633169921));
#32971=CARTESIAN_POINT('Ctrl Pts',(11.1096595733629,-0.313977126381285,
4.37858102033954));
#32972=CARTESIAN_POINT('Ctrl Pts',(11.1573754094257,-0.488245699001722,
3.94065893278431));
#32973=CARTESIAN_POINT('Ctrl Pts',(11.2050912454886,-0.214150733603143,
3.55723066033293));
#32974=CARTESIAN_POINT('Ctrl Pts',(11.2528070815514,0.256602145595791,3.58040428537983));
#32975=CARTESIAN_POINT('Ctrl Pts',(11.3005229176142,0.491713326162588,3.98889911147238));
#32976=CARTESIAN_POINT('Ctrl Pts',(11.3482387536771,0.275276593332242,4.40758805430897));
#32977=CARTESIAN_POINT('Ctrl Pts',(11.3959545897399,-0.193950870829933,
4.45198261532529));
#32978=CARTESIAN_POINT('Ctrl Pts',(11.4436704258028,-0.485070265991237,
4.08131458604192));
#32979=CARTESIAN_POINT('Ctrl Pts',(11.4913862618656,-0.330742172127369,
3.63597412121053));
#32980=CARTESIAN_POINT('Ctrl Pts',(11.5391020979284,0.127311547523522,3.52492422212962));
#32981=CARTESIAN_POINT('Ctrl Pts',(11.5868179339912,0.468453114143607,3.85014371984754));
#32982=CARTESIAN_POINT('Ctrl Pts',(11.6345337700541,0.379406977967949,4.31297854546471));
#32983=CARTESIAN_POINT('Ctrl Pts',(11.6822496061169,-0.0580544240024287,
4.48840035698771));
#32984=CARTESIAN_POINT('Ctrl Pts',(11.7299654421798,-0.44220355512924,4.21531660568344));
#32985=CARTESIAN_POINT('Ctrl Pts',(11.7776812782426,-0.420270357404582,
3.74450430230823));
#32986=CARTESIAN_POINT('Ctrl Pts',(11.8253971143054,-0.0123964237846327,
3.50831762943));
#32987=CARTESIAN_POINT('Ctrl Pts',(11.8731129503683,0.406861336540243,3.72365044295193));
#32988=CARTESIAN_POINT('Ctrl Pts',(11.9208287864311,0.452492071153857,4.1927593068956));
#32989=CARTESIAN_POINT('Ctrl Pts',(11.968544622494,0.0825923743414284,4.48485433333386));
#32990=CARTESIAN_POINT('Ctrl Pts',(12.0162604585568,-0.363153170675764,
4.33170016502878));
#32991=CARTESIAN_POINT('Ctrl Pts',(12.0639762946196,-0.475409571231627,
3.87394063131468));
#32992=CARTESIAN_POINT('Ctrl Pts',(12.1116921306825,-0.151090047408964,
3.53194335553704));
#32993=CARTESIAN_POINT('Ctrl Pts',(12.1594079667453,0.311977791768556,3.61976969834691));
#32994=CARTESIAN_POINT('Ctrl Pts',(12.2071238028081,0.488551624369653,4.05676737776005));
#32995=CARTESIAN_POINT('Ctrl Pts',(12.254839638871,0.216480982979095,4.44163470069774));
#32996=CARTESIAN_POINT('Ctrl Pts',(12.3025554749338,-0.254387476069249,
4.42094208256136));
#32997=CARTESIAN_POINT('Ctrl Pts',(12.3502713109967,-0.49164800158875,4.0136918729824));
#32998=CARTESIAN_POINT('Ctrl Pts',(12.3979871470595,-0.277420602272412,
3.59386820576715));
#32999=CARTESIAN_POINT('Ctrl Pts',(12.4457029831224,0.191566404775332,3.54700161433684));
#33000=CARTESIAN_POINT('Ctrl Pts',(12.4934188191852,0.484635034689867,3.91613041073711));
#33001=CARTESIAN_POINT('Ctrl Pts',(12.541134655248,0.332655855180181,4.362277941457));
#33002=CARTESIAN_POINT('Ctrl Pts',(12.5888504913109,-0.124806314709729,
4.47574006417428));
#33003=CARTESIAN_POINT('Ctrl Pts',(12.6365663273737,-0.4676569254097,4.15232276575852));
#33004=CARTESIAN_POINT('Ctrl Pts',(12.6842821634365,-0.381050985679211,
3.68902512775968));
#33005=CARTESIAN_POINT('Ctrl Pts',(12.7319979994994,0.0554799374235607,
3.5113004999026));
#33006=CARTESIAN_POINT('Ctrl Pts',(12.7797138355622,0.441062780321708,3.78235614259331));
#33007=CARTESIAN_POINT('Ctrl Pts',(12.8274296716251,0.421610885427219,4.2532774884218));
#33008=CARTESIAN_POINT('Ctrl Pts',(12.8751455076879,0.0149872271275763,
4.49161021945745));
#33009=CARTESIAN_POINT('Ctrl Pts',(12.9228613437507,-0.405399432451448,
4.27848972156979));
#33010=CARTESIAN_POINT('Ctrl Pts',(12.9705771798136,-0.453501555338242,
3.80962782724943));
#33011=CARTESIAN_POINT('Ctrl Pts',(13.0182930158764,-0.0851462219395619,
3.51558762841831));
#33012=CARTESIAN_POINT('Ctrl Pts',(13.0660088519392,0.361400197209248,3.66639076405307));
#33013=CARTESIAN_POINT('Ctrl Pts',(13.1137246880021,0.476067254403989,4.1235523942958));
#33014=CARTESIAN_POINT('Ctrl Pts',(13.1614405240649,0.153554426643267,4.46725395975876));
#33015=CARTESIAN_POINT('Ctrl Pts',(13.2091563601278,-0.30996979384252,4.38186902434892));
#33016=CARTESIAN_POINT('Ctrl Pts',(13.2568721961906,-0.488843983144383,
3.94580788806928));
#33017=CARTESIAN_POINT('Ctrl Pts',(13.3045880322534,-0.218805220893238,
3.55951220202843));
#33018=CARTESIAN_POINT('Ctrl Pts',(13.3523038683163,0.252165742455243,3.57772323864086));
#33019=CARTESIAN_POINT('Ctrl Pts',(13.4000197043791,0.491569024438394,3.98371752277252));
#33020=CARTESIAN_POINT('Ctrl Pts',(13.447735540442,0.279556907518101,4.40466425628032));
#33021=CARTESIAN_POINT('Ctrl Pts',(13.4954513765048,-0.189176619112,4.45400157668594));
#33022=CARTESIAN_POINT('Ctrl Pts',(13.5431672125676,-0.484186345555107,
4.08642226350871));
#33023=CARTESIAN_POINT('Ctrl Pts',(13.5908830486304,-0.334560300710407,
3.63948005597396));
#33024=CARTESIAN_POINT('Ctrl Pts',(13.6385988846933,0.122297616148583,3.52360886035071));
#33025=CARTESIAN_POINT('Ctrl Pts',(13.6863147207561,0.466847750307624,3.8452149784873));
#33026=CARTESIAN_POINT('Ctrl Pts',(13.734030556819,0.3826844119832,4.30896256355269));
#33027=CARTESIAN_POINT('Ctrl Pts',(13.7817463928818,-0.0529039102219543,
4.48898507250754));
#33028=CARTESIAN_POINT('Ctrl Pts',(13.8294622289446,-0.439909757638992,
4.21996506537626));
#33029=CARTESIAN_POINT('Ctrl Pts',(13.8771780650075,-0.422939705734467,
3.74894775411238));
#33030=CARTESIAN_POINT('Ctrl Pts',(13.9248939010703,-0.0175776142901187,
3.50847558318244));
#33031=CARTESIAN_POINT('Ctrl Pts',(13.9726097371332,0.403926270823208,3.71937784729135));
#33032=CARTESIAN_POINT('Ctrl Pts',(14.020325573196,0.454498446235019,4.18797975215946));
#33033=CARTESIAN_POINT('Ctrl Pts',(14.0680414092588,0.0876977051117048,
4.48395695817926));
#33034=CARTESIAN_POINT('Ctrl Pts',(14.1157572453217,-0.359637188018331,
4.33550904286807));
#33035=CARTESIAN_POINT('Ctrl Pts',(14.1634730813845,-0.476711717661702,
3.87895801102093));
#33036=CARTESIAN_POINT('Ctrl Pts',(14.2111889174473,-0.156014541823709,
3.53356170012368));
#33037=CARTESIAN_POINT('Ctrl Pts',(14.2589047535102,0.307953188363286,3.61650285707861));
#33038=CARTESIAN_POINT('Ctrl Pts',(14.306620589573,0.4891227672074,4.05161534124029));
#33039=CARTESIAN_POINT('Ctrl Pts',(14.3543364256359,0.2211233828038,4.4393286633369));
#33040=CARTESIAN_POINT('Ctrl Pts',(14.4020522616987,-0.249937006449114,
4.42359971395084));
#33041=CARTESIAN_POINT('Ctrl Pts',(14.4497680977616,-0.491476396904638,
4.01887262932433));
#33042=CARTESIAN_POINT('Ctrl Pts',(14.4974839338244,-0.281685449746218,
3.59681451879656));
#33043=CARTESIAN_POINT('Ctrl Pts',(14.5451997698872,0.186781580201919,3.54500783946397));
#33044=CARTESIAN_POINT('Ctrl Pts',(14.59291560595,0.483724211046603,3.91102746210588));
#33045=CARTESIAN_POINT('Ctrl Pts',(14.6406314420129,0.33645545583349,4.35875193531444));
#33046=CARTESIAN_POINT('Ctrl Pts',(14.6883472780757,-0.119785521504147,
4.47702898621568));
#33047=CARTESIAN_POINT('Ctrl Pts',(14.7360631141386,-0.466025611307368,
4.15724297904063));
#33048=CARTESIAN_POINT('Ctrl Pts',(14.7837789502014,-0.38430721152129,3.69305832471834));
#33049=CARTESIAN_POINT('Ctrl Pts',(14.8314947862642,0.0503264139313189,
3.51074293371195));
#33050=CARTESIAN_POINT('Ctrl Pts',(14.8792106223271,0.438744519099385,3.77771983486548));
#33051=CARTESIAN_POINT('Ctrl Pts',(14.9269264583899,0.42425678142631,4.24882003188202));
#33052=CARTESIAN_POINT('Ctrl Pts',(14.9746422944528,0.0201675133397715,
4.49142496503298));
#33053=CARTESIAN_POINT('Ctrl Pts',(15.0223581305156,-0.402441892563756,
4.28274679124913));
#33054=CARTESIAN_POINT('Ctrl Pts',(15.0700739665785,-0.455482716161518,
3.8144178884426));
#33055=CARTESIAN_POINT('Ctrl Pts',(15.1177898026413,-0.0902467530057116,
3.51651189422706));
#33056=CARTESIAN_POINT('Ctrl Pts',(15.1655056387041,0.357864192060027,3.66260046696357));
#33057=CARTESIAN_POINT('Ctrl Pts',(15.2132214747669,0.47734294310866,4.11852822244656));
#33058=CARTESIAN_POINT('Ctrl Pts',(15.2609373108298,0.15847032463534,4.46560968746574));
#33059=CARTESIAN_POINT('Ctrl Pts',(15.3086531468926,-0.305928031329979,
4.38511461215921));
#33060=CARTESIAN_POINT('Ctrl Pts',(15.3563689829555,-0.489387968817152,
3.95096286275689));
#33061=CARTESIAN_POINT('Ctrl Pts',(15.4040848190183,-0.223435404337718,
3.56184267101825));
#33062=CARTESIAN_POINT('Ctrl Pts',(15.4518006550811,0.24770132994065,3.57508909640066));
#33063=CARTESIAN_POINT('Ctrl Pts',(15.499516491144,0.491370121559653,3.97853774265298));
#33064=CARTESIAN_POINT('Ctrl Pts',(15.5472323272068,0.283806169849271,4.40169551006635));
#33065=CARTESIAN_POINT('Ctrl Pts',(15.5949481632697,-0.184381354552937,
4.4559701097059));
#33066=CARTESIAN_POINT('Ctrl Pts',(15.6426639993325,-0.483248643997369,
4.09152034160055));
#33067=CARTESIAN_POINT('Ctrl Pts',(15.6903798353953,-0.338341267922855,
3.64302603558196));
#33068=CARTESIAN_POINT('Ctrl Pts',(15.7380956714582,0.117270100534806,3.52234641383892));
#33069=CARTESIAN_POINT('Ctrl Pts',(15.785811507521,0.465190531238913,3.84030342991275));
#33070=CARTESIAN_POINT('Ctrl Pts',(15.8335273435838,0.385919339229949,4.30491226354526));
#33071=CARTESIAN_POINT('Ctrl Pts',(15.8812431796467,-0.0477475201261761,
4.48951547388594));
#33072=CARTESIAN_POINT('Ctrl Pts',(15.9289590157095,-0.437567097060412,
4.22458909239344));
#33073=CARTESIAN_POINT('Ctrl Pts',(15.9766748517724,-0.425562075928853,
3.75341909160864));
#33074=CARTESIAN_POINT('Ctrl Pts',(16.0243906878352,-0.0227568523576073,
3.50868813313462));
#33075=CARTESIAN_POINT('Ctrl Pts',(16.072106523898,0.400946338892803,3.71513642180785));
#33076=CARTESIAN_POINT('Ctrl Pts',(16.1198223599609,0.456454337785543,4.1831793175245));
#33077=CARTESIAN_POINT('Ctrl Pts',(16.1675381960237,0.0927932948370443,
4.4830058273823));
#33078=CARTESIAN_POINT('Ctrl Pts',(16.2152540320865,-0.356081258568678,
4.33928065395499));
#33079=CARTESIAN_POINT('Ctrl Pts',(16.2629698681494,-0.477960913216358,
3.88398883549692));
#33080=CARTESIAN_POINT('Ctrl Pts',(16.3106857042122,-0.160921706883503,
3.53523185446324));
#33081=CARTESIAN_POINT('Ctrl Pts',(16.358401540275,0.303894378979202,3.6132786128531));
#33082=CARTESIAN_POINT('Ctrl Pts',(16.4061173763379,0.489639580609251,4.04645757153336));
#33083=CARTESIAN_POINT('Ctrl Pts',(16.4538332124007,0.225741221292456,4.43697382743292));
#33084=CARTESIAN_POINT('Ctrl Pts',(16.5015490484636,-0.245458775012363,
4.42621029389423));
#33085=CARTESIAN_POINT('Ctrl Pts',(16.5492648845264,-0.4912502013546,4.02405128938415));
#33086=CARTESIAN_POINT('Ctrl Pts',(16.5969807205893,-0.285919008936969,
3.59980561575594));
#33087=CARTESIAN_POINT('Ctrl Pts',(16.6446965566521,0.181976008816936,3.54306460296116));
#33088=CARTESIAN_POINT('Ctrl Pts',(16.6924123927149,0.482759657613431,3.90593439612197));
#33089=CARTESIAN_POINT('Ctrl Pts',(16.7401282287778,0.340217684611379,4.35518608070932));
#33090=CARTESIAN_POINT('Ctrl Pts',(16.7878440648406,-0.114751423091257,
4.47826492214097));
#33091=CARTESIAN_POINT('Ctrl Pts',(16.8355599009034,-0.464342533291602,
4.16214572651883));
#33092=CARTESIAN_POINT('Ctrl Pts',(16.8832757369663,-0.387520750342007,
3.69712561530174));
#33093=CARTESIAN_POINT('Ctrl Pts',(16.9309915730291,0.0451673004198413,
3.51023971187451));
#33094=CARTESIAN_POINT('Ctrl Pts',(16.978707409092,0.436377524217892,3.7731082169636));
#33095=CARTESIAN_POINT('Ctrl Pts',(17.0264232451548,0.426855552995382,4.24433493759383));
#33096=CARTESIAN_POINT('Ctrl Pts',(17.0741390812176,0.0253455594402812,
4.49118512545541));
#33097=CARTESIAN_POINT('Ctrl Pts',(17.1218549172805,-0.399439651340385,
4.28697245475663));
#33098=CARTESIAN_POINT('Ctrl Pts',(17.1695707533433,-0.457413284126125,
3.81922856321607));
#33099=CARTESIAN_POINT('Ctrl Pts',(17.2172865894061,-0.0953372598908034,
3.51748986360026));
#33100=CARTESIAN_POINT('Ctrl Pts',(17.265002425469,0.354288437054553,3.6588476466131));
#33101=CARTESIAN_POINT('Ctrl Pts',(17.3127182615318,0.478565610824392,4.11349088504481));
#33102=CARTESIAN_POINT('Ctrl Pts',(17.3604340975947,0.163368620495752,4.46391369745815));
#33103=CARTESIAN_POINT('Ctrl Pts',(17.4081499336575,-0.301852287783465,
4.38831742326589));
#33104=CARTESIAN_POINT('Ctrl Pts',(17.4558657697204,-0.489877595596684,
3.956123284257));
#33105=CARTESIAN_POINT('Ctrl Pts',(17.5035816057832,-0.228040769637767,
3.56422180844494));
#33106=CARTESIAN_POINT('Ctrl Pts',(17.551297441846,0.243209403937772,3.57250215124727));
#33107=CARTESIAN_POINT('Ctrl Pts',(17.5990132779089,0.491116639619549,3.97336034645914));
#33108=CARTESIAN_POINT('Ctrl Pts',(17.6467291139717,0.288023908337871,4.39868214542132));
#33109=CARTESIAN_POINT('Ctrl Pts',(17.6944449500345,-0.179565609787963,
4.45788799572981));
#33110=CARTESIAN_POINT('Ctrl Pts',(17.7421607860973,-0.48225726547346,4.09660825404716));
#33111=CARTESIAN_POINT('Ctrl Pts',(17.7898766221602,-0.342084653792828,
3.64661166616396));
#33112=CARTESIAN_POINT('Ctrl Pts',(17.837592458223,0.112229559114723,3.52113702282083));
#33113=CARTESIAN_POINT('Ctrl Pts',(17.8853082942859,0.463481641013499,3.83540961967535));
#33114=CARTESIAN_POINT('Ctrl Pts',(17.9330241303487,0.389111400387848,4.30082809533052));
#33115=CARTESIAN_POINT('Ctrl Pts',(17.9807399664116,-0.0425858264624495,
4.48999150220845));
#33116=CARTESIAN_POINT('Ctrl Pts',(18.0284558024744,-0.435175833605105,
4.22918817311999));
#33117=CARTESIAN_POINT('Ctrl Pts',(18.0761716385373,-0.428137176707308,
3.75791781814212));
#33118=CARTESIAN_POINT('Ctrl Pts',(18.1238874746,-0.0279335627019553,3.5089552556775));
#33119=CARTESIAN_POINT('Ctrl Pts',(18.1716033106629,0.397921871745719,3.71092663761881));
#33120=CARTESIAN_POINT('Ctrl Pts',(18.2193191467257,0.458359528554279,4.17835853620019));
#33121=CARTESIAN_POINT('Ctrl Pts',(18.2670349827886,0.097878577523561,4.48200104659009));
#33122=CARTESIAN_POINT('Ctrl Pts',(18.3147508188514,-0.352485777302551,
4.34301457935691));
#33123=CARTESIAN_POINT('Ctrl Pts',(18.3624666549143,-0.479157019140895,
3.88903254594255));
#33124=CARTESIAN_POINT('Ctrl Pts',(18.4101824909771,-0.165810997523729,
3.5369536330429));
#33125=CARTESIAN_POINT('Ctrl Pts',(18.4578983270399,0.299801814449608,3.61009732380414));
#33126=CARTESIAN_POINT('Ctrl Pts',(18.5056141631028,0.49010200717001,4.04129464153984));
#33127=CARTESIAN_POINT('Ctrl Pts',(18.5533299991656,0.230333985517487,4.43457045454981));
#33128=CARTESIAN_POINT('Ctrl Pts',(18.6010458352284,-0.24095327917969,4.42877353242069));
#33129=CARTESIAN_POINT('Ctrl Pts',(18.6487616712913,-0.49096944006335,4.0292272779409));
#33130=CARTESIAN_POINT('Ctrl Pts',(18.6964775073541,-0.290120809601049,
3.60284116440841));
#33131=CARTESIAN_POINT('Ctrl Pts',(18.744193343417,0.177150224400508,3.54117212067402));
#33132=CARTESIAN_POINT('Ctrl Pts',(18.7919091794797,0.481741481528227,3.90085177849878));
#33133=CARTESIAN_POINT('Ctrl Pts',(18.8396250155427,0.343942123623612,4.35158077372017));
#33134=CARTESIAN_POINT('Ctrl Pts',(18.8873408516054,-0.109704578635382,
4.47944773466767));
#33135=CARTESIAN_POINT('Ctrl Pts',(18.9350566876684,-0.462607878309702,
4.16703046362027));
#33136=CARTESIAN_POINT('Ctrl Pts',(18.9827725237311,-0.39069124519864,3.70122654773242));
#33137=CARTESIAN_POINT('Ctrl Pts',(19.030488359794,0.0400031699426168,3.50979089028978));
#33138=CARTESIAN_POINT('Ctrl Pts',(19.0782041958568,0.433962058584907,3.76852180111673));
#33139=CARTESIAN_POINT('Ctrl Pts',(19.1259200319197,0.429406911488226,4.23982270375453));
#33140=CARTESIAN_POINT('Ctrl Pts',(19.1736358679825,0.0305207902517796,
4.49089072733801));
#33141=CARTESIAN_POINT('Ctrl Pts',(19.2213517040454,-0.396393042209671,
4.29116624277653));
#33142=CARTESIAN_POINT('Ctrl Pts',(19.2690675401082,-0.459293044881286,
3.82405931712685));
#33143=CARTESIAN_POINT('Ctrl Pts',(19.316783376171,-0.100417177000157,3.51852142809106));
#33144=CARTESIAN_POINT('Ctrl Pts',(19.3644992122339,0.350673329058588,3.65513271950473));
#33145=CARTESIAN_POINT('Ctrl Pts',(19.4122150482967,0.479735122332443,4.10844094226069));
#33146=CARTESIAN_POINT('Ctrl Pts',(19.4599308843596,0.168248769032157,4.46216617689766));
#33147=CARTESIAN_POINT('Ctrl Pts',(19.5076467204224,-0.297743013815871,
4.39147710422109));
#33148=CARTESIAN_POINT('Ctrl Pts',(19.5553625564852,-0.490312813065352,
3.96128857502183));
#33149=CARTESIAN_POINT('Ctrl Pts',(19.603078392548,-0.232620797759261,3.56664935826393));
#33150=CARTESIAN_POINT('Ctrl Pts',(19.6507942286109,0.238690449241969,3.56996267500769));
#33151=CARTESIAN_POINT('Ctrl Pts',(19.6985100646737,0.490808633485035,3.96818593857384));
#33152=CARTESIAN_POINT('Ctrl Pts',(19.7462259007366,0.292209604061002,4.39562444172689));
#33153=CARTESIAN_POINT('Ctrl Pts',(19.7939417367994,-0.174729824492781,
4.45975512619968));
#33154=CARTESIAN_POINT('Ctrl Pts',(19.8416575728622,-0.481212499922896,
4.10168523844358));
#33155=CARTESIAN_POINT('Ctrl Pts',(19.8893734089251,-0.345789702982467,
3.65023692191923));
#33156=CARTESIAN_POINT('Ctrl Pts',(19.9370892449879,0.107175910646637,3.51998011832295));
#33157=CARTESIAN_POINT('Ctrl Pts',(19.9848050810508,0.461722480014006,3.83053541934297));
#33158=CARTESIAN_POINT('Ctrl Pts',(20.0325209171136,0.392257955100357,4.29670800504879));
#33159=CARTESIAN_POINT('Ctrl Pts',(20.0802367531764,-0.0374150865130887,
4.49041783929577));
#33160=CARTESIAN_POINT('Ctrl Pts',(20.1279525892393,-0.432744382500041,
4.23375285658289));
#33161=CARTESIAN_POINT('Ctrl Pts',(20.1756684253021,-0.430649333670284,
3.76246031529274));
#33162=CARTESIAN_POINT('Ctrl Pts',(20.223384261365,-0.033136228617316,3.50924504180455));
#33163=CARTESIAN_POINT('Ctrl Pts',(20.2711000974278,0.394908089060633,3.70680919012016));
#33164=CARTESIAN_POINT('Ctrl Pts',(20.3188159334906,0.460110046434968,4.17340395051402));
#33165=CARTESIAN_POINT('Ctrl Pts',(20.3665317695535,0.103149962306437,4.48116018402389));
#33166=CARTESIAN_POINT('Ctrl Pts',(20.4142476056163,-0.34923165553999,4.34628168153608));
#33167=CARTESIAN_POINT('Ctrl Pts',(20.4540108023354,-0.457800032585507,
3.97025345815189));
#33168=CARTESIAN_POINT('Ctrl Pts',(20.4858213597105,-0.325993724402262,
3.71529210935379));
#33169=CARTESIAN_POINT('Ctrl Pts',(20.509679277742,-0.15096738523986,3.59329490328468));
#33170=CARTESIAN_POINT('Ctrl Pts',(20.5335371957734,0.0630371972956549,
3.57102347342756));
#33171=CARTESIAN_POINT('Ctrl Pts',(20.5573951138048,0.260511246441404,3.65349437971329));
#33172=CARTESIAN_POINT('Ctrl Pts',(20.5812530318362,0.394877283734959,3.82077798440408));
#33173=CARTESIAN_POINT('Ctrl Pts',(20.6051109498677,0.432370081305563,4.03184236506754));
#33174=CARTESIAN_POINT('Ctrl Pts',(20.6289688678991,0.364303478986858,4.23514367899931));
#33175=CARTESIAN_POINT('Ctrl Pts',(20.6528267859305,0.207066376217976,4.38093363836299));
#33176=CARTESIAN_POINT('Ctrl Pts',(20.6766847039619,-0.000757290757721993,
4.43358147160167));
#33177=CARTESIAN_POINT('Ctrl Pts',(20.7005426219933,-0.208420567790133,
4.38020336888205));
#33178=CARTESIAN_POINT('Ctrl Pts',(20.7244005400248,-0.365106210756856,
4.23385701605743));
#33179=CARTESIAN_POINT('Ctrl Pts',(20.7482584580562,-0.432520392530856,
4.03032528343114));
#33180=CARTESIAN_POINT('Ctrl Pts',(20.7721163760876,-0.394167874571092,
3.81937870627435));
#33181=CARTESIAN_POINT('Ctrl Pts',(20.795974294119,-0.259432524437891,3.65259868360638));
#33182=CARTESIAN_POINT('Ctrl Pts',(20.8198322121504,-0.0612578225112809,
3.57076788979259));
#33183=CARTESIAN_POINT('Ctrl Pts',(20.8436901301819,0.151895538690754,3.5938959627232));
#33184=CARTESIAN_POINT('Ctrl Pts',(20.8675480482132,0.327906592802717,3.71632757520176));
#33185=CARTESIAN_POINT('Ctrl Pts',(20.8914059662447,0.423735399567132,3.90812480123879));
#33186=CARTESIAN_POINT('Ctrl Pts',(20.9152638842761,0.415949440063929,4.12238802732943));
#33187=CARTESIAN_POINT('Ctrl Pts',(20.9391218023075,0.30645246920106,4.30672404095661));
#33188=CARTESIAN_POINT('Ctrl Pts',(20.962979720339,0.122019544809087,4.41605767475162));
#33189=CARTESIAN_POINT('Ctrl Pts',(20.9868376383703,-0.0922504941031022,
4.42365387220386));
#33190=CARTESIAN_POINT('Ctrl Pts',(21.0106955564018,-0.28396276796243,4.32765515869354));
#33191=CARTESIAN_POINT('Ctrl Pts',(21.0345534744332,-0.40623841344949,4.15153583326342));
#33192=CARTESIAN_POINT('Ctrl Pts',(21.0584113924646,-0.429177699343215,
3.93836186909709));
#33193=CARTESIAN_POINT('Ctrl Pts',(21.082269310496,-0.347171348131155,3.74026010679315));
#33194=CARTESIAN_POINT('Ctrl Pts',(21.1061272285274,-0.180272145040548,
3.605671823621));
#33195=CARTESIAN_POINT('Ctrl Pts',(21.1299851465589,0.0307085077608185,
3.56750752082027));
#33196=CARTESIAN_POINT('Ctrl Pts',(21.1538430645903,0.234180094072738,3.63509941005724));
#33197=CARTESIAN_POINT('Ctrl Pts',(21.1777009826217,0.380388268371489,3.79191943321731));
#33198=CARTESIAN_POINT('Ctrl Pts',(21.2015589006531,0.433581149524578,3.99962082296209));
#33199=CARTESIAN_POINT('Ctrl Pts',(21.2254168186846,0.380751629084578,4.2074149318183));
#33200=CARTESIAN_POINT('Ctrl Pts',(21.2492747367159,0.234817963878357,4.36449043997717));
#33201=CARTESIAN_POINT('Ctrl Pts',(21.2731326547474,0.0314649101850846,
4.43243810704058));
#33202=CARTESIAN_POINT('Ctrl Pts',(21.2969905727788,-0.179582171132277,
4.39464287755545));
#33203=CARTESIAN_POINT('Ctrl Pts',(21.3208484908102,-0.346716519889314,
4.26034671465164));
#33204=CARTESIAN_POINT('Ctrl Pts',(21.3447064088417,-0.429069235164158,
4.0623886883135));
#33205=CARTESIAN_POINT('Ctrl Pts',(21.368564326873,-0.406502834830527,3.8491749282489));
#33206=CARTESIAN_POINT('Ctrl Pts',(21.3924222449045,-0.284535418465691,
3.67284200661995));
#33207=CARTESIAN_POINT('Ctrl Pts',(21.4162801629359,-0.0929913416969399,
3.5765081259772));
#33208=CARTESIAN_POINT('Ctrl Pts',(21.4401380809674,0.121291651150069,3.58372954422009));
#33209=CARTESIAN_POINT('Ctrl Pts',(21.4639959989987,0.305915531372611,3.69274042788069));
#33210=CARTESIAN_POINT('Ctrl Pts',(21.4878539170302,0.415734731202803,3.87688464650718));
#33211=CARTESIAN_POINT('Ctrl Pts',(21.5117118350615,0.423895464867194,4.09113392265755));
#33212=CARTESIAN_POINT('Ctrl Pts',(21.535569753093,0.328402210690932,4.28309847227994));
#33213=CARTESIAN_POINT('Ctrl Pts',(21.5594276711244,0.152605670504114,4.40583773398234));
#33214=CARTESIAN_POINT('Ctrl Pts',(21.5832855891559,-0.0605071130159612,
4.42933861492812));
#33215=CARTESIAN_POINT('Ctrl Pts',(21.6071435071872,-0.258824259222961,
4.34785450957493));
#33216=CARTESIAN_POINT('Ctrl Pts',(21.6310014252187,-0.39385182381868,4.18131050126406));
#33217=CARTESIAN_POINT('Ctrl Pts',(21.6548593432501,-0.432571889182456,
3.97043113659525));
#33218=CARTESIAN_POINT('Ctrl Pts',(21.6787172612815,-0.365516344619441,
3.76678216446856));
#33219=CARTESIAN_POINT('Ctrl Pts',(21.702575179313,-0.209082097331647,3.62016130585559));
#33220=CARTESIAN_POINT('Ctrl Pts',(21.7264330973443,-0.00152158196427748,
3.56642135455923));
#33221=CARTESIAN_POINT('Ctrl Pts',(21.7502910153758,0.206411001640417,3.61870319251831));
#33222=CARTESIAN_POINT('Ctrl Pts',(21.7741489334072,0.363870472821225,3.76422248622317));
#33223=CARTESIAN_POINT('Ctrl Pts',(21.7980068514386,0.432353701764573,3.96739580449697));
#33224=CARTESIAN_POINT('Ctrl Pts',(21.82186476947,0.395114673548107,4.17854173669174));
#33225=CARTESIAN_POINT('Ctrl Pts',(21.8457226875014,0.261259344941517,4.3460293508861));
#33226=CARTESIAN_POINT('Ctrl Pts',(21.8695806055329,0.0635189899350569,
4.42890336313855));
#33227=CARTESIAN_POINT('Ctrl Pts',(21.8934385235643,-0.14975348833307,4.40689882001058));
#33228=CARTESIAN_POINT('Ctrl Pts',(21.9172964415957,-0.326407159500644,
4.28539643168872));
#33229=CARTESIAN_POINT('Ctrl Pts',(21.9411543596271,-0.423245389017799,
4.09410684177624));
#33230=CARTESIAN_POINT('Ctrl Pts',(21.9650122776585,-0.416588591947193,
3.87980556563057));
#33231=CARTESIAN_POINT('Ctrl Pts',(21.98887019569,-0.30806453650007,3.69489510271888));
#33232=CARTESIAN_POINT('Ctrl Pts',(22.0127281137213,-0.12421031036921,3.58459109808296));
#33233=CARTESIAN_POINT('Ctrl Pts',(22.0365860317528,0.0900167200678817,
3.57586588547707));
#33234=CARTESIAN_POINT('Ctrl Pts',(22.0604439497842,0.282232210442068,3.67085301705332));
#33235=CARTESIAN_POINT('Ctrl Pts',(22.0843018678157,0.405434237512275,3.8463255517439));
#33236=CARTESIAN_POINT('Ctrl Pts',(22.108159785847,0.429496549703537,4.05937567504088));
#33237=CARTESIAN_POINT('Ctrl Pts',(22.1320177038785,0.348535256241736,4.25790682842971));
#33238=CARTESIAN_POINT('Ctrl Pts',(22.1558756219099,0.182347598717988,4.39337273702606));
#33239=CARTESIAN_POINT('Ctrl Pts',(22.1797335399413,-0.0284290137391457,
4.43264829616218));
#33240=CARTESIAN_POINT('Ctrl Pts',(22.2035914579727,-0.232253957950086,
4.36612956178204));
#33241=CARTESIAN_POINT('Ctrl Pts',(22.2274493760041,-0.379286482964224,
4.21008217638027));
#33242=CARTESIAN_POINT('Ctrl Pts',(22.2513072940356,-0.433573131350875,
4.00266397632408));
#33243=CARTESIAN_POINT('Ctrl Pts',(22.275165212067,-0.381839338801546,3.79459436150246));
#33244=CARTESIAN_POINT('Ctrl Pts',(22.2990231300984,-0.236735426869051,
3.63675202040985));
#33245=CARTESIAN_POINT('Ctrl Pts',(22.3228810481298,-0.0337432544318164,
3.56773370504276));
#33246=CARTESIAN_POINT('Ctrl Pts',(22.3467389661613,0.177500062688638,3.60441627341574));
#33247=CARTESIAN_POINT('Ctrl Pts',(22.3705968841926,0.345339779804043,3.73782983856348));
#33248=CARTESIAN_POINT('Ctrl Pts',(22.3944548022241,0.428734513273282,3.93535114928888));
#33249=CARTESIAN_POINT('Ctrl Pts',(22.4183127202555,0.407291980919218,4.1486808655136));
#33250=CARTESIAN_POINT('Ctrl Pts',(22.4421706382869,0.286255462618544,4.32565405918856));
#33251=CARTESIAN_POINT('Ctrl Pts',(22.4660285563183,0.0952216904214238,
4.42299596654013));
#33252=CARTESIAN_POINT('Ctrl Pts',(22.4898864743497,-0.119096386717928,
4.41690383452019));
#33253=CARTESIAN_POINT('Ctrl Pts',(22.5137443923812,-0.304292138366774,
4.30886736509782));
#33254=CARTESIAN_POINT('Ctrl Pts',(22.5376023104126,-0.415080201412036,
4.12530439950267));
#33255=CARTESIAN_POINT('Ctrl Pts',(22.561460228444,-0.424369795825249,3.91110111771763));
#33256=CARTESIAN_POINT('Ctrl Pts',(22.5853181464754,-0.329889515310188,
3.71863599132299));
#33257=CARTESIAN_POINT('Ctrl Pts',(22.6091760645068,-0.154742073939436,
3.59497211022641));
#33258=CARTESIAN_POINT('Ctrl Pts',(22.6330339825383,0.0582436639512456,
3.57034842802071));
#33259=CARTESIAN_POINT('Ctrl Pts',(22.6568919005697,0.256987911016647,3.65078654733876));
#33260=CARTESIAN_POINT('Ctrl Pts',(22.6807498186011,0.39289034562191,3.81661632308649));
#33261=CARTESIAN_POINT('Ctrl Pts',(22.7046077366325,0.432722782933869,4.02728943245291));
#33262=CARTESIAN_POINT('Ctrl Pts',(22.7284656546639,0.366738191089385,4.2312875884069));
#33263=CARTESIAN_POINT('Ctrl Pts',(22.7523235726953,0.211084664509997,4.37873330099785));
#33264=CARTESIAN_POINT('Ctrl Pts',(22.7761814907268,0.00379901600965994,
4.43356145647204));
#33265=CARTESIAN_POINT('Ctrl Pts',(22.8000394087582,-0.204384723485633,
4.3823852668741));
#33266=CARTESIAN_POINT('Ctrl Pts',(22.8238973267896,-0.36265185203719,4.2376794731));
#33267=CARTESIAN_POINT('Ctrl Pts',(22.8398026054772,-0.408954280604672,
4.10250106973657));
#33268=CARTESIAN_POINT('Ctrl Pts',(22.847755244821,-0.414526965927561,4.03345758723954));
#33269=CARTESIAN_POINT('',(22.8,-0.592174260192535,4.04779597854866));
#33270=CARTESIAN_POINT('Ctrl Pts',(22.8,-0.19576256658266,4.36695865185836));
#33271=CARTESIAN_POINT('Ctrl Pts',(22.8,-0.195886593570853,4.36694806728808));
#33272=CARTESIAN_POINT('Ctrl Pts',(22.8,-0.196010613870461,4.36693742279878));
#33273=CARTESIAN_POINT('Ctrl Pts',(22.8,-0.196134627427637,4.36692671841166));
#33274=CARTESIAN_POINT('Ctrl Pts',(22.8,-0.216622178843513,4.36515830948628));
#33275=CARTESIAN_POINT('Ctrl Pts',(22.8,-0.236921239981942,4.36175743074964));
#33276=CARTESIAN_POINT('Ctrl Pts',(22.8,-0.256857422940798,4.35688458679081));
#33277=CARTESIAN_POINT('Ctrl Pts',(22.8,-0.271809560159941,4.35322995382169));
#33278=CARTESIAN_POINT('Ctrl Pts',(22.8,-0.286558947067823,4.34874691155445));
#33279=CARTESIAN_POINT('Ctrl Pts',(22.8,-0.301048271828705,4.34349077646485));
#33280=CARTESIAN_POINT('Ctrl Pts',(22.8,-0.310003423377303,4.3402422133286));
#33281=CARTESIAN_POINT('Ctrl Pts',(22.8,-0.318859482942331,4.33669811041118));
#33282=CARTESIAN_POINT('Ctrl Pts',(22.8,-0.327604744452034,4.33286912874946));
#33283=CARTESIAN_POINT('Ctrl Pts',(22.8,-0.333457186121174,4.33030672489195));
#33284=CARTESIAN_POINT('Ctrl Pts',(22.8,-0.33926207870774,4.32761569029118));
#33285=CARTESIAN_POINT('Ctrl Pts',(22.8,-0.345009487597299,4.32480202294401));
#33286=CARTESIAN_POINT('Ctrl Pts',(22.8,-0.365309066997251,4.31486428146495));
#33287=CARTESIAN_POINT('Ctrl Pts',(22.8,-0.384828901796994,4.30343044333042));
#33288=CARTESIAN_POINT('Ctrl Pts',(22.8,-0.403416958856431,4.29067119823496));
#33289=CARTESIAN_POINT('Ctrl Pts',(22.8,-0.409874425773003,4.28623865303559));
#33290=CARTESIAN_POINT('Ctrl Pts',(22.8,-0.416219739836017,4.28164578247975));
#33291=CARTESIAN_POINT('Ctrl Pts',(22.8,-0.422447327171508,4.27689854297234));
#33292=CARTESIAN_POINT('Ctrl Pts',(22.8,-0.43500295340691,4.2673274905416));
#33293=CARTESIAN_POINT('Ctrl Pts',(22.8,-0.447079966647781,4.25712966465555));
#33294=CARTESIAN_POINT('Ctrl Pts',(22.8,-0.458660056443695,4.24636133358853));
#33295=CARTESIAN_POINT('Ctrl Pts',(22.8,-0.465333929961841,4.24015529539631));
#33296=CARTESIAN_POINT('Ctrl Pts',(22.8,-0.471842796551704,4.23375955955572));
#33297=CARTESIAN_POINT('Ctrl Pts',(22.8,-0.478183280583292,4.22718326898633));
#33298=CARTESIAN_POINT('Ctrl Pts',(22.8,-0.48330469601013,4.22187138494));
#33299=CARTESIAN_POINT('Ctrl Pts',(22.8,-0.488310096860405,4.21644792156372));
#33300=CARTESIAN_POINT('Ctrl Pts',(22.8,-0.49319389770791,4.21092357737429));
#33301=CARTESIAN_POINT('Ctrl Pts',(22.8,-0.509882204568999,4.19204648678071));
#33302=CARTESIAN_POINT('Ctrl Pts',(22.8,-0.525164669297395,4.17198027236651));
#33303=CARTESIAN_POINT('Ctrl Pts',(22.8,-0.538985569877159,4.15095378743758));
#33304=CARTESIAN_POINT('Ctrl Pts',(22.8,-0.553292287721507,4.12918820238033));
#33305=CARTESIAN_POINT('Ctrl Pts',(22.8,-0.566034197593199,4.10639346234103));
#33306=CARTESIAN_POINT('Ctrl Pts',(22.8,-0.577149101532509,4.08276767497818));
#33307=CARTESIAN_POINT('Ctrl Pts',(22.8,-0.582543745751794,4.07130084468266));
#33308=CARTESIAN_POINT('Ctrl Pts',(22.8,-0.587554988912119,4.05963744408228));
#33309=CARTESIAN_POINT('Ctrl Pts',(22.8,-0.592174260192535,4.04779597854866));
#33310=CARTESIAN_POINT('Ctrl Pts',(22.8,-0.592174260192532,4.04779597854869));
#33311=CARTESIAN_POINT('Ctrl Pts',(22.7920473606562,-0.584213376873468,
4.14642833911734));
#33312=CARTESIAN_POINT('Ctrl Pts',(22.7840947213124,-0.551140611244481,
4.24298318064208));
#33313=CARTESIAN_POINT('Ctrl Pts',(22.7761420819686,-0.496922031827459,
4.32571394759471));
#33314=CARTESIAN_POINT('Ctrl Pts',(22.7681894426248,-0.442703452410443,
4.40844471454734));
#33315=CARTESIAN_POINT('Ctrl Pts',(22.760236803281,-0.367339059205388,4.47735140692785));
#33316=CARTESIAN_POINT('Ctrl Pts',(22.7522841639372,-0.280089901523161,
4.52398941366922));
#33317=CARTESIAN_POINT('Ctrl Pts',(22.7444712463773,-0.194373644734646,
4.56980802634291));
#33318=CARTESIAN_POINT('Ctrl Pts',(22.7366583288174,-0.0971865673270821,
4.59413356703531));
#33319=CARTESIAN_POINT('Ctrl Pts',(22.7288454112575,-7.11440487624268E-7,
4.59414971000239));
#33320=CARTESIAN_POINT('Origin',(27.2,0.3,2.9));
#33321=CARTESIAN_POINT('',(29.2,0.3,3.04606079858305));
#33322=CARTESIAN_POINT('',(27.2,0.3,3.04606079858305));
#33323=CARTESIAN_POINT('',(23.3,0.3,3.04606079858305));
#33324=CARTESIAN_POINT('',(29.2,0.3,3.35));
#33325=CARTESIAN_POINT('',(29.2,0.3,2.9));
#33326=CARTESIAN_POINT('',(27.2,0.3,3.35));
#33327=CARTESIAN_POINT('',(27.2,0.3,3.35));
#33328=CARTESIAN_POINT('',(27.2,0.3,2.9));
#33329=CARTESIAN_POINT('Origin',(27.2,0.,3.125));
#33330=CARTESIAN_POINT('',(27.2,-0.3,3.04606079858305));
#33331=CARTESIAN_POINT('Origin',(27.2,0.,4.));
#33332=CARTESIAN_POINT('',(27.2,-0.3,3.35));
#33333=CARTESIAN_POINT('',(27.2,0.3,3.35));
#33334=CARTESIAN_POINT('',(27.2,-0.3,3.35));
#33335=CARTESIAN_POINT('Origin',(27.2,0.3,3.35));
#33336=CARTESIAN_POINT('',(29.2,-0.3,3.35));
#33337=CARTESIAN_POINT('',(29.2,0.3,3.35));
#33338=CARTESIAN_POINT('',(27.2,-0.3,3.35));
#33339=CARTESIAN_POINT('Origin',(27.2,-0.3,3.35));
#33340=CARTESIAN_POINT('',(29.2,-0.3,3.04606079858305));
#33341=CARTESIAN_POINT('',(23.3,-0.3,3.04606079858305));
#33342=CARTESIAN_POINT('',(29.2,-0.3,3.35));
#33343=CARTESIAN_POINT('Origin',(29.2,0.,3.125));
#33344=CARTESIAN_POINT('Origin',(29.2,0.,4.));
#33345=CARTESIAN_POINT('Origin',(23.3,0.,4.));
#33346=CARTESIAN_POINT('',(29.4,-1.22464679914735E-16,5.));
#33347=CARTESIAN_POINT('Origin',(29.4,0.,4.));
#33348=CARTESIAN_POINT('',(23.3,-1.22464679914735E-16,5.));
#33349=CARTESIAN_POINT('',(23.3,-1.22464679914735E-16,5.));
#33350=CARTESIAN_POINT('Origin',(23.3,0.,4.));
#33351=CARTESIAN_POINT('Origin',(29.4,0.,4.));
#33352=CARTESIAN_POINT('Origin',(22.8,0.,4.));
#33353=CARTESIAN_POINT('',(22.8,-1.65327317884893E-16,5.35));
#33354=CARTESIAN_POINT('Origin',(22.8,0.,4.));
#33355=CARTESIAN_POINT('Origin',(22.8,0.,4.));
#33356=CARTESIAN_POINT('Origin',(22.8,0.,4.));
#33357=CARTESIAN_POINT('',(23.3,-1.65327317884893E-16,5.35));
#33358=CARTESIAN_POINT('Origin',(23.3,0.,4.));
#33359=CARTESIAN_POINT('',(22.8,-1.65327317884893E-16,5.35));
#33360=CARTESIAN_POINT('Origin',(23.3,0.,4.));
#33361=CARTESIAN_POINT('Origin',(4.,0.,4.));
#33919=UNCERTAINTY_MEASURE_WITH_UNIT(LENGTH_MEASURE(0.001),#33982,
'DISTANCE_ACCURACY_VALUE',
'Maximum model space distance between geometric entities at asserted c
onnectivities');
#33929=UNCERTAINTY_MEASURE_WITH_UNIT(LENGTH_MEASURE(0.001),#33982,
'DISTANCE_ACCURACY_VALUE',
'Maximum model space distance between geometric entities at asserted c
onnectivities');
#33971=(
GEOMETRIC_REPRESENTATION_CONTEXT(3)
GLOBAL_UNCERTAINTY_ASSIGNED_CONTEXT((#33919))
GLOBAL_UNIT_ASSIGNED_CONTEXT((#33982,#33984,#33985))
REPRESENTATION_CONTEXT('','3D')
);
#33981=(
GEOMETRIC_REPRESENTATION_CONTEXT(3)
GLOBAL_UNCERTAINTY_ASSIGNED_CONTEXT((#33929))
GLOBAL_UNIT_ASSIGNED_CONTEXT((#33982,#33984,#33985))
REPRESENTATION_CONTEXT('','3D')
);
#33982=(
LENGTH_UNIT()
NAMED_UNIT(*)
SI_UNIT(.CENTI.,.METRE.)
);
#33984=(
NAMED_UNIT(*)
PLANE_ANGLE_UNIT()
SI_UNIT($,.RADIAN.)
);
#33985=(
NAMED_UNIT(*)
SI_UNIT($,.STERADIAN.)
SOLID_ANGLE_UNIT()
);
#34027=SHAPE_DEFINITION_REPRESENTATION(#34111,#34223);
#34111=PRODUCT_DEFINITION_SHAPE('',$,#34275);
#34223=SHAPE_REPRESENTATION('',(#14546),#33971);
#34233=PRODUCT_DEFINITION_CONTEXT('part definition',#34388,'design');
#34275=PRODUCT_DEFINITION('Supported TR12x3 screw',
'Supported TR12x3 screw',#34326,#34233);
#34326=PRODUCT_DEFINITION_FORMATION('',$,#34431);
#34388=APPLICATION_CONTEXT(
'Core Data for Automotive Mechanical Design Process');
#34389=PRODUCT_CONTEXT('part definition',#34388,'mechanical');
#34431=PRODUCT('Supported TR12x3 screw','Supported TR12x3 screw',
'Supported TR12x3 screw',(#34389));
#34518=COLOUR_RGB('Black',0.12,0.14,0.17);
#34519=FILL_AREA_STYLE_COLOUR('',#34518);
#34520=FILL_AREA_STYLE('',(#34519));
#34521=SURFACE_STYLE_FILL_AREA(#34520);
#34522=SURFACE_SIDE_STYLE('',(#34521));
#34523=SURFACE_STYLE_USAGE(.BOTH.,#34522);
#34524=PRESENTATION_STYLE_ASSIGNMENT((#34523));
ENDSEC;
END-ISO-10303-21;
